ISO-10303-21;
HEADER;
FILE_DESCRIPTION (('STEP AP214'),
    '1' );
FILE_NAME ('Top rod.step',
    '2026-10-21T18:31:44',
    ( '' ),
    ( '' ),
    'SwSTEP 2.0',
    'SolidWorks 2025',
    '' );
FILE_SCHEMA (( 'AUTOMOTIVE_DESIGN' ));
ENDSEC;

DATA;
#1=CARTESIAN_POINT ( 'NONE',  ( 6.241811971030540640, 75.95141910118948658, -11.97037661190906910 ) ) ;
#2=CARTESIAN_POINT ( 'NONE',  ( 12.50000000000000000, 98.93000000000002103, 1.224646799147353059E-15 ) ) ;
#3=CARTESIAN_POINT ( 'NONE',  ( 7.272992578804308828, 36.97999999999998977, 10.01041549318726709 ) ) ;
#4=CARTESIAN_POINT ( 'NONE',  ( -4.562425571675021274, 41.51584201689734499, 12.70716777987128054 ) ) ;
#5=CARTESIAN_POINT ( 'NONE',  ( -12.91556685892874867, 58.78902204722160718, -3.932462553950937689 ) ) ;
#6=CARTESIAN_POINT ( 'NONE',  ( 4.630764260054621495, 44.84669919125740734, 12.68093428297014569 ) ) ;
#7=CARTESIAN_POINT ( 'NONE',  ( -10.92172942406178926, 54.62999999999999545, -7.935100905948389460 ) ) ;
#8=CARTESIAN_POINT ( 'NONE',  ( 8.860164440870203606, 30.02243855473401979, 10.18733757369393267 ) ) ;
#11=CARTESIAN_POINT ( 'NONE',  ( -7.522916883230899465, 49.46192173470914355, -11.20972055436655523 ) ) ;
#12=CARTESIAN_POINT ( 'NONE',  ( 10.11047073980464361, 63.77503176193906143, -8.949362642739272289 ) ) ;
#13=CARTESIAN_POINT ( 'NONE',  ( 10.29443543732497979, 42.76512297172600796, -8.733575356815638457 ) ) ;
#14=CARTESIAN_POINT ( 'NONE',  ( 1.387885517463281371, 38.72990328888538869, 13.42850322618521552 ) ) ;
#15=EDGE_LOOP ( 'NONE', ( #14246, #2278, #8260, #10211 ) ) ;
#17=CARTESIAN_POINT ( 'NONE',  ( -10.92172942406179104, 49.23000000000000398, 7.935100905948387684 ) ) ;
#19=VERTEX_POINT ( 'NONE', #8191 ) ;
#22=CARTESIAN_POINT ( 'NONE',  ( 4.958471358563230069, 61.00121407256968098, -12.55670518402642521 ) ) ;
#24=CARTESIAN_POINT ( 'NONE',  ( 10.50943839410675196, 72.10666813338646364, 8.474155960609857985 ) ) ;
#25=CARTESIAN_POINT ( 'NONE',  ( 12.25135822064244628, 57.63786423219936239, -5.672709418904434031 ) ) ;
#26=CARTESIAN_POINT ( 'NONE',  ( 11.76794919243112325, 70.43000000000000682, 1.441158131103945434E-15 ) ) ;
#27=CARTESIAN_POINT ( 'NONE',  ( 9.520470885617715595, 76.13000000000000966, 6.917026985038134512 ) ) ;
#28=CARTESIAN_POINT ( 'NONE',  ( -7.237012465003837214, 47.41034925122353627, 11.39682853042513422 ) ) ;
#29=CARTESIAN_POINT ( 'NONE',  ( -10.92172942406178926, 45.62999999999999545, -7.935100905948389460 ) ) ;
#31=CARTESIAN_POINT ( 'NONE',  ( 10.92172942406178926, 38.12999999999999545, 7.935100905948387684 ) ) ;
#36=CARTESIAN_POINT ( 'NONE',  ( 11.39480283653290194, 33.70102987876868639, -7.239802240102667596 ) ) ;
#37=CARTESIAN_POINT ( 'NONE',  ( -4.107118796296879815, 73.32755911965604412, -12.86190453662493383 ) ) ;
#39=VERTEX_POINT ( 'NONE', #5535 ) ;
#41=CARTESIAN_POINT ( 'NONE',  ( -2.167727191357447403, 62.60205656133668839, 13.32483508987561649 ) ) ;
#43=CARTESIAN_POINT ( 'NONE',  ( -13.33648623469416528, 41.00345850548239213, 2.095001394486209367 ) ) ;
#46=CARTESIAN_POINT ( 'NONE',  ( -12.68486621467936359, 44.09791772264757270, 4.641127458682580809 ) ) ;
#47=CARTESIAN_POINT ( 'NONE',  ( 12.50000000000000000, 98.93000000000002103, 1.224646799147353059E-15 ) ) ;
#49=CARTESIAN_POINT ( 'NONE',  ( -4.171729424061787483, 46.32999999999999829, -12.83926296998457417 ) ) ;
#50=CARTESIAN_POINT ( 'NONE',  ( 10.92172942406178926, 44.13000000000000256, 7.935100905948387684 ) ) ;
#51=CARTESIAN_POINT ( 'NONE',  ( -12.09611347903164891, 71.15127006308296131, 6.013594338244640625 ) ) ;
#54=CARTESIAN_POINT ( 'NONE',  ( -13.10508471444031287, 68.04691603053561266, 3.289941233735407256 ) ) ;
#57=CARTESIAN_POINT ( 'NONE',  ( 13.49788837497377969, 54.40198127425698971, 0.8139535183936712492 ) ) ;
#59=CARTESIAN_POINT ( 'NONE',  ( -11.88785451664102411, 64.69331280751505631, -6.397572128427487570 ) ) ;
#61=CARTESIAN_POINT ( 'NONE',  ( -13.32240026865723692, 35.00664116012176663, 2.183159191248645659 ) ) ;
#65=CARTESIAN_POINT ( 'NONE',  ( -1.332730275901221395, 31.22788502858077209, -13.43591754810035432 ) ) ;
#66=CARTESIAN_POINT ( 'NONE',  ( 2.964303633682398686, 73.07342191280697818, -13.17196784541496513 ) ) ;
#70=CARTESIAN_POINT ( 'NONE',  ( -12.68834643456797906, 52.76331015659336998, -4.610928276790117408 ) ) ;
#72=CARTESIAN_POINT ( 'NONE',  ( 9.520470885617715595, 46.12999999999999545, 6.917026985038134512 ) ) ;
#73=CARTESIAN_POINT ( 'NONE',  ( 3.294673121883986422, 50.79846311650262436, 13.09179671531762246 ) ) ;
#74=CARTESIAN_POINT ( 'NONE',  ( -9.961542587724716569, 37.57728390915936956, -9.113131270120877758 ) ) ;
#75=EDGE_CURVE ( 'NONE', #10985, #13128, #6860, .T. ) ;
#76=CARTESIAN_POINT ( 'NONE',  ( 10.08038093372313604, 36.08304225860660353, 8.991274832604577938 ) ) ;
#78=CARTESIAN_POINT ( 'NONE',  ( -11.44756249950965632, 74.19779003843927967, 7.160551751645796159 ) ) ;
#79=CARTESIAN_POINT ( 'NONE',  ( -13.19858737197696286, 77.03056283200281484, 2.845309594670863973 ) ) ;
#81=CARTESIAN_POINT ( 'NONE',  ( -6.071462803580223166, 79.40141861843632398, -12.06817019399647783 ) ) ;
#84=CARTESIAN_POINT ( 'NONE',  ( 1.982521523170245906E-06, 77.68005525700222336, 13.49999999999970690 ) ) ;
#86=CARTESIAN_POINT ( 'NONE',  ( 3.636496289402154414, 51.82999999999999829, 11.19198476289190936 ) ) ;
#90=CARTESIAN_POINT ( 'NONE',  ( -8.290587820170616240, 40.49598020429036183, -10.65487298274420525 ) ) ;
#91=CARTESIAN_POINT ( 'NONE',  ( -2.747897566831316141, 34.27880424421546479, -13.21738048412783151 ) ) ;
#92=CARTESIAN_POINT ( 'NONE',  ( 13.48604648626630542, 75.45114278836371113, -0.6137407349411325708 ) ) ;
#94=CARTESIAN_POINT ( 'NONE',  ( -11.76794919243112325, 32.92999999999999972, -2.882316262207890869E-15 ) ) ;
#95=CARTESIAN_POINT ( 'NONE',  ( -6.586690174280394494, 41.43750565762731952, 11.78692872275349579 ) ) ;
#96=CARTESIAN_POINT ( 'NONE',  ( -4.171426067996565124, 58.32999100947719029, -12.83948131572000584 ) ) ;
#97=CARTESIAN_POINT ( 'NONE',  ( 6.370293526262202022, 44.91380087981439573, 11.90272333445460262 ) ) ;
#101=CARTESIAN_POINT ( 'NONE',  ( -4.171729424061791036, 58.53000000000000114, 12.83926296998457239 ) ) ;
#102=CARTESIAN_POINT ( 'NONE',  ( -11.20551244324089524, 49.64703832191597854, -7.529055542132852885 ) ) ;
#103=CARTESIAN_POINT ( 'NONE',  ( 13.46801799936566724, 63.39787863554747815, 0.9304553811726751222 ) ) ;
#104=CARTESIAN_POINT ( 'NONE',  ( 11.68815242529539411, 42.17840658691920908, 6.773979411268512330 ) ) ;
#105=CARTESIAN_POINT ( 'NONE',  ( 4.417203864861311224, 38.83887425577129449, 12.75710294833973357 ) ) ;
#107=CARTESIAN_POINT ( 'NONE',  ( -4.026122579657434919, 70.32476532614168718, -12.88571505164192033 ) ) ;
#108=CARTESIAN_POINT ( 'NONE',  ( -13.49999999999999822, 48.77999999999998693, -4.386415899144240349 ) ) ;
#111=CARTESIAN_POINT ( 'NONE',  ( -4.477815178396856055, 43.34114203380904229, -12.73627368523690606 ) ) ;
#113=CARTESIAN_POINT ( 'NONE',  ( 6.392086272904786703, 60.94536626219394293, -11.89080869004308205 ) ) ;
#115=CARTESIAN_POINT ( 'NONE',  ( 2.453092984686562339, 71.76820780413271450, 13.27525308931726578 ) ) ;
#116=CARTESIAN_POINT ( 'NONE',  ( 13.40373713238982489, 66.48610201136790465, -1.609300758946977661 ) ) ;
#117=CARTESIAN_POINT ( 'NONE',  ( 4.966293671374200969, 56.85915651247563574, 12.55332637815666708 ) ) ;
#118=CARTESIAN_POINT ( 'NONE',  ( 3.636496289402154414, 66.82999999999999829, 11.19198476289190936 ) ) ;
#119=CARTESIAN_POINT ( 'NONE',  ( 9.520470885617715595, 64.12999999999999545, 6.917026985038134512 ) ) ;
#120=CARTESIAN_POINT ( 'NONE',  ( -3.966664967154714727, 47.53736456333449922, 12.90422583550607527 ) ) ;
#121=CARTESIAN_POINT ( 'NONE',  ( -13.49999999999999822, 45.78000000000000114, -4.386415899144240349 ) ) ;
#122=CARTESIAN_POINT ( 'NONE',  ( -8.224360503536546367E-15, 78.17999999999999261, -13.50000000000000000 ) ) ;
#124=CARTESIAN_POINT ( 'NONE',  ( -3.802315511192875697, 56.54328190446157976, 12.95363457325665202 ) ) ;
#126=CARTESIAN_POINT ( 'NONE',  ( -4.171729424061791036, 40.52999999999999403, 12.83926296998457239 ) ) ;
#128=CARTESIAN_POINT ( 'NONE',  ( 13.48850798719686317, 33.44917238739969889, -0.5569197484580091784 ) ) ;
#130=EDGE_LOOP ( 'NONE', ( #12331, #307, #5558 ) ) ;
#132=CARTESIAN_POINT ( 'NONE',  ( -2.372100534622330059, 62.59470822479858043, 13.29057958102706571 ) ) ;
#137=CARTESIAN_POINT ( 'NONE',  ( -13.22798356179965751, 44.02531610866294187, 2.697370474855687927 ) ) ;
#139=EDGE_CURVE ( 'NONE', #3044, #15045, #14019, .T. ) ;
#140=CARTESIAN_POINT ( 'NONE',  ( 13.50000000000000355, 42.57999999999999829, -4.386415899144233244 ) ) ;
#141=CARTESIAN_POINT ( 'NONE',  ( -13.50000000000000000, 48.92999999999999972, -3.306546357697853733E-15 ) ) ;
#142=CARTESIAN_POINT ( 'NONE',  ( -13.48995242675199790, 70.94917795696534313, 0.5552773507619721549 ) ) ;
#143=( BOUNDED_CURVE ( )  B_SPLINE_CURVE ( 1, ( #8817, #14343 ),
 .UNSPECIFIED., .F., .F. ) 
 B_SPLINE_CURVE_WITH_KNOTS ( ( 2, 2 ),
 ( 0.000000000000000000, 1.000000000000000000 ),
 .UNSPECIFIED. ) 
 CURVE ( )  GEOMETRIC_REPRESENTATION_ITEM ( )  RATIONAL_B_SPLINE_CURVE ( ( 0.9782075210486875783, 0.9782075210486875783 ) ) 
 REPRESENTATION_ITEM ( '' )  );
#145=CARTESIAN_POINT ( 'NONE',  ( -11.47846244632648549, 67.66437547590606982, -7.110784611987690518 ) ) ;
#147=CARTESIAN_POINT ( 'NONE',  ( 12.45812093344438587, 54.62011758101717618, -5.223734028880926417 ) ) ;
#148=CARTESIAN_POINT ( 'NONE',  ( -11.89319909969382039, 64.69371209007049117, -6.387634285403382073 ) ) ;
#149=VERTEX_POINT ( 'NONE', #9845 ) ;
#151=CARTESIAN_POINT ( 'NONE',  ( -12.98939268596651786, 34.79855291303425702, -3.677969189785255555 ) ) ;
#152=ORIENTED_EDGE ( 'NONE', *, *, #6438, .T. ) ;
#153=CARTESIAN_POINT ( 'NONE',  ( 13.08478391751391001, 78.54823588313601590, -3.322629509287643224 ) ) ;
#156=CARTESIAN_POINT ( 'NONE',  ( -9.949531856098463578, 31.57665661914821342, -9.126009350303103673 ) ) ;
#157=CARTESIAN_POINT ( 'NONE',  ( 10.34601424054412000, 72.76232993950749517, -8.672412499177319489 ) ) ;
#163=CARTESIAN_POINT ( 'NONE',  ( -10.92172942406178926, 70.62999999999999545, -7.935100905948389460 ) ) ;
#164=CARTESIAN_POINT ( 'NONE',  ( -12.03726189314226858, 53.15526546510770345, 6.112069937274645426 ) ) ;
#165=CARTESIAN_POINT ( 'NONE',  ( -7.272992578804307939, 44.47999999999999687, -10.01041549318726886 ) ) ;
#166=CARTESIAN_POINT ( 'NONE',  ( -13.50000000000000000, 69.93000000000000682, -3.306546357697853733E-15 ) ) ;
#168=CARTESIAN_POINT ( 'NONE',  ( 11.95757905990039127, 69.66142261759961229, -6.266300119430860072 ) ) ;
#169=CARTESIAN_POINT ( 'NONE',  ( -4.427829777958112167, 37.33925957768354920, -12.75364605705754606 ) ) ;
#170=CARTESIAN_POINT ( 'NONE',  ( 3.589871069019304972, 35.80905818983445954, 13.01962489795650768 ) ) ;
#172=CARTESIAN_POINT ( 'NONE',  ( -10.34620055824173868, 74.26233662262045243, 8.672923399463462246 ) ) ;
#173=CARTESIAN_POINT ( 'NONE',  ( -13.29880297559754609, 76.84835896960053958, -2.322037454927736277 ) ) ;
#174=DIRECTION ( 'NONE',  ( 0.000000000000000000, -1.000000000000000000, 0.000000000000000000 ) ) ;
#176=CARTESIAN_POINT ( 'NONE',  ( -8.380961239563070819, 80.93000000000004945, 9.227099233226635278 ) ) ;
#179=CARTESIAN_POINT ( 'NONE',  ( 9.520470885617715595, 46.12999999999999545, 6.917026985038134512 ) ) ;
#181=CARTESIAN_POINT ( 'NONE',  ( 6.750022565184456980, 31.92926174983938026, 11.69132992304556495 ) ) ;
#182=CARTESIAN_POINT ( 'NONE',  ( 10.14927042510883481, 75.08716984626934732, 8.902032665787164234 ) ) ;
#183=EDGE_CURVE ( 'NONE', #10985, #14307, #6879, .T. ) ;
#186=CARTESIAN_POINT ( 'NONE',  ( 0.000000000000000000, 0.000000000000000000, 0.000000000000000000 ) ) ;
#187=CARTESIAN_POINT ( 'NONE',  ( -6.864354898698485918, 41.42600474588421378, 11.62474807620217376 ) ) ;
#188=CARTESIAN_POINT ( 'NONE',  ( -6.117255243659908359, 58.40366678541308687, -12.03616728541428493 ) ) ;
#190=CARTESIAN_POINT ( 'NONE',  ( -4.171729424061787483, 54.33000000000000540, -12.83926296998457417 ) ) ;
#192=CARTESIAN_POINT ( 'NONE',  ( -13.49999999999999822, 57.78000000000000114, -4.386415899144240349 ) ) ;
#193=CARTESIAN_POINT ( 'NONE',  ( -11.00427691244374273, 49.63475489259692353, -7.821558401853768494 ) ) ;
#194=CARTESIAN_POINT ( 'NONE',  ( 11.36089011803204407, 63.70299262790948802, -7.293906877826991320 ) ) ;
#195=CARTESIAN_POINT ( 'NONE',  ( 13.46351984225201548, 42.39558882709123111, 0.9962785372066437217 ) ) ;
#196=CARTESIAN_POINT ( 'NONE',  ( 3.151611543758418676, 38.79326144612200267, 13.13455959399786899 ) ) ;
#198=CARTESIAN_POINT ( 'NONE',  ( -3.974014160384248928, 70.32289088885870854, -12.90183134154761113 ) ) ;
#200=CIRCLE ( 'NONE', #2424, 5.000000000000000000 ) ;
#202=CARTESIAN_POINT ( 'NONE',  ( -11.06052376482290889, 43.63819014080397807, -7.740673448246946364 ) ) ;
#203=CARTESIAN_POINT ( 'NONE',  ( -7.499999999999999112, 105.5999945338998174, 8.557281619885976909 ) ) ;
#204=CARTESIAN_POINT ( 'NONE',  ( 10.49915709197846603, 60.75394407136035113, -8.486442428007933358 ) ) ;
#206=EDGE_CURVE ( 'NONE', #10449, #12592, #1531, .T. ) ;
#208=CARTESIAN_POINT ( 'NONE',  ( 12.91036043465679128, 66.57159231767617769, -3.948717839537223551 ) ) ;
#209=CARTESIAN_POINT ( 'NONE',  ( 10.83372828063143523, 57.12494043467410165, 8.055071804621336540 ) ) ;
#210=CARTESIAN_POINT ( 'NONE',  ( 3.636496289402157078, 62.03000000000000114, -11.19198476289190936 ) ) ;
#211=CARTESIAN_POINT ( 'NONE',  ( -11.76794919243112325, 71.78000000000000114, -3.823638476888998827 ) ) ;
#212=CARTESIAN_POINT ( 'NONE',  ( -8.395919747993797699, 47.35978594638820738, 10.59303779737377127 ) ) ;
#213=CARTESIAN_POINT ( 'NONE',  ( -10.92172942406179104, 46.22999999999999687, 7.935100905948387684 ) ) ;
#214=FACE_OUTER_BOUND ( 'NONE', #12871, .T. ) ;
#216=CARTESIAN_POINT ( 'NONE',  ( -9.167797302161076800, 56.32288307047150511, 9.914146655588314871 ) ) ;
#219=CARTESIAN_POINT ( 'NONE',  ( 12.00723290083941208, 33.65759935958783444, -6.170612997742742856 ) ) ;
#223=ORIENTED_EDGE ( 'NONE', *, *, #9601, .T. ) ;
#224=CARTESIAN_POINT ( 'NONE',  ( -5.623820243337235958, 62.47578838716487581, 12.27284524967300605 ) ) ;
#225=VERTEX_POINT ( 'NONE', #3915 ) ;
#226=CARTESIAN_POINT ( 'NONE',  ( -13.39469296682190347, 40.86889263995428934, -1.754359878167341513 ) ) ;
#228=CARTESIAN_POINT ( 'NONE',  ( -12.06034990428044118, 44.15344642025849708, 6.066424416400918673 ) ) ;
#230=CARTESIAN_POINT ( 'NONE',  ( -8.691771469529815392E-16, 38.67999999999999972, 14.19474002721660355 ) ) ;
#231=CARTESIAN_POINT ( 'NONE',  ( 4.171729424061791924, 45.03000000000000114, -12.83926296998457239 ) ) ;
#232=CARTESIAN_POINT ( 'NONE',  ( -13.49234022047965809, 70.91385223794031845, -0.4697109487732297195 ) ) ;
#234=CARTESIAN_POINT ( 'NONE',  ( -11.77082077961090967, 67.68472015259277441, -6.610832368286345684 ) ) ;
#236=CARTESIAN_POINT ( 'NONE',  ( 10.59104740856127513, 54.74884203901541468, -8.371597748919196391 ) ) ;
#237=EDGE_CURVE ( 'NONE', #1377, #15607, #758, .T. ) ;
#238=CARTESIAN_POINT ( 'NONE',  ( -3.290095754100384351, 64.29827642083250794, -13.09294913094749191 ) ) ;
#240=CARTESIAN_POINT ( 'NONE',  ( -4.171729424061791036, 64.53000000000000114, 12.83926296998457239 ) ) ;
#241=CARTESIAN_POINT ( 'NONE',  ( -12.55115401018059451, 35.11056623410730992, 4.971969969848257342 ) ) ;
#242=VECTOR ( 'NONE', #6179, 1000.000000000000000 ) ;
#243=ORIENTED_EDGE ( 'NONE', *, *, #10979, .T. ) ;
#244=CARTESIAN_POINT ( 'NONE',  ( 13.49341015684798428, 78.44682598755416336, -0.4906469715254504482 ) ) ;
#245=CARTESIAN_POINT ( 'NONE',  ( 4.171729424061789260, 49.82999999999999829, 12.83926296998457417 ) ) ;
#247=CARTESIAN_POINT ( 'NONE',  ( 4.352178298388634126, 73.02340726775082658, -12.78109873716751466 ) ) ;
#250=CARTESIAN_POINT ( 'NONE',  ( -8.343458848123582072, 68.38000000000000966, 11.48378591275254124 ) ) ;
#251=CARTESIAN_POINT ( 'NONE',  ( -11.21331758585850302, 52.64752326776081048, -7.517415214335143148 ) ) ;
#252=CARTESIAN_POINT ( 'NONE',  ( -11.76794919243112325, 45.07999999999999829, 3.823638476888994386 ) ) ;
#253=CARTESIAN_POINT ( 'NONE',  ( -13.50000000000000000, 63.92999999999999972, -3.306546357697853733E-15 ) ) ;
#256=CARTESIAN_POINT ( 'NONE',  ( 5.092513312360757105, 68.86389884904878045, 12.50266640507283000 ) ) ;
#259=CARTESIAN_POINT ( 'NONE',  ( -11.29815970959385041, 74.20716711713330938, 7.389293316686909030 ) ) ;
#260=CARTESIAN_POINT ( 'NONE',  ( -12.61936853585583940, 76.75616687913201019, -4.797075133751028453 ) ) ;
#266=CARTESIAN_POINT ( 'NONE',  ( -11.76794919243112325, 47.77999999999999403, -3.823638476888998827 ) ) ;
#268=CARTESIAN_POINT ( 'NONE',  ( 4.171729424061789260, 34.82999999999999829, 12.83926296998457417 ) ) ;
#269=CARTESIAN_POINT ( 'NONE',  ( 13.50148544713888299, 75.42278577149087937, 0.2035154836122704258 ) ) ;
#271=CARTESIAN_POINT ( 'NONE',  ( -12.43921031607001559, 41.12117747016043978, 5.245971347666045226 ) ) ;
#272=CARTESIAN_POINT ( 'NONE',  ( 1.218593159756304667, 52.13618204610553875, -13.44511257352553812 ) ) ;
#274=CARTESIAN_POINT ( 'NONE',  ( 8.248366389433876122, 36.86592902745724132, -10.68712329661759775 ) ) ;
#276=DIRECTION ( 'NONE',  ( 0.000000000000000000, -1.000000000000000000, 0.000000000000000000 ) ) ;
#278=CARTESIAN_POINT ( 'NONE',  ( -13.41492977785779850, 49.87660617796947093, -1.535378149569272654 ) ) ;
#279=CARTESIAN_POINT ( 'NONE',  ( 10.79904798291853396, 63.12286850203628319, 8.103746682478284669 ) ) ;
#280=CARTESIAN_POINT ( 'NONE',  ( 13.31859340417926241, 42.35255605562811354, 2.205733818516509182 ) ) ;
#281=CARTESIAN_POINT ( 'NONE',  ( 0.4450114281468046107, 38.69606526914740385, 13.49999999987193888 ) ) ;
#283=CARTESIAN_POINT ( 'NONE',  ( 3.636496289402154414, 72.83000000000001251, 11.19198476289190936 ) ) ;
#284=CARTESIAN_POINT ( 'NONE',  ( -3.533847551473688675, 70.30706370493864199, -13.03589947523510340 ) ) ;
#285=CARTESIAN_POINT ( 'NONE',  ( -12.50000000000000000, 98.93000000000002103, -8.999999999999996447 ) ) ;
#287=CARTESIAN_POINT ( 'NONE',  ( -11.15159978092055937, 43.64371703910293832, -7.608695226596760897 ) ) ;
#288=CARTESIAN_POINT ( 'NONE',  ( -7.500000000000000000, 106.2138518220599650, -8.084116494856630197 ) ) ;
#289=CARTESIAN_POINT ( 'NONE',  ( 10.55235452259542051, 60.75099516396964106, -8.420101235079211932 ) ) ;
#292=CARTESIAN_POINT ( 'NONE',  ( 13.45831588147710178, 66.39312768838394163, 1.061907957825456883 ) ) ;
#293=CARTESIAN_POINT ( 'NONE',  ( 10.60402044222889373, 57.11187693063078541, 8.355290479010609062 ) ) ;
#294=CARTESIAN_POINT ( 'NONE',  ( -3.636496289402153081, 56.32999999999999829, -11.19198476289190936 ) ) ;
#295=CARTESIAN_POINT ( 'NONE',  ( 11.76794919243112325, 64.28000000000000114, 3.823638476888996607 ) ) ;
#296=CARTESIAN_POINT ( 'NONE',  ( -12.44014281442525949, 47.12117745437350180, 5.246275075209847927 ) ) ;
#297=CARTESIAN_POINT ( 'NONE',  ( 5.553566080697077467, 45.97850270378070547, -12.30479239002528935 ) ) ;
#299=CARTESIAN_POINT ( 'NONE',  ( 0.2547235083979552117, 31.17084125670657357, -13.49760154729842476 ) ) ;
#300=CARTESIAN_POINT ( 'NONE',  ( -5.563626996627561994, 56.47811886027594142, 12.30024710206874694 ) ) ;
#302=CARTESIAN_POINT ( 'NONE',  ( -13.50000000000000000, 51.93000000000000682, -3.306546357697853733E-15 ) ) ;
#304=CARTESIAN_POINT ( 'NONE',  ( 1.276060874233202469, 32.72588244700077098, 13.43956583305223873 ) ) ;
#306=CARTESIAN_POINT ( 'NONE',  ( 4.086892649892674534, 40.03309646582929560, -12.86683993615205424 ) ) ;
#307=ORIENTED_EDGE ( 'NONE', *, *, #8201, .F. ) ;
#308=CARTESIAN_POINT ( 'NONE',  ( -5.300476046473269420, 62.48820044638870996, 12.41629279154124710 ) ) ;
#310=CARTESIAN_POINT ( 'NONE',  ( -13.46982610043145812, 40.96195804405107310, 0.9247321941779073073 ) ) ;
#312=CARTESIAN_POINT ( 'NONE',  ( -13.49104613329688007, 43.91131453512677751, -0.5374766152377549178 ) ) ;
#313=CARTESIAN_POINT ( 'NONE',  ( 13.50000000000000355, 65.57999999999998408, -4.386415899144233244 ) ) ;
#314=CARTESIAN_POINT ( 'NONE',  ( 4.171729424061791924, 31.02999999999999403, -12.83926296998457239 ) ) ;
#315=CARTESIAN_POINT ( 'NONE',  ( 4.171729424061791924, 48.02999999999999403, -12.83926296998457239 ) ) ;
#316=CARTESIAN_POINT ( 'NONE',  ( -9.629907599157546016, 46.56016663611932671, -9.461235684485890474 ) ) ;
#317=CARTESIAN_POINT ( 'NONE',  ( -11.63915563610238735, 67.67541942150826628, -6.840021065327532845 ) ) ;
#320=CARTESIAN_POINT ( 'NONE',  ( 12.41362727660819409, 54.23603978842571394, 5.323407497928233312 ) ) ;
#321=CARTESIAN_POINT ( 'NONE',  ( -4.350728866308207543, 64.33618153779571003, -12.78724907277022282 ) ) ;
#323=CARTESIAN_POINT ( 'NONE',  ( -8.343458848123582072, 64.37999999999998124, 11.48378591275253768 ) ) ;
#324=CARTESIAN_POINT ( 'NONE',  ( -13.25540151110283915, 35.02074204735390595, 2.572278351385800743 ) ) ;
#325=ORIENTED_EDGE ( 'NONE', *, *, #12398, .T. ) ;
#326=CARTESIAN_POINT ( 'NONE',  ( 12.90178577204087063, 78.28740904515449017, 3.975375597352175383 ) ) ;
#327=CARTESIAN_POINT ( 'NONE',  ( -7.500000000000000000, 98.93000000000002103, 1.224646799147353059E-15 ) ) ;
#328=CARTESIAN_POINT ( 'NONE',  ( -8.891200544363830713E-16, 37.67999999999999261, 13.50000000000000000 ) ) ;
#329=CARTESIAN_POINT ( 'NONE',  ( 11.03100386637765595, 72.72352357107607190, -7.783825102783979766 ) ) ;
#330=CARTESIAN_POINT ( 'NONE',  ( 2.306785515682943544, 79.09706103861046245, -13.30169983709586035 ) ) ;
#332=CARTESIAN_POINT ( 'NONE',  ( 13.50000000000000000, 63.42999999999999972, 1.653273178848926867E-15 ) ) ;
#333=CARTESIAN_POINT ( 'NONE',  ( -13.45789989295631983, 52.96690304976064567, 1.065472127645539890 ) ) ;
#334=CARTESIAN_POINT ( 'NONE',  ( 7.272992578804308828, 39.97999999999999687, 10.01041549318726709 ) ) ;
#336=CARTESIAN_POINT ( 'NONE',  ( 4.171729424061791924, 60.03000000000000114, -12.83926296998457239 ) ) ;
#337=CARTESIAN_POINT ( 'NONE',  ( -8.891200544363830713E-16, 34.67999999999999261, 13.50000000000000000 ) ) ;
#338=CARTESIAN_POINT ( 'NONE',  ( 5.057394672961640580, 68.86257603500035884, 12.51691328543133785 ) ) ;
#339=CARTESIAN_POINT ( 'NONE',  ( 0.000000000000000000, -1.200000000000000030E-05, 0.000000000000000000 ) ) ;
#342=CARTESIAN_POINT ( 'NONE',  ( -12.53724792357792417, 74.11243421711593271, 5.024370009789406843 ) ) ;
#343=CARTESIAN_POINT ( 'NONE',  ( -6.452387276988709175, 76.41704375434667895, -11.86051681251366574 ) ) ;
#344=DIRECTION ( 'NONE',  ( 0.000000000000000000, -1.000000000000000000, 0.000000000000000000 ) ) ;
#345=CARTESIAN_POINT ( 'NONE',  ( 12.50000000000000000, 98.93000000000002103, 9.000000000000000000 ) ) ;
#349=CARTESIAN_POINT ( 'NONE',  ( -9.520470885617717371, 33.22999999999999687, 6.917026985038133624 ) ) ;
#351=CARTESIAN_POINT ( 'NONE',  ( -9.367636073990613710, 32.31297664171835038, 9.721046613647347456 ) ) ;
#353=CARTESIAN_POINT ( 'NONE',  ( 11.98090966731797913, 75.20012104151170718, 6.225558393635502341 ) ) ;
#356=CARTESIAN_POINT ( 'NONE',  ( 5.883989548015875926, 30.92926152634062475, 10.19133431864935879 ) ) ;
#357=CARTESIAN_POINT ( 'NONE',  ( 4.171729424061791924, 84.03000000000000114, -12.83926296998457239 ) ) ;
#358=CARTESIAN_POINT ( 'NONE',  ( 4.717239269204677399, 52.01011083281174052, -12.64902143884823893 ) ) ;
#361=DIRECTION ( 'NONE',  ( 0.000000000000000000, 0.000000000000000000, 1.000000000000000000 ) ) ;
#364=CARTESIAN_POINT ( 'NONE',  ( 9.731717852235492572, 63.06533615564348594, 9.356802677010852776 ) ) ;
#365=CARTESIAN_POINT ( 'NONE',  ( 13.41797430850394690, 42.37741962985320043, 1.511824690427647111 ) ) ;
#366=CARTESIAN_POINT ( 'NONE',  ( 6.007520941189540054, 48.96077821041167510, -12.08973124302788449 ) ) ;
#369=CARTESIAN_POINT ( 'NONE',  ( -7.272992578804310604, 78.38000000000000966, 10.01041549318726886 ) ) ;
#373=ORIENTED_EDGE ( 'NONE', *, *, #8679, .F. ) ;
#374=CARTESIAN_POINT ( 'NONE',  ( -7.499999999999998224, 106.0143933292129503, -8.253836299850743075 ) ) ;
#375=CARTESIAN_POINT ( 'NONE',  ( 13.37389533385238671, 60.49657913131436970, -1.904068468163566230 ) ) ;
#379=CARTESIAN_POINT ( 'NONE',  ( 11.37538673181245130, 66.15763038601566848, 7.273122068539749741 ) ) ;
#380=CARTESIAN_POINT ( 'NONE',  ( 2.785878927130813844E-06, 56.68007738487546732, 13.49999999999942979 ) ) ;
#381=EDGE_CURVE ( 'NONE', #2740, #4566, #8901, .T. ) ;
#382=CARTESIAN_POINT ( 'NONE',  ( 7.272992578804308828, 57.97999999999999687, 10.01041549318726709 ) ) ;
#383=CARTESIAN_POINT ( 'NONE',  ( 13.49999999999999822, 35.28000000000000114, 4.386415899144237684 ) ) ;
#384=CARTESIAN_POINT ( 'NONE',  ( 2.272985001014427788E-15, 71.17999999999999261, -12.37355403259654985 ) ) ;
#385=CARTESIAN_POINT ( 'NONE',  ( -12.57369232349585175, 46.75164900414807789, -4.914502090225122188 ) ) ;
#386=CARTESIAN_POINT ( 'NONE',  ( 6.864326658960421490, 45.92603133891358169, -11.62547684485642030 ) ) ;
#388=CARTESIAN_POINT ( 'NONE',  ( 5.441320307982408622, 30.98247815750375977, -12.35517929490900535 ) ) ;
#389=CARTESIAN_POINT ( 'NONE',  ( -5.530913952003127854, 56.47938171940309360, 12.31500263983988397 ) ) ;
#391=CARTESIAN_POINT ( 'NONE',  ( -3.715634683528351356, 50.54639745666956685, 12.97889439479828688 ) ) ;
#392=FACE_OUTER_BOUND ( 'NONE', #17425, .T. ) ;
#396=CARTESIAN_POINT ( 'NONE',  ( -13.46679717695066003, 61.96273041894593803, 0.9463406209475275777 ) ) ;
#397=EDGE_LOOP ( 'NONE', ( #3454, #14162, #14933, #4128 ) ) ;
#400=CARTESIAN_POINT ( 'NONE',  ( -12.76959190857851212, 43.77205537680598724, -4.381403554202501383 ) ) ;
#402=CARTESIAN_POINT ( 'NONE',  ( -13.49999999999999822, 37.77999999999998693, -4.386415899144240349 ) ) ;
#403=CARTESIAN_POINT ( 'NONE',  ( -8.343458848123576743, 45.47999999999998977, -11.48378591275254301 ) ) ;
#405=CARTESIAN_POINT ( 'NONE',  ( -1.743841339441459137, 46.24267996541158965, -13.38863380285367910 ) ) ;
#406=CARTESIAN_POINT ( 'NONE',  ( -5.259139341736429607, 67.37018746444084627, -12.43396276512746823 ) ) ;
#408=CARTESIAN_POINT ( 'NONE',  ( 3.272540978394824940, 53.79766787922819304, 13.09734638618094138 ) ) ;
#409=CARTESIAN_POINT ( 'NONE',  ( -2.209888104562151234, 64.25951276812958213, -13.32892421627443724 ) ) ;
#410=ORIENTED_EDGE ( 'NONE', *, *, #17256, .F. ) ;
#411=CARTESIAN_POINT ( 'NONE',  ( -8.111752993934361555, 34.48789724560310788, -10.79119880849037472 ) ) ;
#413=CARTESIAN_POINT ( 'NONE',  ( 13.45153961929852748, 78.46975942807824822, -1.146847328308098879 ) ) ;
#416=VECTOR ( 'NONE', #15327, 1000.000000000000000 ) ;
#418=CARTESIAN_POINT ( 'NONE',  ( 13.42160645633606286, 72.48917881215648151, -1.700578753849256941 ) ) ;
#420=CARTESIAN_POINT ( 'NONE',  ( -4.171729424061787483, 58.32999999999999829, -12.83926296998457417 ) ) ;
#421=CARTESIAN_POINT ( 'NONE',  ( -13.46160622163430176, 52.96521979142928416, 1.017449871812443618 ) ) ;
#423=CARTESIAN_POINT ( 'NONE',  ( 3.636496289402154414, 39.82999999999999829, 11.19198476289190936 ) ) ;
#425=CARTESIAN_POINT ( 'NONE',  ( 8.343458848123578520, 55.97999999999998977, 11.48378591275254124 ) ) ;
#426=CARTESIAN_POINT ( 'NONE',  ( 1.511718349539964201, 50.73435581608389100, 13.41509433142833885 ) ) ;
#428=CARTESIAN_POINT ( 'NONE',  ( 4.442947237195123300, 68.83971558705859195, 12.75121963132532343 ) ) ;
#430=DIRECTION ( 'NONE',  ( 0.000000000000000000, 0.000000000000000000, -1.000000000000000000 ) ) ;
#432=CARTESIAN_POINT ( 'NONE',  ( -13.33044600843074612, 73.85509119750386731, -2.135332589583271545 ) ) ;
#433=CARTESIAN_POINT ( 'NONE',  ( -2.187775580252431684, 76.25866090160262445, -13.32182888840495139 ) ) ;
#434=DIRECTION ( 'NONE',  ( 1.000000000000000000, 0.000000000000000000, 0.000000000000000000 ) ) ;
#435=DIRECTION ( 'NONE',  ( 0.000000000000000000, 0.000000000000000000, -1.000000000000000000 ) ) ;
#438=CARTESIAN_POINT ( 'NONE',  ( 11.76794919243112325, 34.28000000000000114, 3.823638476888997051 ) ) ;
#440=CARTESIAN_POINT ( 'NONE',  ( -1.636861439990225930, 32.62114992449928508, 13.40040588940331112 ) ) ;
#441=CARTESIAN_POINT ( 'NONE',  ( 1.678346760273044636, 74.74034482231108711, 13.39582455766600866 ) ) ;
#443=CARTESIAN_POINT ( 'NONE',  ( -9.520470885617715595, 32.63000000000000256, -6.917026985038136289 ) ) ;
#444=CARTESIAN_POINT ( 'NONE',  ( -13.49999999999999822, 84.78000000000001535, -4.386415899144240349 ) ) ;
#445=CARTESIAN_POINT ( 'NONE',  ( 10.26872965863894471, 51.76653688478288018, -8.764966814524187910 ) ) ;
#447=CARTESIAN_POINT ( 'NONE',  ( -5.433831064015286927, 38.48323282879334073, 12.36477467734148483 ) ) ;
#448=CARTESIAN_POINT ( 'NONE',  ( 5.755010883477707395, 36.97068350995541408, -12.21187340796739207 ) ) ;
#451=CARTESIAN_POINT ( 'NONE',  ( 6.814633543800678872, 62.93188781794702180, 11.65614756620777115 ) ) ;
#452=CARTESIAN_POINT ( 'NONE',  ( 13.47189594166342097, 42.46064207325136408, -0.8869200912900612188 ) ) ;
#453=CARTESIAN_POINT ( 'NONE',  ( 10.86073516050613641, 48.73349978075351885, -8.018644299739561276 ) ) ;
#456=ORIENTED_EDGE ( 'NONE', *, *, #3724, .T. ) ;
#457=CARTESIAN_POINT ( 'NONE',  ( 7.272992578804308828, 66.98000000000000398, 10.01041549318726886 ) ) ;
#461=EDGE_LOOP ( 'NONE', ( #13360, #12852 ) ) ;
#463=FACE_OUTER_BOUND ( 'NONE', #11574, .T. ) ;
#467=CARTESIAN_POINT ( 'NONE',  ( 12.56982549204153976, 66.25104303858046251, 4.931975050715497133 ) ) ;
#468=CARTESIAN_POINT ( 'NONE',  ( 0.4447238818697385465, 56.69608407970753206, 13.49999999965100805 ) ) ;
#469=CARTESIAN_POINT ( 'NONE',  ( -9.520470885617717371, 57.23000000000000398, 6.917026985038133624 ) ) ;
#470=CARTESIAN_POINT ( 'NONE',  ( -7.272992578804307939, 65.48000000000000398, -10.01041549318726886 ) ) ;
#471=CARTESIAN_POINT ( 'NONE',  ( -13.45448328032910901, 46.96959999993933366, 1.138838731259335768 ) ) ;
#472=CARTESIAN_POINT ( 'NONE',  ( 9.149453984131964646, 45.82364388978120928, -9.926606263152381260 ) ) ;
#473=CARTESIAN_POINT ( 'NONE',  ( 4.340711467061829865, 70.02384940047436146, -12.81345992402683365 ) ) ;
#475=CARTESIAN_POINT ( 'NONE',  ( 10.77555668018642976, 30.73860136405477661, -8.141750913204777618 ) ) ;
#477=CARTESIAN_POINT ( 'NONE',  ( -3.318711775807452913, 50.56063369891364800, 13.08625922055076174 ) ) ;
#478=CARTESIAN_POINT ( 'NONE',  ( 12.85438585762840091, 33.28169117570074320, 4.130889853976885462 ) ) ;
#482=EDGE_CURVE ( 'NONE', #6493, #2917, #12344, .T. ) ;
#483=EDGE_LOOP ( 'NONE', ( #13081, #14244, #14288, #13557 ) ) ;
#484=CARTESIAN_POINT ( 'NONE',  ( -12.86035813447160514, 62.07770165908708293, 4.111105408976296616 ) ) ;
#485=ORIENTED_EDGE ( 'NONE', *, *, #139, .F. ) ;
#488=CARTESIAN_POINT ( 'NONE',  ( 10.82670249703553722, 48.12451974694700141, 8.064369848088544401 ) ) ;
#490=CARTESIAN_POINT ( 'NONE',  ( 10.92172942406178926, 33.13000000000000256, 7.935100905948387684 ) ) ;
#491=CARTESIAN_POINT ( 'NONE',  ( 8.343458848123578520, 40.97999999999998977, 11.48378591275254124 ) ) ;
#492=CARTESIAN_POINT ( 'NONE',  ( -0.5656080267661869332, 46.20032726311463733, -13.48884909811126676 ) ) ;
#493=CARTESIAN_POINT ( 'NONE',  ( -11.00247426292009933, 67.63473743967996654, -7.822801183469714204 ) ) ;
#495=CARTESIAN_POINT ( 'NONE',  ( 9.838722238819098465, 54.07056626371765162, 9.256620450124710686 ) ) ;
#496=ORIENTED_EDGE ( 'NONE', *, *, #13515, .F. ) ;
#497=CARTESIAN_POINT ( 'NONE',  ( -2.994742845161742384, 64.28778625662059198, -13.16386178499985782 ) ) ;
#499=ORIENTED_EDGE ( 'NONE', *, *, #16100, .T. ) ;
#501=CARTESIAN_POINT ( 'NONE',  ( -10.71871353429217244, 34.61762525966922510, -8.218939176556370185 ) ) ;
#503=CARTESIAN_POINT ( 'NONE',  ( 10.91305626273815577, 78.12916640448000294, 7.952299940727153960 ) ) ;
#505=CARTESIAN_POINT ( 'NONE',  ( 11.90602345876549073, 72.66532707484691400, -6.363701510510520798 ) ) ;
#507=CARTESIAN_POINT ( 'NONE',  ( -13.49999999999999822, 59.07999999999999119, 4.386415899144235908 ) ) ;
#508=CARTESIAN_POINT ( 'NONE',  ( -4.120143485240188141, 52.32813700730908835, -12.85633956262296174 ) ) ;
#509=CARTESIAN_POINT ( 'NONE',  ( -11.76794919243112325, 35.77999999999999403, -3.823638476888998827 ) ) ;
#510=CARTESIAN_POINT ( 'NONE',  ( 13.50000000000000355, 59.57999999999999829, -4.386415899144233244 ) ) ;
#513=CARTESIAN_POINT ( 'NONE',  ( 7.978366338076175346, 68.98190559513436426, 10.89111902590045489 ) ) ;
#514=DIRECTION ( 'NONE',  ( 0.000000000000000000, 0.000000000000000000, 1.000000000000000000 ) ) ;
#515=CARTESIAN_POINT ( 'NONE',  ( -8.343458848123578520, 72.48000000000000398, -11.48378591275254124 ) ) ;
#517=CARTESIAN_POINT ( 'NONE',  ( -11.11816795611437669, 73.64147893977222736, -7.662807821280736675 ) ) ;
#519=ADVANCED_FACE ( 'NONE', ( #7494 ), #12874, .T. ) ;
#521=FACE_OUTER_BOUND ( 'NONE', #11792, .T. ) ;
#522=CARTESIAN_POINT ( 'NONE',  ( -1.245860404445607248E-06, 40.18000018109674443, -13.49999999999994316 ) ) ;
#524=CARTESIAN_POINT ( 'NONE',  ( 11.76794919243112325, 40.42999999999999972, 1.441158131103945434E-15 ) ) ;
#525=CARTESIAN_POINT ( 'NONE',  ( -11.27597249832626680, 32.20855542261740823, 7.423102544681950299 ) ) ;
#526=CARTESIAN_POINT ( 'NONE',  ( 8.989377126757293723, 75.02817402051516638, 10.09332704491346178 ) ) ;
#527=CARTESIAN_POINT ( 'NONE',  ( 4.171729424061789260, 61.82999999999999829, 12.83926296998457417 ) ) ;
#530=CARTESIAN_POINT ( 'NONE',  ( -10.92172942406178926, 84.62999999999999545, -7.935100905948389460 ) ) ;
#531=CARTESIAN_POINT ( 'NONE',  ( 0.9721905075920033168, 52.14504527273197709, -13.46523144585630405 ) ) ;
#532=CARTESIAN_POINT ( 'NONE',  ( -4.278914508684592555, 38.52614286959915546, 12.80401563806038467 ) ) ;
#533=CARTESIAN_POINT ( 'NONE',  ( 8.272675178529885542, 36.86482438541639794, -10.66831387527186870 ) ) ;
#535=CARTESIAN_POINT ( 'NONE',  ( -1.117795391647952385, 49.22012975758181597, -13.45637554176790474 ) ) ;
#536=CARTESIAN_POINT ( 'NONE',  ( 11.32484296497576182, 63.15460178810015890, 7.350387779789046228 ) ) ;
#537=CARTESIAN_POINT ( 'NONE',  ( 1.536173093022593195, 41.73525089061148918, 13.41486744188283353 ) ) ;
#538=CARTESIAN_POINT ( 'NONE',  ( 7.996676220521883316, 48.87726588079390666, -10.87843020462947408 ) ) ;
#539=CIRCLE ( 'NONE', #3640, 5.000000000000000000 ) ;
#542=CARTESIAN_POINT ( 'NONE',  ( -3.636496289402155746, 66.53000000000000114, 11.19198476289190936 ) ) ;
#547=CARTESIAN_POINT ( 'NONE',  ( -8.711848673603300952, 80.92999999999996419, -8.870066681593291591 ) ) ;
#550=CARTESIAN_POINT ( 'NONE',  ( 11.01344701655966141, 66.13478396425333017, 7.819520221991368203 ) ) ;
#551=CARTESIAN_POINT ( 'NONE',  ( 4.171729424061791924, 82.03000000000000114, -12.83926296998457239 ) ) ;
#552=CARTESIAN_POINT ( 'NONE',  ( 11.76794919243112325, 64.28000000000000114, 3.823638476888996607 ) ) ;
#553=CARTESIAN_POINT ( 'NONE',  ( 0.2252273365623476686, 31.65984393938649433, 15.45843899586302150 ) ) ;
#554=CARTESIAN_POINT ( 'NONE',  ( 3.636496289402154414, 60.82999999999999829, 11.19198476289190936 ) ) ;
#555=CARTESIAN_POINT ( 'NONE',  ( -12.02347592906994223, 46.70319524133616795, -6.153424168697559260 ) ) ;
#557=AXIS2_PLACEMENT_3D ( 'NONE', #4417, #434, #9826 ) ;
#559=CARTESIAN_POINT ( 'NONE',  ( 11.57959441606064210, 45.68864039077092798, -6.943265149869812802 ) ) ;
#560=CARTESIAN_POINT ( 'NONE',  ( 0.2775435840573023394, 70.17002100411404797, -13.49725908783516992 ) ) ;
#562=CARTESIAN_POINT ( 'NONE',  ( 5.567119034035452607, 30.97772632656147351, -12.29926522190035598 ) ) ;
#563=CARTESIAN_POINT ( 'NONE',  ( -13.34493095579965249, 55.85834049113790911, -2.045602713796132122 ) ) ;
#564=CARTESIAN_POINT ( 'NONE',  ( -2.048896823861042105, 50.60635182041035307, 13.34364247030556250 ) ) ;
#565=CARTESIAN_POINT ( 'NONE',  ( 7.866633879235673810, 32.97690999812699175, 10.98016867868767577 ) ) ;
#567=CARTESIAN_POINT ( 'NONE',  ( 12.02160876111696197, 39.65648020511805782, -6.142793857136727986 ) ) ;
#568=VERTEX_POINT ( 'NONE', #11553 ) ;
#569=CARTESIAN_POINT ( 'NONE',  ( -8.701713178450388497, 62.34501137507039203, 10.32135525206011728 ) ) ;
#570=ORIENTED_EDGE ( 'NONE', *, *, #3900, .F. ) ;
#571=CARTESIAN_POINT ( 'NONE',  ( -13.11924471136216397, 40.81678185826124405, -3.187056428934428087 ) ) ;
#574=CARTESIAN_POINT ( 'NONE',  ( 13.15187946546656050, 48.32156802418281671, 3.057686379087630968 ) ) ;
#576=CARTESIAN_POINT ( 'NONE',  ( 13.50000000000000355, 36.57999999999999119, -4.386415899144233244 ) ) ;
#577=CARTESIAN_POINT ( 'NONE',  ( -0.01842263577481551701, 46.18066228095146641, -13.49998821522327752 ) ) ;
#580=CARTESIAN_POINT ( 'NONE',  ( 6.577638901403147109, 53.92217061882819706, 11.78917697844675594 ) ) ;
#581=EDGE_LOOP ( 'NONE', ( #8546, #6039, #16821, #16086 ) ) ;
#582=CARTESIAN_POINT ( 'NONE',  ( -8.480464519948240465, 64.50466462916871535, -10.50531813445047113 ) ) ;
#584=CARTESIAN_POINT ( 'NONE',  ( 3.388210979464494343, 67.05813739842785992, -13.07109493271608436 ) ) ;
#585=CARTESIAN_POINT ( 'NONE',  ( -5.518765897211704186, 34.38014941849128547, -12.32043976184162837 ) ) ;
#587=CARTESIAN_POINT ( 'NONE',  ( 4.034064007385466333, 77.82502602479080167, 12.88362052288852055 ) ) ;
#590=CYLINDRICAL_SURFACE ( 'NONE', #10543, 13.50000000000000000 ) ;
#591=CARTESIAN_POINT ( 'NONE',  ( 11.10478898303382067, 72.14066452316153288, 7.682293661016322162 ) ) ;
#593=CARTESIAN_POINT ( 'NONE',  ( -4.171729424061787483, 67.32999999999999829, -12.83926296998457417 ) ) ;
#594=CARTESIAN_POINT ( 'NONE',  ( -4.026030641589963821, 52.32476109287100741, -12.88609862687250285 ) ) ;
#596=CARTESIAN_POINT ( 'NONE',  ( 7.272992578804311492, 34.87999999999999545, -10.01041549318726709 ) ) ;
#597=CARTESIAN_POINT ( 'NONE',  ( 13.49999999999999822, 53.27999999999998693, 4.386415899144237684 ) ) ;
#598=CARTESIAN_POINT ( 'NONE',  ( -8.891200544363830713E-16, 49.67999999999999261, 13.50000000000000000 ) ) ;
#600=CARTESIAN_POINT ( 'NONE',  ( 9.993611225536259468, 69.07888461794802026, 9.076221008718828642 ) ) ;
#604=CARTESIAN_POINT ( 'NONE',  ( -10.51965532506071455, 73.60722549432360040, -8.461029959376727305 ) ) ;
#611=CARTESIAN_POINT ( 'NONE',  ( -11.76794919243112325, 41.92999999999999261, -2.882316262207890869E-15 ) ) ;
#612=CARTESIAN_POINT ( 'NONE',  ( -11.27205087680846773, 32.20880266355328558, 7.429057979085468943 ) ) ;
#613=CARTESIAN_POINT ( 'NONE',  ( 2.274101073109970006, 74.76175775842119720, 13.30899290276055069 ) ) ;
#616=CARTESIAN_POINT ( 'NONE',  ( -8.343458848123582072, 79.37999999999999545, 11.48378591275254124 ) ) ;
#617=EDGE_CURVE ( 'NONE', #11528, #3781, #9980, .T. ) ;
#618=CARTESIAN_POINT ( 'NONE',  ( 9.922981821730571639, 51.78482716919520357, -9.154569396628096101 ) ) ;
#620=CARTESIAN_POINT ( 'NONE',  ( 1.759800498587698492, 37.11690690510804558, -13.39206196151561912 ) ) ;
#621=DIRECTION ( 'NONE',  ( 0.000000000000000000, 0.000000000000000000, -1.000000000000000000 ) ) ;
#622=CARTESIAN_POINT ( 'NONE',  ( 8.549612433556128696E-08, 65.68000242247177312, 13.49999999999999822 ) ) ;
#623=VECTOR ( 'NONE', #13863, 1000.000000000000000 ) ;
#624=CARTESIAN_POINT ( 'NONE',  ( 7.135932271715804909, 62.94537907865952064, 11.45987087908721769 ) ) ;
#625=CARTESIAN_POINT ( 'NONE',  ( 2.967265984436029846, 41.78676304960944066, 13.16990152412644477 ) ) ;
#626=CARTESIAN_POINT ( 'NONE',  ( 10.00082048966772952, 48.78101140217790288, -9.079552510824187905 ) ) ;
#629=CARTESIAN_POINT ( 'NONE',  ( -3.636496289402155746, 69.53000000000001535, 11.19198476289190936 ) ) ;
#632=CARTESIAN_POINT ( 'NONE',  ( -2.081804195782924971, 43.25485282119976205, -13.33860214849647718 ) ) ;
#635=CARTESIAN_POINT ( 'NONE',  ( 12.91505872096568908, 66.28907917036056574, 3.930856618993244567 ) ) ;
#637=CARTESIAN_POINT ( 'NONE',  ( 9.520470885617717371, 46.73000000000000398, -6.917026985038131848 ) ) ;
#638=CARTESIAN_POINT ( 'NONE',  ( 9.235079662642815990, 32.03187319105528985, 10.25657514373247992 ) ) ;
#639=CARTESIAN_POINT ( 'NONE',  ( -7.272992578804307939, 56.47999999999998977, -10.01041549318726886 ) ) ;
#641=CARTESIAN_POINT ( 'NONE',  ( -10.67851723851311974, 46.61476266519934342, -8.293634792068681705 ) ) ;
#642=CARTESIAN_POINT ( 'NONE',  ( 5.599984837145694172, 45.97674325351677282, -12.28377481317420816 ) ) ;
#643=CARTESIAN_POINT ( 'NONE',  ( 7.438616558803111900, 69.90178393563131465, -11.26982506745944512 ) ) ;
#645=CARTESIAN_POINT ( 'NONE',  ( 10.32066366485157616, 30.76371262851852606, -8.702842429855374817 ) ) ;
#646=CARTESIAN_POINT ( 'NONE',  ( -11.08589355985044911, 56.22027713396840198, 7.704122408052090698 ) ) ;
#647=CARTESIAN_POINT ( 'NONE',  ( -2.103279777628626945, 50.60437299590867610, 13.33515391181352605 ) ) ;
#648=CARTESIAN_POINT ( 'NONE',  ( 2.327276230778790644, 32.76365894630023234, 13.30533770644748159 ) ) ;
#649=CARTESIAN_POINT ( 'NONE',  ( 3.628474543935842789, 43.04958345259967700, -13.00536312147723095 ) ) ;
#650=CARTESIAN_POINT ( 'NONE',  ( 12.21724735566978204, 39.64072623559641073, -5.747072418630094326 ) ) ;
#651=ORIENTED_EDGE ( 'NONE', *, *, #15700, .T. ) ;
#652=CARTESIAN_POINT ( 'NONE',  ( -13.47981080816064825, 61.90441198062364236, -0.7403440101722559286 ) ) ;
#658=CARTESIAN_POINT ( 'NONE',  ( 13.04930443264937523, 48.30669093399095004, 3.459466926551658439 ) ) ;
#659=CARTESIAN_POINT ( 'NONE',  ( 8.527674399818419460, 57.85321952167059578, -10.46888370426456305 ) ) ;
#660=CARTESIAN_POINT ( 'NONE',  ( 7.403926216836778984, 78.90321946119443908, -11.28912104649029047 ) ) ;
#661=CARTESIAN_POINT ( 'NONE',  ( -7.272992578804310604, 81.38000000000000966, 10.01041549318726709 ) ) ;
#662=CARTESIAN_POINT ( 'NONE',  ( 8.343458848123578520, 37.98000000000000398, 11.48378591275254124 ) ) ;
#667=CARTESIAN_POINT ( 'NONE',  ( 3.259877015350815199, 53.79722067765693083, 13.10050803911334327 ) ) ;
#668=VERTEX_POINT ( 'NONE', #841 ) ;
#669=LINE ( 'NONE', #8991, #3297 ) ;
#670=ORIENTED_EDGE ( 'NONE', *, *, #3900, .T. ) ;
#672=CARTESIAN_POINT ( 'NONE',  ( -5.523541487972947195, 34.38033358995659938, -12.31829916344299214 ) ) ;
#675=CARTESIAN_POINT ( 'NONE',  ( 4.443323578948271901, 77.83982787778398915, 12.74793837166312827 ) ) ;
#678=DIRECTION ( 'NONE',  ( 1.224646799147353207E-16, 0.000000000000000000, -1.000000000000000000 ) ) ;
#679=CARTESIAN_POINT ( 'NONE',  ( 13.37510286910101520, 72.36596172307848462, 1.832109072391795879 ) ) ;
#681=CARTESIAN_POINT ( 'NONE',  ( 2.607531440858944223E-15, 67.17999999999999261, -14.19474002721660355 ) ) ;
#682=CARTESIAN_POINT ( 'NONE',  ( -0.09279092634077520940, 71.67666048054469741, 13.49999999999947420 ) ) ;
#684=CARTESIAN_POINT ( 'NONE',  ( -10.92172942406178926, 57.63000000000000256, -7.935100905948389460 ) ) ;
#687=CARTESIAN_POINT ( 'NONE',  ( 2.924053257345435538E-06, 68.68008145904181561, 13.49999999999936584 ) ) ;
#691=CARTESIAN_POINT ( 'NONE',  ( -13.49546379884621672, 73.91715910944417089, -0.3713218310782592235 ) ) ;
#692=CARTESIAN_POINT ( 'NONE',  ( -11.51278214438144865, 65.19318789086543120, 7.050241511786378368 ) ) ;
#698=CARTESIAN_POINT ( 'NONE',  ( -3.636496289402155746, 39.52999999999999403, 11.19198476289190936 ) ) ;
#700=CARTESIAN_POINT ( 'NONE',  ( 13.50000000000000355, 80.57999999999998408, -4.386415899144233244 ) ) ;
#701=CARTESIAN_POINT ( 'NONE',  ( -13.47700622531958281, 31.90260597682616961, -0.7909189831980687480 ) ) ;
#702=CARTESIAN_POINT ( 'NONE',  ( 8.411976504965995360, 75.00153989494273787, 10.55890256502399893 ) ) ;
#703=CARTESIAN_POINT ( 'NONE',  ( -0.1736909584870764689, 53.67375392313818594, 13.49917744846566947 ) ) ;
#704=CARTESIAN_POINT ( 'NONE',  ( -13.49999999999999822, 78.78000000000001535, -4.386415899144240349 ) ) ;
#705=CARTESIAN_POINT ( 'NONE',  ( 12.64183604165299002, 51.60150530966055982, -4.736456310785323254 ) ) ;
#706=( BOUNDED_CURVE ( )  B_SPLINE_CURVE ( 2, ( #9426, #14775, #11974, #14606, #5437, #2665, #14858, #8096, #31, #10824, #16186, #2488, #1184 ),
 .UNSPECIFIED., .F., .F. ) 
 B_SPLINE_CURVE_WITH_KNOTS ( ( 3, 2, 2, 2, 2, 2, 3 ),
 ( 0.8472222222222222099, 0.8499999999999999778, 0.8555555555555555136, 0.8611111111111111605, 0.8666666666666666963, 0.8722222222222222321, 0.8750000000000000000 ),
 .UNSPECIFIED. ) 
 CURVE ( )  GEOMETRIC_REPRESENTATION_ITEM ( )  RATIONAL_B_SPLINE_CURVE ( ( 0.9755282581475768211, 0.9755282581475768211, 1.000000000000000000, 0.9510565162951535312, 1.000000000000000000, 0.9510565162951535312, 1.000000000000000000, 0.9510565162951535312, 1.000000000000000000, 0.9510565162951535312, 1.000000000000000000, 0.9755282581475768211, 0.9755282581475768211 ) ) 
 REPRESENTATION_ITEM ( '' )  );
#707=CARTESIAN_POINT ( 'NONE',  ( -10.76081525048536669, 38.23950894326511474, 8.153236926004757024 ) ) ;
#708=CARTESIAN_POINT ( 'NONE',  ( 10.70183563093194756, 36.74286887062785212, -8.241591107763712287 ) ) ;
#711=CARTESIAN_POINT ( 'NONE',  ( -0.1280143735402073379, 49.18460186041409088, -13.49947902730419003 ) ) ;
#712=CARTESIAN_POINT ( 'NONE',  ( 1.753268986668952691E-06, 80.68004880551006863, 13.49999999999977263 ) ) ;
#713=CARTESIAN_POINT ( 'NONE',  ( 4.918125156431671030, 41.85716231917498931, 12.58089576358123018 ) ) ;
#714=CARTESIAN_POINT ( 'NONE',  ( 13.49969884940630749, 48.42553229603143450, 0.1310880700171220270 ) ) ;
#717=VERTEX_POINT ( 'NONE', #5009 ) ;
#718=CARTESIAN_POINT ( 'NONE',  ( -11.76794919243112325, 62.78000000000000114, -3.823638476888998827 ) ) ;
#720=CARTESIAN_POINT ( 'NONE',  ( 4.171729424061789260, 55.83000000000000540, 12.83926296998457417 ) ) ;
#723=CARTESIAN_POINT ( 'NONE',  ( 0.8979998255002190621, 76.14771127606977075, -13.47011368339567028 ) ) ;
#724=CARTESIAN_POINT ( 'NONE',  ( 9.520470885617715595, 34.13000000000000256, 6.917026985038134512 ) ) ;
#726=CARTESIAN_POINT ( 'NONE',  ( 10.18058291654429226, 66.08880080020819037, 8.866023803930167091 ) ) ;
#727=CARTESIAN_POINT ( 'NONE',  ( -8.343458848123576743, 79.48000000000000398, -11.48378591275254301 ) ) ;
#729=CARTESIAN_POINT ( 'NONE',  ( 3.636496289402157078, 53.03000000000000114, -11.19198476289190936 ) ) ;
#731=CARTESIAN_POINT ( 'NONE',  ( -12.66924821184278471, 59.09957427317683454, 4.683659793808636174 ) ) ;
#732=CARTESIAN_POINT ( 'NONE',  ( 13.11471341724209339, 45.54378698212244103, -3.202259077053928760 ) ) ;
#733=CARTESIAN_POINT ( 'NONE',  ( 10.13354921526377694, 69.77373695534940623, -8.919712814319055383 ) ) ;
#735=CARTESIAN_POINT ( 'NONE',  ( 13.16708594564997625, 30.53565923579080632, -2.981442588050036147 ) ) ;
#736=CARTESIAN_POINT ( 'NONE',  ( -13.25266014676319948, 55.83927541273924788, -2.572670256372855402 ) ) ;
#737=CARTESIAN_POINT ( 'NONE',  ( 0.000000000000000000, 80.93000000000000682, 0.000000000000000000 ) ) ;
#738=CARTESIAN_POINT ( 'NONE',  ( 9.851210787350034082, 63.78852028479234093, -9.230592214737045609 ) ) ;
#739=CARTESIAN_POINT ( 'NONE',  ( 5.548650298709674189, 42.97870115387426893, -12.30718966409141402 ) ) ;
#740=CARTESIAN_POINT ( 'NONE',  ( 10.20108122339417633, 39.77014993735368620, -8.842797910576575049 ) ) ;
#741=ORIENTED_EDGE ( 'NONE', *, *, #14173, .F. ) ;
#742=CARTESIAN_POINT ( 'NONE',  ( -9.821826846477060613, 62.29041452375334842, 9.272265874321597323 ) ) ;
#743=VERTEX_POINT ( 'NONE', #8020 ) ;
#744=EDGE_CURVE ( 'NONE', #9540, #568, #8793, .T. ) ;
#745=ORIENTED_EDGE ( 'NONE', *, *, #12188, .T. ) ;
#748=CARTESIAN_POINT ( 'NONE',  ( 6.741581593082713653, 47.92895949507889242, 11.69643156837649656 ) ) ;
#749=CARTESIAN_POINT ( 'NONE',  ( 10.51843927637086651, 57.75287643017565387, -8.462433850046046757 ) ) ;
#750=CARTESIAN_POINT ( 'NONE',  ( 4.994996160112292749, 78.99980127340818115, -12.54197035550941841 ) ) ;
#751=CARTESIAN_POINT ( 'NONE',  ( 2.272985001014427788E-15, 83.17999999999999261, -12.37355403259654985 ) ) ;
#756=CARTESIAN_POINT ( 'NONE',  ( 11.45940115419385208, 54.16325699306285912, 7.140252089711898620 ) ) ;
#758=B_SPLINE_CURVE_WITH_KNOTS ( 'NONE', 3,
 ( #15839, #9332, #3744, #9160, #14508, #1088, #6502, #17260, #5172, #15924, #7913, #3833, #11968, #14600, #13288, #1176, #17348, #5259, #2569, #7999, #6667, #12051, #17429, #10728, #16093, #22, #15027, #8086, #7022, #13451, #113, #11079, #11166, #2743, #1516, #16452, #8173, #5781, #1691, #4448, #12133, #9855, #12219, #1606, #6754, #5425, #4087, #9764, #12490, #1426, #9503, #10901, #204, #4355, #289, #6843, #16272, #5610, #15109, #5698, #5519, #1337, #13623, #8263, #2657, #12401, #13706, #10991, #2920, #13537, #6932, #10814, #14940, #8350, #16177, #14850, #3008, #4178, #9590, #2832, #8438, #7106, #12310, #16360, #375, #4267, #9677, #13792, #16541, #7348, #15612, #9199, #11663, #8934, #3607, #7604, #7867, #5032, #14293, #7690, #3520, #11749, #5212, #10602, #4857, #3870, #15966, #10432, #14463, #12899, #12982, #13069, #14637, #865, #2352, #1129, #2524, #2178, #11837, #11921, #10345, #6193, #6541, #954, #15879, #6275, #6366, #15791, #4944, #9285, #15699, #14550, #11580, #9018, #17039, #14375, #16955, #2263, #3698, #10260, #13156, #3786, #9111, #7784, #1042, #17214, #5125, #2435, #13241, #17300, #10947, #9720, #4308, #1558, #13323, #5302, #2788, #1215, #12263, #6626, #5383, #13663, #14719, #9545, #2608, #12005, #8127, #12087, #10684, #16314, #15066, #7952, #17470, #6890, #17387, #16050, #9370, #14983 ),
 .UNSPECIFIED., .F., .F.,
 ( 4, 2, 2, 2, 2, 2, 1, 1, 1, 1, 2, 1, 2, 2, 1, 1, 2, 2, 2, 2, 1, 1, 1, 1, 2, 2, 1, 1, 1, 2, 2, 2, 2, 1, 2, 2, 1, 1, 1, 1, 1, 1, 2, 2, 1, 2, 2, 2, 1, 2, 2, 1, 1, 2, 2, 2, 2, 1, 2, 2, 2, 2, 2, 1, 2, 2, 1, 2, 2, 2, 2, 2, 2, 1, 1, 2, 2, 2, 2, 1, 2, 2, 1, 1, 2, 2, 2, 1, 1, 2, 2, 2, 1, 1, 2, 2, 2, 2, 2, 1, 1, 1, 1, 1, 1, 2, 2, 1, 2, 2, 4 ),
 ( 0.3872708296481242041, 0.3881928204034852392, 0.3891148111588463299, 0.3893453088476865886, 0.3894029332698966672, 0.3894173393754491452, 0.3894317454810016788, 0.3894605576921067458, 0.3895758065365268474, 0.3900368019142073650, 0.3904977972918879381, 0.3906130461363080397, 0.3906418583474131068, 0.3906562644529655848, 0.3906706705585181183, 0.3907282949807281969, 0.3909587926695684557, 0.3918807834249295463, 0.3918951895304820243, 0.3919095956360345578, 0.3919384078471396249, 0.3919960322693496479, 0.3921112811137698051, 0.3923417788026100639, 0.3928027741802905815, 0.3937247649356516721, 0.3941857603133321897, 0.3943010091577523468, 0.3943586335799624254, 0.3943874457910674369, 0.3944162580021724485, 0.3946467556910127072, 0.3955687464463736869, 0.3956263708685837654, 0.3956551830796887770, 0.3956839952907937885, 0.3957992441352139457, 0.3960297418240542044, 0.3964907372017347220, 0.3967212348905749808, 0.3968364837349951380, 0.3968941081572052165, 0.3969085142627576945, 0.3969229203683102281, 0.3969517325794152396, 0.3974127279570957572, 0.3983347187124566813, 0.3992567094678176609, 0.3993719583122378181, 0.3994007705233428296, 0.3994151766288953631, 0.3994295827344478411, 0.3994872071566579197, 0.3997177048454981785, 0.4001787002231786405, 0.4011006909785396202, 0.4015616863562200822, 0.4017921840450603410, 0.4019074328894804427, 0.4019650573116905212, 0.4020226817339005443, 0.4038666632446225035, 0.4043276586223029656, 0.4043852830445130442, 0.4044140952556180557, 0.4044429074667230672, 0.4045581563111432244, 0.4047886539999834277, 0.4057106447553444073, 0.4066326355107053869, 0.4068631331995455902, 0.4069207576217556688, 0.4069351637273082023, 0.4069495698328606803, 0.4069783820439656918, 0.4070936308883857935, 0.4075546262660660890, 0.4080156216437463290, 0.4081308704881664307, 0.4081596826992714422, 0.4081668857520476812, 0.4081740888048239202, 0.4081884949103764537, 0.4082461193325864768, 0.4084766170214266245, 0.4093986077767871601, 0.4095138566212072617, 0.4096291054656273078, 0.4098596031544674556, 0.4103205985321477511, 0.4112425892875082867, 0.4117035846651885822, 0.4118188335096086283, 0.4118764579318186514, 0.4119052701429236629, 0.4119340823540286745, 0.4121645800428688222, 0.4130865707982294133, 0.4132018196426495149, 0.4133170684870696165, 0.4135475661759097088, 0.4140085615535900043, 0.4142390592424301521, 0.4143543080868502537, 0.4144119325090602768, 0.4144263386146128103, 0.4144407447201652883, 0.4144695569312702998, 0.4149305523089505399, 0.4158525430643110199, 0.4167745338196714999 ),
 .UNSPECIFIED. ) ;
#760=VERTEX_POINT ( 'NONE', #15288 ) ;
#761=CARTESIAN_POINT ( 'NONE',  ( 7.444293037381387812, 66.90149083381143669, -11.26317529503627313 ) ) ;
#763=CARTESIAN_POINT ( 'NONE',  ( 0.000000000000000000, 80.93000000000000682, 0.000000000000000000 ) ) ;
#764=CARTESIAN_POINT ( 'NONE',  ( -2.148228375852590410, 59.60282902806525840, 13.33692188568706705 ) ) ;
#767=CARTESIAN_POINT ( 'NONE',  ( 11.75193945976005239, 72.67664319563640163, -6.644281148718726548 ) ) ;
#769=CARTESIAN_POINT ( 'NONE',  ( 4.171729424061791924, 49.02999999999999403, -12.83926296998457239 ) ) ;
#770=CARTESIAN_POINT ( 'NONE',  ( -0.3780938980182780851, 71.66640514842048049, 13.49470503427916945 ) ) ;
#771=CARTESIAN_POINT ( 'NONE',  ( -8.691771469529815392E-16, 52.67999999999999261, 14.19474002721660355 ) ) ;
#772=CARTESIAN_POINT ( 'NONE',  ( 2.138189944381248875, 76.75688142232026223, 13.49999999999999645 ) ) ;
#774=CARTESIAN_POINT ( 'NONE',  ( 1.966889197916937837, 68.75072210823383045, 13.35595523036250576 ) ) ;
#778=CARTESIAN_POINT ( 'NONE',  ( -5.177089779691129046, 65.49289956726600792, 12.46787024327672633 ) ) ;
#782=CARTESIAN_POINT ( 'NONE',  ( -9.520470885617715595, 32.63000000000000256, -6.917026985038136289 ) ) ;
#783=CARTESIAN_POINT ( 'NONE',  ( -3.042841478767011054, 40.28940726252261584, -13.15311736850856938 ) ) ;
#784=CARTESIAN_POINT ( 'NONE',  ( -12.03159204543364780, 32.15617227854212246, 6.137766210929217259 ) ) ;
#785=CARTESIAN_POINT ( 'NONE',  ( 3.375819219972439278, 74.80137919260076274, 13.07174965501556230 ) ) ;
#787=CARTESIAN_POINT ( 'NONE',  ( 13.46198083254162725, 51.46580788858824462, -1.034634726011374184 ) ) ;
#788=CARTESIAN_POINT ( 'NONE',  ( -11.18084545031510402, 38.21448949798586625, 7.565677266412778046 ) ) ;
#789=CARTESIAN_POINT ( 'NONE',  ( 12.44984635716159715, 36.62057801016818104, -5.234570041864336609 ) ) ;
#792=CARTESIAN_POINT ( 'NONE',  ( -7.030094859684152375, 77.41919333245768087, 11.52885090067665175 ) ) ;
#794=CARTESIAN_POINT ( 'NONE',  ( 0.2843415538626123951, 41.69023294723046291, 13.49779373366518698 ) ) ;
#795=CARTESIAN_POINT ( 'NONE',  ( 12.23498167705813344, 48.63917152218695605, -5.705760255632154276 ) ) ;
#798=CARTESIAN_POINT ( 'NONE',  ( 9.520470885617715595, 70.12999999999999545, 6.917026985038134512 ) ) ;
#802=CARTESIAN_POINT ( 'NONE',  ( -11.52888015854885317, 80.93000000000003524, -3.329402692648984363 ) ) ;
#806=CARTESIAN_POINT ( 'NONE',  ( 3.636496289402157078, 50.03000000000000114, -11.19198476289190936 ) ) ;
#807=CARTESIAN_POINT ( 'NONE',  ( -13.48016638762386599, 58.90472283406352716, -0.7316414589621201836 ) ) ;
#808=CARTESIAN_POINT ( 'NONE',  ( 13.50576839576328148, 45.45902382363403404, -0.8387148265821507964 ) ) ;
#809=CARTESIAN_POINT ( 'NONE',  ( 5.653963835669364002, 69.97463459799799068, -12.25898929304140950 ) ) ;
#812=CARTESIAN_POINT ( 'NONE',  ( 13.32379934013461309, 30.35364490307813057, 2.175025330243249400 ) ) ;
#813=CARTESIAN_POINT ( 'NONE',  ( -13.47793799092467637, 55.90337191138781492, -0.7714925420567289027 ) ) ;
#814=CARTESIAN_POINT ( 'NONE',  ( -12.91175531483703054, 50.07169591931079822, 3.951675568982145226 ) ) ;
#815=CARTESIAN_POINT ( 'NONE',  ( 1.109962791137624416, 64.14012643174706341, -13.46178866848010536 ) ) ;
#816=LINE ( 'NONE', #900, #2037 ) ;
#817=CARTESIAN_POINT ( 'NONE',  ( 13.07068574514433656, 39.55030779099601546, -3.378615318188594951 ) ) ;
#819=CARTESIAN_POINT ( 'NONE',  ( -11.98598919180274436, 61.70066361133849853, -6.212500231099927106 ) ) ;
#820=ORIENTED_EDGE ( 'NONE', *, *, #10454, .T. ) ;
#821=ORIENTED_EDGE ( 'NONE', *, *, #14507, .F. ) ;
#824=CARTESIAN_POINT ( 'NONE',  ( 11.54494251065839450, 57.69100095235108938, -6.997463023747798161 ) ) ;
#825=CARTESIAN_POINT ( 'NONE',  ( 5.294469476691438636, 78.98865934249140253, -12.42107284422839975 ) ) ;
#826=VECTOR ( 'NONE', #344, 1000.000000000000000 ) ;
#827=CARTESIAN_POINT ( 'NONE',  ( -11.76794919243112325, 80.93000000000000682, -2.882316262207890869E-15 ) ) ;
#828=CARTESIAN_POINT ( 'NONE',  ( -13.50000000000000000, 39.92999999999999972, -3.306546357697853733E-15 ) ) ;
#829=CARTESIAN_POINT ( 'NONE',  ( 0.07528598782886079810, 65.68270963596916090, 13.50000000000771827 ) ) ;
#834=CARTESIAN_POINT ( 'NONE',  ( -8.343458848123578520, 78.47999999999998977, -11.48378591275254124 ) ) ;
#835=CARTESIAN_POINT ( 'NONE',  ( 3.981673202811145451, 34.03692019505243138, -12.90035025641783584 ) ) ;
#836=ORIENTED_EDGE ( 'NONE', *, *, #12423, .T. ) ;
#838=EDGE_LOOP ( 'NONE', ( #11462, #9974, #13042, #2651 ) ) ;
#841=CARTESIAN_POINT ( 'NONE',  ( 2.445080149700053643E-15, 42.17999999999999261, -13.50000000000000000 ) ) ;
#842=CARTESIAN_POINT ( 'NONE',  ( -0.08603315895956636927, 59.67690236815970195, 13.49999999999913136 ) ) ;
#843=CARTESIAN_POINT ( 'NONE',  ( 12.00000000000000533, 98.93000000000002103, 1.224646799147353059E-15 ) ) ;
#844=CARTESIAN_POINT ( 'NONE',  ( 12.50000000000000000, 98.93000000000002103, 1.224646799147353059E-15 ) ) ;
#845=CARTESIAN_POINT ( 'NONE',  ( 1.326799508617756862, 71.72767848700497950, 13.44100117757941071 ) ) ;
#846=CARTESIAN_POINT ( 'NONE',  ( 8.343458848123583849, 54.87999999999999545, -11.48378591275253768 ) ) ;
#847=CARTESIAN_POINT ( 'NONE',  ( -5.550346829431017426, 52.38132149445374353, -12.30848393326122903 ) ) ;
#851=CARTESIAN_POINT ( 'NONE',  ( 2.310673249324077805, 68.76308373099037397, 13.30456027256653506 ) ) ;
#853=CARTESIAN_POINT ( 'NONE',  ( 8.244216993401655813, 54.86656887803838600, -10.69961692430309519 ) ) ;
#855=CARTESIAN_POINT ( 'NONE',  ( -5.222546564494585652, 65.49121520183372525, 12.44892348364579959 ) ) ;
#856=FACE_OUTER_BOUND ( 'NONE', #7014, .T. ) ;
#857=CARTESIAN_POINT ( 'NONE',  ( -11.89990621330880316, 40.69421425333050735, -6.375126892817447377 ) ) ;
#858=CARTESIAN_POINT ( 'NONE',  ( -4.245309975859792750, 35.52737123023494803, 12.81530032056034685 ) ) ;
#863=CARTESIAN_POINT ( 'NONE',  ( -11.84847161218580958, 31.69039032213071749, -6.470251712010556489 ) ) ;
#864=DIRECTION ( 'NONE',  ( 0.000000000000000000, -0.000000000000000000, 1.000000000000000000 ) ) ;
#865=CARTESIAN_POINT ( 'NONE',  ( 11.66667137561951506, 60.17734808128163593, 6.792565863938680337 ) ) ;
#867=CARTESIAN_POINT ( 'NONE',  ( 0.000000000000000000, 80.93000000000000682, 0.000000000000000000 ) ) ;
#869=CARTESIAN_POINT ( 'NONE',  ( -8.691771469529815392E-16, 73.67999999999999261, 14.19474002721660355 ) ) ;
#870=CARTESIAN_POINT ( 'NONE',  ( 11.70511894169415790, 51.67995204303867496, -6.726098610477120765 ) ) ;
#871=CARTESIAN_POINT ( 'NONE',  ( -13.33075286816964322, 38.00475805412492036, 2.131075495770263117 ) ) ;
#872=CARTESIAN_POINT ( 'NONE',  ( 13.07195708592954730, 36.55011500055716311, -3.373404994585333938 ) ) ;
#875=CARTESIAN_POINT ( 'NONE',  ( -11.06054324169216230, 77.22177975307495501, 7.745344326915604150 ) ) ;
#876=CARTESIAN_POINT ( 'NONE',  ( -4.416226258374795322, 80.52113410087463308, 12.75764956076284840 ) ) ;
#877=CARTESIAN_POINT ( 'NONE',  ( 0.1409280224492138189, 41.68508833901529442, 13.49999999997910116 ) ) ;
#882=CARTESIAN_POINT ( 'NONE',  ( -3.636496289402155746, 57.53000000000000114, 11.19198476289190936 ) ) ;
#886=CARTESIAN_POINT ( 'NONE',  ( 0.8688120066860616220, 76.14876072707028243, -13.47201481489776675 ) ) ;
#889=CARTESIAN_POINT ( 'NONE',  ( -11.76794919243112325, 51.07999999999999829, 3.823638476888994386 ) ) ;
#890=LINE ( 'NONE', #1157, #7795 ) ;
#891=CARTESIAN_POINT ( 'NONE',  ( -12.14234156378920737, 59.14700413339190277, 5.904461971908546047 ) ) ;
#892=CARTESIAN_POINT ( 'NONE',  ( 10.42207727469415524, 45.10182129088688185, 8.580813032019420916 ) ) ;
#893=CARTESIAN_POINT ( 'NONE',  ( 13.40814881853847318, 69.37525059538582184, 1.572674541139606141 ) ) ;
#894=CIRCLE ( 'NONE', #12755, 12.00000000000000178 ) ;
#895=CARTESIAN_POINT ( 'NONE',  ( 4.274400199475617335, 80.83369808617747765, 12.80560251886253731 ) ) ;
#896=CARTESIAN_POINT ( 'NONE',  ( 11.95805636813460104, 30.66140720589453039, -6.265947899127372267 ) ) ;
#897=CARTESIAN_POINT ( 'NONE',  ( -12.51544737404857344, 56.11421971867084579, 5.067590151480188432 ) ) ;
#898=CARTESIAN_POINT ( 'NONE',  ( -5.838308194493356140, 50.46740077971483629, 12.17325453446762040 ) ) ;
#899=CARTESIAN_POINT ( 'NONE',  ( 5.325587175574985288, 63.98723509382200803, -12.40517262089496597 ) ) ;
#900=CARTESIAN_POINT ( 'NONE',  ( 1.653273178848926472E-15, 80.93000000000000682, 13.50000000000000000 ) ) ;
#901=CARTESIAN_POINT ( 'NONE',  ( 11.98396937526130124, 39.65939841873632332, -6.215724125712108972 ) ) ;
#902=VERTEX_POINT ( 'NONE', #13766 ) ;
#903=LINE ( 'NONE', #11788, #7523 ) ;
#904=CARTESIAN_POINT ( 'NONE',  ( -10.05880256514230986, 61.58230886132751891, -9.003917470233888665 ) ) ;
#906=ORIENTED_EDGE ( 'NONE', *, *, #10979, .F. ) ;
#907=CARTESIAN_POINT ( 'NONE',  ( -10.43129681812944476, 40.60213892834825344, -8.569776200266453259 ) ) ;
#912=CARTESIAN_POINT ( 'NONE',  ( 5.012090283648058531, 47.86087352477124313, 12.53511619697896329 ) ) ;
#913=AXIS2_PLACEMENT_3D ( 'NONE', #4187, #4365, #9687 ) ;
#914=CARTESIAN_POINT ( 'NONE',  ( 11.55553819978283769, 57.69029574722926412, -6.979941511154718725 ) ) ;
#915=CARTESIAN_POINT ( 'NONE',  ( 7.183560718835745540, 78.91260539477536895, -11.43007281236147143 ) ) ;
#916=CARTESIAN_POINT ( 'NONE',  ( 3.636496289402157078, 83.03000000000000114, -11.19198476289190936 ) ) ;
#922=CIRCLE ( 'NONE', #10257, 4.000000000000004441 ) ;
#923=LINE ( 'NONE', #5273, #11771 ) ;
#924=CARTESIAN_POINT ( 'NONE',  ( 3.020329884759706207, 34.07140041091936666, -13.15781035347679229 ) ) ;
#926=CARTESIAN_POINT ( 'NONE',  ( 8.464728390624178894E-06, 46.17999963826949994, -13.49999999999734790 ) ) ;
#931=CARTESIAN_POINT ( 'NONE',  ( -4.454599061965374140, 59.51975211702684021, 12.75138711840418893 ) ) ;
#935=CARTESIAN_POINT ( 'NONE',  ( -4.171729424061791036, 53.52999999999999403, 12.83926296998457239 ) ) ;
#936=CARTESIAN_POINT ( 'NONE',  ( -5.052807978041880865, 71.49763661691018513, 12.52071977299732630 ) ) ;
#937=CARTESIAN_POINT ( 'NONE',  ( 13.49999999999999822, 77.27999999999998693, 4.386415899144236796 ) ) ;
#939=CARTESIAN_POINT ( 'NONE',  ( 1.977490458657884753, 68.75110324043748733, 13.35439718596144765 ) ) ;
#943=CARTESIAN_POINT ( 'NONE',  ( -5.384056574969746656, 65.48512799171378163, 12.38010029700703996 ) ) ;
#944=CARTESIAN_POINT ( 'NONE',  ( 2.894739436579920166E-06, 50.68008041434205069, 13.49999999999938005 ) ) ;
#945=CARTESIAN_POINT ( 'NONE',  ( -11.25500439539402464, 35.20987436177090046, 7.454859297479469404 ) ) ;
#947=ORIENTED_EDGE ( 'NONE', *, *, #7215, .F. ) ;
#948=CARTESIAN_POINT ( 'NONE',  ( 2.138189944381242213, 51.10311857767973009, -13.49999999999999822 ) ) ;
#952=CARTESIAN_POINT ( 'NONE',  ( -12.49172365619227598, 32.11631608597728871, 5.120886946257767747 ) ) ;
#954=CARTESIAN_POINT ( 'NONE',  ( 11.24200432374102299, 60.14937899929235243, 7.477721340839896591 ) ) ;
#956=CARTESIAN_POINT ( 'NONE',  ( -7.158319469831337045, 53.41367405225197018, 11.44589433405317536 ) ) ;
#957=CARTESIAN_POINT ( 'NONE',  ( -11.76794919243112325, 59.92999999999999972, -2.882316262207890869E-15 ) ) ;
#958=CARTESIAN_POINT ( 'NONE',  ( 13.50000000000000000, 77.42999999999999261, 1.653273178848926867E-15 ) ) ;
#959=CARTESIAN_POINT ( 'NONE',  ( 13.49112894113379646, 51.44683640026539706, -0.4894624279518585142 ) ) ;
#960=CARTESIAN_POINT ( 'NONE',  ( -9.629163158805681633, 38.29992217420160472, 9.465125892876324443 ) ) ;
#961=CARTESIAN_POINT ( 'NONE',  ( 11.23715272735747206, 36.71099532258286047, -7.481738776993401174 ) ) ;
#963=CARTESIAN_POINT ( 'NONE',  ( -5.417673612917023540, 74.48380672519944312, 12.36591168787385087 ) ) ;
#964=CARTESIAN_POINT ( 'NONE',  ( 1.982521523170245906E-06, 77.68005525700222336, 13.49999999999970690 ) ) ;
#965=CARTESIAN_POINT ( 'NONE',  ( -4.708371381723156723, 80.51042602726658970, 12.65400907433436117 ) ) ;
#966=CYLINDRICAL_SURFACE ( 'NONE', #9419, 13.50000000000000000 ) ;
#971=CARTESIAN_POINT ( 'NONE',  ( 9.520470885617717371, 55.73000000000000398, -6.917026985038131848 ) ) ;
#974=B_SPLINE_CURVE_WITH_KNOTS ( 'NONE', 3,
 ( #15714, #3972, #5048, #13169, #2623, #8056, #11852, #3618, #9034, #13337, #13420, #1309, #9127, #17227, #2364, #7967, #14735, #2277, #14388, #7704, #7798, #7878, #9384, #17314, #5228, #10445, #9212, #15980, #1055, #6467, #10699, #6724, #12102, #13256, #1143, #4957, #15892, #3883, #5138, #6554, #16066, #14651, #6640, #10613 ),
 .UNSPECIFIED., .F., .F.,
 ( 4, 2, 2, 2, 2, 2, 2, 2, 2, 2, 2, 2, 2, 2, 2, 2, 2, 2, 2, 2, 2, 4 ),
 ( 0.03689401835950767428, 0.03766257893388839234, 0.03843113950826911041, 0.03919970008264982847, 0.03996826065703055347, 0.04073682123141127154, 0.04150538180579198960, 0.04304250295455346043, 0.04457962410331492431, 0.04611674525207638820, 0.04765386640083785902, 0.04919098754959932984, 0.05072810869836079373, 0.05226522984712225761, 0.05380235099588372844, 0.05533947214464519232, 0.05687659329340666314, 0.05764515386778737427, 0.05841371444216809927, 0.05995083559092950765, 0.06071939616531019102, 0.06148795673969087439 ),
 .UNSPECIFIED. ) ;
#975=CARTESIAN_POINT ( 'NONE',  ( 12.17141580355952080, 75.64447568897026031, -5.840979099278275299 ) ) ;
#976=CARTESIAN_POINT ( 'NONE',  ( -1.010931998681471075E-07, 71.67999718330101189, 13.49999999999999822 ) ) ;
#978=CARTESIAN_POINT ( 'NONE',  ( -13.50000000000000000, 73.92999999999999261, -3.306546357697853733E-15 ) ) ;
#979=CARTESIAN_POINT ( 'NONE',  ( -11.76794919243112325, 47.77999999999999403, -3.823638476888998827 ) ) ;
#981=CARTESIAN_POINT ( 'NONE',  ( -11.07966164616091298, 59.22065182733356181, 7.713049733970735566 ) ) ;
#982=CARTESIAN_POINT ( 'NONE',  ( 13.40951939699013806, 45.37387384954418224, 1.609924743746272036 ) ) ;
#983=CARTESIAN_POINT ( 'NONE',  ( 10.56082941162724609, 69.75074268295333013, -8.413808112793510929 ) ) ;
#984=CARTESIAN_POINT ( 'NONE',  ( 0.2979893671971325930, 80.69079410851497869, 13.49999999993527311 ) ) ;
#985=CARTESIAN_POINT ( 'NONE',  ( 13.49835112770431955, 30.43830851857264008, -0.2430632257887174463 ) ) ;
#987=CARTESIAN_POINT ( 'NONE',  ( -4.651663545995293525, 55.34748731497323604, -12.67467349376107677 ) ) ;
#988=CARTESIAN_POINT ( 'NONE',  ( -12.66557966946106184, 50.09907455509510044, 4.673096744009077597 ) ) ;
#989=CARTESIAN_POINT ( 'NONE',  ( 2.844419195333417250, 64.07772472696797195, -13.19709045098189826 ) ) ;
#990=CARTESIAN_POINT ( 'NONE',  ( 13.16029344000198620, 42.53708686388746685, -3.020864121732791396 ) ) ;
#991=CARTESIAN_POINT ( 'NONE',  ( 12.52796351933140429, 39.24719058125410953, 5.030018464370217046 ) ) ;
#993=CARTESIAN_POINT ( 'NONE',  ( -8.704689286822198113, 70.51503155829134073, -10.32237615012925858 ) ) ;
#994=CARTESIAN_POINT ( 'NONE',  ( -9.897107763165278627, 61.57380692958660262, -9.182555981961492364 ) ) ;
#996=ORIENTED_EDGE ( 'NONE', *, *, #2626, .F. ) ;
#997=CARTESIAN_POINT ( 'NONE',  ( -8.167758447988427761, 40.49042146826998589, -10.74885325159674565 ) ) ;
#1001=DIRECTION ( 'NONE',  ( -1.000000000000000000, 0.000000000000000000, 0.000000000000000000 ) ) ;
#1003=CARTESIAN_POINT ( 'NONE',  ( 13.39390915008829630, 57.37105770510941483, 1.689157604109823074 ) ) ;
#1004=CARTESIAN_POINT ( 'NONE',  ( 12.20311627183846959, 78.64184583226609959, -5.773582477899624976 ) ) ;
#1005=CARTESIAN_POINT ( 'NONE',  ( -7.272992578804310604, 75.37999999999999545, 10.01041549318726709 ) ) ;
#1006=CARTESIAN_POINT ( 'NONE',  ( -13.50000000000000000, 36.92999999999999972, -3.306546357697853733E-15 ) ) ;
#1007=CARTESIAN_POINT ( 'NONE',  ( 3.636496289402154414, 75.83000000000001251, 11.19198476289190936 ) ) ;
#1013=CARTESIAN_POINT ( 'NONE',  ( 9.827588045523224736, 33.78981817295442625, -9.258195743607105399 ) ) ;
#1014=CARTESIAN_POINT ( 'NONE',  ( -13.48486571972425274, 73.90797088387792257, -0.6398426247094320951 ) ) ;
#1015=ORIENTED_EDGE ( 'NONE', *, *, #14814, .T. ) ;
#1019=ORIENTED_EDGE ( 'NONE', *, *, #6979, .F. ) ;
#1022=CARTESIAN_POINT ( 'NONE',  ( -4.783579317106955386, 44.50765774798735919, 12.62540879120737536 ) ) ;
#1023=CARTESIAN_POINT ( 'NONE',  ( -7.500000000000000000, 98.93000000000002103, 9.000000000000000000 ) ) ;
#1024=CARTESIAN_POINT ( 'NONE',  ( 9.116104188755297599, 66.82557654486986110, -9.969699158624095503 ) ) ;
#1025=VECTOR ( 'NONE', #3269, 1000.000000000000000 ) ;
#1026=CARTESIAN_POINT ( 'NONE',  ( -4.171729424061791036, 50.53000000000000114, 12.83926296998457239 ) ) ;
#1027=CARTESIAN_POINT ( 'NONE',  ( -5.791868581402612293, 71.46924316949180422, 12.19443570704414093 ) ) ;
#1029=CARTESIAN_POINT ( 'NONE',  ( -1.270456549871447738, 68.63430995385745348, 13.44010555243231053 ) ) ;
#1032=CARTESIAN_POINT ( 'NONE',  ( 4.606558825016942471, 55.01407570091451760, -12.68986247441658932 ) ) ;
#1036=CARTESIAN_POINT ( 'NONE',  ( -1.945342937830138563, 65.61008263105732397, 13.36017202698423922 ) ) ;
#1037=CARTESIAN_POINT ( 'NONE',  ( -8.512854481965995035, 62.35381330728030491, 10.47804304773685224 ) ) ;
#1038=CARTESIAN_POINT ( 'NONE',  ( -8.740105143331430071, 35.34338649247177955, 10.29126063676346980 ) ) ;
#1039=CARTESIAN_POINT ( 'NONE',  ( -2.919924463492937772, 40.28498943413073619, -13.18046540264134237 ) ) ;
#1040=CARTESIAN_POINT ( 'NONE',  ( -13.49990871899026601, 31.94501881797403442, 0.4409628020136921456 ) ) ;
#1042=CARTESIAN_POINT ( 'NONE',  ( 8.139855941678256102, 59.98916145259055099, 10.77923023974760497 ) ) ;
#1044=CARTESIAN_POINT ( 'NONE',  ( -1.412718313214967214, 53.62924654513680878, 13.42809310199930728 ) ) ;
#1045=CARTESIAN_POINT ( 'NONE',  ( 7.272992578804308828, 54.98000000000000398, 10.01041549318726709 ) ) ;
#1046=CARTESIAN_POINT ( 'NONE',  ( 10.92172942406179104, 77.73000000000000398, -7.935100905948385908 ) ) ;
#1047=CARTESIAN_POINT ( 'NONE',  ( 11.44877280849391532, 51.69754644816881495, -7.157341881666669181 ) ) ;
#1048=CARTESIAN_POINT ( 'NONE',  ( -12.56737935825091945, 38.10897242895168802, 4.930623318646805586 ) ) ;
#1050=CARTESIAN_POINT ( 'NONE',  ( 11.88911771378908711, 36.66659916247261464, -6.395327377679192793 ) ) ;
#1052=CARTESIAN_POINT ( 'NONE',  ( -0.3656471757371563269, 74.66685158956377677, 13.49665596708117654 ) ) ;
#1053=CARTESIAN_POINT ( 'NONE',  ( -12.11600929618134970, 77.14899403401574318, 5.954317193221099203 ) ) ;
#1055=CARTESIAN_POINT ( 'NONE',  ( 7.499999999999999112, 108.3824470675415341, 4.067225351102826458 ) ) ;
#1058=ORIENTED_EDGE ( 'NONE', *, *, #12188, .F. ) ;
#1059=CARTESIAN_POINT ( 'NONE',  ( 11.76794919243112325, 55.42999999999999972, 1.441158131103945434E-15 ) ) ;
#1061=CARTESIAN_POINT ( 'NONE',  ( 13.50000000000000355, 56.57999999999999829, -4.386415899144233244 ) ) ;
#1063=CARTESIAN_POINT ( 'NONE',  ( 10.58057089751780566, 75.74942444919939533, -8.384628530423594128 ) ) ;
#1064=DIRECTION ( 'NONE',  ( -1.000000000000000000, -0.000000000000000000, -0.000000000000000000 ) ) ;
#1065=CARTESIAN_POINT ( 'NONE',  ( 3.041627741621593994, 65.78941339898256047, 13.15297391146506101 ) ) ;
#1066=CARTESIAN_POINT ( 'NONE',  ( 10.92172942406179104, 75.73000000000000398, -7.935100905948385908 ) ) ;
#1067=CARTESIAN_POINT ( 'NONE',  ( 9.520470885617715595, 40.12999999999999545, 6.917026985038134512 ) ) ;
#1068=DIRECTION ( 'NONE',  ( 0.000000000000000000, -1.000000000000000000, 0.000000000000000000 ) ) ;
#1069=CARTESIAN_POINT ( 'NONE',  ( -9.927680929899530327, 59.28455817258709004, 9.148293018334287652 ) ) ;
#1070=CARTESIAN_POINT ( 'NONE',  ( 12.47446446985702906, 45.24145293083233810, 5.182912669380336013 ) ) ;
#1071=CARTESIAN_POINT ( 'NONE',  ( 13.35909562912327608, 69.36166794184582329, 1.954686695093853732 ) ) ;
#1073=CARTESIAN_POINT ( 'NONE',  ( 12.05249706929546072, 30.65406261480569583, -6.081942500887944192 ) ) ;
#1074=CARTESIAN_POINT ( 'NONE',  ( -7.530017562689784505, 55.46222776646441588, -11.20493419439256755 ) ) ;
#1075=CARTESIAN_POINT ( 'NONE',  ( -13.48049505424421568, 49.90497277773586404, -0.7254708853913678368 ) ) ;
#1076=CARTESIAN_POINT ( 'NONE',  ( 9.418187565439815501, 63.81058986697370017, -9.677497028817999336 ) ) ;
#1077=CARTESIAN_POINT ( 'NONE',  ( 12.45500488473927092, 42.62014939293063520, -5.223402740974586678 ) ) ;
#1078=CARTESIAN_POINT ( 'NONE',  ( 12.50570607633773967, 39.24506257281584709, 5.085017721920233491 ) ) ;
#1081=CARTESIAN_POINT ( 'NONE',  ( -9.879805435650132139, 70.57295972474388179, -9.199969855269857888 ) ) ;
#1082=CARTESIAN_POINT ( 'NONE',  ( -10.11877999215449542, 61.58546918468492493, -8.936496873947890052 ) ) ;
#1088=CARTESIAN_POINT ( 'NONE',  ( 2.852439471677590710, 61.07744184195599502, -13.19548016026537773 ) ) ;
#1089=CARTESIAN_POINT ( 'NONE',  ( 13.38817278408007105, 57.36945051200932966, 1.734111481910428409 ) ) ;
#1090=EDGE_CURVE ( 'NONE', #902, #15411, #10862, .T. ) ;
#1091=CARTESIAN_POINT ( 'NONE',  ( 11.76794919243112680, 67.57999999999998408, -3.823638476888993942 ) ) ;
#1092=CARTESIAN_POINT ( 'NONE',  ( 11.76794919243112325, 73.42999999999999261, 1.441158131103945434E-15 ) ) ;
#1095=CARTESIAN_POINT ( 'NONE',  ( 2.445080149700053643E-15, 42.17999999999999261, -13.50000000000000000 ) ) ;
#1098=CARTESIAN_POINT ( 'NONE',  ( 7.500000000000000888, 98.93000000000002103, 9.000000000000000000 ) ) ;
#1099=CARTESIAN_POINT ( 'NONE',  ( -2.522983078673279752E-14, 34.17999999999999972, -13.50000000000000000 ) ) ;
#1100=CARTESIAN_POINT ( 'NONE',  ( -8.446523378668436166, 73.50299463280887835, -10.53513265744836502 ) ) ;
#1101=ORIENTED_EDGE ( 'NONE', *, *, #3547, .F. ) ;
#1102=ORIENTED_EDGE ( 'NONE', *, *, #4492, .T. ) ;
#1103=CARTESIAN_POINT ( 'NONE',  ( 9.520470885617717371, 79.72999999999998977, -6.917026985038131848 ) ) ;
#1104=ORIENTED_EDGE ( 'NONE', *, *, #15443, .T. ) ;
#1106=AXIS2_PLACEMENT_3D ( 'NONE', #10248, #3509, #12716 ) ;
#1107=CARTESIAN_POINT ( 'NONE',  ( -8.267728653884569567, 44.36549807078887397, 10.69103896247519003 ) ) ;
#1109=CARTESIAN_POINT ( 'NONE',  ( 9.716038052031565897, 66.79547513456357422, -9.373145993641442075 ) ) ;
#1111=CARTESIAN_POINT ( 'NONE',  ( 2.607531440858944223E-15, 55.17999999999998550, -14.19474002721660355 ) ) ;
#1112=CARTESIAN_POINT ( 'NONE',  ( -11.83577994726966054, 71.17054626581648336, 6.493405617986467426 ) ) ;
#1116=CARTESIAN_POINT ( 'NONE',  ( -13.42211799135032990, 67.98038489383687022, 1.448088636224807102 ) ) ;
#1121=CARTESIAN_POINT ( 'NONE',  ( -13.38213899561058895, 64.99218069301205958, 1.780040424083840556 ) ) ;
#1122=CARTESIAN_POINT ( 'NONE',  ( -4.052283961879332708, 35.53437198618238568, 12.87817188429518467 ) ) ;
#1124=CARTESIAN_POINT ( 'NONE',  ( -11.76794919243112325, 32.77999999999999403, -3.823638476888998827 ) ) ;
#1127=CARTESIAN_POINT ( 'NONE',  ( -3.203942090712391888, 31.29520102517548708, -13.11476468382334737 ) ) ;
#1129=CARTESIAN_POINT ( 'NONE',  ( 11.65241955595561585, 60.17635480250425672, 6.816973529922489838 ) ) ;
#1130=EDGE_CURVE ( 'NONE', #10403, #10678, #7750, .T. ) ;
#1132=CARTESIAN_POINT ( 'NONE',  ( -6.089806512862788956, 53.45753655534689841, 12.05607447093654017 ) ) ;
#1133=CARTESIAN_POINT ( 'NONE',  ( 2.272985001014427788E-15, 53.17999999999999972, -12.37355403259654985 ) ) ;
#1134=CARTESIAN_POINT ( 'NONE',  ( 13.49999999999999822, 77.27999999999998693, 4.386415899144237684 ) ) ;
#1135=CARTESIAN_POINT ( 'NONE',  ( 11.00335429800770548, 51.13480760581911255, 7.825213182322699801 ) ) ;
#1136=CARTESIAN_POINT ( 'NONE',  ( -9.597058931428728457, 37.55844031602762101, -9.501180398282993878 ) ) ;
#1137=CARTESIAN_POINT ( 'NONE',  ( 13.35040085901588824, 36.35962275902586072, 2.008008797607404361 ) ) ;
#1139=CARTESIAN_POINT ( 'NONE',  ( -5.988508216935491291, 74.46151138467401154, 12.09920782539440154 ) ) ;
#1140=CARTESIAN_POINT ( 'NONE',  ( -12.09693526138493525, 77.15052554825793152, 5.992971486588084318 ) ) ;
#1141=CARTESIAN_POINT ( 'NONE',  ( -12.98374536458790196, 79.79765901695760988, -3.704304229944536786 ) ) ;
#1143=CARTESIAN_POINT ( 'NONE',  ( 7.499999999999999112, 106.5829119071944717, 7.723695278929457508 ) ) ;
#1147=CARTESIAN_POINT ( 'NONE',  ( -9.520470885617715595, 53.62999999999999545, -6.917026985038136289 ) ) ;
#1151=CARTESIAN_POINT ( 'NONE',  ( 6.051126895917462001, 75.95900626949409684, -12.06810164290940968 ) ) ;
#1154=CARTESIAN_POINT ( 'NONE',  ( 0.3314664981419376266, 65.69191830627838158, 13.49594832441332670 ) ) ;
#1155=CARTESIAN_POINT ( 'NONE',  ( -4.171729424061791036, 68.53000000000000114, 12.83926296998457239 ) ) ;
#1156=CARTESIAN_POINT ( 'NONE',  ( -11.76794919243112325, 42.08000000000000540, 3.823638476888994386 ) ) ;
#1157=CARTESIAN_POINT ( 'NONE',  ( 0.000000000000000000, 80.93000000000000682, -13.50000000000000000 ) ) ;
#1158=CARTESIAN_POINT ( 'NONE',  ( -12.86588924449608484, 58.78300137090919009, -4.092555612934534182 ) ) ;
#1159=CARTESIAN_POINT ( 'NONE',  ( 12.95119434482599630, 45.29360578691247952, 3.810224031054839422 ) ) ;
#1160=CARTESIAN_POINT ( 'NONE',  ( 12.58190901537911977, 69.60887662769496842, -4.936570319405274354 ) ) ;
#1163=CARTESIAN_POINT ( 'NONE',  ( -10.10275593513610737, 55.58463057449298361, -8.954572238356126590 ) ) ;
#1164=CARTESIAN_POINT ( 'NONE',  ( -13.46222882471981741, 49.96493226193709347, 1.009247901310075690 ) ) ;
#1165=CARTESIAN_POINT ( 'NONE',  ( 11.27120675886632029, 63.70861490660946203, -7.431139975753272786 ) ) ;
#1166=CARTESIAN_POINT ( 'NONE',  ( 7.715407790152941203, 42.88976810797701233, -11.08212475357666449 ) ) ;
#1167=CARTESIAN_POINT ( 'NONE',  ( 12.58936429392694301, 39.25315851018460478, 4.875368239649940705 ) ) ;
#1169=CARTESIAN_POINT ( 'NONE',  ( -11.69253541478880720, 70.67755481803949635, -6.804811722709197319 ) ) ;
#1170=CARTESIAN_POINT ( 'NONE',  ( -3.338982230527045569, 61.29999130979701505, -13.08671784421840023 ) ) ;
#1176=CARTESIAN_POINT ( 'NONE',  ( 3.934034384636251325, 61.03850454420580007, -12.91965331869873346 ) ) ;
#1178=CARTESIAN_POINT ( 'NONE',  ( 7.656218467254686466, 71.96771731040691122, 11.11903937377953611 ) ) ;
#1179=CARTESIAN_POINT ( 'NONE',  ( 13.42377694829353985, 57.38002766246249564, 1.436435505632925658 ) ) ;
#1180=CARTESIAN_POINT ( 'NONE',  ( 11.76794919243112325, 73.27999999999998693, 3.823638476888996607 ) ) ;
#1181=CARTESIAN_POINT ( 'NONE',  ( -7.272992578804310604, 81.38000000000000966, 10.01041549318726709 ) ) ;
#1182=CARTESIAN_POINT ( 'NONE',  ( -9.886435270270100162, 47.28669829188292795, 9.192848475936937547 ) ) ;
#1183=PRODUCT_DEFINITION_CONTEXT ( 'detailed design', #1448, 'design' ) ;
#1184=CARTESIAN_POINT ( 'NONE',  ( -8.891200544363830713E-16, 37.67999999999999261, 13.50000000000000000 ) ) ;
#1188=CARTESIAN_POINT ( 'NONE',  ( 4.369696808009779332, 34.02284990421056676, -12.77326014878184424 ) ) ;
#1189=CARTESIAN_POINT ( 'NONE',  ( -4.416228722299345044, 73.33875342350749804, -12.76045521491836432 ) ) ;
#1192=CARTESIAN_POINT ( 'NONE',  ( 9.520470885617717371, 73.73000000000000398, -6.917026985038131848 ) ) ;
#1196=CARTESIAN_POINT ( 'NONE',  ( -10.12244397357995140, 44.27432646096063706, 8.932308212114547175 ) ) ;
#1198=CARTESIAN_POINT ( 'NONE',  ( -4.171729424061787483, 40.32999999999999829, -12.83926296998457417 ) ) ;
#1199=CARTESIAN_POINT ( 'NONE',  ( -11.83839496929498125, 71.17035886798730360, 6.488638129243179620 ) ) ;
#1202=CARTESIAN_POINT ( 'NONE',  ( -11.66904316095729222, 68.18248099459721345, 6.788478734277004989 ) ) ;
#1204=CARTESIAN_POINT ( 'NONE',  ( 3.111368884622620623, 55.06813134461953751, -13.13662995333488226 ) ) ;
#1208=CARTESIAN_POINT ( 'NONE',  ( -13.34368233115651492, 65.00195984828552298, 2.053198378037492056 ) ) ;
#1209=CARTESIAN_POINT ( 'NONE',  ( -7.063482594716048446, 35.41767491092237918, 11.50466891869187691 ) ) ;
#1212=CARTESIAN_POINT ( 'NONE',  ( -8.029972511114698008, 31.48422938242913105, -10.85219181568965929 ) ) ;
#1215=CARTESIAN_POINT ( 'NONE',  ( 5.573835160001226363, 59.88200068511800822, 12.30730957908311751 ) ) ;
#1217=CARTESIAN_POINT ( 'NONE',  ( -7.325695255518703597, 53.40656810623330131, 11.33985798352976992 ) ) ;
#1218=CARTESIAN_POINT ( 'NONE',  ( -7.576616670048093940E-16, 51.68000000000000682, 12.37355403259654985 ) ) ;
#1219=CARTESIAN_POINT ( 'NONE',  ( -13.49999999999999822, 67.07999999999999829, 4.386415899144235908 ) ) ;
#1220=CARTESIAN_POINT ( 'NONE',  ( 5.686689245591225905, 50.88656960456093259, 12.25087184074811120 ) ) ;
#1221=CARTESIAN_POINT ( 'NONE',  ( -10.20473357957621197, 37.59009158050992738, -8.838276559641728980 ) ) ;
#1222=CARTESIAN_POINT ( 'NONE',  ( 9.231307355299586348, 36.04034459707229132, 9.850538178411547108 ) ) ;
#1225=CARTESIAN_POINT ( 'NONE',  ( -6.087077674780319470, 74.45759876751071715, 12.04979220636686144 ) ) ;
#1226=CARTESIAN_POINT ( 'NONE',  ( -12.47207658550254905, 76.74188438275474766, -5.167046129524251796 ) ) ;
#1227=CARTESIAN_POINT ( 'NONE',  ( -10.97791022018516394, 79.63287582280005950, -7.869652631373966756 ) ) ;
#1228=CARTESIAN_POINT ( 'NONE',  ( 0.000000000000000000, 102.9300000000000068, 0.000000000000000000 ) ) ;
#1230=CARTESIAN_POINT ( 'NONE',  ( -11.76794919243112325, 51.07999999999999829, 3.823638476888994830 ) ) ;
#1235=CARTESIAN_POINT ( 'NONE',  ( 8.595313431481731214, 75.84998225435066388, -10.41012029664250349 ) ) ;
#1237=CARTESIAN_POINT ( 'NONE',  ( 9.520470885617717371, 43.72999999999999687, -6.917026985038131848 ) ) ;
#1238=CARTESIAN_POINT ( 'NONE',  ( -12.52061518882791269, 41.11351867588017228, 5.048379448138805792 ) ) ;
#1239=CARTESIAN_POINT ( 'NONE',  ( -8.868632591895519113, 58.52285990151153783, -10.17867040326453143 ) ) ;
#1240=CARTESIAN_POINT ( 'NONE',  ( 0.000000000000000000, 102.9300000000000068, 0.000000000000000000 ) ) ;
#1242=LINE ( 'NONE', #14668, #12967 ) ;
#1243=CARTESIAN_POINT ( 'NONE',  ( -0.5643014959054915014, 55.20029019360543998, -13.48820175703197677 ) ) ;
#1244=ADVANCED_FACE ( 'NONE', ( #9982 ), #16343, .T. ) ;
#1245=CARTESIAN_POINT ( 'NONE',  ( -13.25473226480498035, 49.83966860457066161, -2.561852220214583919 ) ) ;
#1246=CARTESIAN_POINT ( 'NONE',  ( 10.70554398665652585, 63.74254191304165573, -8.236043843619819782 ) ) ;
#1247=CARTESIAN_POINT ( 'NONE',  ( 10.11861299488508514, 42.77454474994834754, -8.937100350925991421 ) ) ;
#1248=CARTESIAN_POINT ( 'NONE',  ( 13.22408915331992674, 39.33228484707264272, 2.764232869092419609 ) ) ;
#1250=CARTESIAN_POINT ( 'NONE',  ( -12.90681428308145939, 70.78796989954061303, -3.960305618596332788 ) ) ;
#1256=CARTESIAN_POINT ( 'NONE',  ( 6.434165136549590436, 47.91625709899204821, 11.86847022325157752 ) ) ;
#1258=CARTESIAN_POINT ( 'NONE',  ( 2.397323522673310947, 71.76623511769916774, 13.28545270918177934 ) ) ;
#1259=CARTESIAN_POINT ( 'NONE',  ( 13.36276861424025775, 57.36259551922253053, 1.924898818614698470 ) ) ;
#1260=CARTESIAN_POINT ( 'NONE',  ( -9.520470885617715595, 68.62999999999999545, -6.917026985038136289 ) ) ;
#1261=CARTESIAN_POINT ( 'NONE',  ( -8.343458848123582072, 37.37999999999999545, 11.48378591275254124 ) ) ;
#1262=CARTESIAN_POINT ( 'NONE',  ( -3.636496289402155746, 72.53000000000000114, 11.19198476289190936 ) ) ;
#1263=CARTESIAN_POINT ( 'NONE',  ( -11.46982637885754563, 47.19613723285193174, 7.120329246312594229 ) ) ;
#1264=DIRECTION ( 'NONE',  ( 0.000000000000000000, 0.000000000000000000, 1.000000000000000000 ) ) ;
#1270=CARTESIAN_POINT ( 'NONE',  ( 12.20205365874035408, 33.64198225340590653, -5.778782258580305253 ) ) ;
#1271=CARTESIAN_POINT ( 'NONE',  ( -3.691467218196870625, 73.31271651008955814, -12.98552287576125330 ) ) ;
#1273=ORIENTED_EDGE ( 'NONE', *, *, #14405, .T. ) ;
#1274=CARTESIAN_POINT ( 'NONE',  ( 7.272992578804308828, 75.98000000000000398, 10.01041549318726886 ) ) ;
#1277=CARTESIAN_POINT ( 'NONE',  ( -0.1540485588782081749, 44.67444256847909401, 13.49999999998640554 ) ) ;
#1279=CARTESIAN_POINT ( 'NONE',  ( -8.343458848123576743, 46.48000000000000398, -11.48378591275254301 ) ) ;
#1280=CARTESIAN_POINT ( 'NONE',  ( -13.39973178939295373, 70.87272364588611140, -1.642340154095887517 ) ) ;
#1282=CARTESIAN_POINT ( 'NONE',  ( -12.75809247443173788, 67.77074377949604411, -4.416153755955929405 ) ) ;
#1284=CARTESIAN_POINT ( 'NONE',  ( 13.48422240914645442, 54.45333625655221965, -0.6766818701643474432 ) ) ;
#1286=DIRECTION ( 'NONE',  ( 0.000000000000000000, -1.000000000000000000, 0.000000000000000000 ) ) ;
#1287=CARTESIAN_POINT ( 'NONE',  ( -12.97482353139810130, 64.79664418661724312, -3.729052729424082280 ) ) ;
#1288=CARTESIAN_POINT ( 'NONE',  ( -12.56949574550154836, 35.10876493811377941, 4.925247007018846546 ) ) ;
#1289=EDGE_LOOP ( 'NONE', ( #4809, #499, #4215, #3994 ) ) ;
#1290=DIRECTION ( 'NONE',  ( 0.000000000000000000, -1.000000000000000000, 0.000000000000000000 ) ) ;
#1291=CIRCLE ( 'NONE', #16234, 9.500000000000021316 ) ;
#1292=CARTESIAN_POINT ( 'NONE',  ( -10.28350456035710003, 31.59411424244996880, -8.747300393376729488 ) ) ;
#1293=CARTESIAN_POINT ( 'NONE',  ( 4.040337042483869823, 73.03468595069342939, -12.88447105581200169 ) ) ;
#1297=CARTESIAN_POINT ( 'NONE',  ( -9.907842913857002998, 53.28558844465230493, 9.169773063847259209 ) ) ;
#1299=CARTESIAN_POINT ( 'NONE',  ( -7.272992578804307939, 47.47999999999998977, -10.01041549318726886 ) ) ;
#1300=CARTESIAN_POINT ( 'NONE',  ( 13.50000000000000000, 68.43000000000000682, 1.653273178848926867E-15 ) ) ;
#1301=CARTESIAN_POINT ( 'NONE',  ( 4.977012011971282845, 50.85955796876759649, 12.54907956735184982 ) ) ;
#1303=CARTESIAN_POINT ( 'NONE',  ( -7.545992825712033003, 37.46287733677418430, -11.19724308666464019 ) ) ;
#1304=CARTESIAN_POINT ( 'NONE',  ( 13.37272337869130823, 36.36494487923371821, 1.858079212359092569 ) ) ;
#1306=CARTESIAN_POINT ( 'NONE',  ( -11.21338182703946451, 74.21242793460713472, 7.517659778229184298 ) ) ;
#1307=CARTESIAN_POINT ( 'NONE',  ( -12.52141048085782948, 76.74656338183874027, -5.046232787786422591 ) ) ;
#1308=CARTESIAN_POINT ( 'NONE',  ( -13.15667449852409021, 80.03835353115930218, 3.056836537833763856 ) ) ;
#1309=CARTESIAN_POINT ( 'NONE',  ( 7.500000000000000000, 106.5806336763438793, -7.726132535793191813 ) ) ;
#1312=CARTESIAN_POINT ( 'NONE',  ( 9.520470885617717371, 49.72999999999999687, -6.917026985038131848 ) ) ;
#1316=CARTESIAN_POINT ( 'NONE',  ( 10.92172942406178926, 35.13000000000000256, 7.935100905948387684 ) ) ;
#1317=CARTESIAN_POINT ( 'NONE',  ( 10.95438131901840961, 75.72796546381928806, -7.891384625383862428 ) ) ;
#1319=CARTESIAN_POINT ( 'NONE',  ( -7.272992578804310604, 42.37999999999999545, 10.01041549318726709 ) ) ;
#1320=CARTESIAN_POINT ( 'NONE',  ( -9.383695827828427483, 41.31213889170596332, 9.705529900550189382 ) ) ;
#1321=CARTESIAN_POINT ( 'NONE',  ( -5.764561566141782833, 58.38968915241470370, -12.20736831470176398 ) ) ;
#1323=CARTESIAN_POINT ( 'NONE',  ( -13.49999999999999822, 55.08000000000000540, 4.386415899144235020 ) ) ;
#1324=CYLINDRICAL_SURFACE ( 'NONE', #9888, 5.000000000000000000 ) ;
#1325=CARTESIAN_POINT ( 'NONE',  ( -10.10360367143677429, 55.58467546146358274, -8.953613654375507380 ) ) ;
#1326=CARTESIAN_POINT ( 'NONE',  ( -10.78023278508444349, 49.62152785118134801, -8.131429254652333682 ) ) ;
#1327=CARTESIAN_POINT ( 'NONE',  ( 11.45531800585675519, 63.69692067607217467, -7.143501120740932464 ) ) ;
#1328=CARTESIAN_POINT ( 'NONE',  ( 12.00345388897867061, 42.65789368871043763, -6.178225835024248269 ) ) ;
#1330=ORIENTED_EDGE ( 'NONE', *, *, #4889, .T. ) ;
#1331=CARTESIAN_POINT ( 'NONE',  ( -8.121902954028387356, 70.48834023284237560, -10.78388806788330534 ) ) ;
#1337=CARTESIAN_POINT ( 'NONE',  ( 11.49604287478703135, 60.69423318969604964, -7.077870380912349546 ) ) ;
#1339=CARTESIAN_POINT ( 'NONE',  ( 7.579234238537092772, 71.96436601207575734, 11.17165930700318910 ) ) ;
#1340=CARTESIAN_POINT ( 'NONE',  ( 12.81014742043414678, 57.58654023661487997, -4.352113031915539665 ) ) ;
#1342=CARTESIAN_POINT ( 'NONE',  ( -9.520470885617717371, 72.23000000000000398, 6.917026985038133624 ) ) ;
#1343=CARTESIAN_POINT ( 'NONE',  ( 3.636496289402157078, 77.03000000000000114, -11.19198476289190936 ) ) ;
#1344=ADVANCED_FACE ( 'NONE', ( #11290 ), #14355, .F. ) ;
#1345=CARTESIAN_POINT ( 'NONE',  ( -10.34620229525405577, 47.26236668688625997, 8.674891611129472935 ) ) ;
#1346=CARTESIAN_POINT ( 'NONE',  ( -12.50000000000000000, 102.9300000000000210, 1.714505518806294638E-15 ) ) ;
#1352=CARTESIAN_POINT ( 'NONE',  ( 13.48916840549102325, 33.44861295401204160, -0.5407753439385338812 ) ) ;
#1353=CARTESIAN_POINT ( 'NONE',  ( -9.418482302422065189, 73.54949279931506112, -9.674530453309715838 ) ) ;
#1354=ORIENTED_EDGE ( 'NONE', *, *, #5085, .T. ) ;
#1355=EDGE_LOOP ( 'NONE', ( #1938, #7619, #9625, #947 ) ) ;
#1356=CARTESIAN_POINT ( 'NONE',  ( -10.92172942406178926, 42.63000000000000256, -7.935100905948389460 ) ) ;
#1358=CARTESIAN_POINT ( 'NONE',  ( -13.32969872981109738, 41.00498912793175066, 2.137555216804883695 ) ) ;
#1360=CARTESIAN_POINT ( 'NONE',  ( -0.6995756356649440733, 44.65484589472355736, 13.48186430673500347 ) ) ;
#1362=AXIS2_PLACEMENT_3D ( 'NONE', #12059, #5527, #1264 ) ;
#1363=CARTESIAN_POINT ( 'NONE',  ( 13.49999999999999822, 45.28000000000000114, 4.386415899144237684 ) ) ;
#1364=CARTESIAN_POINT ( 'NONE',  ( 2.607531440858944223E-15, 45.17999999999999972, -14.19474002721660355 ) ) ;
#1365=CARTESIAN_POINT ( 'NONE',  ( -13.41563146330035572, 70.87746431999256913, -1.508872100732321142 ) ) ;
#1366=ADVANCED_FACE ( 'NONE', ( #1900 ), #14271, .T. ) ;
#1367=( BOUNDED_CURVE ( )  B_SPLINE_CURVE ( 2, ( #15529, #8936, #10347, #6194, #11665, #2180, #7606, #7255, #3438, #4601, #527, #3352, #12984 ),
 .UNSPECIFIED., .F., .F. ) 
 B_SPLINE_CURVE_WITH_KNOTS ( ( 3, 2, 2, 2, 2, 2, 3 ),
 ( 0.4027777777777777901, 0.4055555555555555580, 0.4111111111111110938, 0.4166666666666666852, 0.4222222222222222210, 0.4277777777777777568, 0.4305555555555555247 ),
 .UNSPECIFIED. ) 
 CURVE ( )  GEOMETRIC_REPRESENTATION_ITEM ( )  RATIONAL_B_SPLINE_CURVE ( ( 0.9755282581475768211, 0.9755282581475768211, 1.000000000000000000, 0.9510565162951535312, 1.000000000000000000, 0.9510565162951535312, 1.000000000000000000, 0.9510565162951535312, 1.000000000000000000, 0.9510565162951535312, 1.000000000000000000, 0.9755282581475770431, 0.9755282581475768211 ) ) 
 REPRESENTATION_ITEM ( '' )  );
#1369=CARTESIAN_POINT ( 'NONE',  ( -12.00546221442099082, 67.70198623451226183, -6.182780363064463103 ) ) ;
#1371=CARTESIAN_POINT ( 'NONE',  ( 13.50008151215212671, 54.43042949225134208, -0.01282350395396137689 ) ) ;
#1374=CARTESIAN_POINT ( 'NONE',  ( -12.01698627149207255, 64.70299437077932225, -6.156538469565180804 ) ) ;
#1375=CARTESIAN_POINT ( 'NONE',  ( -13.50000000000000000, 63.92999999999999972, -3.306546357697853733E-15 ) ) ;
#1376=CARTESIAN_POINT ( 'NONE',  ( -13.47844695735242126, 34.96030382913254897, 0.8794953320084257786 ) ) ;
#1377=VERTEX_POINT ( 'NONE', #16754 ) ;
#1379=CARTESIAN_POINT ( 'NONE',  ( -0.2969749873785103578, 31.19067812498207104, -13.50000000000000711 ) ) ;
#1380=CARTESIAN_POINT ( 'NONE',  ( 5.463127872796244233, 72.98208016960933264, -12.34858486968830427 ) ) ;
#1384=CARTESIAN_POINT ( 'NONE',  ( -13.46935105989159354, 52.89853437352409316, -0.9121747106428150786 ) ) ;
#1387=CARTESIAN_POINT ( 'NONE',  ( -7.272992578804307939, 50.47999999999999687, -10.01041549318726886 ) ) ;
#1388=CARTESIAN_POINT ( 'NONE',  ( -8.343458848123582072, 64.37999999999998124, 11.48378591275254124 ) ) ;
#1389=CARTESIAN_POINT ( 'NONE',  ( 4.440954443873683211, 50.83963344985475885, 12.75191637729435357 ) ) ;
#1390=CARTESIAN_POINT ( 'NONE',  ( -5.576691037129440254, 37.38238622676195888, -12.29433165838705300 ) ) ;
#1391=CARTESIAN_POINT ( 'NONE',  ( 4.653539263734507436, 35.84745211565388701, 12.67597189436627403 ) ) ;
#1393=CARTESIAN_POINT ( 'NONE',  ( -11.25831317180859692, 74.20964794744398318, 7.449907306601299517 ) ) ;
#1394=CARTESIAN_POINT ( 'NONE',  ( -10.39579503320424436, 76.60004714428708894, -8.615611839668220640 ) ) ;
#1395=CARTESIAN_POINT ( 'NONE',  ( -9.858077159528473743, 79.57156653839524552, -9.233591285681558958 ) ) ;
#1397=CARTESIAN_POINT ( 'NONE',  ( 4.992525441480580639, 80.92999999999996419, 12.45192268195276952 ) ) ;
#1398=DIRECTION ( 'NONE',  ( -0.000000000000000000, -1.000000000000000000, -0.000000000000000000 ) ) ;
#1400=CARTESIAN_POINT ( 'NONE',  ( -3.636496289402153081, 44.32999999999999829, -11.19198476289190936 ) ) ;
#1404=CARTESIAN_POINT ( 'NONE',  ( -5.683316182202581501, 40.38652174635834058, -12.24545745996583257 ) ) ;
#1406=CARTESIAN_POINT ( 'NONE',  ( 10.26510932771960505, 75.09330710058536340, 8.767992633449631867 ) ) ;
#1408=CARTESIAN_POINT ( 'NONE',  ( -3.636496289402153081, 44.32999999999999829, -11.19198476289190936 ) ) ;
#1409=CARTESIAN_POINT ( 'NONE',  ( -11.68127071909253090, 41.18172457130780373, 6.770866295227015996 ) ) ;
#1410=CARTESIAN_POINT ( 'NONE',  ( -8.422466027777701925, 58.50203747567191215, -10.55087072492730726 ) ) ;
#1411=CARTESIAN_POINT ( 'NONE',  ( -8.891200544363830713E-16, 58.67999999999999261, 13.50000000000000000 ) ) ;
#1412=CARTESIAN_POINT ( 'NONE',  ( 6.750022862106053623, 29.92926176209967437, 11.69132975161703669 ) ) ;
#1414=CARTESIAN_POINT ( 'NONE',  ( -13.47356114761061896, 49.90085270701082720, -0.8452802774780980855 ) ) ;
#1415=CARTESIAN_POINT ( 'NONE',  ( 13.36701738278523699, 63.49611584409814213, -1.890200968080443911 ) ) ;
#1416=CARTESIAN_POINT ( 'NONE',  ( 12.32211066819836986, 42.22827443285392235, 5.515240709522629459 ) ) ;
#1417=CARTESIAN_POINT ( 'NONE',  ( 1.448380041428809273, 38.73207828558371801, 13.42211311086453485 ) ) ;
#1424=CARTESIAN_POINT ( 'NONE',  ( -5.008917595718572535, 43.36076862181904801, -12.53804254533077689 ) ) ;
#1425=CARTESIAN_POINT ( 'NONE',  ( -7.499999999999998224, 108.4757119436330584, 3.584587286925195126 ) ) ;
#1426=CARTESIAN_POINT ( 'NONE',  ( 9.798639380625722595, 60.79125297211457735, -9.294035878196183376 ) ) ;
#1429=CARTESIAN_POINT ( 'NONE',  ( 12.77134458573675602, 66.58771978361312449, -4.375411503001064517 ) ) ;
#1430=CARTESIAN_POINT ( 'NONE',  ( 3.922183893232446650, 56.82075162799759482, 12.92321760331618030 ) ) ;
#1431=CARTESIAN_POINT ( 'NONE',  ( -11.76794919243112325, 68.77999999999998693, -3.823638476888998827 ) ) ;
#1432=CARTESIAN_POINT ( 'NONE',  ( 11.76794919243112680, 64.57999999999999829, -3.823638476888993942 ) ) ;
#1433=CARTESIAN_POINT ( 'NONE',  ( -7.335511309088512455, 47.40615135898282517, 11.33352093287819073 ) ) ;
#1434=DIRECTION ( 'NONE',  ( 0.000000000000000000, -1.000000000000000000, 0.000000000000000000 ) ) ;
#1437=CARTESIAN_POINT ( 'NONE',  ( -2.198133652130575211, 56.60094066944324709, 13.31991233539677921 ) ) ;
#1439=DIRECTION ( 'NONE',  ( 0.000000000000000000, -1.000000000000000000, 0.000000000000000000 ) ) ;
#1440=CARTESIAN_POINT ( 'NONE',  ( 12.00158882157005991, 33.65803713169809441, -6.181575385805966327 ) ) ;
#1441=CARTESIAN_POINT ( 'NONE',  ( -9.967793045472657099, 73.57753319009304960, -9.105432612504264611 ) ) ;
#1444=ADVANCED_FACE ( 'NONE', ( #7582 ), #6173, .T. ) ;
#1446=CARTESIAN_POINT ( 'NONE',  ( -5.032544374794751363, 62.49832613186128327, 12.52840728639462853 ) ) ;
#1448=APPLICATION_CONTEXT ( 'automotive_design' ) ;
#1450=CARTESIAN_POINT ( 'NONE',  ( -13.18851637220922690, 44.03230396172555317, 2.886947055359128100 ) ) ;
#1453=CARTESIAN_POINT ( 'NONE',  ( 10.92172942406179104, 45.72999999999999687, -7.935100905948385908 ) ) ;
#1454=CARTESIAN_POINT ( 'NONE',  ( 8.343458848123578520, 49.97999999999998977, 11.48378591275254124 ) ) ;
#1455=CARTESIAN_POINT ( 'NONE',  ( -13.49749511909229938, 70.92107257862903680, -0.2602492951671970256 ) ) ;
#1457=CARTESIAN_POINT ( 'NONE',  ( -2.939452924911615028, 67.28569332682523907, -13.17610025439934418 ) ) ;
#1460=CARTESIAN_POINT ( 'NONE',  ( 13.42620872007250021, 54.48099588213615618, -1.465427023774013238 ) ) ;
#1461=CARTESIAN_POINT ( 'NONE',  ( -13.12121150380120405, 65.04454592078904795, 3.225014459927483479 ) ) ;
#1462=EDGE_CURVE ( 'NONE', #15411, #6381, #10321, .T. ) ;
#1464=CARTESIAN_POINT ( 'NONE',  ( -2.138189944381236884, 63.25688142232026223, -13.50000000000000000 ) ) ;
#1465=CARTESIAN_POINT ( 'NONE',  ( -13.01212560558737685, 34.80158386758054689, -3.596716132205523220 ) ) ;
#1466=EDGE_LOOP ( 'NONE', ( #9715, #8478, #9152, #5189 ) ) ;
#1467=CARTESIAN_POINT ( 'NONE',  ( 12.85971963305189902, 78.28239814670027386, 4.108247630965401243 ) ) ;
#1468=CARTESIAN_POINT ( 'NONE',  ( 1.653273178848926472E-15, 80.93000000000000682, 13.50000000000000000 ) ) ;
#1469=CARTESIAN_POINT ( 'NONE',  ( -3.039705960452427469, 31.28929609180920579, -13.15420631222019132 ) ) ;
#1470=CARTESIAN_POINT ( 'NONE',  ( 10.29308383338549859, 72.76519627777207688, -8.735152889481485161 ) ) ;
#1475=CARTESIAN_POINT ( 'NONE',  ( 4.171729424061789260, 71.82999999999999829, 12.83926296998457417 ) ) ;
#1476=CARTESIAN_POINT ( 'NONE',  ( -11.66078065398632191, 52.67688486108551160, -6.805658509415644097 ) ) ;
#1478=CARTESIAN_POINT ( 'NONE',  ( -7.576616670048093940E-16, 45.67999999999999261, 12.37355403259654985 ) ) ;
#1479=CARTESIAN_POINT ( 'NONE',  ( 4.171729424061791924, 63.03000000000000114, -12.83926296998457239 ) ) ;
#1481=CARTESIAN_POINT ( 'NONE',  ( 13.41380563842359486, 69.37697373310895443, 1.523135287452938691 ) ) ;
#1482=CARTESIAN_POINT ( 'NONE',  ( -4.726456801501960570, 37.35019383979712870, -12.64734214246707822 ) ) ;
#1483=CARTESIAN_POINT ( 'NONE',  ( 13.50017362217845118, 36.42540073931617428, 0.1282887782157201839 ) ) ;
#1485=CARTESIAN_POINT ( 'NONE',  ( -12.08134441457838371, 74.15176713050708202, 6.024497238434195268 ) ) ;
#1486=CARTESIAN_POINT ( 'NONE',  ( -13.29890090237351608, 76.84837936454550800, -2.321472569501058292 ) ) ;
#1487=AXIS2_PLACEMENT_3D ( 'NONE', #5312, #5135, #10525 ) ;
#1489=CARTESIAN_POINT ( 'NONE',  ( -12.38400671196816383, 79.73365040721881769, -5.379209168480316272 ) ) ;
#1490=CARTESIAN_POINT ( 'NONE',  ( -0.7362654489766442545, 80.93000000000003524, 13.00758670406994355 ) ) ;
#1491=FACE_OUTER_BOUND ( 'NONE', #16923, .T. ) ;
#1493=CARTESIAN_POINT ( 'NONE',  ( 3.636496289402157078, 50.03000000000000114, -11.19198476289190936 ) ) ;
#1497=CARTESIAN_POINT ( 'NONE',  ( 11.38591239875901273, 75.15846830473550710, 7.253424416596073954 ) ) ;
#1499=CARTESIAN_POINT ( 'NONE',  ( 11.76794919243112325, 31.42999999999999972, 1.441158131103945434E-15 ) ) ;
#1500=CARTESIAN_POINT ( 'NONE',  ( -8.136154617392147514, 41.37131206498728631, 10.78203447320519182 ) ) ;
#1501=CARTESIAN_POINT ( 'NONE',  ( -6.420066188578533506, 58.41575564973159373, -11.88523871910323670 ) ) ;
#1502=CARTESIAN_POINT ( 'NONE',  ( 4.399052845997258210, 44.83819265409231036, 12.76382163886394672 ) ) ;
#1504=FACE_OUTER_BOUND ( 'NONE', #15495, .T. ) ;
#1506=CARTESIAN_POINT ( 'NONE',  ( -8.651203465105309576, 49.51225507058038744, -10.37610565160799858 ) ) ;
#1507=CARTESIAN_POINT ( 'NONE',  ( 11.51013096457343110, 63.69335374111208381, -7.054565399514032720 ) ) ;
#1508=CARTESIAN_POINT ( 'NONE',  ( 10.57057823592805335, 42.11001419281064528, 8.397306183127296819 ) ) ;
#1509=CARTESIAN_POINT ( 'NONE',  ( 4.962292416515707849, 38.85892357782116591, 12.55684533990331175 ) ) ;
#1510=ORIENTED_EDGE ( 'NONE', *, *, #617, .F. ) ;
#1511=CARTESIAN_POINT ( 'NONE',  ( -3.961846529824640584, 70.32245338488193909, -12.90557292749110019 ) ) ;
#1514=CARTESIAN_POINT ( 'NONE',  ( -2.416183868245585842, 43.26687697742507055, -13.28262826839602084 ) ) ;
#1516=CARTESIAN_POINT ( 'NONE',  ( 6.542732549386596652, 60.93925339870889957, -11.80881426700419468 ) ) ;
#1519=CARTESIAN_POINT ( 'NONE',  ( 13.10901505835366265, 66.54634616873129005, -3.274170164232866664 ) ) ;
#1520=CARTESIAN_POINT ( 'NONE',  ( 4.906913175764546331, 56.85693511058605765, 12.57669196521769095 ) ) ;
#1521=CARTESIAN_POINT ( 'NONE',  ( 7.272992578804311492, 58.88000000000000256, -10.01041549318726709 ) ) ;
#1522=CARTESIAN_POINT ( 'NONE',  ( 11.76794919243112325, 70.28000000000000114, 3.823638476888996607 ) ) ;
#1523=CARTESIAN_POINT ( 'NONE',  ( -8.816587287286456132, 47.33998666666719402, 10.23251018546078583 ) ) ;
#1524=ADVANCED_FACE ( 'NONE', ( #13135, #17104 ), #5011, .F. ) ;
#1528=CARTESIAN_POINT ( 'NONE',  ( -7.972521863940812636, 56.37881760393914021, 10.91819665946111151 ) ) ;
#1531=CIRCLE ( 'NONE', #9464, 6.000000000000000000 ) ;
#1532=CARTESIAN_POINT ( 'NONE',  ( 11.22862360393084202, 33.71149563479018241, -7.494544542091995609 ) ) ;
#1536=CARTESIAN_POINT ( 'NONE',  ( -3.886324430026127708, 62.54026215031276337, 12.92852040802742053 ) ) ;
#1539=CARTESIAN_POINT ( 'NONE',  ( -13.25829652241704970, 44.01964385073794261, 2.543230693382868335 ) ) ;
#1541=CARTESIAN_POINT ( 'NONE',  ( -8.343458848123576743, 31.47999999999999687, -11.48378591275254301 ) ) ;
#1542=CARTESIAN_POINT ( 'NONE',  ( 8.343458848123578520, 46.97999999999998977, 11.48378591275254124 ) ) ;
#1543=CARTESIAN_POINT ( 'NONE',  ( -13.48705080653788002, 70.90931382874535416, -0.6006972830549630604 ) ) ;
#1545=CARTESIAN_POINT ( 'NONE',  ( -2.845161873668661023, 67.28236192527593573, -13.19680914032984553 ) ) ;
#1547=CARTESIAN_POINT ( 'NONE',  ( 13.06806765790989822, 54.30935285006482616, 3.387711129923342668 ) ) ;
#1549=CARTESIAN_POINT ( 'NONE',  ( -3.720992066526385145, 64.31351913756894589, -12.97891995391547404 ) ) ;
#1551=CARTESIAN_POINT ( 'NONE',  ( -13.31284211965473219, 35.00873797297208512, 2.241149820570724760 ) ) ;
#1552=ORIENTED_EDGE ( 'NONE', *, *, #5033, .F. ) ;
#1553=CARTESIAN_POINT ( 'NONE',  ( 13.41149850370572238, 78.37616975112200635, 1.543702408172776375 ) ) ;
#1557=CARTESIAN_POINT ( 'NONE',  ( 11.12432746466444478, 72.71790841392339644, -7.648681935121548925 ) ) ;
#1558=CARTESIAN_POINT ( 'NONE',  ( 6.558562036928162087, 59.92140053412916245, 11.79980395858304298 ) ) ;
#1560=VECTOR ( 'NONE', #15768, 1000.000000000000000 ) ;
#1561=CARTESIAN_POINT ( 'NONE',  ( 13.49999999999999822, 75.28000000000000114, 4.386415899144237684 ) ) ;
#1562=CARTESIAN_POINT ( 'NONE',  ( -13.47525611461717610, 52.90179884393261034, -0.8176782787010556941 ) ) ;
#1563=CARTESIAN_POINT ( 'NONE',  ( 9.520470885617715595, 49.13000000000000256, 6.917026985038134512 ) ) ;
#1564=CARTESIAN_POINT ( 'NONE',  ( 13.50000000000000355, 62.57999999999999119, -4.386415899144233244 ) ) ;
#1566=CARTESIAN_POINT ( 'NONE',  ( 1.689034877922362510, 50.74073306604915246, 13.39397960069070059 ) ) ;
#1567=CARTESIAN_POINT ( 'NONE',  ( 7.506036428011613637, 68.96118737518608555, 11.22175974229874562 ) ) ;
#1571=CARTESIAN_POINT ( 'NONE',  ( -13.03759029931439350, 74.05493905520845033, 3.503315162420880924 ) ) ;
#1573=CARTESIAN_POINT ( 'NONE',  ( -13.03456398638965119, 76.80422654878610444, -3.523612153066970620 ) ) ;
#1574=CARTESIAN_POINT ( 'NONE',  ( -2.011276037618017209, 79.25206798469932323, -13.37631185983492799 ) ) ;
#1579=CARTESIAN_POINT ( 'NONE',  ( 11.76794919243112325, 46.42999999999999972, 1.441158131103945434E-15 ) ) ;
#1581=CARTESIAN_POINT ( 'NONE',  ( 13.50000000000000355, 35.57999999999999829, -4.386415899144233244 ) ) ;
#1582=CARTESIAN_POINT ( 'NONE',  ( 13.26855327705798615, 75.34217119327314549, 2.493469984181274857 ) ) ;
#1584=AXIS2_PLACEMENT_3D ( 'NONE', #6330, #11719, #17184 ) ;
#1586=CARTESIAN_POINT ( 'NONE',  ( -11.16325391095078601, 41.21556957424302681, 7.591565366864450048 ) ) ;
#1588=CARTESIAN_POINT ( 'NONE',  ( 4.626088177006855595, 52.01347804022521615, -12.68284349646924092 ) ) ;
#1589=CARTESIAN_POINT ( 'NONE',  ( 1.156423937993576345, 44.72144737391447222, 13.45781478867673897 ) ) ;
#1590=CARTESIAN_POINT ( 'NONE',  ( 0.000000000000000000, 80.93000000000000682, -12.00000000000000178 ) ) ;
#1593=CARTESIAN_POINT ( 'NONE',  ( -12.15092532215536636, 49.71386956109132171, -5.882865350636430790 ) ) ;
#1594=CARTESIAN_POINT ( 'NONE',  ( 10.65813095105755970, 63.11492048044581082, 8.285788074620803911 ) ) ;
#1595=B_SPLINE_CURVE_WITH_KNOTS ( 'NONE', 3,
 ( #17292, #9278, #7859, #13150, #9011, #13234, #10337, #11914, #5024, #6358, #3692, #4938, #15957, #5295, #13317, #15692, #14368, #1122, #858, #11831, #14458, #5205, #14630, #17119, #3598, #10423, #3863, #16043, #7684, #9192, #6535, #9105, #11655, #2345, #1209, #17209, #10595, #17033, #6618, #2256, #1038, #2515, #3951, #3780, #7777, #7944, #9364, #6446, #11998, #17380, #11741, #10677, #14714, #15783, #7597, #12975, #5119, #6268, #14541, #13063, #945, #10511, #15873, #2428, #11114, #14886, #9802, #15060, #16125, #12170, #9627, #241, #1288, #13399, #6702, #4214, #2958, #12081, #8121, #17462, #324, #1551, #61, #4302, #8211, #1640, #4036, #13488, #2869, #5465, #10847, #7057, #16215, #1376, #12438, #2781, #4126, #16400, #6790, #9539, #9450, #16486, #14977, #6970, #13573, #12348, #2602, #8301, #6884, #4392, #5377, #14799, #1465, #151, #13741, #10762, #2690, #13657, #5647, #12256, #5557, #10941, #16306, #11028, #5733, #8387, #9714, #8033, #16663, #3046, #15148, #11286, #4657, #501, #11203, #8476, #15499, #16578, #7224, #13827, #5907, #13916, #12698, #16840, #4483, #4571, #12610, #9978, #10065, #1727, #7141, #12786, #15325, #411, #3229, #14003, #8649, #4744, #7405, #1980, #1896, #10148, #7313, #12527, #3411, #672, #5819, #585, #5996, #11378, #9892, #15240, #16750, #6085, #11464, #15415, #1810, #3321, #3138, #8736, #8563, #14095, #3979, #16337, #10877, #91, #12287, #12375, #2809, #13683, #4244, #9654, #9307 ),
 .UNSPECIFIED., .F., .F.,
 ( 4, 2, 1, 1, 2, 2, 1, 2, 2, 2, 2, 1, 2, 2, 1, 2, 2, 2, 1, 2, 2, 1, 2, 2, 1, 1, 1, 2, 2, 1, 1, 2, 2, 2, 2, 2, 1, 1, 1, 1, 2, 2, 2, 1, 1, 2, 2, 2, 2, 2, 2, 1, 1, 2, 2, 1, 1, 2, 2, 2, 1, 2, 2, 1, 2, 2, 2, 2, 2, 2, 2, 2, 2, 1, 2, 2, 1, 1, 1, 1, 2, 2, 1, 2, 2, 1, 1, 1, 2, 2, 2, 2, 1, 1, 2, 2, 2, 2, 2, 1, 1, 2, 2, 1, 1, 2, 2, 2, 2, 2, 1, 1, 2, 2, 2, 2, 4 ),
 ( 0.8872638927956195687, 0.8881829932133823435, 0.8882978807656026765, 0.8883553245417128430, 0.8883696854857403569, 0.8883840464297679818, 0.8884127683178230095, 0.8886425434222637865, 0.8891020936311452294, 0.8900211940489080042, 0.8902509691533487812, 0.8903658567055691142, 0.8903945785936241419, 0.8904233004816792807, 0.8904807442577894472, 0.8909402944666708901, 0.8918593948844337760, 0.8923189450933152189, 0.8923763888694253854, 0.8924051107574805242, 0.8924338326455355519, 0.8925487201977559959, 0.8927784953021966619, 0.8936975957199596587, 0.8941571459288411017, 0.8943869210332818787, 0.8944443648093920451, 0.8944587257534195590, 0.8944659062254333159, 0.8944730866974471839, 0.8945018085855022116, 0.8946166961377225446, 0.8955357965554855415, 0.8964548969732485384, 0.8964836188613036771, 0.8964907993333174341, 0.8964979798053311910, 0.8965123407493587049, 0.8965697845254688714, 0.8966846720776892044, 0.8969144471821298703, 0.8973739973910110912, 0.8982930978087736440, 0.8984079853609939770, 0.8984654291371041435, 0.8984941510251591712, 0.8985228729132143100, 0.8987526480176549759, 0.8992121982265361968, 0.9001312986442987496, 0.9003610737487394156, 0.9004759613009596375, 0.9005334050770698040, 0.9005477660210974289, 0.9005549464931111858, 0.9005621269651249428, 0.9005908488531799705, 0.9010503990620614134, 0.9019694994798241883, 0.9024290496887056312, 0.9025439372409259642, 0.9025726591289811029, 0.9026013810170361307, 0.9026588247931462972, 0.9028885998975869631, 0.9038077003153497380, 0.9042672505242311809, 0.9044970256286718469, 0.9045544694047820133, 0.9046119131808921798, 0.9047268007331125128, 0.9056459011508752877, 0.9065650015686380625, 0.9066224453447482290, 0.9066368062887758539, 0.9066439867607896108, 0.9066511672328033677, 0.9066798891208585065, 0.9067947766730788395, 0.9070245517775195054, 0.9074841019864009484, 0.9084032024041638342, 0.9086329775086046112, 0.9086616993966596389, 0.9086688798686735069, 0.9086760603406872638, 0.9086904212847147777, 0.9087478650608250552, 0.9088627526130454992, 0.9093223028219273862, 0.9102414032396911603, 0.9104711783441321593, 0.9105860658963526033, 0.9106435096724627698, 0.9106722315605179086, 0.9107009534485730473, 0.9111605036574549343, 0.9120796040752185974, 0.9125391542841004844, 0.9126540418363209284, 0.9127114856124312059, 0.9127186660844449628, 0.9127258465564587198, 0.9127402075004863446, 0.9127689293885414834, 0.9129987044929823714, 0.9134582547018642584, 0.9136880298063051464, 0.9139178049107460344, 0.9143773551196279215, 0.9146071302240688095, 0.9147220177762893645, 0.9147507396643443922, 0.9147794615523995310, 0.9148369053285098085, 0.9157560057462735825, 0.9166751061640373566 ),
 .UNSPECIFIED. ) ;
#1596=CARTESIAN_POINT ( 'NONE',  ( 13.37184084406137430, 42.36507920723824583, 1.857074438056610433 ) ) ;
#1597=CARTESIAN_POINT ( 'NONE',  ( 4.259800649283492113, 38.83317359495975296, 12.81031967732963750 ) ) ;
#1599=CARTESIAN_POINT ( 'NONE',  ( 2.272985001014427393E-15, 77.17999999999999261, -12.37355403259654807 ) ) ;
#1604=CARTESIAN_POINT ( 'NONE',  ( -5.745312699652264321, 43.38893832881636570, -12.21663294598238814 ) ) ;
#1605=CARTESIAN_POINT ( 'NONE',  ( -7.500000000000000000, 106.2113042096659257, 8.086389325435060726 ) ) ;
#1606=CARTESIAN_POINT ( 'NONE',  ( 9.270367474829679821, 60.81777984582654994, -9.813849793336233418 ) ) ;
#1608=LINE ( 'NONE', #1780, #9666 ) ;
#1609=CARTESIAN_POINT ( 'NONE',  ( 13.44655200584734622, 66.38838457564831685, 1.200152482059077208 ) ) ;
#1610=CARTESIAN_POINT ( 'NONE',  ( 1.669445390708271804, 56.74002890137526833, 13.39659988532823220 ) ) ;
#1611=CARTESIAN_POINT ( 'NONE',  ( -9.520470885617715595, 62.63000000000000256, -6.917026985038136289 ) ) ;
#1612=CARTESIAN_POINT ( 'NONE',  ( -11.76794919243112325, 68.77999999999998693, -3.823638476888998827 ) ) ;
#1614=CARTESIAN_POINT ( 'NONE',  ( -13.38138642673853340, 46.86721787022950991, -1.795383226577773828 ) ) ;
#1615=CARTESIAN_POINT ( 'NONE',  ( -2.138189944381279073, 45.25688142232026934, -13.49999999999998579 ) ) ;
#1617=CARTESIAN_POINT ( 'NONE',  ( 5.882695696613415848, 30.96571419329114860, -12.15092755760450594 ) ) ;
#1618=CARTESIAN_POINT ( 'NONE',  ( -1.553209143042241003, 56.62434124648177658, 13.41219526395410533 ) ) ;
#1620=CARTESIAN_POINT ( 'NONE',  ( -8.891200544363830713E-16, 40.67999999999999261, 13.50000000000000000 ) ) ;
#1621=CARTESIAN_POINT ( 'NONE',  ( 13.29512141749893495, 33.34760041236136630, 2.343023588158895887 ) ) ;
#1625=CARTESIAN_POINT ( 'NONE',  ( -5.813220906962667023, 62.46839348748255816, 12.18503415927900235 ) ) ;
#1629=CARTESIAN_POINT ( 'NONE',  ( -11.73445831788195015, 44.17842776096925661, 6.691153486874162226 ) ) ;
#1631=CARTESIAN_POINT ( 'NONE',  ( 8.343458848123583849, 33.87999999999998835, -11.48378591275253768 ) ) ;
#1632=CARTESIAN_POINT ( 'NONE',  ( 8.343458848123578520, 43.97999999999999687, 11.48378591275254124 ) ) ;
#1633=CARTESIAN_POINT ( 'NONE',  ( -9.608163084644951724, 46.55906845273868555, -9.483316201871774709 ) ) ;
#1634=CARTESIAN_POINT ( 'NONE',  ( -10.11174617855943048, 67.58510651382286483, -8.944425511103352378 ) ) ;
#1636=CARTESIAN_POINT ( 'NONE',  ( 13.49936567077070571, 54.43455718009003874, -0.1330465375380656678 ) ) ;
#1637=CARTESIAN_POINT ( 'NONE',  ( -10.37798312408888357, 64.59933206745596124, -8.634316133104666946 ) ) ;
#1638=ORIENTED_EDGE ( 'NONE', *, *, #6605, .F. ) ;
#1640=CARTESIAN_POINT ( 'NONE',  ( -13.34459694652892736, 35.00157342978971542, 2.042509889357819297 ) ) ;
#1643=CARTESIAN_POINT ( 'NONE',  ( 11.86781241222626804, 78.19182051743750606, 6.434699402502147336 ) ) ;
#1644=LINE ( 'NONE', #16667, #16889 ) ;
#1645=CARTESIAN_POINT ( 'NONE',  ( -2.138189944381236884, 36.25688142232026934, -13.50000000000000000 ) ) ;
#1646=CARTESIAN_POINT ( 'NONE',  ( 8.269754895910567782, 72.86495716742260242, -10.67059466400652212 ) ) ;
#1647=CARTESIAN_POINT ( 'NONE',  ( 0.2546894329666128942, 79.17084467311261164, -13.49793087839145045 ) ) ;
#1649=CARTESIAN_POINT ( 'NONE',  ( 10.92172942406179104, 60.72999999999999687, -7.935100905948385908 ) ) ;
#1650=CARTESIAN_POINT ( 'NONE',  ( -12.66562697099517010, 53.09995439154507579, 4.693458508799205120 ) ) ;
#1651=CARTESIAN_POINT ( 'NONE',  ( 11.76794919243112325, 40.42999999999999972, 1.441158131103945434E-15 ) ) ;
#1652=CARTESIAN_POINT ( 'NONE',  ( 10.92172942406178926, 62.13000000000000256, 7.935100905948387684 ) ) ;
#1654=AXIS2_PLACEMENT_3D ( 'NONE', #13119, #7658, #6418 ) ;
#1655=CARTESIAN_POINT ( 'NONE',  ( 9.824684847845674085, 69.07009303822928814, 9.259413530656892988 ) ) ;
#1656=CARTESIAN_POINT ( 'NONE',  ( 1.203083463835363736E-13, 37.18000000000000682, -13.50000000000000000 ) ) ;
#1657=CARTESIAN_POINT ( 'NONE',  ( -1.844924112955495524E-14, 72.18000000000000682, -13.50000000000000000 ) ) ;
#1659=CARTESIAN_POINT ( 'NONE',  ( -6.548632089216652297, 74.43902180796270329, 11.80836097895562808 ) ) ;
#1660=CARTESIAN_POINT ( 'NONE',  ( -6.667109426283460927, 76.42579604055075038, -11.74159768812344851 ) ) ;
#1661=CARTESIAN_POINT ( 'NONE',  ( 4.178864255851000829E-14, 67.68000000000000682, 13.50000000000000000 ) ) ;
#1667=CARTESIAN_POINT ( 'NONE',  ( 11.76794919243112325, 34.42999999999999261, 1.441158131103945434E-15 ) ) ;
#1669=CARTESIAN_POINT ( 'NONE',  ( -8.224381812979805417, 32.36732010438169738, 10.71482383986382914 ) ) ;
#1670=CARTESIAN_POINT ( 'NONE',  ( 13.06412971713287163, 75.55120420896997757, -3.402724263452373776 ) ) ;
#1672=CARTESIAN_POINT ( 'NONE',  ( -10.92172942406178926, 81.63000000000000966, -7.935100905948389460 ) ) ;
#1673=DIRECTION ( 'NONE',  ( 0.000000000000000000, -1.000000000000000000, 0.000000000000000000 ) ) ;
#1674=CARTESIAN_POINT ( 'NONE',  ( -1.563903264707652063, 38.62376394199530694, 13.40911344051972165 ) ) ;
#1675=CARTESIAN_POINT ( 'NONE',  ( 0.06699739813339644634, 37.17759102313722508, -13.49985266111775140 ) ) ;
#1676=CARTESIAN_POINT ( 'NONE',  ( -2.138189944381240881, 58.60311857767971588, 13.49999999999999822 ) ) ;
#1677=CARTESIAN_POINT ( 'NONE',  ( 9.335235950531815854E-15, 58.17999999999999972, -13.50000000000000178 ) ) ;
#1678=CARTESIAN_POINT ( 'NONE',  ( 7.724747335437769813, 62.97064110457201025, 11.07293518791896325 ) ) ;
#1679=CARTESIAN_POINT ( 'NONE',  ( 13.49647439015347494, 42.44165888383876251, -0.3403877991304248285 ) ) ;
#1680=CARTESIAN_POINT ( 'NONE',  ( 5.946050977868895693, 48.96319313644542603, -12.12000444874419181 ) ) ;
#1682=ORIENTED_EDGE ( 'NONE', *, *, #4123, .T. ) ;
#1683=CARTESIAN_POINT ( 'NONE',  ( -11.76794919243112325, 71.78000000000000114, -3.823638476888998827 ) ) ;
#1684=CARTESIAN_POINT ( 'NONE',  ( -1.762261258681115050, 70.24333474961797208, -13.38630411701529432 ) ) ;
#1689=CARTESIAN_POINT ( 'NONE',  ( -11.10596490569379746, 43.64093710854871233, -7.675131488725745577 ) ) ;
#1690=CARTESIAN_POINT ( 'NONE',  ( -7.499999999999999112, 102.9300000000000068, 9.367496997597601904 ) ) ;
#1691=CARTESIAN_POINT ( 'NONE',  ( 7.888673446950843271, 60.88244582797990034, -10.96439275093654331 ) ) ;
#1694=CARTESIAN_POINT ( 'NONE',  ( 10.20567559529917467, 66.09011338957789405, 8.837093107525932467 ) ) ;
#1695=CARTESIAN_POINT ( 'NONE',  ( 3.272928082058740973, 56.79766793957027460, 13.09725250748105019 ) ) ;
#1696=CARTESIAN_POINT ( 'NONE',  ( -3.636496289402153081, 59.32999999999999829, -11.19198476289190936 ) ) ;
#1697=CARTESIAN_POINT ( 'NONE',  ( 13.50000000000000000, 35.42999999999999972, 1.653273178848926867E-15 ) ) ;
#1698=CARTESIAN_POINT ( 'NONE',  ( -7.272992578804307939, 62.47999999999998977, -10.01041549318726886 ) ) ;
#1699=CARTESIAN_POINT ( 'NONE',  ( -12.88439216619325656, 46.78478293884005978, -4.045317359391656709 ) ) ;
#1700=CARTESIAN_POINT ( 'NONE',  ( 10.60034612014990785, 45.74832029320175764, -8.359593683353010007 ) ) ;
#1703=CARTESIAN_POINT ( 'NONE',  ( 0.1761290692243684397, 31.17366705685581607, -13.49886709375031835 ) ) ;
#1704=CARTESIAN_POINT ( 'NONE',  ( -5.514694689034828734, 56.48000644630477751, 12.32227558934507883 ) ) ;
#1706=CARTESIAN_POINT ( 'NONE',  ( 2.445080149700053643E-15, 54.17999999999999972, -13.50000000000000000 ) ) ;
#1708=CARTESIAN_POINT ( 'NONE',  ( 1.263604227248463552, 32.72543457727589100, 13.44074022279856528 ) ) ;
#1711=ORIENTED_EDGE ( 'NONE', *, *, #5923, .T. ) ;
#1712=CARTESIAN_POINT ( 'NONE',  ( -8.583784865206528281, 62.35052710088542227, 10.42004576716591480 ) ) ;
#1714=ADVANCED_FACE ( 'NONE', ( #8585 ), #16330, .T. ) ;
#1717=CARTESIAN_POINT ( 'NONE',  ( -12.93062576379450768, 43.79088317389158647, -3.882584947338488135 ) ) ;
#1719=CARTESIAN_POINT ( 'NONE',  ( -11.76794919243112325, 83.78000000000001535, -3.823638476888998827 ) ) ;
#1720=CARTESIAN_POINT ( 'NONE',  ( -2.510641289628237960, 46.27027268115869418, -13.26455288760042173 ) ) ;
#1721=CARTESIAN_POINT ( 'NONE',  ( -10.95561095866379908, 67.63197757295462509, -7.888270207410369217 ) ) ;
#1723=CARTESIAN_POINT ( 'NONE',  ( 4.858184606947299145, 53.85511469388424644, 12.59567537307139951 ) ) ;
#1724=CARTESIAN_POINT ( 'NONE',  ( -3.509521865719293032, 64.30599818513977084, -13.03769156727985745 ) ) ;
#1727=CARTESIAN_POINT ( 'NONE',  ( -8.582817366808168202, 34.50940347922665552, -10.42175089031515611 ) ) ;
#1729=VERTEX_POINT ( 'NONE', #9648 ) ;
#1730=CARTESIAN_POINT ( 'NONE',  ( 13.34788994058796696, 78.35896427393043950, 2.029892894008967108 ) ) ;
#1732=CARTESIAN_POINT ( 'NONE',  ( 2.445080149700053643E-15, 36.17999999999999972, -13.50000000000000000 ) ) ;
#1733=CARTESIAN_POINT ( 'NONE',  ( 13.47366125695251426, 72.39648660452563433, 0.9517480377630386235 ) ) ;
#1734=CARTESIAN_POINT ( 'NONE',  ( 7.210737393588035005, 78.91145283978082148, -11.41294504455507131 ) ) ;
#1736=CARTESIAN_POINT ( 'NONE',  ( -13.50000000000000000, 58.92999999999999972, -3.306546357697853733E-15 ) ) ;
#1737=CARTESIAN_POINT ( 'NONE',  ( -13.13863893109200021, 52.81756508269278072, -3.169477223746528960 ) ) ;
#1739=CARTESIAN_POINT ( 'NONE',  ( 10.92172942406179104, 56.73000000000000398, -7.935100905948385908 ) ) ;
#1744=CARTESIAN_POINT ( 'NONE',  ( 10.91172338423278987, 69.12941896017710519, 7.948908212395449091 ) ) ;
#1745=DIRECTION ( 'NONE',  ( 0.000000000000000000, 1.000000000000000000, 0.000000000000000000 ) ) ;
#1746=CARTESIAN_POINT ( 'NONE',  ( -13.49999999999999822, 72.77999999999998693, -4.386415899144240349 ) ) ;
#1748=CARTESIAN_POINT ( 'NONE',  ( -12.62315583374951800, 73.75659150799306474, -4.786044459331560752 ) ) ;
#1749=CARTESIAN_POINT ( 'NONE',  ( -2.404533931440186567, 76.26645795944742190, -13.28413785449006035 ) ) ;
#1755=CARTESIAN_POINT ( 'NONE',  ( -11.76794919243112325, 39.07999999999999119, 3.823638476888994830 ) ) ;
#1758=CARTESIAN_POINT ( 'NONE',  ( -9.417534539751688527, 32.31048376298131330, 9.672654054616247166 ) ) ;
#1759=CARTESIAN_POINT ( 'NONE',  ( 13.09947432517387433, 75.54609923471080890, -3.264907772012195508 ) ) ;
#1761=CARTESIAN_POINT ( 'NONE',  ( 11.76794919243112325, 31.42999999999999972, 1.441158131103945434E-15 ) ) ;
#1762=CARTESIAN_POINT ( 'NONE',  ( 8.323493681088855567, 51.86260169611556847, -10.63262715383440415 ) ) ;
#1764=CARTESIAN_POINT ( 'NONE',  ( -3.350167926867789969, 38.55967038338359032, 13.08738360368760567 ) ) ;
#1765=CARTESIAN_POINT ( 'NONE',  ( 5.881545760074193829, 36.96579597873309098, -12.15211109713918169 ) ) ;
#1766=DIRECTION ( 'NONE',  ( 0.000000000000000000, 1.000000000000000000, 0.000000000000000000 ) ) ;
#1767=CARTESIAN_POINT ( 'NONE',  ( -0.7119081483307314606, 49.20556749876198666, -13.48189764473124974 ) ) ;
#1768=CARTESIAN_POINT ( 'NONE',  ( 9.615195027071965939, 63.05942374218840030, 9.476182696171701281 ) ) ;
#1769=CARTESIAN_POINT ( 'NONE',  ( 13.48083382501841676, 42.40518313085501489, 0.7192385255011690681 ) ) ;
#1770=CARTESIAN_POINT ( 'NONE',  ( 9.370505335838927863, 48.81306206236823897, -9.728736506576064258 ) ) ;
#1773=CARTESIAN_POINT ( 'NONE',  ( -11.76794919243112325, 65.78000000000000114, -3.823638476888998827 ) ) ;
#1774=CARTESIAN_POINT ( 'NONE',  ( -3.982813593950979669, 70.32320728644485541, -12.89911927572956252 ) ) ;
#1778=CARTESIAN_POINT ( 'NONE',  ( -7.500000000000000000, 103.4443346693207957, -9.346209313438659905 ) ) ;
#1780=CARTESIAN_POINT ( 'NONE',  ( 1.469576158976823947E-15, 108.9300000000000068, 12.00000000000000178 ) ) ;
#1781=CARTESIAN_POINT ( 'NONE',  ( 12.02417248861142340, 66.20348976307651867, 6.144749074482731999 ) ) ;
#1782=CARTESIAN_POINT ( 'NONE',  ( 4.951365981876046263, 56.85859764264212401, 12.55922057576340833 ) ) ;
#1783=CARTESIAN_POINT ( 'NONE',  ( -7.272992578804310604, 60.37999999999998835, 10.01041549318726709 ) ) ;
#1784=CARTESIAN_POINT ( 'NONE',  ( -11.76794919243112325, 68.93000000000000682, -2.882316262207890869E-15 ) ) ;
#1785=CARTESIAN_POINT ( 'NONE',  ( -13.48997199921942780, 46.94790804180549770, 0.5203843874578459872 ) ) ;
#1786=CARTESIAN_POINT ( 'NONE',  ( 9.145645418827751172, 45.82382894212507551, -9.930115241637599510 ) ) ;
#1787=CARTESIAN_POINT ( 'NONE',  ( 1.760363844716795079, 70.11686978712239693, -13.39198461572166110 ) ) ;
#1788=EDGE_CURVE ( 'NONE', #3997, #4566, #5670, .T. ) ;
#1789=CARTESIAN_POINT ( 'NONE',  ( 5.939077118726382665, 30.96351101756093982, -12.12376556905278058 ) ) ;
#1790=CARTESIAN_POINT ( 'NONE',  ( -8.628727929195679991, 56.34842528014506513, 10.38244214053023384 ) ) ;
#1791=CARTESIAN_POINT ( 'NONE',  ( 10.92172942406179104, 53.72999999999999687, -7.935100905948385908 ) ) ;
#1792=CARTESIAN_POINT ( 'NONE',  ( 4.453605494073674009, 32.84020350842553171, 12.74473092711098943 ) ) ;
#1794=CARTESIAN_POINT ( 'NONE',  ( 4.336380559087108288, 40.02405505865456803, -12.78459519145104828 ) ) ;
#1795=CARTESIAN_POINT ( 'NONE',  ( -8.847428061141151545, 62.33815899834955587, 10.19748488632688854 ) ) ;
#1797=CARTESIAN_POINT ( 'NONE',  ( -13.48607429853445439, 40.95120110529397550, 0.6154623111518494616 ) ) ;
#1799=CARTESIAN_POINT ( 'NONE',  ( -10.92836780634199023, 44.22976925262064896, 7.928318132319670752 ) ) ;
#1801=CARTESIAN_POINT ( 'NONE',  ( 2.607531440858944223E-15, 34.17999999999999972, -14.19474002721660355 ) ) ;
#1802=CARTESIAN_POINT ( 'NONE',  ( -9.615460584619185624, 46.55943716852689818, -9.475913135533545528 ) ) ;
#1803=CARTESIAN_POINT ( 'NONE',  ( -3.396000859129791216, 67.30175415131174077, -13.06908703928144533 ) ) ;
#1805=CARTESIAN_POINT ( 'NONE',  ( 10.64234380851644524, 54.11403152435825348, 8.306118739732548661 ) ) ;
#1807=CARTESIAN_POINT ( 'NONE',  ( -9.211117710370606559, 64.53893790892921345, -9.889622180093912363 ) ) ;
#1810=CARTESIAN_POINT ( 'NONE',  ( -4.131518063981246769, 34.32854624200039950, -12.85268223519957687 ) ) ;
#1812=CARTESIAN_POINT ( 'NONE',  ( 10.56254081286317614, 78.10946437613924331, 8.407613947475192973 ) ) ;
#1815=CARTESIAN_POINT ( 'NONE',  ( 13.14030536245351222, 72.54035111403283054, -3.109320234174559161 ) ) ;
#1817=CARTESIAN_POINT ( 'NONE',  ( 8.343458848123583849, 60.88000000000000256, -11.48378591275253768 ) ) ;
#1818=CARTESIAN_POINT ( 'NONE',  ( -2.407714511490748777, 52.26657253894821054, -13.28356114519097808 ) ) ;
#1819=CARTESIAN_POINT ( 'NONE',  ( -9.520470885617717371, 42.22999999999999687, 6.917026985038133624 ) ) ;
#1820=CARTESIAN_POINT ( 'NONE',  ( -8.343458848123582072, 61.38000000000000256, 11.48378591275254124 ) ) ;
#1823=CARTESIAN_POINT ( 'NONE',  ( 7.856379207180958169, 68.97648971074549706, 10.97942687797863748 ) ) ;
#1824=CARTESIAN_POINT ( 'NONE',  ( 0.000000000000000000, 80.93000000000000682, -13.50000000000000000 ) ) ;
#1825=CARTESIAN_POINT ( 'NONE',  ( -13.49999999999999822, 79.07999999999999829, 4.386415899144235020 ) ) ;
#1827=CARTESIAN_POINT ( 'NONE',  ( -13.35165232598691709, 73.86010075147470388, -1.995846695151413330 ) ) ;
#1828=CARTESIAN_POINT ( 'NONE',  ( -7.122883083305794116, 76.44482685471382410, -11.46806178800632203 ) ) ;
#1829=CARTESIAN_POINT ( 'NONE',  ( 0.000000000000000000, 80.93000000000000682, -13.50000000000000000 ) ) ;
#1834=CARTESIAN_POINT ( 'NONE',  ( -7.272992578804307939, 38.47999999999999687, -10.01041549318727064 ) ) ;
#1838=CARTESIAN_POINT ( 'NONE',  ( -6.956384866273832124, 32.42216814373086464, 11.56991202652051420 ) ) ;
#1841=FACE_OUTER_BOUND ( 'NONE', #9495, .T. ) ;
#1843=CARTESIAN_POINT ( 'NONE',  ( 13.49999999999999822, 83.28000000000001535, 4.386415899144237684 ) ) ;
#1844=CARTESIAN_POINT ( 'NONE',  ( 7.503935912028310007, 51.89890203572196725, -11.22317663737363702 ) ) ;
#1846=CARTESIAN_POINT ( 'NONE',  ( -4.382597213356913102, 38.52237731888514105, 12.76882425985456315 ) ) ;
#1847=CARTESIAN_POINT ( 'NONE',  ( 1.101915621515684673, 37.14046543417862267, -13.45675805337361020 ) ) ;
#1849=CARTESIAN_POINT ( 'NONE',  ( -0.003440076053688929415, 49.18012369244059556, -13.50000000096518171 ) ) ;
#1850=CARTESIAN_POINT ( 'NONE',  ( 7.090050658895051150, 62.94344369233374437, 11.48830835003065687 ) ) ;
#1852=CARTESIAN_POINT ( 'NONE',  ( 12.30163302192313957, 48.63347965893699865, -5.560926583519345989 ) ) ;
#1855=CARTESIAN_POINT ( 'NONE',  ( 3.636496289402157078, 68.03000000000000114, -11.19198476289190936 ) ) ;
#1859=CARTESIAN_POINT ( 'NONE',  ( -0.6361984379052563199, 43.20287484601561800, -13.48515643269810482 ) ) ;
#1860=CARTESIAN_POINT ( 'NONE',  ( 6.616676866212972294E-07, 41.68001839382905160, 13.49999999999996625 ) ) ;
#1861=CIRCLE ( 'NONE', #6680, 6.000000000000001776 ) ;
#1864=CARTESIAN_POINT ( 'NONE',  ( 10.19862847849394605, 66.08974497899659184, 8.845225045481868165 ) ) ;
#1865=CARTESIAN_POINT ( 'NONE',  ( 8.343458848123583849, 81.87999999999999545, -11.48378591275253768 ) ) ;
#1866=CARTESIAN_POINT ( 'NONE',  ( 11.76794919243112325, 61.42999999999999972, 1.441158131103945434E-15 ) ) ;
#1867=CARTESIAN_POINT ( 'NONE',  ( -3.636496289402155746, 60.53000000000000114, 11.19198476289190936 ) ) ;
#1868=CARTESIAN_POINT ( 'NONE',  ( -11.31655382394981402, 46.65401601797371001, -7.361090251168096010 ) ) ;
#1869=CARTESIAN_POINT ( 'NONE',  ( 10.61521234890549437, 45.74748869403295259, -8.340708075779714292 ) ) ;
#1870=CARTESIAN_POINT ( 'NONE',  ( 8.064323603043568767, 69.87423201233190184, -10.82667199018000659 ) ) ;
#1871=CARTESIAN_POINT ( 'NONE',  ( 11.01673963448572735, 30.72451013036616274, -7.811118219500425397 ) ) ;
#1872=CARTESIAN_POINT ( 'NONE',  ( -13.48103072664150659, 55.90526753793167103, -0.7160923547902818820 ) ) ;
#1874=CARTESIAN_POINT ( 'NONE',  ( -2.021419200856401144, 50.60735096884870643, 13.34783266993481909 ) ) ;
#1875=CYLINDRICAL_SURFACE ( 'NONE', #10447, 13.50000000000000000 ) ;
#1877=CARTESIAN_POINT ( 'NONE',  ( 11.60007046564512123, 39.68814104347146809, -6.930948736540742061 ) ) ;
#1878=ORIENTED_EDGE ( 'NONE', *, *, #1885, .T. ) ;
#1879=CARTESIAN_POINT ( 'NONE',  ( -10.54291226894605948, 62.25176954414765618, 8.434806978981946202 ) ) ;
#1884=CARTESIAN_POINT ( 'NONE',  ( 9.586328625881087362, 48.05796286996289268, 9.505570431087681627 ) ) ;
#1885=EDGE_CURVE ( 'NONE', #15852, #4556, #12330, .T. ) ;
#1886=CARTESIAN_POINT ( 'NONE',  ( 8.343458848123583849, 65.87999999999999545, -11.48378591275253768 ) ) ;
#1887=CARTESIAN_POINT ( 'NONE',  ( 2.607531440858944223E-15, 31.18000000000000327, -14.19474002721660355 ) ) ;
#1888=CARTESIAN_POINT ( 'NONE',  ( -10.92172942406178926, 39.62999999999999545, -7.935100905948389460 ) ) ;
#1889=CARTESIAN_POINT ( 'NONE',  ( -0.6981953365487996166, 46.20509056809714821, -13.48253838120680648 ) ) ;
#1890=CARTESIAN_POINT ( 'NONE',  ( -0.1384335662044163251, 67.18497756035941393, -13.49929041167511201 ) ) ;
#1892=CARTESIAN_POINT ( 'NONE',  ( 4.704861780774831637, 53.84940395589381268, 12.65445563452911770 ) ) ;
#1896=CARTESIAN_POINT ( 'NONE',  ( -5.977070597187598366, 34.39803108597568126, -12.10626348371989103 ) ) ;
#1898=CARTESIAN_POINT ( 'NONE',  ( 10.45317117374106886, 78.10352698524791037, 8.542904918776255130 ) ) ;
#1900=FACE_OUTER_BOUND ( 'NONE', #13899, .T. ) ;
#1902=CARTESIAN_POINT ( 'NONE',  ( -4.171729424061791036, 37.53000000000000114, 12.83926296998457239 ) ) ;
#1903=CARTESIAN_POINT ( 'NONE',  ( 11.44827556181972561, 72.16254353962827395, 7.154521231752505095 ) ) ;
#1905=CARTESIAN_POINT ( 'NONE',  ( 13.49999999999999822, 60.28000000000000114, 4.386415899144237684 ) ) ;
#1906=CARTESIAN_POINT ( 'NONE',  ( -5.895724195551247604, 52.39485670314912369, -12.14464293266051698 ) ) ;
#1907=CARTESIAN_POINT ( 'NONE',  ( 9.520470885617717371, 37.72999999999999687, -6.917026985038131848 ) ) ;
#1909=CARTESIAN_POINT ( 'NONE',  ( -13.49999999999999822, 57.77999999999999403, -4.386415899144240349 ) ) ;
#1912=CARTESIAN_POINT ( 'NONE',  ( 12.49006955709644195, 69.24340693049718709, 5.129082213196267226 ) ) ;
#1913=CARTESIAN_POINT ( 'NONE',  ( 10.92172942406179104, 71.73000000000000398, -7.935100905948385908 ) ) ;
#1915=CARTESIAN_POINT ( 'NONE',  ( -10.57228623158748526, 73.61011962570297840, -8.395047735362636487 ) ) ;
#1916=CARTESIAN_POINT ( 'NONE',  ( -7.192128558827187490, 76.44775770338405607, -11.42468648059192837 ) ) ;
#1918=FACE_OUTER_BOUND ( 'NONE', #7402, .T. ) ;
#1921=CARTESIAN_POINT ( 'NONE',  ( -9.520470885617717371, 39.23000000000000398, 6.917026985038133624 ) ) ;
#1924=CARTESIAN_POINT ( 'NONE',  ( -9.596645353049856553, 32.30153765603851213, 9.496518015433528248 ) ) ;
#1925=CARTESIAN_POINT ( 'NONE',  ( 8.345963094611027699, 74.99851540925725146, 10.61115790671126824 ) ) ;
#1927=CARTESIAN_POINT ( 'NONE',  ( -13.49999999999999822, 81.77999999999998693, -4.386415899144240349 ) ) ;
#1928=CARTESIAN_POINT ( 'NONE',  ( -2.514712666923160089, 58.27041958369694186, -13.26394781517377197 ) ) ;
#1929=( BOUNDED_CURVE ( )  B_SPLINE_CURVE ( 2, ( #12029, #11772, #5236, #7889, #15901, #11944, #10793, #17324, #15814, #3719, #6734 ),
 .UNSPECIFIED., .F., .F. ) 
 B_SPLINE_CURVE_WITH_KNOTS ( ( 3, 2, 2, 2, 2, 3 ),
 ( 0.9583333333333333703, 0.9611111111111111382, 0.9666666666666666741, 0.9722222222222222099, 0.9777777777777777457, 0.9814746766279994761 ),
 .UNSPECIFIED. ) 
 CURVE ( )  GEOMETRIC_REPRESENTATION_ITEM ( )  RATIONAL_B_SPLINE_CURVE ( ( 0.9755282581475768211, 0.9755282581475768211, 1.000000000000000000, 0.9510565162951535312, 1.000000000000000000, 0.9510565162951535312, 1.000000000000000000, 0.9510565162951535312, 1.000000000000000000, 0.9674309604458272149, 0.9782075210486875783 ) ) 
 REPRESENTATION_ITEM ( '' )  );
#1930=CARTESIAN_POINT ( 'NONE',  ( -6.972538664597516700, 38.42149079469095341, 11.56005070210786734 ) ) ;
#1931=DIRECTION ( 'NONE',  ( 0.000000000000000000, -1.000000000000000000, 0.000000000000000000 ) ) ;
#1933=CARTESIAN_POINT ( 'NONE',  ( -0.03211762735042347078, 49.18115476286282473, -13.49996724290573979 ) ) ;
#1934=CARTESIAN_POINT ( 'NONE',  ( 2.637116012700283285, 62.77482290688431021, 13.23992697210385572 ) ) ;
#1935=CARTESIAN_POINT ( 'NONE',  ( 3.009781244587141025, 41.78827560020220488, 13.16026029025977628 ) ) ;
#1936=CARTESIAN_POINT ( 'NONE',  ( 11.19356376271605313, 48.71361357092671085, -7.550568776909073243 ) ) ;
#1938=ORIENTED_EDGE ( 'NONE', *, *, #15386, .T. ) ;
#1939=CARTESIAN_POINT ( 'NONE',  ( 11.76794919243112680, 64.57999999999999829, -3.823638476888993942 ) ) ;
#1943=CARTESIAN_POINT ( 'NONE',  ( -0.2574321900957359799, 43.18925615523563266, -13.49768559512680532 ) ) ;
#1944=CARTESIAN_POINT ( 'NONE',  ( 0.8771553176865662937, 76.14846073976488583, -13.47147415929084246 ) ) ;
#1946=CARTESIAN_POINT ( 'NONE',  ( 10.41011842078191485, 66.10092527843147536, 8.596008750921665609 ) ) ;
#1947=CARTESIAN_POINT ( 'NONE',  ( 3.636496289402157078, 47.02999999999999403, -11.19198476289190936 ) ) ;
#1948=CARTESIAN_POINT ( 'NONE',  ( -11.76794919243112325, 60.07999999999999119, 3.823638476888994386 ) ) ;
#1949=CARTESIAN_POINT ( 'NONE',  ( -13.49209704812250088, 46.94588263088257207, 0.4618880482851102087 ) ) ;
#1951=CARTESIAN_POINT ( 'NONE',  ( 11.79604064620621706, 45.67344517854842678, -6.565341261686152841 ) ) ;
#1952=CARTESIAN_POINT ( 'NONE',  ( 5.408880282457495525, 69.98389750586773062, -12.36993325487214790 ) ) ;
#1954=CARTESIAN_POINT ( 'NONE',  ( 8.881221276511888973, 30.83659605439422791, -10.16962065716281849 ) ) ;
#1956=CARTESIAN_POINT ( 'NONE',  ( -10.72093770326768336, 56.24171596241757953, 8.207164309218791587 ) ) ;
#1957=CARTESIAN_POINT ( 'NONE',  ( -2.321280251217487045, 50.59645969408896349, 13.29947824124915634 ) ) ;
#1958=DIRECTION ( 'NONE',  ( 0.000000000000000000, -1.000000000000000000, 0.000000000000000000 ) ) ;
#1959=AXIS2_PLACEMENT_3D ( 'NONE', #10154, #3233, #8653 ) ;
#1960=CARTESIAN_POINT ( 'NONE',  ( 5.377587941663005466, 42.98529261702660165, -12.38364086756679860 ) ) ;
#1961=CARTESIAN_POINT ( 'NONE',  ( 10.14338171936946154, 39.77323046559094166, -8.908990778934798627 ) ) ;
#1962=ORIENTED_EDGE ( 'NONE', *, *, #16117, .F. ) ;
#1963=CARTESIAN_POINT ( 'NONE',  ( -12.59302166875140649, 62.10670518965311970, 4.872780399208760826 ) ) ;
#1967=CARTESIAN_POINT ( 'NONE',  ( 12.40660301870904547, 48.23542586493246631, 5.339298433682001743 ) ) ;
#1968=CARTESIAN_POINT ( 'NONE',  ( 4.871064484081401247, 58.00440576964228967, -12.59088220141806680 ) ) ;
#1969=CARTESIAN_POINT ( 'NONE',  ( -9.520470885617715595, 74.62999999999999545, -6.917026985038136289 ) ) ;
#1971=CARTESIAN_POINT ( 'NONE',  ( -9.640625755184249357, 46.56070477685496201, -9.450320721539682722 ) ) ;
#1975=CARTESIAN_POINT ( 'NONE',  ( 5.053712973672062070, 53.86243577901412749, 12.51843150850086950 ) ) ;
#1976=VERTEX_POINT ( 'NONE', #6169 ) ;
#1980=CARTESIAN_POINT ( 'NONE',  ( -6.490732267001422251, 34.41855503382694081, -11.84349393051573252 ) ) ;
#1982=CARTESIAN_POINT ( 'NONE',  ( 10.46369314345858115, 78.10409437138895328, 8.530013921288347234 ) ) ;
#1985=CARTESIAN_POINT ( 'NONE',  ( 12.53173586800322248, 72.61303021391049128, -5.039560880771795759 ) ) ;
#1986=CARTESIAN_POINT ( 'NONE',  ( 7.868511876303293739, 66.88295471898928213, -10.96986588721461686 ) ) ;
#1988=CARTESIAN_POINT ( 'NONE',  ( 8.343458848123583849, 66.87999999999998124, -11.48378591275253768 ) ) ;
#1989=CARTESIAN_POINT ( 'NONE',  ( -5.803408828651975604, 52.39120852067574674, -12.18894770220534340 ) ) ;
#1990=CARTESIAN_POINT ( 'NONE',  ( -7.576616670048093940E-16, 36.67999999999999972, 12.37355403259654985 ) ) ;
#1992=CARTESIAN_POINT ( 'NONE',  ( -4.171729424061787483, 54.33000000000000540, -12.83926296998457417 ) ) ;
#1993=CARTESIAN_POINT ( 'NONE',  ( 4.171729424061789260, 76.83000000000001251, 12.83926296998457417 ) ) ;
#1995=CARTESIAN_POINT ( 'NONE',  ( -8.590017591600245694, 68.35022873601761262, 10.41449206865405586 ) ) ;
#1998=CARTESIAN_POINT ( 'NONE',  ( 4.171729424061791924, 72.03000000000000114, -12.83926296998457239 ) ) ;
#2000=CARTESIAN_POINT ( 'NONE',  ( -13.49051361190299225, 73.91252456243813640, -0.5067315784123872513 ) ) ;
#2001=CARTESIAN_POINT ( 'NONE',  ( -7.185958069586803276, 76.44749624477539385, -11.42856400538557438 ) ) ;
#2003=FACE_OUTER_BOUND ( 'NONE', #13021, .T. ) ;
#2005=CARTESIAN_POINT ( 'NONE',  ( -9.520470885617715595, 38.62999999999999545, -6.917026985038136289 ) ) ;
#2007=CARTESIAN_POINT ( 'NONE',  ( -0.5930734014913793262, 40.20132500410929310, -13.49999994548272930 ) ) ;
#2008=CARTESIAN_POINT ( 'NONE',  ( -7.025999278210586674, 32.41925472474766678, 11.52783640645312246 ) ) ;
#2009=CARTESIAN_POINT ( 'NONE',  ( 8.444502319668561796, 75.00303538791125391, 10.53290446549366344 ) ) ;
#2011=CARTESIAN_POINT ( 'NONE',  ( 4.171729424061789260, 79.82999999999999829, 12.83926296998457417 ) ) ;
#2012=CARTESIAN_POINT ( 'NONE',  ( 13.23734291971121735, 51.52354072660591555, -2.650047768604904430 ) ) ;
#2013=CARTESIAN_POINT ( 'NONE',  ( -12.89949653176691236, 38.07337467622953397, 3.996097449710631189 ) ) ;
#2015=CARTESIAN_POINT ( 'NONE',  ( 6.225595394061742560, 36.95216596563231803, -11.98154833774320593 ) ) ;
#2018=PLANE ( 'NONE',  #7825 ) ;
#2020=CARTESIAN_POINT ( 'NONE',  ( 0.2399344713086168090, 62.68862715799873797, 13.49787121004495205 ) ) ;
#2021=CARTESIAN_POINT ( 'NONE',  ( -11.84443143481805549, 80.93000000000000682, 1.125603796807419066 ) ) ;
#2022=B_SPLINE_CURVE_WITH_KNOTS ( 'NONE', 3,
 ( #14856, #8183, #9599, #13544, #6852, #8359, #4186, #14950, #297, #2840, #7197, #642, #15213, #3110, #5791, #12667, #9863, #386, #12584, #16550, #16807, #16722, #15298, #3291, #3017, #11176, #13887, #8537, #4629, #1786, #472, #3381, #5881, #11261, #14150, #16639, #4544, #6053, #9949, #3200, #4457, #12844, #10036, #1700, #1869, #8620, #8707, #15384, #13974, #14066, #8448, #7284, #559, #5966, #15470, #11347, #1951, #13802, #2039, #12500, #7376, #15119, #7114, #12753, #8792, #4714, #11435, #7463, #10117, #9773, #4364, #732, #6140, #11519, #2377, #808, #4971, #14403, #8963, #13271, #14319, #4885, #6569, #10374, #13096, #4800, #15554, #982, #8880, #14235, #16896, #7812, #6305, #10202, #2120, #1159, #15820, #3466, #13185, #7546, #1070, #6395, #12924, #15728, #6220, #2207, #3636, #9228, #9050, #11606, #16982, #5153, #10287, #15639, #3549, #7634, #13012, #2291, #892, #10460, #14582, #11690, #17067, #7720, #6483, #11778, #17154, #5065, #3725, #9143, #14490, #11868, #7894, #17243, #10546, #15906, #3815, #2463, #16345, #97, #10713, #9661, #8334, #4252, #12294, #14833, #10886, #9401, #13607, #6, #10975, #7982, #16255, #14750, #1502, #5411, #15011, #13351, #5328, #12204, #3985, #9574, #10627, #5241, #15992, #13520, #6917, #3896, #17413, #9314, #2902, #13689, #1589, #6826, #14664 ),
 .UNSPECIFIED., .F., .F.,
 ( 4, 2, 1, 1, 1, 2, 2, 1, 2, 2, 2, 2, 2, 2, 2, 2, 2, 1, 2, 2, 1, 1, 1, 2, 2, 1, 2, 2, 2, 2, 2, 2, 2, 2, 2, 2, 2, 2, 1, 1, 2, 2, 2, 2, 1, 2, 2, 1, 1, 2, 2, 2, 2, 2, 2, 2, 2, 2, 2, 2, 1, 2, 2, 1, 1, 1, 1, 1, 1, 2, 2, 1, 2, 2, 2, 2, 1, 1, 1, 2, 2, 1, 1, 1, 2, 2, 2, 2, 1, 2, 2, 1, 1, 2, 2, 2, 2, 2, 2, 1, 1, 2, 2, 4 ),
 ( 0.6813842983133263642, 0.6850787074223488871, 0.6853096079916627392, 0.6853384705628270401, 0.6853529018484091351, 0.6853601174912001825, 0.6853673331339912300, 0.6854250582763197208, 0.6855405085609765914, 0.6860023096996044067, 0.6864641108382321111, 0.6866950114075460743, 0.6868104616922029448, 0.6868681868345314356, 0.6869259119768599264, 0.6878495142541154461, 0.6883113153927431505, 0.6883401779639074514, 0.6883473936066984988, 0.6883546092494895463, 0.6883690405350716413, 0.6884267656774001320, 0.6885422159620571136, 0.6887731165313710768, 0.6896967188086268186, 0.6898121690932838002, 0.6898410316644479900, 0.6898698942356122910, 0.6899276193779407818, 0.6901585199472547449, 0.6906203210858826713, 0.6910821222245104867, 0.6913130227938244499, 0.6914284730784814315, 0.6915439233631384131, 0.6924675256403942658, 0.6933911279176502296, 0.6936220284869641928, 0.6937374787716211744, 0.6937952039139496652, 0.6938240664851138551, 0.6938529290562781560, 0.6943147301949060823, 0.6961619347494177878, 0.6962773850340747694, 0.6963062476052389593, 0.6963206788908211653, 0.6963351101764032602, 0.6963928353187317510, 0.6966237358880457142, 0.6970855370266736406, 0.6980091393039293823, 0.6984709404425573087, 0.6987018410118712719, 0.6987595661541997627, 0.6988172912965282535, 0.6989327415811852351, 0.6998563438584410878, 0.7007799461356968296, 0.7012417472743247560, 0.7012706098454890569, 0.7012850411310711518, 0.7012994724166532468, 0.7013571975589817376, 0.7014726478436387191, 0.7017035484129525713, 0.7021653495515804977, 0.7023962501208944609, 0.7025117004055514425, 0.7025405629767156324, 0.7025549942622977273, 0.7025694255478798222, 0.7026271506902083130, 0.7035507529674639438, 0.7037816535367779069, 0.7038105161079420968, 0.7038393786791063977, 0.7038971038214348885, 0.7040125541060918701, 0.7044743552447196855, 0.7053979575219755382, 0.7058597586606033536, 0.7060906592299173168, 0.7062061095145742984, 0.7062638346569027892, 0.7063215597992312800, 0.7072451620764870217, 0.7074760626458009849, 0.7075049252169652858, 0.7075193565025473807, 0.7075265721453384282, 0.7075337877881294757, 0.7075915129304579665, 0.7077069632151149481, 0.7081687643537428745, 0.7086305654923708008, 0.7087460157770278935, 0.7087604470626099884, 0.7087748783481920833, 0.7088037409193563843, 0.7088614660616848751, 0.7090923666309989493, 0.7100159689082550241, 0.7109395711855112099 ),
 .UNSPECIFIED. ) ;
#2023=CARTESIAN_POINT ( 'NONE',  ( 13.46220260918281575, 48.46811850303037517, -1.097924244589963738 ) ) ;
#2025=ORIENTED_EDGE ( 'NONE', *, *, #5375, .F. ) ;
#2026=CARTESIAN_POINT ( 'NONE',  ( -11.76794919243112325, 63.07999999999999829, 3.823638476888994830 ) ) ;
#2033=CARTESIAN_POINT ( 'NONE',  ( 12.47450349530925351, 66.24198063057153263, 5.166296410220359903 ) ) ;
#2034=CARTESIAN_POINT ( 'NONE',  ( 6.750022565184456980, 31.92926174983938026, 11.69132992304556495 ) ) ;
#2035=CARTESIAN_POINT ( 'NONE',  ( -9.520470885617715595, 50.62999999999999545, -6.917026985038136289 ) ) ;
#2037=VECTOR ( 'NONE', #11526, 1000.000000000000000 ) ;
#2038=CARTESIAN_POINT ( 'NONE',  ( -9.949452233774618293, 59.28342264085854652, 9.124606215017720956 ) ) ;
#2039=CARTESIAN_POINT ( 'NONE',  ( 11.81973372649256149, 45.67171577755837575, -6.522591581979077624 ) ) ;
#2040=CARTESIAN_POINT ( 'NONE',  ( 9.936708544982330693, 69.78412393671250413, -9.139967157036311463 ) ) ;
#2041=CARTESIAN_POINT ( 'NONE',  ( -11.52888015854957793, 80.93000000000003524, 3.329402692645399675 ) ) ;
#2042=CARTESIAN_POINT ( 'NONE',  ( 12.02698711349998817, 30.65606005353055963, -6.132014165155652563 ) ) ;
#2043=CARTESIAN_POINT ( 'NONE',  ( -13.45917019767884426, 55.96633912471227745, 1.049381195819143242 ) ) ;
#2044=CARTESIAN_POINT ( 'NONE',  ( -3.622045108825971305, 50.54975662805617986, 13.00518533329681148 ) ) ;
#2045=CARTESIAN_POINT ( 'NONE',  ( 13.29382772739631058, 33.34733514712192459, 2.350360117349177713 ) ) ;
#2046=CARTESIAN_POINT ( 'NONE',  ( 0.6483769335424683922, 43.15676486429432401, -13.48533567729083416 ) ) ;
#2047=CARTESIAN_POINT ( 'NONE',  ( 11.20965635938246585, 39.71270877404705146, -7.522876792059077999 ) ) ;
#2049=CARTESIAN_POINT ( 'NONE',  ( -13.46752786525881795, 61.89760212117944604, -0.9386075886148094183 ) ) ;
#2051=AXIS2_PLACEMENT_3D ( 'NONE', #7764, #8829, #13136 ) ;
#2055=CARTESIAN_POINT ( 'NONE',  ( 4.737298224311091488, 58.00936883926053866, -12.64152061320751663 ) ) ;
#2056=CARTESIAN_POINT ( 'NONE',  ( 7.310637651931115144, 78.90721144323025271, -11.34975570436828285 ) ) ;
#2058=CARTESIAN_POINT ( 'NONE',  ( 3.636496289402154414, 78.82999999999999829, 11.19198476289190936 ) ) ;
#2059=CARTESIAN_POINT ( 'NONE',  ( -13.50000000000000000, 42.92999999999999261, -3.306546357697853733E-15 ) ) ;
#2062=CARTESIAN_POINT ( 'NONE',  ( 7.041864955729037590, 53.94154545869297834, 11.52006337894699861 ) ) ;
#2067=CARTESIAN_POINT ( 'NONE',  ( 6.299111959984896814, 66.94929370039956495, -11.94646788586564057 ) ) ;
#2069=CARTESIAN_POINT ( 'NONE',  ( 1.553912808195373474, 77.73587740583015204, 13.41073184109523453 ) ) ;
#2073=CARTESIAN_POINT ( 'NONE',  ( 12.18022657597662040, 72.21555684226325411, 5.843038593813369097 ) ) ;
#2075=CARTESIAN_POINT ( 'NONE',  ( -4.171729424061787483, 49.32999999999999829, -12.83926296998457417 ) ) ;
#2076=CARTESIAN_POINT ( 'NONE',  ( -0.3661892661420289574, 71.66683318614190057, 13.49503404522676853 ) ) ;
#2077=CARTESIAN_POINT ( 'NONE',  ( -4.171729424061787483, 51.32999999999999829, -12.83926296998457417 ) ) ;
#2079=CARTESIAN_POINT ( 'NONE',  ( -10.72979123883553676, 68.24212118105015179, 8.239908094999801591 ) ) ;
#2081=CARTESIAN_POINT ( 'NONE',  ( 2.138189944381238661, 70.75688142232027644, 13.50000000000000000 ) ) ;
#2083=CARTESIAN_POINT ( 'NONE',  ( -2.522042593689474810, 65.58931665179493109, 13.26232815706891266 ) ) ;
#2088=DIRECTION ( 'NONE',  ( 0.000000000000000000, 0.000000000000000000, -1.000000000000000000 ) ) ;
#2089=CARTESIAN_POINT ( 'NONE',  ( -3.476970977993532941, 40.30499584707952465, -13.04628310429154148 ) ) ;
#2090=CARTESIAN_POINT ( 'NONE',  ( -12.92717612063876587, 31.79057794579883023, -3.890979012274611737 ) ) ;
#2091=CARTESIAN_POINT ( 'NONE',  ( 5.607300059319721974, 74.88362207002212756, 12.28117982223269600 ) ) ;
#2092=EDGE_CURVE ( 'NONE', #13131, #5168, #14123, .T. ) ;
#2095=CARTESIAN_POINT ( 'NONE',  ( 2.607531440858944223E-15, 72.18000000000000682, -14.19474002721660355 ) ) ;
#2096=CARTESIAN_POINT ( 'NONE',  ( 12.64609271680043179, 51.60106898862535019, -4.725079458178631064 ) ) ;
#2097=CARTESIAN_POINT ( 'NONE',  ( -13.48282497468361818, 37.90642807506478107, -0.6813083995204127774 ) ) ;
#2098=CARTESIAN_POINT ( 'NONE',  ( 12.02800223548316616, 36.65598124211443576, -6.130211025472831921 ) ) ;
#2101=CARTESIAN_POINT ( 'NONE',  ( -0.8913732225149532118, 77.64795571117363693, 13.47771292552425670 ) ) ;
#2103=FACE_OUTER_BOUND ( 'NONE', #1466, .T. ) ;
#2104=CARTESIAN_POINT ( 'NONE',  ( 13.50015753368874094, 48.42919927454262563, 0.02489017590083256182 ) ) ;
#2106=ORIENTED_EDGE ( 'NONE', *, *, #13611, .F. ) ;
#2107=CARTESIAN_POINT ( 'NONE',  ( 11.76794919243112325, 70.43000000000000682, 1.441158131103945434E-15 ) ) ;
#2109=DIRECTION ( 'NONE',  ( 1.000000000000000000, 0.000000000000000000, 0.000000000000000000 ) ) ;
#2111=CARTESIAN_POINT ( 'NONE',  ( -0.4699532509952931147, 43.19689778629660282, -13.49182028397187949 ) ) ;
#2112=CARTESIAN_POINT ( 'NONE',  ( 3.456996083615943238, 76.05570077164072984, -13.05020998474081395 ) ) ;
#2115=CARTESIAN_POINT ( 'NONE',  ( 3.099211176354089492, 65.79143792051837636, 13.13944202385564353 ) ) ;
#2116=CARTESIAN_POINT ( 'NONE',  ( -10.92172942406178926, 79.63000000000000966, -7.935100905948389460 ) ) ;
#2118=CARTESIAN_POINT ( 'NONE',  ( -3.636496289402155746, 51.53000000000000114, 11.19198476289190936 ) ) ;
#2119=CARTESIAN_POINT ( 'NONE',  ( -13.46443399275077368, 58.96388886014217690, 0.9794471126550197138 ) ) ;
#2120=CARTESIAN_POINT ( 'NONE',  ( 12.97091200036834913, 45.29613835854244286, 3.742550467659857549 ) ) ;
#2122=DIRECTION ( 'NONE',  ( 0.000000000000000000, -1.000000000000000000, 0.000000000000000000 ) ) ;
#2123=CARTESIAN_POINT ( 'NONE',  ( 13.49064639646111630, 30.44728826658618459, -0.5025169752740217266 ) ) ;
#2124=CARTESIAN_POINT ( 'NONE',  ( -11.06336247766528480, 56.22163178693907071, 7.736410992500679207 ) ) ;
#2126=CARTESIAN_POINT ( 'NONE',  ( 8.065371710061997490, 63.87419627703715008, -10.82612419346579102 ) ) ;
#2128=CARTESIAN_POINT ( 'NONE',  ( 8.413557601958773446, 39.85841225840349011, -10.55875124266192522 ) ) ;
#2130=CARTESIAN_POINT ( 'NONE',  ( -8.150177880934091235, 61.48915199108306240, -10.78270659849790647 ) ) ;
#2133=ORIENTED_EDGE ( 'NONE', *, *, #9524, .F. ) ;
#2136=CARTESIAN_POINT ( 'NONE',  ( 12.61240584875263160, 48.25424400694961236, 4.854618120513341850 ) ) ;
#2137=( BOUNDED_SURFACE ( )  B_SPLINE_SURFACE ( 1, 2, ( 
 ( #13118, #6161, #2143, #11537, #16916, #12944, #11626, #6326, #4908, #15661, #3569, #13033, #11713, #17089, #3662, #5986, #5090, #1181, #5176, #3749, #4007, #14854, #8179, #10567, #17434, #10482, #15842, #2398, #8093, #10820, #17264, #7833, #9251, #16014, #14772, #16098, #15928, #12138, #5430, #13372, #16182, #13292, #17178, #4094, #2748, #9509, #1343, #3920, #5347, #3837, #2662, #6592, #27, #14512, #1007, #6507, #13206, #14604, #6417, #2484, #7918, #11802, #11972, #17353, #13457, #11889, #6759, #5265, #10651, #9163, #1092, #9337, #14687, #2574, #8006, #9423, #1262, #6673, #12056, #10734, #8269, #211, #16636, #8535, #5879, #384, #11174, #11258, #10909, #6849, #9861, #1522, #8356, #13630, #4454, #5704, #4541, #3108, #15034, #3198, #1784, #1612, #16548, #14948, #7029, #11086, #5616, #9947, #10998, #15209, #12407, #13542, #5789, #12497, #6939, #3015, #7195, #15295, #16278, #7112, #12582, #16366, #13884, #470, #2838, #16459, #12318, #4184, #4274, #1432, #12227, #295, #119, #9683, #5525, #4361, #9771, #9596, #2926, #15116, #13714, #8445, #13799, #1698, #15704, #13972, #11344, #10604, #7787, #12665, #11842, #7282, #17217, #15970, #554, #3610, #1867, #17042, #3701, #1948, #957, #8704, #6279, #5128, #17303, #14064, #7694, #10519, #7373, #11923, #7869, #8618, #5964, #17128, #10034, #3289, #16720, #15882, #12751, #4627, #13072, #15382, #10348, #639, #6369, #11666, #4947, #15794, #9022, #14378, #2267, #11752, #5037, #1045, #2355, #10436, #9116, #14466, #13159, #6456, #3789, #9202, #14553, #2437, #13245, #1133, #6544, #2527, #6894, #4226, #7956, #14641, #13327, #5477, #16318, #1218, #9373, #6629, #2611, #12009, #9638, #6802, #17390, #1387, #16054, #2793, #16227, #14808, #8224, #5306, #2702, #13667, #1563, #10687, #3961, #14724, #8042, #5386, #13409, #8132, #4137, #13496, #12358, #1299, #10858, #6713, #12091, #12180, #9460, #3872, #13584, #14899, #72, #9549, #17474, #1478, #10771, #16135, #12267, #252, #4046, #11040, #14988, #165, #5569, #10952, #2880, #8312, #6983, #5657, #9288, #11389, #8398, #4404, #9724, #15160, #2969, #16761, #1819, #13752, #13925, #11126, #15336, #11297, #9902, #8660, #15069, #15249, #8748, #14106, #1651, #7067, #12449, #334, #423, #5743, #3147, #16675, #8573, #16500, #5917, #4668, #6095, #9814, #9989, #15426, #13838, #6006, #1907, #3059, #7235, #8487, #7152, #12536, #14016, #1990, #12621, #7324, #5830, #16411, #4493, #509, #4314, #11213, #4581, #16587, #12708, #596, #10075, #3334, #7416, #12798, #724, #6388, #16888, #7540, #3628, #16783, #15530, #12470, #3169, #7086, #4515, #8681, #7171, #5939, #13858, #11234, #4690, #4776, #1761, #12641, #10095, #12559, #16871, #12817, #3441 ),
 ( #15271, #444, #530, #5855, #11318, #10179, #357, #3263, #9837, #5763, #7257, #1843, #13773, #6028, #7350, #16698, #14040, #16611, #4603, #11146, #8594, #1927, #1672, #13946, #16522, #8770, #9923, #4429, #15445, #14125, #15183, #3084, #8509, #15357, #2011, #10009, #12729, #616, #11411, #3354, #7437, #704, #6114, #11495, #3522, #7789, #9118, #2269, #1046, #7521, #958, #1134, #6545, #16957, #4860, #10263, #15614, #10350, #8937, #11753, #14467, #17129, #14296, #15795, #14554, #8856, #2182, #2356, #13246, #6280, #15883, #11844, #7610, #5039, #12986, #869, #11668, #6457, #11924, #17219, #5129, #17043, #14209, #10520, #9203, #2095, #12902, #2438, #15705, #9024, #17305, #6895, #10773, #9289, #6631, #5658, #2794, #7958, #12268, #2529, #166, #3874, #13328, #16137, #14642, #12093, #16228, #14725, #13497, #3963, #1300, #5570, #12359, #9375, #2703, #10953, #2613, #6984, #2881, #1219, #12011, #12181, #5307, #16056, #17391, #16319, #8043, #10689, #8133, #13410, #5388, #4048, #6715, #9639, #14809, #4227, #17475, #1388, #6803, #10859, #253, #9550, #14989, #14900, #8225, #13585, #1479, #8313, #13668, #1564, #4315, #16676, #1652, #3239, #13839, #5918, #15250, #1820, #12451, #2970, #3148, #12800, #16502, #12622, #13753, #9903, #336, #7236, #11391, #510, #9725, #15071, #8400, #4670, #5745, #11298, #11128, #7068, #16588, #3061, #4406, #1909, #684, #6097, #8488, #15338, #9816, #15162, #1739, #6008, #8750, #7153, #12538, #425, #13926, #12710, #14018, #5831, #10076, #3336, #4582, #14108, #11214, #4494, #1992, #16413, #7418, #16763, #9991, #8662, #8574, #597, #7326, #15427, #16853, #771, #4755, #10161, #15510, #12883, #3422, #8837, #11477, #14195, #2077, #7502, #9396, #5324, #10794, #11123, #16498, #6345, #9617, #1454, #8468, #9530, #16479, #8378, #14968, #12159, #141, #6872, #5547, #16570, #7132, #5811, #315, #9792, #11194, #10838, #6781, #15139, #12247, #1542, #10931, #3037, #5637, #4476, #12519, #9706, #14873, #16298, #16204, #403, #2859, #1364, #231, #4115, #12339, #11019, #16390, #9882, #50, #1632, #2768, #12429, #15231, #3128, #13477, #6160, #2059, #11454, #14171, #8640, #7394, #7214, #8724, #16915, #4907, #12774, #15660, #2142, #13991, #491, #4820, #7567, #5897, #11277, #4561, #10136, #828, #9967, #1888, #3218, #7302, #5985, #6239, #16828, #11367, #3400, #10053, #10221, #15574, #662, #15403, #11712, #17263, #1261, #4995, #9073, #1006, #3748, #14511, #5175, #12317, #15033, #13713, #9770, #3014, #8444, #1697, #383, #12496, #5788, #4006, #14771, #8092, #13456, #5878, #8703, #3197, #13883, #7281, #3378, #11173, #4626, #15468, #4540, #15208, #10033, #7372, #7194, #11257, #638, #12664, #553, #5963 ) ),
 .UNSPECIFIED., .F., .F., .T. ) 
 B_SPLINE_SURFACE_WITH_KNOTS ( ( 2, 2 ),
 ( 3, 2, 2, 2, 2, 2, 2, 2, 2, 2, 2, 2, 2, 2, 2, 2, 2, 2, 2, 2, 2, 2, 2, 2, 2, 2, 2, 2, 2, 2, 2, 2, 2, 2, 2, 2, 2, 2, 2, 2, 2, 2, 2, 2, 2, 2, 2, 2, 2, 2, 2, 2, 2, 2, 2, 2, 2, 2, 2, 2, 2, 2, 2, 2, 2, 2, 2, 2, 2, 2, 2, 2, 2, 2, 2, 2, 2, 2, 2, 2, 2, 2, 2, 2, 2, 2, 2, 2, 2, 2, 2, 2, 2, 2, 2, 2, 2, 2, 2, 2, 2, 2, 2, 2, 2, 2, 2, 2, 2, 2, 2, 2, 2, 2, 2, 2, 2, 2, 2, 2, 2, 2, 2, 2, 2, 2, 2, 2, 2, 2, 2, 2, 2, 2, 2, 2, 2, 2, 2, 2, 2, 2, 2, 2, 2, 2, 2, 2, 2, 2, 2, 2, 2, 2, 2, 2, 2, 2, 2, 2, 2, 2, 2, 2, 2, 2, 2, 2, 2, 2, 2, 2, 2, 2, 2, 2, 2, 2, 3 ),
 ( 0.000000000000000000, 1.000000000000000000 ),
 ( 0.000000000000000000, 0.005555555555555555768, 0.01111111111111111154, 0.01666666666666666644, 0.02222222222222222307, 0.02777777777777777624, 0.03333333333333333287, 0.03888888888888888951, 0.04444444444444444614, 0.05000000000000000278, 0.05555555555555555247, 0.06111111111111110911, 0.06666666666666666574, 0.07222222222222221544, 0.07777777777777777901, 0.08333333333333332871, 0.08888888888888889228, 0.09444444444444444198, 0.1000000000000000056, 0.1055555555555555552, 0.1111111111111111049, 0.1166666666666666685, 0.1222222222222222182, 0.1277777777777777679, 0.1333333333333333315, 0.1388888888888888951, 0.1444444444444444309, 0.1499999999999999944, 0.1555555555555555580, 0.1611111111111111216, 0.1666666666666666574, 0.1722222222222222210, 0.1777777777777777846, 0.1833333333333333204, 0.1888888888888888840, 0.1944444444444444475, 0.2000000000000000111, 0.2055555555555555469, 0.2111111111111111105, 0.2166666666666666741, 0.2222222222222222099, 0.2277777777777777735, 0.2333333333333333370, 0.2388888888888889006, 0.2444444444444444364, 0.2500000000000000000, 0.2555555555555555358, 0.2611111111111111271, 0.2666666666666666630, 0.2722222222222221988, 0.2777777777777777901, 0.2833333333333333259, 0.2888888888888888618, 0.2944444444444444531, 0.2999999999999999889, 0.3055555555555555802, 0.3111111111111111160, 0.3166666666666666519, 0.3222222222222222432, 0.3277777777777777790, 0.3333333333333333148, 0.3388888888888889062, 0.3444444444444444420, 0.3499999999999999778, 0.3555555555555555691, 0.3611111111111111049, 0.3666666666666666408, 0.3722222222222222321, 0.3777777777777777679, 0.3833333333333333592, 0.3888888888888888951, 0.3944444444444444309, 0.4000000000000000222, 0.4055555555555555580, 0.4111111111111110938, 0.4166666666666666852, 0.4222222222222222210, 0.4277777777777777568, 0.4333333333333333481, 0.4388888888888888840, 0.4444444444444444198, 0.4500000000000000111, 0.4555555555555555469, 0.4611111111111111382, 0.4666666666666666741, 0.4722222222222222099, 0.4777777777777778012, 0.4833333333333333370, 0.4888888888888888729, 0.4944444444444444642, 0.5000000000000000000, 0.5055555555555555358, 0.5111111111111110716, 0.5166666666666667185, 0.5222222222222222543, 0.5277777777777777901, 0.5333333333333333259, 0.5388888888888888618, 0.5444444444444443976, 0.5500000000000000444, 0.5555555555555555802, 0.5611111111111111160, 0.5666666666666666519, 0.5722222222222221877, 0.5777777777777777235, 0.5833333333333333703, 0.5888888888888889062, 0.5944444444444444420, 0.5999999999999999778, 0.6055555555555555136, 0.6111111111111111605, 0.6166666666666666963, 0.6222222222222222321, 0.6277777777777777679, 0.6333333333333333037, 0.6388888888888888395, 0.6444444444444444864, 0.6500000000000000222, 0.6555555555555555580, 0.6611111111111110938, 0.6666666666666666297, 0.6722222222222222765, 0.6777777777777778123, 0.6833333333333333481, 0.6888888888888888840, 0.6944444444444444198, 0.6999999999999999556, 0.7055555555555556024, 0.7111111111111111382, 0.7166666666666666741, 0.7222222222222222099, 0.7277777777777777457, 0.7333333333333332815, 0.7388888888888889284, 0.7444444444444444642, 0.7500000000000000000, 0.7555555555555555358, 0.7611111111111110716, 0.7666666666666667185, 0.7722222222222222543, 0.7777777777777777901, 0.7833333333333333259, 0.7888888888888888618, 0.7944444444444443976, 0.8000000000000000444, 0.8055555555555555802, 0.8111111111111111160, 0.8166666666666666519, 0.8222222222222221877, 0.8277777777777777235, 0.8333333333333333703, 0.8388888888888889062, 0.8444444444444444420, 0.8499999999999999778, 0.8555555555555555136, 0.8611111111111111605, 0.8666666666666666963, 0.8722222222222222321, 0.8777777777777777679, 0.8833333333333333037, 0.8888888888888888395, 0.8944444444444444864, 0.9000000000000000222, 0.9055555555555555580, 0.9111111111111110938, 0.9166666666666666297, 0.9222222222222222765, 0.9277777777777778123, 0.9333333333333333481, 0.9388888888888888840, 0.9444444444444444198, 0.9499999999999999556, 0.9555555555555556024, 0.9611111111111111382, 0.9666666666666666741, 0.9722222222222222099, 0.9777777777777777457, 0.9814746766279994761, 0.9912894233942795008 ),
 .UNSPECIFIED. ) 
 GEOMETRIC_REPRESENTATION_ITEM ( )  RATIONAL_B_SPLINE_SURFACE ( (
 ( 1.000000000000000000, 0.9510565162951535312, 1.000000000000000000, 0.9510565162951535312, 1.000000000000000000, 0.9510565162951535312, 1.000000000000000000, 0.9510565162951535312, 1.000000000000000000, 0.9510565162951535312, 1.000000000000000000, 0.9510565162951535312, 1.000000000000000000, 0.9510565162951535312, 1.000000000000000000, 0.9510565162951535312, 1.000000000000000000, 0.9510565162951535312, 1.000000000000000000, 0.9510565162951535312, 1.000000000000000000, 0.9510565162951535312, 1.000000000000000000, 0.9510565162951535312, 1.000000000000000000, 0.9510565162951535312, 1.000000000000000000, 0.9510565162951535312, 1.000000000000000000, 0.9510565162951535312, 1.000000000000000000, 0.9510565162951535312, 1.000000000000000000, 0.9510565162951535312, 1.000000000000000000, 0.9510565162951535312, 1.000000000000000000, 0.9510565162951535312, 1.000000000000000000, 0.9510565162951535312, 1.000000000000000000, 0.9510565162951535312, 1.000000000000000000, 0.9510565162951535312, 1.000000000000000000, 0.9510565162951535312, 1.000000000000000000, 0.9510565162951535312, 1.000000000000000000, 0.9510565162951535312, 1.000000000000000000, 0.9510565162951535312, 1.000000000000000000, 0.9510565162951535312, 1.000000000000000000, 0.9510565162951535312, 1.000000000000000000, 0.9510565162951535312, 1.000000000000000000, 0.9510565162951535312, 1.000000000000000000, 0.9510565162951535312, 1.000000000000000000, 0.9510565162951535312, 1.000000000000000000, 0.9510565162951535312, 1.000000000000000000, 0.9510565162951535312, 1.000000000000000000, 0.9510565162951535312, 1.000000000000000000, 0.9510565162951535312, 1.000000000000000000, 0.9510565162951535312, 1.000000000000000000, 0.9510565162951535312, 1.000000000000000000, 0.9510565162951535312, 1.000000000000000000, 0.9510565162951535312, 1.000000000000000000, 0.9510565162951535312, 1.000000000000000000, 0.9510565162951535312, 1.000000000000000000, 0.9510565162951535312, 1.000000000000000000, 0.9510565162951535312, 1.000000000000000000, 0.9510565162951535312, 1.000000000000000000, 0.9510565162951535312, 1.000000000000000000, 0.9510565162951535312, 1.000000000000000000, 0.9510565162951535312, 1.000000000000000000, 0.9510565162951535312, 1.000000000000000000, 0.9510565162951535312, 1.000000000000000000, 0.9510565162951535312, 1.000000000000000000, 0.9510565162951535312, 1.000000000000000000, 0.9510565162951535312, 1.000000000000000000, 0.9510565162951535312, 1.000000000000000000, 0.9510565162951535312, 1.000000000000000000, 0.9510565162951535312, 1.000000000000000000, 0.9510565162951535312, 1.000000000000000000, 0.9510565162951535312, 1.000000000000000000, 0.9510565162951535312, 1.000000000000000000, 0.9510565162951535312, 1.000000000000000000, 0.9510565162951535312, 1.000000000000000000, 0.9510565162951535312, 1.000000000000000000, 0.9510565162951535312, 1.000000000000000000, 0.9510565162951535312, 1.000000000000000000, 0.9510565162951535312, 1.000000000000000000, 0.9510565162951535312, 1.000000000000000000, 0.9510565162951535312, 1.000000000000000000, 0.9510565162951535312, 1.000000000000000000, 0.9510565162951535312, 1.000000000000000000, 0.9510565162951535312, 1.000000000000000000, 0.9510565162951535312, 1.000000000000000000, 0.9510565162951535312, 1.000000000000000000, 0.9510565162951535312, 1.000000000000000000, 0.9510565162951535312, 1.000000000000000000, 0.9510565162951535312, 1.000000000000000000, 0.9510565162951535312, 1.000000000000000000, 0.9510565162951535312, 1.000000000000000000, 0.9510565162951535312, 1.000000000000000000, 0.9510565162951535312, 1.000000000000000000, 0.9510565162951535312, 1.000000000000000000, 0.9510565162951535312, 1.000000000000000000, 0.9510565162951535312, 1.000000000000000000, 0.9510565162951535312, 1.000000000000000000, 0.9510565162951535312, 1.000000000000000000, 0.9510565162951535312, 1.000000000000000000, 0.9510565162951535312, 1.000000000000000000, 0.9510565162951535312, 1.000000000000000000, 0.9510565162951535312, 1.000000000000000000, 0.9510565162951535312, 1.000000000000000000, 0.9510565162951535312, 1.000000000000000000, 0.9510565162951535312, 1.000000000000000000, 0.9510565162951535312, 1.000000000000000000, 0.9510565162951535312, 1.000000000000000000, 0.9510565162951535312, 1.000000000000000000, 0.9510565162951535312, 1.000000000000000000, 0.9510565162951535312, 1.000000000000000000, 0.9510565162951535312, 1.000000000000000000, 0.9510565162951535312, 1.000000000000000000, 0.9510565162951535312, 1.000000000000000000, 0.9510565162951535312, 1.000000000000000000, 0.9510565162951535312, 1.000000000000000000, 0.9510565162951535312, 1.000000000000000000, 0.9510565162951535312, 1.000000000000000000, 0.9510565162951535312, 1.000000000000000000, 0.9510565162951535312, 1.000000000000000000, 0.9510565162951535312, 1.000000000000000000, 0.9510565162951535312, 1.000000000000000000, 0.9510565162951535312, 1.000000000000000000, 0.9510565162951535312, 1.000000000000000000, 0.9510565162951535312, 1.000000000000000000, 0.9510565162951535312, 1.000000000000000000, 0.9510565162951535312, 1.000000000000000000, 0.9510565162951535312, 1.000000000000000000, 0.9510565162951535312, 1.000000000000000000, 0.9510565162951535312, 1.000000000000000000, 0.9510565162951535312, 1.000000000000000000, 0.9510565162951535312, 1.000000000000000000, 0.9510565162951535312, 1.000000000000000000, 0.9510565162951535312, 1.000000000000000000, 0.9510565162951535312, 1.000000000000000000, 0.9510565162951535312, 1.000000000000000000, 0.9510565162951535312, 1.000000000000000000, 0.9510565162951535312, 1.000000000000000000, 0.9510565162951535312, 1.000000000000000000, 0.9510565162951535312, 1.000000000000000000, 0.9510565162951535312, 1.000000000000000000, 0.9510565162951535312, 1.000000000000000000, 0.9510565162951535312, 1.000000000000000000, 0.9510565162951535312, 1.000000000000000000, 0.9510565162951535312, 1.000000000000000000, 0.9510565162951535312, 1.000000000000000000, 0.9510565162951535312, 1.000000000000000000, 0.9510565162951535312, 1.000000000000000000, 0.9510565162951535312, 1.000000000000000000, 0.9510565162951535312, 1.000000000000000000, 0.9510565162951535312, 1.000000000000000000, 0.9510565162951535312, 1.000000000000000000, 0.9510565162951535312, 1.000000000000000000, 0.9510565162951535312, 1.000000000000000000, 0.9510565162951535312, 1.000000000000000000, 0.9510565162951535312, 1.000000000000000000, 0.9510565162951535312, 1.000000000000000000, 0.9510565162951535312, 1.000000000000000000, 0.9510565162951535312, 1.000000000000000000, 0.9510565162951535312, 1.000000000000000000, 0.9510565162951535312, 1.000000000000000000, 0.9510565162951535312, 1.000000000000000000, 0.9510565162951535312, 1.000000000000000000, 0.9510565162951535312, 1.000000000000000000, 0.9510565162951535312, 1.000000000000000000, 0.9510565162951535312, 1.000000000000000000, 0.9510565162951535312, 1.000000000000000000, 0.9510565162951535312, 1.000000000000000000, 0.9510565162951535312, 1.000000000000000000, 0.9510565162951535312, 1.000000000000000000, 0.9510565162951535312, 1.000000000000000000, 0.9510565162951535312, 1.000000000000000000, 0.9510565162951535312, 1.000000000000000000, 0.9510565162951535312, 1.000000000000000000, 0.9510565162951535312, 1.000000000000000000, 0.9510565162951535312, 1.000000000000000000, 0.9510565162951535312, 1.000000000000000000, 0.9510565162951535312, 1.000000000000000000, 0.9510565162951535312, 1.000000000000000000, 0.9510565162951535312, 1.000000000000000000, 0.9510565162951535312, 1.000000000000000000, 0.9510565162951535312, 1.000000000000000000, 0.9510565162951535312, 1.000000000000000000, 0.9510565162951535312, 1.000000000000000000, 0.9510565162951535312, 1.000000000000000000, 0.9510565162951535312, 1.000000000000000000, 0.9510565162951535312, 1.000000000000000000, 0.9510565162951535312, 1.000000000000000000, 0.9510565162951535312, 1.000000000000000000, 0.9510565162951535312, 1.000000000000000000, 0.9510565162951535312, 1.000000000000000000, 0.9674309604458272149, 0.9782075210486875783, 0.9782075210486875783, 0.9782075210486875783),
 ( 1.000000000000000000, 0.9510565162951535312, 1.000000000000000000, 0.9510565162951535312, 1.000000000000000000, 0.9510565162951535312, 1.000000000000000000, 0.9510565162951535312, 1.000000000000000000, 0.9510565162951535312, 1.000000000000000000, 0.9510565162951535312, 1.000000000000000000, 0.9510565162951535312, 1.000000000000000000, 0.9510565162951535312, 1.000000000000000000, 0.9510565162951535312, 1.000000000000000000, 0.9510565162951535312, 1.000000000000000000, 0.9510565162951535312, 1.000000000000000000, 0.9510565162951535312, 1.000000000000000000, 0.9510565162951535312, 1.000000000000000000, 0.9510565162951535312, 1.000000000000000000, 0.9510565162951535312, 1.000000000000000000, 0.9510565162951535312, 1.000000000000000000, 0.9510565162951535312, 1.000000000000000000, 0.9510565162951535312, 1.000000000000000000, 0.9510565162951535312, 1.000000000000000000, 0.9510565162951535312, 1.000000000000000000, 0.9510565162951535312, 1.000000000000000000, 0.9510565162951535312, 1.000000000000000000, 0.9510565162951535312, 1.000000000000000000, 0.9510565162951535312, 1.000000000000000000, 0.9510565162951535312, 1.000000000000000000, 0.9510565162951535312, 1.000000000000000000, 0.9510565162951535312, 1.000000000000000000, 0.9510565162951535312, 1.000000000000000000, 0.9510565162951535312, 1.000000000000000000, 0.9510565162951535312, 1.000000000000000000, 0.9510565162951535312, 1.000000000000000000, 0.9510565162951535312, 1.000000000000000000, 0.9510565162951535312, 1.000000000000000000, 0.9510565162951535312, 1.000000000000000000, 0.9510565162951535312, 1.000000000000000000, 0.9510565162951535312, 1.000000000000000000, 0.9510565162951535312, 1.000000000000000000, 0.9510565162951535312, 1.000000000000000000, 0.9510565162951535312, 1.000000000000000000, 0.9510565162951535312, 1.000000000000000000, 0.9510565162951535312, 1.000000000000000000, 0.9510565162951535312, 1.000000000000000000, 0.9510565162951535312, 1.000000000000000000, 0.9510565162951535312, 1.000000000000000000, 0.9510565162951535312, 1.000000000000000000, 0.9510565162951535312, 1.000000000000000000, 0.9510565162951535312, 1.000000000000000000, 0.9510565162951535312, 1.000000000000000000, 0.9510565162951535312, 1.000000000000000000, 0.9510565162951535312, 1.000000000000000000, 0.9510565162951535312, 1.000000000000000000, 0.9510565162951535312, 1.000000000000000000, 0.9510565162951535312, 1.000000000000000000, 0.9510565162951535312, 1.000000000000000000, 0.9510565162951535312, 1.000000000000000000, 0.9510565162951535312, 1.000000000000000000, 0.9510565162951535312, 1.000000000000000000, 0.9510565162951535312, 1.000000000000000000, 0.9510565162951535312, 1.000000000000000000, 0.9510565162951535312, 1.000000000000000000, 0.9510565162951535312, 1.000000000000000000, 0.9510565162951535312, 1.000000000000000000, 0.9510565162951535312, 1.000000000000000000, 0.9510565162951535312, 1.000000000000000000, 0.9510565162951535312, 1.000000000000000000, 0.9510565162951535312, 1.000000000000000000, 0.9510565162951535312, 1.000000000000000000, 0.9510565162951535312, 1.000000000000000000, 0.9510565162951535312, 1.000000000000000000, 0.9510565162951535312, 1.000000000000000000, 0.9510565162951535312, 1.000000000000000000, 0.9510565162951535312, 1.000000000000000000, 0.9510565162951535312, 1.000000000000000000, 0.9510565162951535312, 1.000000000000000000, 0.9510565162951535312, 1.000000000000000000, 0.9510565162951535312, 1.000000000000000000, 0.9510565162951535312, 1.000000000000000000, 0.9510565162951535312, 1.000000000000000000, 0.9510565162951535312, 1.000000000000000000, 0.9510565162951535312, 1.000000000000000000, 0.9510565162951535312, 1.000000000000000000, 0.9510565162951535312, 1.000000000000000000, 0.9510565162951535312, 1.000000000000000000, 0.9510565162951535312, 1.000000000000000000, 0.9510565162951535312, 1.000000000000000000, 0.9510565162951535312, 1.000000000000000000, 0.9510565162951535312, 1.000000000000000000, 0.9510565162951535312, 1.000000000000000000, 0.9510565162951535312, 1.000000000000000000, 0.9510565162951535312, 1.000000000000000000, 0.9510565162951535312, 1.000000000000000000, 0.9510565162951535312, 1.000000000000000000, 0.9510565162951535312, 1.000000000000000000, 0.9510565162951535312, 1.000000000000000000, 0.9510565162951535312, 1.000000000000000000, 0.9510565162951535312, 1.000000000000000000, 0.9510565162951535312, 1.000000000000000000, 0.9510565162951535312, 1.000000000000000000, 0.9510565162951535312, 1.000000000000000000, 0.9510565162951535312, 1.000000000000000000, 0.9510565162951535312, 1.000000000000000000, 0.9510565162951535312, 1.000000000000000000, 0.9510565162951535312, 1.000000000000000000, 0.9510565162951535312, 1.000000000000000000, 0.9510565162951535312, 1.000000000000000000, 0.9510565162951535312, 1.000000000000000000, 0.9510565162951535312, 1.000000000000000000, 0.9510565162951535312, 1.000000000000000000, 0.9510565162951535312, 1.000000000000000000, 0.9510565162951535312, 1.000000000000000000, 0.9510565162951535312, 1.000000000000000000, 0.9510565162951535312, 1.000000000000000000, 0.9510565162951535312, 1.000000000000000000, 0.9510565162951535312, 1.000000000000000000, 0.9510565162951535312, 1.000000000000000000, 0.9510565162951535312, 1.000000000000000000, 0.9510565162951535312, 1.000000000000000000, 0.9510565162951535312, 1.000000000000000000, 0.9510565162951535312, 1.000000000000000000, 0.9510565162951535312, 1.000000000000000000, 0.9510565162951535312, 1.000000000000000000, 0.9510565162951535312, 1.000000000000000000, 0.9510565162951535312, 1.000000000000000000, 0.9510565162951535312, 1.000000000000000000, 0.9510565162951535312, 1.000000000000000000, 0.9510565162951535312, 1.000000000000000000, 0.9510565162951535312, 1.000000000000000000, 0.9510565162951535312, 1.000000000000000000, 0.9510565162951535312, 1.000000000000000000, 0.9510565162951535312, 1.000000000000000000, 0.9510565162951535312, 1.000000000000000000, 0.9510565162951535312, 1.000000000000000000, 0.9510565162951535312, 1.000000000000000000, 0.9510565162951535312, 1.000000000000000000, 0.9510565162951535312, 1.000000000000000000, 0.9510565162951535312, 1.000000000000000000, 0.9510565162951535312, 1.000000000000000000, 0.9510565162951535312, 1.000000000000000000, 0.9510565162951535312, 1.000000000000000000, 0.9510565162951535312, 1.000000000000000000, 0.9510565162951535312, 1.000000000000000000, 0.9510565162951535312, 1.000000000000000000, 0.9510565162951535312, 1.000000000000000000, 0.9510565162951535312, 1.000000000000000000, 0.9510565162951535312, 1.000000000000000000, 0.9510565162951535312, 1.000000000000000000, 0.9510565162951535312, 1.000000000000000000, 0.9510565162951535312, 1.000000000000000000, 0.9510565162951535312, 1.000000000000000000, 0.9510565162951535312, 1.000000000000000000, 0.9510565162951535312, 1.000000000000000000, 0.9510565162951535312, 1.000000000000000000, 0.9510565162951535312, 1.000000000000000000, 0.9510565162951535312, 1.000000000000000000, 0.9510565162951535312, 1.000000000000000000, 0.9510565162951535312, 1.000000000000000000, 0.9510565162951535312, 1.000000000000000000, 0.9510565162951535312, 1.000000000000000000, 0.9510565162951535312, 1.000000000000000000, 0.9510565162951535312, 1.000000000000000000, 0.9510565162951535312, 1.000000000000000000, 0.9510565162951535312, 1.000000000000000000, 0.9510565162951535312, 1.000000000000000000, 0.9510565162951535312, 1.000000000000000000, 0.9510565162951535312, 1.000000000000000000, 0.9510565162951535312, 1.000000000000000000, 0.9510565162951535312, 1.000000000000000000, 0.9510565162951535312, 1.000000000000000000, 0.9510565162951535312, 1.000000000000000000, 0.9510565162951535312, 1.000000000000000000, 0.9510565162951535312, 1.000000000000000000, 0.9510565162951535312, 1.000000000000000000, 0.9510565162951535312, 1.000000000000000000, 0.9510565162951535312, 1.000000000000000000, 0.9510565162951535312, 1.000000000000000000, 0.9510565162951535312, 1.000000000000000000, 0.9674309604458272149, 0.9782075210486875783, 0.9782075210486875783, 0.9782075210486875783) ) ) 
 REPRESENTATION_ITEM ( '' )  SURFACE ( )  );
#2138=ADVANCED_FACE ( 'NONE', ( #7657 ), #2137, .T. ) ;
#2139=CARTESIAN_POINT ( 'NONE',  ( 2.279044047469930501, 58.09805576578575170, -13.30646307545504392 ) ) ;
#2140=CARTESIAN_POINT ( 'NONE',  ( 10.96618175729265054, 78.72740224806844367, -7.873708902144001875 ) ) ;
#2141=CARTESIAN_POINT ( 'NONE',  ( 9.520470885617717371, 76.73000000000000398, -6.917026985038131848 ) ) ;
#2142=CARTESIAN_POINT ( 'NONE',  ( 13.49999999999999822, 41.28000000000000114, 4.386415899144237684 ) ) ;
#2143=CARTESIAN_POINT ( 'NONE',  ( -9.520470885617715595, 83.62999999999999545, -6.917026985038136289 ) ) ;
#2144=CARTESIAN_POINT ( 'NONE',  ( -0.3003120841998243029, 47.66920191232892279, 13.49667088445732688 ) ) ;
#2145=CIRCLE ( 'NONE', #8670, 12.00000000000000178 ) ;
#2146=CARTESIAN_POINT ( 'NONE',  ( 8.343458848123580296, 40.97999999999998977, 11.48378591275253768 ) ) ;
#2147=CARTESIAN_POINT ( 'NONE',  ( -0.1072688110503501047, 67.18385698782702775, -13.49957998319009711 ) ) ;
#2149=CARTESIAN_POINT ( 'NONE',  ( -13.50000000000000000, 78.93000000000000682, -3.306546357697853733E-15 ) ) ;
#2150=CARTESIAN_POINT ( 'NONE',  ( 10.33907932670936169, 33.76270983375775359, -8.680815796010884711 ) ) ;
#2151=ORIENTED_EDGE ( 'NONE', *, *, #3966, .F. ) ;
#2154=CARTESIAN_POINT ( 'NONE',  ( 5.313600336010172676, 66.98769782423862296, -12.41030752995400377 ) ) ;
#2157=CARTESIAN_POINT ( 'NONE',  ( -7.125339594746328942, 59.41507076714115243, 11.46659377414734493 ) ) ;
#2158=DIRECTION ( 'NONE',  ( -1.000000000000000000, -0.000000000000000000, -0.000000000000000000 ) ) ;
#2159=FACE_OUTER_BOUND ( 'NONE', #12436, .T. ) ;
#2160=CARTESIAN_POINT ( 'NONE',  ( 7.441533999091377360, 71.95841347386840425, 11.26395245896506658 ) ) ;
#2161=CARTESIAN_POINT ( 'NONE',  ( 2.607531440858944223E-15, 52.17999999999998550, -14.19474002721660355 ) ) ;
#2162=CARTESIAN_POINT ( 'NONE',  ( 2.000520122481862502E-14, 73.67999999999999261, 13.50000000000000000 ) ) ;
#2165=CARTESIAN_POINT ( 'NONE',  ( -11.60114662261267071, 68.18707878082513218, 6.904087372892822039 ) ) ;
#2167=CARTESIAN_POINT ( 'NONE',  ( 1.124411942366441597, 55.13962006267097848, -13.46143473974375304 ) ) ;
#2169=CARTESIAN_POINT ( 'NONE',  ( -2.487099657241000017, 65.59057316322061126, 13.26893666242352054 ) ) ;
#2173=ORIENTED_EDGE ( 'NONE', *, *, #16812, .T. ) ;
#2175=CARTESIAN_POINT ( 'NONE',  ( 13.50000000000000000, 80.43000000000000682, 1.653273178848926867E-15 ) ) ;
#2176=CARTESIAN_POINT ( 'NONE',  ( -12.54118595349893361, 32.11158997754159827, 4.998678152965537969 ) ) ;
#2177=CARTESIAN_POINT ( 'NONE',  ( 3.692898783743682856, 74.81278297373158637, 12.98509198411088228 ) ) ;
#2178=CARTESIAN_POINT ( 'NONE',  ( 11.65057582055373864, 60.17622677577021761, 6.820123597281462224 ) ) ;
#2180=CARTESIAN_POINT ( 'NONE',  ( 13.50000000000000355, 62.57999999999999829, -4.386415899144233244 ) ) ;
#2182=CARTESIAN_POINT ( 'NONE',  ( 4.171729424061791924, 75.03000000000000114, -12.83926296998457239 ) ) ;
#2183=CARTESIAN_POINT ( 'NONE',  ( 12.63195413649815535, 51.60251507868900944, -4.762774090562415630 ) ) ;
#2184=CARTESIAN_POINT ( 'NONE',  ( -13.47802306467995059, 37.90338780716024303, -0.7702094408733768383 ) ) ;
#2185=CARTESIAN_POINT ( 'NONE',  ( 13.03650423020505400, 36.55508012865420397, -3.507091010788072616 ) ) ;
#2188=CARTESIAN_POINT ( 'NONE',  ( -3.365647742148276667, 74.55898446082595399, 13.07385443055280660 ) ) ;
#2189=CARTESIAN_POINT ( 'NONE',  ( -10.65461094870909164, 77.24527756324417282, 8.290314445817193345 ) ) ;
#2190=CARTESIAN_POINT ( 'NONE',  ( -10.92172942406179104, 61.22999999999999687, 7.935100905948387684 ) ) ;
#2191=CARTESIAN_POINT ( 'NONE',  ( 8.190734026114112609, 41.99145286735084426, 10.73174394289365985 ) ) ;
#2195=CARTESIAN_POINT ( 'NONE',  ( -9.520470885617715595, 59.63000000000000256, -6.917026985038136289 ) ) ;
#2199=CARTESIAN_POINT ( 'NONE',  ( 3.635492542842543084, 76.04928109828082938, -13.00127780319107806 ) ) ;
#2202=CARTESIAN_POINT ( 'NONE',  ( 3.145715289543748128, 65.79306979106382869, 13.12842161919002670 ) ) ;
#2203=CARTESIAN_POINT ( 'NONE',  ( 13.50000000000000355, 78.57999999999999829, -4.386415899144233244 ) ) ;
#2204=CARTESIAN_POINT ( 'NONE',  ( -7.272992578804307939, 53.47999999999998977, -10.01041549318726886 ) ) ;
#2206=CARTESIAN_POINT ( 'NONE',  ( -11.02082988299614286, 59.22417995457187345, 7.797019995292360228 ) ) ;
#2207=CARTESIAN_POINT ( 'NONE',  ( 11.48013075663052085, 45.16464998993217250, 7.103285909153894906 ) ) ;
#2208=CARTESIAN_POINT ( 'NONE',  ( 13.49953346300133106, 69.46047903813546043, -0.8869165812264260262 ) ) ;
#2210=CARTESIAN_POINT ( 'NONE',  ( 13.48560614430077997, 30.45153926847759962, -0.6251654576716944023 ) ) ;
#2211=CARTESIAN_POINT ( 'NONE',  ( -13.47260917658593193, 55.90032134080831838, -0.8602528088475849266 ) ) ;
#2213=CARTESIAN_POINT ( 'NONE',  ( -9.432887964969109973, 50.30984541438331092, 9.660289610433199670 ) ) ;
#2214=CARTESIAN_POINT ( 'NONE',  ( -8.697098998243532012E-15, 64.18000000000002103, -13.50000000000000000 ) ) ;
#2215=CARTESIAN_POINT ( 'NONE',  ( 0.07425440749237978422, 43.17733885071987032, -13.49982472904942732 ) ) ;
#2216=CARTESIAN_POINT ( 'NONE',  ( 13.46618916530301036, 39.46328916441213863, -0.9623342693608205600 ) ) ;
#2218=CARTESIAN_POINT ( 'NONE',  ( -4.397621424999290873, 61.33820228455973478, -12.76403019915171555 ) ) ;
#2224=CARTESIAN_POINT ( 'NONE',  ( 12.04482945923018633, 48.20494489326199528, 6.111791024390479166 ) ) ;
#2225=CARTESIAN_POINT ( 'NONE',  ( 5.704148017373132262, 57.97276112297371498, -12.24361770659877457 ) ) ;
#2226=CARTESIAN_POINT ( 'NONE',  ( 6.299136856153257469, 78.94920042450097242, -11.94284805450234010 ) ) ;
#2227=CARTESIAN_POINT ( 'NONE',  ( -3.636496289402155746, 78.53000000000000114, 11.19198476289190936 ) ) ;
#2231=DIRECTION ( 'NONE',  ( 0.000000000000000000, 0.000000000000000000, -1.000000000000000000 ) ) ;
#2234=CARTESIAN_POINT ( 'NONE',  ( 8.446640517145640834E-14, 43.67999999999999972, 13.50000000000000000 ) ) ;
#2235=CARTESIAN_POINT ( 'NONE',  ( -5.485275766071775660E-07, 44.67998473833578998, 13.49999999999997691 ) ) ;
#2241=CARTESIAN_POINT ( 'NONE',  ( 9.615105497588862349, 78.05941236408771999, 9.479011185318192645 ) ) ;
#2242=CARTESIAN_POINT ( 'NONE',  ( -3.928050693157006279, 59.53876161140142642, 12.91596041159252017 ) ) ;
#2243=DIRECTION ( 'NONE',  ( 0.000000000000000000, -1.000000000000000000, 0.000000000000000000 ) ) ;
#2245=CARTESIAN_POINT ( 'NONE',  ( 13.49999999999999822, 57.27999999999998693, 4.386415899144237684 ) ) ;
#2246=CARTESIAN_POINT ( 'NONE',  ( -3.386623526537360984, 71.55827636354801768, 13.06887847014471227 ) ) ;
#2250=CARTESIAN_POINT ( 'NONE',  ( -10.16858038536860498, 68.27292781118869414, 8.923254920740927076 ) ) ;
#2252=CARTESIAN_POINT ( 'NONE',  ( 9.298704918573795553, 54.81635208236939150, -9.786940185098014666 ) ) ;
#2254=CARTESIAN_POINT ( 'NONE',  ( -10.68045398250339417, 65.24396876513357313, 8.268639436869602122 ) ) ;
#2256=CARTESIAN_POINT ( 'NONE',  ( -8.224397711408583334, 35.36732474013189886, 10.71481292070565772 ) ) ;
#2259=DIRECTION ( 'NONE',  ( 0.000000000000000000, 0.000000000000000000, -1.000000000000000000 ) ) ;
#2261=CARTESIAN_POINT ( 'NONE',  ( -12.24136337498707405, 32.13941087148443643, 5.715357471406067980 ) ) ;
#2263=CARTESIAN_POINT ( 'NONE',  ( 9.831567778977319705, 60.07019766675954742, 9.264193167865414580 ) ) ;
#2265=CARTESIAN_POINT ( 'NONE',  ( -6.840429191180986912, 53.42702653096863941, 11.64059165842057553 ) ) ;
#2267=CARTESIAN_POINT ( 'NONE',  ( 11.76794919243112325, 55.42999999999999972, 1.441158131103945434E-15 ) ) ;
#2269=CARTESIAN_POINT ( 'NONE',  ( 8.343458848123583849, 77.88000000000000966, -11.48378591275253768 ) ) ;
#2270=CARTESIAN_POINT ( 'NONE',  ( 13.20536309241330741, 51.52922293589633540, -2.805526866140447328 ) ) ;
#2271=CARTESIAN_POINT ( 'NONE',  ( -9.877648899171177277, 38.28753466289869323, 9.213888813852227244 ) ) ;
#2272=CARTESIAN_POINT ( 'NONE',  ( 13.48665105718879964, 36.45067642936791685, -0.6002990102808697381 ) ) ;
#2274=CARTESIAN_POINT ( 'NONE',  ( -0.1742961825528621111, 74.67372405737431507, 13.49999999999610623 ) ) ;
#2275=CARTESIAN_POINT ( 'NONE',  ( -1.766402340420361483, 77.61635299055969028, 13.39115807898696353 ) ) ;
#2276=CARTESIAN_POINT ( 'NONE',  ( -0.8900910583040317903, 80.64811563240033365, 13.47797476431978581 ) ) ;
#2277=CARTESIAN_POINT ( 'NONE',  ( 7.500000000000000000, 108.3768542179257963, -4.091673783487169480 ) ) ;
#2278=ORIENTED_EDGE ( 'NONE', *, *, #5501, .T. ) ;
#2281=CARTESIAN_POINT ( 'NONE',  ( 7.272992578804311492, 55.87999999999999545, -10.01041549318726886 ) ) ;
#2283=CARTESIAN_POINT ( 'NONE',  ( 13.50000000000000000, 56.42999999999999972, 1.653273178848926867E-15 ) ) ;
#2284=CARTESIAN_POINT ( 'NONE',  ( 12.02097210324364518, 75.65652335936121631, -6.143864682141557232 ) ) ;
#2286=CARTESIAN_POINT ( 'NONE',  ( -10.92172942406178926, 73.62999999999999545, -7.935100905948389460 ) ) ;
#2288=CARTESIAN_POINT ( 'NONE',  ( -7.272992578804307939, 47.47999999999998977, -10.01041549318726886 ) ) ;
#2290=CARTESIAN_POINT ( 'NONE',  ( -13.43445895775833598, 58.88303016948394486, -1.354977829824218771 ) ) ;
#2291=CARTESIAN_POINT ( 'NONE',  ( 10.43514330751975194, 45.10252430648384347, 8.564926864381755323 ) ) ;
#2292=CARTESIAN_POINT ( 'NONE',  ( 13.10873240010329077, 69.54468864661862426, -3.226680269542550050 ) ) ;
#2294=LINE ( 'NONE', #16984, #4983 ) ;
#2295=CARTESIAN_POINT ( 'NONE',  ( 12.02303304563724673, 30.65636901295595607, -6.139761926991930352 ) ) ;
#2296=CARTESIAN_POINT ( 'NONE',  ( -7.135146516150340901, 55.44532162981700907, -11.46164669714722528 ) ) ;
#2297=CARTESIAN_POINT ( 'NONE',  ( -13.24244078534688818, 50.02386753338626590, 2.657835324058360094 ) ) ;
#2298=CARTESIAN_POINT ( 'NONE',  ( 7.466952291864066282, 63.90051593161832955, -11.24819315821802768 ) ) ;
#2299=CARTESIAN_POINT ( 'NONE',  ( 12.99392763564549291, 42.56084116897148562, -3.661734528280473189 ) ) ;
#2300=CARTESIAN_POINT ( 'NONE',  ( 13.43182422821157118, 39.38122741038952768, 1.395845098213416957 ) ) ;
#2301=ORIENTED_EDGE ( 'NONE', *, *, #9840, .T. ) ;
#2302=CARTESIAN_POINT ( 'NONE',  ( -7.631036692897547269, 70.46660093273136738, -11.13720947216162216 ) ) ;
#2303=CARTESIAN_POINT ( 'NONE',  ( -12.16104664928658963, 61.71474001778207708, -5.861914737776502626 ) ) ;
#2305=ORIENTED_EDGE ( 'NONE', *, *, #4294, .F. ) ;
#2306=CARTESIAN_POINT ( 'NONE',  ( -12.71421417626428152, 40.76452965150037500, -4.584416513558855932 ) ) ;
#2307=EDGE_LOOP ( 'NONE', ( #15806, #11981, #15306, #5419 ) ) ;
#2310=CARTESIAN_POINT ( 'NONE',  ( 3.942382125243764524, 47.82151681360642215, 12.91477671872532618 ) ) ;
#2312=CARTESIAN_POINT ( 'NONE',  ( 10.52817469841624387, 57.75233781933106059, -8.450342176037976216 ) ) ;
#2313=CARTESIAN_POINT ( 'NONE',  ( 12.19096715004470788, 78.64285588553632067, -5.799165764274725632 ) ) ;
#2314=CARTESIAN_POINT ( 'NONE',  ( -11.76794919243112325, 81.07999999999998408, 3.823638476888994386 ) ) ;
#2316=EDGE_CURVE ( 'NONE', #11794, #717, #890, .T. ) ;
#2319=CARTESIAN_POINT ( 'NONE',  ( 2.445080149700053643E-15, 75.17999999999999261, -13.50000000000000000 ) ) ;
#2323=CARTESIAN_POINT ( 'NONE',  ( 6.429988302422167123, 33.94387318707013890, -11.87465190390881453 ) ) ;
#2324=CARTESIAN_POINT ( 'NONE',  ( -12.44080865564263583, 73.73893818206965989, -5.243278813652959336 ) ) ;
#2327=DIRECTION ( 'NONE',  ( 0.000000000000000000, 0.000000000000000000, -1.000000000000000000 ) ) ;
#2330=CARTESIAN_POINT ( 'NONE',  ( -8.356910137473439804, 59.36152714647494832, 10.62299724927810729 ) ) ;
#2333=CARTESIAN_POINT ( 'NONE',  ( 4.171729424061789260, 53.83000000000000540, 12.83926296998457417 ) ) ;
#2334=CARTESIAN_POINT ( 'NONE',  ( -5.941256636048077411, 71.46338852619901161, 12.12314389860511277 ) ) ;
#2335=ADVANCED_FACE ( 'NONE', ( #8961 ), #6302, .T. ) ;
#2338=CARTESIAN_POINT ( 'NONE',  ( -4.083439365806073695, 68.53322352374333093, 12.86826179363684197 ) ) ;
#2340=CARTESIAN_POINT ( 'NONE',  ( 9.456157084575252725, 54.80849625928562574, -9.635361094816037308 ) ) ;
#2343=CARTESIAN_POINT ( 'NONE',  ( -9.809219749064693517, 65.29068444701793794, 9.275196495002377972 ) ) ;
#2345=CARTESIAN_POINT ( 'NONE',  ( -7.048305978417979567, 35.41831309511212567, 11.51397633767918904 ) ) ;
#2348=CARTESIAN_POINT ( 'NONE',  ( 13.50000000000000355, 50.58000000000000540, -4.386415899144233244 ) ) ;
#2349=CARTESIAN_POINT ( 'NONE',  ( -4.132008100336891587, 40.32855870418434563, -12.85265726257471108 ) ) ;
#2350=CARTESIAN_POINT ( 'NONE',  ( -13.25105815227180805, 32.02163500762459591, 2.596925824824028339 ) ) ;
#2351=CARTESIAN_POINT ( 'NONE',  ( 0.5158602612934328757, 73.16145157157426127, -13.49014129109500360 ) ) ;
#2352=CARTESIAN_POINT ( 'NONE',  ( 11.66024569017766410, 60.17689946827382386, 6.803589074568463957 ) ) ;
#2354=CARTESIAN_POINT ( 'NONE',  ( -2.138718998850744679, 53.60317316735872595, 13.33842984004382970 ) ) ;
#2355=CARTESIAN_POINT ( 'NONE',  ( 3.636496289402154414, 54.83000000000000540, 11.19198476289190936 ) ) ;
#2356=CARTESIAN_POINT ( 'NONE',  ( 8.343458848123583849, 74.88000000000000966, -11.48378591275253768 ) ) ;
#2357=CARTESIAN_POINT ( 'NONE',  ( 11.09074627470785401, 51.72008494892603636, -7.700087750201487502 ) ) ;
#2358=CARTESIAN_POINT ( 'NONE',  ( -12.57349182499318019, 38.10837077157162867, 4.915015114056598300 ) ) ;
#2359=CARTESIAN_POINT ( 'NONE',  ( 13.48517604768645661, 36.45179642338925419, -0.6325697479206738860 ) ) ;
#2362=CARTESIAN_POINT ( 'NONE',  ( -3.925525489409863233, 77.53884384066057578, 12.91671140569806830 ) ) ;
#2363=CARTESIAN_POINT ( 'NONE',  ( -7.076833851983480805, 80.41718626680707871, 11.49927917534153110 ) ) ;
#2364=CARTESIAN_POINT ( 'NONE',  ( 7.500000000000001776, 107.4971863040494497, -6.484415072061725738 ) ) ;
#2365=EDGE_LOOP ( 'NONE', ( #13383, #9938, #16647, #3030 ) ) ;
#2369=CARTESIAN_POINT ( 'NONE',  ( 11.76794919243112325, 61.42999999999999972, 1.441158131103945434E-15 ) ) ;
#2371=CARTESIAN_POINT ( 'NONE',  ( 10.55733521878493697, 75.75071791524901244, -8.413839998617302030 ) ) ;
#2372=CYLINDRICAL_SURFACE ( 'NONE', #11067, 13.50000000000000000 ) ;
#2373=CARTESIAN_POINT ( 'NONE',  ( -4.171729424061791036, 71.53000000000000114, 12.83926296998457239 ) ) ;
#2374=CARTESIAN_POINT ( 'NONE',  ( 11.76794919243112325, 40.42999999999999972, 1.441158131103945434E-15 ) ) ;
#2376=CARTESIAN_POINT ( 'NONE',  ( -10.14977031755370263, 59.27292367458827727, 8.902714087877939164 ) ) ;
#2377=CARTESIAN_POINT ( 'NONE',  ( 13.41602063970378289, 45.49023818299943400, -1.729735045551601402 ) ) ;
#2378=CARTESIAN_POINT ( 'NONE',  ( 13.41279318566184209, 69.49145390545891132, -1.766636264389374489 ) ) ;
#2379=CARTESIAN_POINT ( 'NONE',  ( 6.173563035904286345, 80.90543369209835589, 12.02534506568683170 ) ) ;
#2380=CARTESIAN_POINT ( 'NONE',  ( 11.66233170971271704, 30.17662848724782521, 6.809971670536899779 ) ) ;
#2381=CARTESIAN_POINT ( 'NONE',  ( -9.573451043744061195, 55.55711678553799970, -9.523417059222403225 ) ) ;
#2382=CARTESIAN_POINT ( 'NONE',  ( -13.48277841417289302, 49.90646545391939526, -0.6818155833736215810 ) ) ;
#2384=CARTESIAN_POINT ( 'NONE',  ( 10.17565235674593005, 42.77150727048867651, -8.872034920332040997 ) ) ;
#2385=CARTESIAN_POINT ( 'NONE',  ( 11.19208411514268420, 39.14620708772159219, 7.549024317084779057 ) ) ;
#2387=CARTESIAN_POINT ( 'NONE',  ( -12.72731565556658673, 70.76746085843132050, -4.502049236143019328 ) ) ;
#2388=CARTESIAN_POINT ( 'NONE',  ( -10.21469213217646121, 61.59053157756512320, -8.827045802700096644 ) ) ;
#2389=( BOUNDED_CURVE ( )  B_SPLINE_CURVE ( 2, ( #4661, #8740, #3232, #14006, #14098, #7060, #9717, #5736, #15153, #15418, #10068, #11289, #3325 ),
 .UNSPECIFIED., .F., .F. ) 
 B_SPLINE_CURVE_WITH_KNOTS ( ( 3, 2, 2, 2, 2, 2, 3 ),
 ( 0.6805555555555555802, 0.6833333333333333481, 0.6888888888888888840, 0.6944444444444444198, 0.6999999999999999556, 0.7055555555555556024, 0.7083333333333333703 ),
 .UNSPECIFIED. ) 
 CURVE ( )  GEOMETRIC_REPRESENTATION_ITEM ( )  RATIONAL_B_SPLINE_CURVE ( ( 0.9755282581475768211, 0.9755282581475768211, 1.000000000000000000, 0.9510565162951535312, 1.000000000000000000, 0.9510565162951535312, 1.000000000000000000, 0.9510565162951535312, 1.000000000000000000, 0.9510565162951535312, 1.000000000000000000, 0.9755282581475768211, 0.9755282581475768211 ) ) 
 REPRESENTATION_ITEM ( '' )  );
#2392=VERTEX_POINT ( 'NONE', #9312 ) ;
#2396=CARTESIAN_POINT ( 'NONE',  ( 13.37052541849207188, 57.49521496994567826, -1.865347435624440164 ) ) ;
#2397=CARTESIAN_POINT ( 'NONE',  ( -11.76794919243112325, 71.92999999999999261, -2.882316262207890869E-15 ) ) ;
#2398=CARTESIAN_POINT ( 'NONE',  ( 7.272992578804311492, 79.87999999999999545, -10.01041549318726709 ) ) ;
#2403=DIRECTION ( 'NONE',  ( -1.000000000000000000, -0.000000000000000000, -0.000000000000000000 ) ) ;
#2405=CARTESIAN_POINT ( 'NONE',  ( -7.982953728650207026, 73.48208634606795897, -10.88794980213214103 ) ) ;
#2407=EDGE_CURVE ( 'NONE', #3478, #14678, #6480, .T. ) ;
#2409=CARTESIAN_POINT ( 'NONE',  ( -11.76794919243112325, 74.78000000000000114, -3.823638476888998827 ) ) ;
#2413=CARTESIAN_POINT ( 'NONE',  ( -7.479440193669519843, 44.39995570584004980, 11.23875935782371371 ) ) ;
#2415=CARTESIAN_POINT ( 'NONE',  ( 10.12510679658022461, 66.77424677226939309, -8.932337163854400686 ) ) ;
#2416=CARTESIAN_POINT ( 'NONE',  ( 8.343458848123583849, 51.87999999999999545, -11.48378591275253768 ) ) ;
#2417=CARTESIAN_POINT ( 'NONE',  ( -5.514649017516719098, 71.48002869512200164, 12.32322048284371263 ) ) ;
#2419=CARTESIAN_POINT ( 'NONE',  ( -12.85543916597470115, 68.07811659554265304, 4.121900813656875329 ) ) ;
#2421=CARTESIAN_POINT ( 'NONE',  ( 4.683651263586128266, 55.01126310294681332, -12.66170012766897557 ) ) ;
#2424=AXIS2_PLACEMENT_3D ( 'NONE', #10229, #3318, #15585 ) ;
#2425=CARTESIAN_POINT ( 'NONE',  ( -7.387617763983256758, 65.40391021994592791, 11.29955664239258084 ) ) ;
#2427=CARTESIAN_POINT ( 'NONE',  ( 8.446640517145640834E-14, 43.67999999999999972, 13.50000000000000000 ) ) ;
#2428=CARTESIAN_POINT ( 'NONE',  ( -11.39564835574532964, 35.20092729567576839, 7.239028663105881556 ) ) ;
#2433=CARTESIAN_POINT ( 'NONE',  ( -13.31326865110370328, 32.00865534729634021, 2.238786097854670754 ) ) ;
#2434=FACE_OUTER_BOUND ( 'NONE', #6319, .T. ) ;
#2435=CARTESIAN_POINT ( 'NONE',  ( 7.029870786644410785, 59.94104792918457747, 11.52738832307962369 ) ) ;
#2436=CARTESIAN_POINT ( 'NONE',  ( -7.696137532356187805, 53.39059926922609378, 11.09266641989247049 ) ) ;
#2437=CARTESIAN_POINT ( 'NONE',  ( -7.272992578804307939, 53.47999999999998977, -10.01041549318726886 ) ) ;
#2438=CARTESIAN_POINT ( 'NONE',  ( 8.343458848123583849, 71.87999999999998124, -11.48378591275253768 ) ) ;
#2439=CARTESIAN_POINT ( 'NONE',  ( 9.077726944796655317, 51.03253575000494635, 10.00638466558158512 ) ) ;
#2440=CARTESIAN_POINT ( 'NONE',  ( -11.71421975593653997, 37.68063548265865137, -6.711783420003171408 ) ) ;
#2441=CARTESIAN_POINT ( 'NONE',  ( 2.303310151039730247, 35.76279920576850913, 13.30420860107493652 ) ) ;
#2443=CARTESIAN_POINT ( 'NONE',  ( -3.216530273324876621, 74.56434933806751530, 13.11174169623774333 ) ) ;
#2444=B_SPLINE_CURVE_WITH_KNOTS ( 'NONE', 3,
 ( #15986, #4154, #9566, #181 ),
 .UNSPECIFIED., .F., .F.,
 ( 4, 4 ),
 ( 0.000000000000000000, 1.000000000000000000 ),
 .UNSPECIFIED. ) ;
#2445=CARTESIAN_POINT ( 'NONE',  ( -6.363446314678021132, 77.44652370057923463, 11.90615704593929536 ) ) ;
#2447=CARTESIAN_POINT ( 'NONE',  ( -13.49462269136053827, 79.94511885973835774, 0.4405215047912745541 ) ) ;
#2448=CARTESIAN_POINT ( 'NONE',  ( -1.328659818498353332E-07, 59.67999629905246195, 13.49999999999999822 ) ) ;
#2449=ORIENTED_EDGE ( 'NONE', *, *, #3081, .T. ) ;
#2450=CARTESIAN_POINT ( 'NONE',  ( 0.000000000000000000, 80.93000000000000682, -13.50000000000000000 ) ) ;
#2453=CARTESIAN_POINT ( 'NONE',  ( -11.76794919243112325, 54.07999999999999829, 3.823638476888994830 ) ) ;
#2457=CARTESIAN_POINT ( 'NONE',  ( 9.024310119946591158, 75.82999935558571281, -10.05502432205268626 ) ) ;
#2459=CARTESIAN_POINT ( 'NONE',  ( 10.92172942406178926, 69.12999999999999545, 7.935100905948387684 ) ) ;
#2460=CARTESIAN_POINT ( 'NONE',  ( 11.76794919243112325, 37.42999999999999972, 1.441158131103945434E-15 ) ) ;
#2462=CARTESIAN_POINT ( 'NONE',  ( -12.57014003203463304, 58.75104985464606955, -4.931354137584416542 ) ) ;
#2463=CARTESIAN_POINT ( 'NONE',  ( 6.882857235644580740, 44.93490147452389039, 11.61738766344687868 ) ) ;
#2464=CARTESIAN_POINT ( 'NONE',  ( 11.94122772029547619, 69.66266832655985297, -6.297391191416378931 ) ) ;
#2465=CARTESIAN_POINT ( 'NONE',  ( -4.171729424061787483, 66.32999999999999829, -12.83926296998457417 ) ) ;
#2467=CARTESIAN_POINT ( 'NONE',  ( -3.638089963872648269, 55.31079992990586192, -13.00509624865515690 ) ) ;
#2468=CARTESIAN_POINT ( 'NONE',  ( -11.02862702592511290, 50.22370839642280060, 7.785847849197222281 ) ) ;
#2469=CARTESIAN_POINT ( 'NONE',  ( 12.90275692282559028, 63.28756754940194185, 3.971062145897854556 ) ) ;
#2470=CARTESIAN_POINT ( 'NONE',  ( 11.93121478369607402, 42.66342760203531270, -6.316342296523080435 ) ) ;
#2471=CARTESIAN_POINT ( 'NONE',  ( 9.269155314290372871, 39.04219773109588232, 9.814949453710875460 ) ) ;
#2473=CARTESIAN_POINT ( 'NONE',  ( -13.31540386738444681, 70.85153878471251687, -2.233583993245589649 ) ) ;
#2474=CARTESIAN_POINT ( 'NONE',  ( -4.261210048699548558, 61.33323415936689571, -12.81044948870924394 ) ) ;
#2477=ORIENTED_EDGE ( 'NONE', *, *, #4272, .T. ) ;
#2480=CARTESIAN_POINT ( 'NONE',  ( 5.076768451170277530, 47.86330475330473178, 12.50906521756310141 ) ) ;
#2481=CARTESIAN_POINT ( 'NONE',  ( 10.64294614749145573, 72.11408737100931887, 8.305316784397419383 ) ) ;
#2482=CARTESIAN_POINT ( 'NONE',  ( 13.41154217937975446, 57.37612970769495746, 1.546557898521643937 ) ) ;
#2483=CARTESIAN_POINT ( 'NONE',  ( -3.636496289402155746, 66.53000000000000114, 11.19198476289190936 ) ) ;
#2484=CARTESIAN_POINT ( 'NONE',  ( -11.76794919243112325, 75.08000000000001251, 3.823638476888994386 ) ) ;
#2485=CARTESIAN_POINT ( 'NONE',  ( -1.150288393095961981, 47.63866982340532985, 13.45354997221035909 ) ) ;
#2488=CARTESIAN_POINT ( 'NONE',  ( 2.138189944381238661, 37.75688142232025513, 13.50000000000000000 ) ) ;
#2489=CARTESIAN_POINT ( 'NONE',  ( -13.50000000000000000, 75.92999999999999261, -3.306546357697853733E-15 ) ) ;
#2491=( BOUNDED_CURVE ( )  B_SPLINE_CURVE ( 2, ( #9497, #10896, #14844, #16088, #17, #13531, #15023, #108, #16265, #3996, #2738, #4172, #14760 ),
 .UNSPECIFIED., .F., .F. ) 
 B_SPLINE_CURVE_WITH_KNOTS ( ( 3, 2, 2, 2, 2, 2, 3 ),
 ( 0.6527777777777777901, 0.6555555555555555580, 0.6611111111111110938, 0.6666666666666666297, 0.6722222222222222765, 0.6777777777777778123, 0.6805555555555555802 ),
 .UNSPECIFIED. ) 
 CURVE ( )  GEOMETRIC_REPRESENTATION_ITEM ( )  RATIONAL_B_SPLINE_CURVE ( ( 0.9755282581475768211, 0.9755282581475768211, 1.000000000000000000, 0.9510565162951535312, 1.000000000000000000, 0.9510565162951535312, 1.000000000000000000, 0.9510565162951535312, 1.000000000000000000, 0.9510565162951535312, 1.000000000000000000, 0.9755282581475768211, 0.9755282581475768211 ) ) 
 REPRESENTATION_ITEM ( '' )  );
#2493=CARTESIAN_POINT ( 'NONE',  ( 9.964133567250449630, 33.78271751155136116, -9.110518748047969240 ) ) ;
#2494=CARTESIAN_POINT ( 'NONE',  ( -9.651932366745469949, 73.56128327655086707, -9.438761847476623501 ) ) ;
#2497=CARTESIAN_POINT ( 'NONE',  ( 7.272992578804311492, 73.87999999999999545, -10.01041549318726886 ) ) ;
#2501=CIRCLE ( 'NONE', #557, 4.000000000000004441 ) ;
#2502=CARTESIAN_POINT ( 'NONE',  ( -7.379967326026998009, 44.40423310405564905, 11.30426345811079258 ) ) ;
#2504=CARTESIAN_POINT ( 'NONE',  ( 13.40272165065616150, 66.48640177007516172, -1.617736196660548575 ) ) ;
#2505=CARTESIAN_POINT ( 'NONE',  ( 13.49999999999999822, 48.27999999999998693, 4.386415899144237684 ) ) ;
#2506=CARTESIAN_POINT ( 'NONE',  ( -8.178477986879377326, 71.36909458440034371, 10.74071161083785420 ) ) ;
#2509=CARTESIAN_POINT ( 'NONE',  ( -13.50000235157018480, 67.93091628171310958, 0.02679276516280407541 ) ) ;
#2511=CARTESIAN_POINT ( 'NONE',  ( 4.849954924687469138, 55.00518118710664339, -12.59872946003133620 ) ) ;
#2514=CARTESIAN_POINT ( 'NONE',  ( -13.21884357211656180, 65.02777525366441580, 2.766200456887108583 ) ) ;
#2515=CARTESIAN_POINT ( 'NONE',  ( -8.992723398997755524, 35.33141607309799070, 10.07310997216105974 ) ) ;
#2521=CARTESIAN_POINT ( 'NONE',  ( -2.757445517627192810, 31.27914755613021924, -13.21542082288816289 ) ) ;
#2522=CARTESIAN_POINT ( 'NONE',  ( -3.320475467054404886E-07, 70.18000001193918536, -13.49999999999999467 ) ) ;
#2524=CARTESIAN_POINT ( 'NONE',  ( 11.65227599590961027, 60.17634486657772186, 6.817218417200347602 ) ) ;
#2526=CARTESIAN_POINT ( 'NONE',  ( -3.961000965835436816, 53.53757305567045677, 12.90588582463717060 ) ) ;
#2527=CARTESIAN_POINT ( 'NONE',  ( 7.272992578804311492, 52.87999999999998835, -10.01041549318726709 ) ) ;
#2529=CARTESIAN_POINT ( 'NONE',  ( -13.49999999999999822, 70.08000000000001251, 4.386415899144235908 ) ) ;
#2531=CARTESIAN_POINT ( 'NONE',  ( 13.22222055999062462, 51.33170938898963698, 2.778060537294016363 ) ) ;
#2532=CARTESIAN_POINT ( 'NONE',  ( -11.86684622039495274, 37.69174919575652183, -6.436470158516030438 ) ) ;
#2533=CARTESIAN_POINT ( 'NONE',  ( 13.43970656773339201, 36.38377728058151206, 1.324025325594676783 ) ) ;
#2536=CARTESIAN_POINT ( 'NONE',  ( -11.18368045070454464, 76.64568724800108157, -7.561459486735044422 ) ) ;
#2537=CARTESIAN_POINT ( 'NONE',  ( -11.67291695571009313, 80.18266643954832773, 6.796720356239053906 ) ) ;
#2539=DIRECTION ( 'NONE',  ( 0.000000000000000000, 0.000000000000000000, -1.000000000000000000 ) ) ;
#2540=DIRECTION ( 'NONE',  ( 0.000000000000000000, 0.000000000000000000, 1.000000000000000000 ) ) ;
#2542=CARTESIAN_POINT ( 'NONE',  ( 2.272985001014427393E-15, 59.17999999999999261, -12.37355403259654807 ) ) ;
#2546=CARTESIAN_POINT ( 'NONE',  ( 2.138189944381238661, 34.75688142232025513, 13.50000000000000000 ) ) ;
#2547=CARTESIAN_POINT ( 'NONE',  ( 8.363171565773356519, 75.86070654028085869, -10.59829022713068092 ) ) ;
#2548=CARTESIAN_POINT ( 'NONE',  ( 10.92172942406179104, 68.73000000000000398, -7.935100905948385908 ) ) ;
#2549=CARTESIAN_POINT ( 'NONE',  ( -7.272992578804310604, 36.37999999999998835, 10.01041549318726709 ) ) ;
#2551=EDGE_CURVE ( 'NONE', #11530, #3044, #6962, .T. ) ;
#2552=CARTESIAN_POINT ( 'NONE',  ( -10.83358975528349255, 58.62471529981993257, -8.055956318462602184 ) ) ;
#2553=CARTESIAN_POINT ( 'NONE',  ( 2.445080149700053643E-15, 51.18000000000000682, -13.50000000000000000 ) ) ;
#2554=CARTESIAN_POINT ( 'NONE',  ( 13.14266044583062332, 69.53951601861682263, -3.086384239676795538 ) ) ;
#2556=CARTESIAN_POINT ( 'NONE',  ( 10.61848859199797168, 30.11238384093089948, 8.344967852243197370 ) ) ;
#2557=CARTESIAN_POINT ( 'NONE',  ( -0.5765868356256266258, 55.20073193861872340, -13.48768407954960580 ) ) ;
#2558=CARTESIAN_POINT ( 'NONE',  ( -4.997904479726364535, 50.49965712629579428, 12.54491501226717709 ) ) ;
#2559=CARTESIAN_POINT ( 'NONE',  ( 13.36443380739206077, 63.49676886780871143, -1.908453827262113656 ) ) ;
#2560=CARTESIAN_POINT ( 'NONE',  ( 8.019993042041946296, 42.87621988591261157, -10.85980660541363640 ) ) ;
#2561=CARTESIAN_POINT ( 'NONE',  ( 10.63937102846270832, 39.11358967386987473, 8.313624546134036564 ) ) ;
#2563=CARTESIAN_POINT ( 'NONE',  ( -13.39749578736152102, 70.87207924715265506, -1.660457757727584527 ) ) ;
#2569=CARTESIAN_POINT ( 'NONE',  ( 4.672230816173793322, 61.01172198417896197, -12.66586740219305973 ) ) ;
#2571=CARTESIAN_POINT ( 'NONE',  ( 4.228388219011975480, 71.83122618453306529, 12.85116208698753404 ) ) ;
#2572=CARTESIAN_POINT ( 'NONE',  ( 13.37669266512173394, 57.36630447280914780, 1.821840660456907068 ) ) ;
#2573=CARTESIAN_POINT ( 'NONE',  ( -7.272992578804310604, 72.38000000000000966, 10.01041549318726709 ) ) ;
#2574=CARTESIAN_POINT ( 'NONE',  ( 7.272992578804308828, 72.98000000000000398, 10.01041549318726709 ) ) ;
#2575=CARTESIAN_POINT ( 'NONE',  ( -3.779418409325009609, 47.54410635614043201, 12.96019630752388174 ) ) ;
#2576=CARTESIAN_POINT ( 'NONE',  ( -4.171729424061791036, 46.53000000000000114, 12.83926296998457239 ) ) ;
#2580=CARTESIAN_POINT ( 'NONE',  ( 1.203083463835363736E-13, 37.18000000000000682, -13.50000000000000000 ) ) ;
#2581=CARTESIAN_POINT ( 'NONE',  ( 13.07329398270627152, 33.54991537887530484, -3.368011412300191854 ) ) ;
#2582=CARTESIAN_POINT ( 'NONE',  ( -1.904792500483675433, 73.24848043052601554, -13.36599649914418286 ) ) ;
#2585=CARTESIAN_POINT ( 'NONE',  ( 11.76794919243112325, 79.28000000000000114, 3.823638476888997051 ) ) ;
#2586=EDGE_LOOP ( 'NONE', ( #11460, #6153, #3710, #7044 ) ) ;
#2589=ADVANCED_FACE ( 'NONE', ( #4853 ), #14290, .T. ) ;
#2590=CARTESIAN_POINT ( 'NONE',  ( -10.39000254332373530, 44.26011697933602562, 8.621106295591292934 ) ) ;
#2592=CARTESIAN_POINT ( 'NONE',  ( -8.343458848123582072, 44.37999999999998835, 11.48378591275254124 ) ) ;
#2593=CARTESIAN_POINT ( 'NONE',  ( -8.131449393936593495, 71.37121561422294747, 10.77635893735787853 ) ) ;
#2596=CARTESIAN_POINT ( 'NONE',  ( -13.09738736950409610, 67.81195449946297060, -3.320732649296348260 ) ) ;
#2598=CARTESIAN_POINT ( 'NONE',  ( 12.68800670179988543, 54.59854656979176468, -4.665911999866591664 ) ) ;
#2601=CARTESIAN_POINT ( 'NONE',  ( -13.49368735088633109, 64.91235305258140897, -0.5046298214861710818 ) ) ;
#2602=CARTESIAN_POINT ( 'NONE',  ( -13.39406886664265350, 34.86875242566303967, -1.758890122878330242 ) ) ;
#2604=CYLINDRICAL_SURFACE ( 'NONE', #6183, 13.50000000000000000 ) ;
#2605=CARTESIAN_POINT ( 'NONE',  ( -3.526462373425089947, 31.30679734055596342, -13.03315977265726389 ) ) ;
#2606=DIRECTION ( 'NONE',  ( 0.000000000000000000, 0.000000000000000000, -1.000000000000000000 ) ) ;
#2608=CARTESIAN_POINT ( 'NONE',  ( 3.543844789428542974, 59.80725957930280856, 13.02736174611344389 ) ) ;
#2610=CARTESIAN_POINT ( 'NONE',  ( -1.158615910969277962, 53.63836784856319184, 13.45283109147737122 ) ) ;
#2611=CARTESIAN_POINT ( 'NONE',  ( -9.520470885617717371, 51.22999999999999687, 6.917026985038133624 ) ) ;
#2613=CARTESIAN_POINT ( 'NONE',  ( -4.171729424061791036, 67.53000000000000114, 12.83926296998457239 ) ) ;
#2614=CARTESIAN_POINT ( 'NONE',  ( 8.568141767261806763, 51.00872231198475504, 10.43334200729065131 ) ) ;
#2616=CARTESIAN_POINT ( 'NONE',  ( -12.93551790015123615, 37.79160025195344730, -3.863825158923987590 ) ) ;
#2617=CARTESIAN_POINT ( 'NONE',  ( 13.30751972784499948, 36.35018164686414366, 2.271560209828621169 ) ) ;
#2619=CARTESIAN_POINT ( 'NONE',  ( -6.252194047236812935, 74.45099389143528867, 11.96513968989806642 ) ) ;
#2620=CARTESIAN_POINT ( 'NONE',  ( -13.48669916444661254, 76.95072171427733565, 0.6016804198428439276 ) ) ;
#2621=CARTESIAN_POINT ( 'NONE',  ( -13.04843550171840327, 80.05451087008829347, 3.490901052320607878 ) ) ;
#2623=CARTESIAN_POINT ( 'NONE',  ( 7.500000000000000888, 104.2017679084708135, -9.199276322163095543 ) ) ;
#2626=EDGE_CURVE ( 'NONE', #14369, #5101, #4644, .T. ) ;
#2627=CARTESIAN_POINT ( 'NONE',  ( 7.272992578804311492, 49.88000000000000256, -10.01041549318726886 ) ) ;
#2632=CARTESIAN_POINT ( 'NONE',  ( -10.28591867025567552, 40.59439376045062886, -8.743580910627192893 ) ) ;
#2633=DIRECTION ( 'NONE',  ( 0.000000000000000000, 0.000000000000000000, 1.000000000000000000 ) ) ;
#2634=CARTESIAN_POINT ( 'NONE',  ( 12.97379061124320643, 75.56364355911627229, -3.737309416985219901 ) ) ;
#2636=CARTESIAN_POINT ( 'NONE',  ( -9.520470885617715595, 41.63000000000000256, -6.917026985038136289 ) ) ;
#2637=CARTESIAN_POINT ( 'NONE',  ( -9.319118815187000138, 41.31534473877036362, 9.767498538115876983 ) ) ;
#2638=CARTESIAN_POINT ( 'NONE',  ( -12.72549284276933612, 58.76724356285878059, -4.507839643634814486 ) ) ;
#2640=CARTESIAN_POINT ( 'NONE',  ( 0.000000000000000000, 80.93000000000000682, 0.000000000000000000 ) ) ;
#2642=CARTESIAN_POINT ( 'NONE',  ( -10.32427104660286510, 55.59635412314061398, -8.699356681262834456 ) ) ;
#2643=CARTESIAN_POINT ( 'NONE',  ( -10.10486216940530646, 49.58475825896382361, -8.952216472663192093 ) ) ;
#2644=CARTESIAN_POINT ( 'NONE',  ( 12.72780439611452685, 63.59248189055149680, -4.500512707593768980 ) ) ;
#2646=CARTESIAN_POINT ( 'NONE',  ( 11.94735587504193397, 42.66220391500009868, -6.285819396456265196 ) ) ;
#2647=CARTESIAN_POINT ( 'NONE',  ( 13.48226358575459471, 39.45385880521023125, -0.6919323233915973814 ) ) ;
#2649=CARTESIAN_POINT ( 'NONE',  ( -13.39560391571467868, 70.87153809504057733, -1.675667837312355690 ) ) ;
#2651=ORIENTED_EDGE ( 'NONE', *, *, #4834, .F. ) ;
#2657=CARTESIAN_POINT ( 'NONE',  ( 11.56708140751954517, 60.68951295404890089, -6.960795543196039326 ) ) ;
#2659=CARTESIAN_POINT ( 'NONE',  ( 7.631122679475396353, 71.96662365772242254, 11.13625026764144721 ) ) ;
#2660=CARTESIAN_POINT ( 'NONE',  ( 13.35787352930365657, 57.49841857882535123, -1.953818782010021904 ) ) ;
#2661=CARTESIAN_POINT ( 'NONE',  ( -7.272992578804310604, 66.37999999999999545, 10.01041549318726709 ) ) ;
#2662=CARTESIAN_POINT ( 'NONE',  ( 11.76794919243112325, 76.42999999999999261, 1.441158131103945434E-15 ) ) ;
#2663=CARTESIAN_POINT ( 'NONE',  ( -9.902832463360342174, 47.28584755916202909, 9.175181509501756594 ) ) ;
#2665=CARTESIAN_POINT ( 'NONE',  ( 13.50000000000000355, 38.57999999999999829, -4.386415899144233244 ) ) ;
#2668=CARTESIAN_POINT ( 'NONE',  ( -10.92172942406178926, 51.62999999999999545, -7.935100905948389460 ) ) ;
#2669=CARTESIAN_POINT ( 'NONE',  ( 10.37937675924905889, 33.76051463339396719, -8.632437102218030844 ) ) ;
#2670=CARTESIAN_POINT ( 'NONE',  ( -6.569835995856939448, 73.42170974065275857, -11.80192330709520299 ) ) ;
#2671=ORIENTED_EDGE ( 'NONE', *, *, #5983, .F. ) ;
#2673=B_SPLINE_CURVE_WITH_KNOTS ( 'NONE', 3,
 ( #6068, #3397, #11709, #7740, #3658, #14251, #2139, #9070, #16912, #4904, #11451, #7564, #17086, #3309, #8810, #4645, #11365, #15656, #8722, #5982, #8981, #14168, #10133, #2055, #14080, #14336, #14423, #4991, #1968, #7392, #10218, #2225, #10303, #6157, #15487, #11534, #15748, #4817, #12770, #659, #10393, #16825, #12941, #11623, #7479, #12860, #749, #2312, #15571, #3566, #7654, #13030, #3482, #8896, #16998, #824, #914, #6323, #10732, #4092, #12136, #14769, #16096, #5173, #25, #14852, #3835, #4004, #9421, #5263, #9507, #8004, #8176, #1340, #3918, #17432, #15925, #2660, #6590, #5428, #14509, #2396, #10565, #13370, #5345, #9249, #17261, #14602, #15840, #8090, #16180, #6757, #9161, #7831, #10649, #13454, #10818, #1179, #2482, #11970, #2746, #13203, #7915, #1003, #6414, #1089, #2572, #1259, #13290, #5086, #17351, #11798, #16012, #17175, #10480, #3746, #11887, #6504, #6671, #12054, #9335, #14684, #9859, #9945, #15031, #15206, #11171, #209, #7191, #15293, #16364, #5786, #16546, #293, #16634, #3012, #3195, #13881, #16457, #12494, #10996, #4538, #8354, #13540, #8533, #9594, #5614, #8442, #4452, #12225, #6847, #117, #15114, #1782, #5523, #1520, #10907, #11255, #1430, #16276, #13797, #1695, #7110, #4182, #4271, #14945, #2836, #2924, #8267, #13628, #3106, #6937, #12315, #9681, #13711, #1610, #12580, #5876, #7027, #12405, #5702, #11083, #4359, #468, #380 ),
 .UNSPECIFIED., .F., .F.,
 ( 4, 2, 2, 2, 1, 2, 2, 1, 2, 2, 2, 2, 1, 2, 2, 1, 1, 2, 2, 2, 2, 2, 2, 2, 2, 2, 2, 1, 1, 1, 1, 1, 1, 2, 2, 1, 2, 2, 2, 1, 2, 2, 1, 2, 2, 2, 2, 2, 1, 1, 2, 2, 2, 1, 2, 2, 1, 2, 1, 2, 2, 1, 1, 2, 2, 2, 2, 2, 1, 1, 1, 1, 1, 2, 2, 2, 2, 1, 1, 2, 2, 2, 2, 2, 2, 2, 2, 2, 2, 1, 2, 2, 1, 1, 1, 1, 2, 1, 2, 2, 1, 1, 2, 2, 2, 2, 1, 2, 2, 1, 1, 4 ),
 ( 0.4460935527485729302, 0.4470126776020930115, 0.4474722400288530522, 0.4477020212422330725, 0.4477594665455780776, 0.4477738278714143427, 0.4477881891972506079, 0.4478169118489230827, 0.4479318024556130928, 0.4488509273091330631, 0.4493104897358931038, 0.4494253803425830585, 0.4494541029942555888, 0.4494612836571736936, 0.4494684643200918539, 0.4494828256459280635, 0.4495402709492730686, 0.4497700521626530890, 0.4506891770161732258, 0.4516083018696933071, 0.4518380830830733275, 0.4520678642964533478, 0.4525274267232133885, 0.4534465515767335253, 0.4543656764302536066, 0.4544231217335986117, 0.4544805670369436168, 0.4545954576436336270, 0.4548252388570136473, 0.4552848012837737435, 0.4555145824971537638, 0.4556294731038437740, 0.4556869184071887791, 0.4557156410588613094, 0.4557300023846975190, 0.4557443637105337841, 0.4562039261372938248, 0.4566634885640538100, 0.4568932697774338303, 0.4569507150807788354, 0.4569650764066151005, 0.4569794377324513102, 0.4570081603841238405, 0.4571230509908138506, 0.4589613006978539023, 0.4594208631246138874, 0.4594495857762864177, 0.4594783084279588925, 0.4595357537313038976, 0.4596506443379939078, 0.4598804255513739281, 0.4603399879781339132, 0.4605697691915139336, 0.4606846597982039437, 0.4607133824498764740, 0.4607421051015489488, 0.4607995504048939539, 0.4617186752584139797, 0.4619484564717940001, 0.4619628177976302097, 0.4619771791234664748, 0.4620059017751390051, 0.4620633470784839547, 0.4621782376851739649, 0.4626378001119338945, 0.4635569249654538093, 0.4644760498189737241, 0.4644832304818918289, 0.4644904111448099893, 0.4645047724706462544, 0.4645334951223187292, 0.4645909404256636788, 0.4647058310323536889, 0.4649356122457336538, 0.4653951746724935834, 0.4663142995260133872, 0.4667738619527733168, 0.4668887525594632715, 0.4669461978628082766, 0.4669749205144807513, 0.4670036431661532816, 0.4672334243795331910, 0.4681525492330529392, 0.4690716740865726320, 0.4693014552999525413, 0.4695312365133325061, 0.4699907989400923247, 0.4709099237936120730, 0.4718290486471317657, 0.4719439392538217759, 0.4719726619054942507, 0.4719870232313305158, 0.4720013845571667255, 0.4720588298605117306, 0.4722886110738916954, 0.4727481735006515695, 0.4732077359274114992, 0.4732220972532477643, 0.4732292779161658691, 0.4732364585790839739, 0.4732651812307565042, 0.4733226265341014538, 0.4734375171407914640, 0.4736672983541714288, 0.4741268607809313584, 0.4743566419943113788, 0.4744715326010013334, 0.4744858939268375986, 0.4745002552526738082, 0.4745289779043463385, 0.4745864232076913436, 0.4755055480612112584 ),
 .UNSPECIFIED. ) ;
#2675=EDGE_CURVE ( 'NONE', #4872, #4556, #17316, .T. ) ;
#2677=CARTESIAN_POINT ( 'NONE',  ( -0.3134612214510462680, 44.66872117570036949, 13.49736608497514645 ) ) ;
#2679=CARTESIAN_POINT ( 'NONE',  ( 8.343458848123578520, 38.97999999999998266, 11.48378591275254124 ) ) ;
#2680=CARTESIAN_POINT ( 'NONE',  ( -13.50006591323950289, 70.92792592063743484, -0.06117401498312825814 ) ) ;
#2684=CARTESIAN_POINT ( 'NONE',  ( -11.67270096012221714, 68.18223154335983338, 6.782186488376318323 ) ) ;
#2686=CARTESIAN_POINT ( 'NONE',  ( 13.06145935877203001, 54.55171067861751055, -3.416583277388366202 ) ) ;
#2688=CARTESIAN_POINT ( 'NONE',  ( -2.811464633627016061E-07, 74.67999216907730897, 13.49999999999999289 ) ) ;
#2689=CARTESIAN_POINT ( 'NONE',  ( -13.38153342487016673, 64.99234170124786658, 1.784551494147652795 ) ) ;
#2690=CARTESIAN_POINT ( 'NONE',  ( -12.91999168696053779, 34.78966554277187129, -3.915358232556644946 ) ) ;
#2692=ORIENTED_EDGE ( 'NONE', *, *, #482, .F. ) ;
#2695=CARTESIAN_POINT ( 'NONE',  ( -5.815297001295619772, 31.39166481203774239, -12.18434089980365442 ) ) ;
#2696=CARTESIAN_POINT ( 'NONE',  ( 6.123937747468421122, 72.95612668926172262, -12.03133095083381221 ) ) ;
#2700=( BOUNDED_CURVE ( )  B_SPLINE_CURVE ( 2, ( #10226, #5836, #14260, #11219, #8580, #1825, #2149, #7573, #12951, #834, #6245, #14993, #17269 ),
 .UNSPECIFIED., .F., .F. ) 
 B_SPLINE_CURVE_WITH_KNOTS ( ( 3, 2, 2, 2, 2, 2, 3 ),
 ( 0.09722222222222222376, 0.1000000000000000056, 0.1055555555555555552, 0.1111111111111111049, 0.1166666666666666685, 0.1222222222222222182, 0.1249999999999999861 ),
 .UNSPECIFIED. ) 
 CURVE ( )  GEOMETRIC_REPRESENTATION_ITEM ( )  RATIONAL_B_SPLINE_CURVE ( ( 0.9755282581475768211, 0.9755282581475768211, 1.000000000000000000, 0.9510565162951535312, 1.000000000000000000, 0.9510565162951535312, 1.000000000000000000, 0.9510565162951535312, 1.000000000000000000, 0.9510565162951535312, 1.000000000000000000, 0.9755282581475768211, 0.9755282581475768211 ) ) 
 REPRESENTATION_ITEM ( '' )  );
#2701=CARTESIAN_POINT ( 'NONE',  ( -13.45991843043591096, 52.96599441791912000, 1.039553241502096492 ) ) ;
#2702=CARTESIAN_POINT ( 'NONE',  ( 11.76794919243112325, 49.42999999999999972, 1.441158131103945434E-15 ) ) ;
#2703=CARTESIAN_POINT ( 'NONE',  ( 4.171729424061789260, 67.82999999999999829, 12.83926296998457417 ) ) ;
#2704=CARTESIAN_POINT ( 'NONE',  ( 8.159022896083504506, 50.99002612469284657, 10.75553822827256667 ) ) ;
#2705=VECTOR ( 'NONE', #5945, 1000.000000000000000 ) ;
#2706=CARTESIAN_POINT ( 'NONE',  ( -8.560159368989697981, 37.50835171243769395, -10.44038914743977919 ) ) ;
#2707=CARTESIAN_POINT ( 'NONE',  ( 13.48543408635378960, 36.40015360244564846, 0.8552198172808073151 ) ) ;
#2709=CARTESIAN_POINT ( 'NONE',  ( -12.98187037175444480, 74.06246690446607772, 3.705372543562173604 ) ) ;
#2710=CARTESIAN_POINT ( 'NONE',  ( -11.15111956154761153, 76.64367872175508012, -7.609542610069594204 ) ) ;
#2711=CARTESIAN_POINT ( 'NONE',  ( -13.50011421399957534, 79.90048673417217628, -0.8580047538210755498 ) ) ;
#2713=CARTESIAN_POINT ( 'NONE',  ( -6.556136581996924839, 80.92999999999997840, 10.79013235404389803 ) ) ;
#2716=CARTESIAN_POINT ( 'NONE',  ( -3.636496289402153081, 50.32999999999999829, -11.19198476289190936 ) ) ;
#2720=CARTESIAN_POINT ( 'NONE',  ( -12.16229058013323971, 40.71428809225115941, -5.874955487704208501 ) ) ;
#2722=CARTESIAN_POINT ( 'NONE',  ( 11.36553548705029115, 75.15715277410380679, 7.285283613151663396 ) ) ;
#2723=FACE_OUTER_BOUND ( 'NONE', #6773, .T. ) ;
#2724=CARTESIAN_POINT ( 'NONE',  ( -9.520470885617715595, 44.62999999999999545, -6.917026985038136289 ) ) ;
#2725=CARTESIAN_POINT ( 'NONE',  ( -11.25855217171127798, 41.20965883259114548, 7.449731759125929109 ) ) ;
#2726=CARTESIAN_POINT ( 'NONE',  ( -5.791125120803746640, 58.39073047950922302, -12.19479843928588281 ) ) ;
#2729=CARTESIAN_POINT ( 'NONE',  ( 4.171729424061791924, 60.03000000000000114, -12.83926296998457239 ) ) ;
#2731=CARTESIAN_POINT ( 'NONE',  ( -0.2755667434418575534, 55.18990795935741289, -13.49760167474381589 ) ) ;
#2732=CARTESIAN_POINT ( 'NONE',  ( -12.38440713219831935, 49.73388119143891117, -5.378281758800909529 ) ) ;
#2733=CARTESIAN_POINT ( 'NONE',  ( 11.58332279299003709, 63.68852283645756529, -6.934441872440040733 ) ) ;
#2734=CARTESIAN_POINT ( 'NONE',  ( 10.70653119882778093, 42.11765279685179308, 8.223170724734634618 ) ) ;
#2735=CARTESIAN_POINT ( 'NONE',  ( 5.972384284050402670, 38.89754117051403881, 12.11500310741538478 ) ) ;
#2737=CARTESIAN_POINT ( 'NONE',  ( 8.343458848123583849, 74.87999999999999545, -11.48378591275253768 ) ) ;
#2738=CARTESIAN_POINT ( 'NONE',  ( -4.171729424061787483, 48.32999999999999829, -12.83926296998457417 ) ) ;
#2740=VERTEX_POINT ( 'NONE', #14652 ) ;
#2741=CARTESIAN_POINT ( 'NONE',  ( -5.678969180980832476, 43.38635333003058037, -12.24742126128782793 ) ) ;
#2742=CARTESIAN_POINT ( 'NONE',  ( 5.896062637422001984, 80.92999999999999261, -12.11648925032761070 ) ) ;
#2743=CARTESIAN_POINT ( 'NONE',  ( 6.457115167747857321, 60.94273233830644898, -11.85567478446476208 ) ) ;
#2746=CARTESIAN_POINT ( 'NONE',  ( 13.39657427826484692, 57.37181503160490337, 1.667884572635154772 ) ) ;
#2747=CARTESIAN_POINT ( 'NONE',  ( 2.272985001014427788E-15, 68.18000000000000682, -12.37355403259654985 ) ) ;
#2748=CARTESIAN_POINT ( 'NONE',  ( -3.636496289402153081, 77.32999999999999829, -11.19198476289190936 ) ) ;
#2749=CARTESIAN_POINT ( 'NONE',  ( -9.452515638101248285, 47.30908623721830253, 9.648130606565771927 ) ) ;
#2757=CARTESIAN_POINT ( 'NONE',  ( 13.08972554372986075, 33.54752892044167822, -3.303546669638452116 ) ) ;
#2758=CARTESIAN_POINT ( 'NONE',  ( -9.668918040932872771, 73.56214475094522243, -9.421380043680995797 ) ) ;
#2761=CARTESIAN_POINT ( 'NONE',  ( -1.878130797603207114, 62.61247834605533313, 13.36956684767648973 ) ) ;
#2764=CARTESIAN_POINT ( 'NONE',  ( -12.00637140143189541, 44.15767552562060416, 6.172567600639201402 ) ) ;
#2767=CARTESIAN_POINT ( 'NONE',  ( -10.92172942406179104, 47.23000000000000398, 7.935100905948387684 ) ) ;
#2768=CARTESIAN_POINT ( 'NONE',  ( 4.171729424061789260, 43.82999999999999829, 12.83926296998457417 ) ) ;
#2769=CARTESIAN_POINT ( 'NONE',  ( -13.21610071135663311, 71.02858066329746123, 2.789574207621230872 ) ) ;
#2773=CARTESIAN_POINT ( 'NONE',  ( -13.20639446093759695, 67.82980414093228205, -2.833402894642628400 ) ) ;
#2775=CARTESIAN_POINT ( 'NONE',  ( 11.52508508714884705, 54.69232931852840807, -7.030130978255333396 ) ) ;
#2777=FACE_OUTER_BOUND ( 'NONE', #14696, .T. ) ;
#2778=CARTESIAN_POINT ( 'NONE',  ( -11.86422739765571599, 64.69155293540576679, -6.441358199379890515 ) ) ;
#2779=ORIENTED_EDGE ( 'NONE', *, *, #75, .T. ) ;
#2780=CARTESIAN_POINT ( 'NONE',  ( -10.92172942406178926, 63.63000000000000256, -7.935100905948389460 ) ) ;
#2781=CARTESIAN_POINT ( 'NONE',  ( -13.50004905279464751, 34.92235202864698351, -0.2160710017874167832 ) ) ;
#2783=CARTESIAN_POINT ( 'NONE',  ( 13.40346092485427576, 78.37380768283490795, 1.611608511483868966 ) ) ;
#2784=CARTESIAN_POINT ( 'NONE',  ( -8.891200544363830713E-16, 49.67999999999999261, 13.50000000000000000 ) ) ;
#2786=CARTESIAN_POINT ( 'NONE',  ( 8.443682917512239428, 72.85701949107047426, -10.53438822433166422 ) ) ;
#2788=CARTESIAN_POINT ( 'NONE',  ( 5.983891046846114392, 59.89805057951193135, 12.10717649698468001 ) ) ;
#2790=CARTESIAN_POINT ( 'NONE',  ( -4.171729424061791036, 74.53000000000000114, 12.83926296998457239 ) ) ;
#2791=CARTESIAN_POINT ( 'NONE',  ( -13.43529243779076765, 52.88326165438618887, -1.348469057933256110 ) ) ;
#2792=VECTOR ( 'NONE', #14285, 1000.000000000000114 ) ;
#2793=CARTESIAN_POINT ( 'NONE',  ( 2.272985001014427788E-15, 50.17999999999999261, -12.37355403259654985 ) ) ;
#2794=CARTESIAN_POINT ( 'NONE',  ( -4.171729424061791036, 70.53000000000001535, 12.83926296998457239 ) ) ;
#2795=CARTESIAN_POINT ( 'NONE',  ( 8.299058230608185482, 50.99636966829371687, 10.64802582075173021 ) ) ;
#2796=CARTESIAN_POINT ( 'NONE',  ( -11.99645458172713752, 37.70142398792544469, -6.195780018836668290 ) ) ;
#2797=CARTESIAN_POINT ( 'NONE',  ( 13.15610773373603948, 36.32156525380936074, 3.060187894280851140 ) ) ;
#2799=CARTESIAN_POINT ( 'NONE',  ( -10.47229713462876610, 74.25542378161327406, 8.519458686554706617 ) ) ;
#2800=CARTESIAN_POINT ( 'NONE',  ( -13.22110634326003975, 76.83180770776795043, -2.777616017796241898 ) ) ;
#2801=CARTESIAN_POINT ( 'NONE',  ( -12.31517163679457916, 80.13229876729300827, 5.530790380342764045 ) ) ;
#2803=CARTESIAN_POINT ( 'NONE',  ( 0.000000000000000000, 80.93000000000000682, 0.000000000000000000 ) ) ;
#2805=CARTESIAN_POINT ( 'NONE',  ( 2.272985001014427393E-15, 44.17999999999999261, -12.37355403259654807 ) ) ;
#2809=CARTESIAN_POINT ( 'NONE',  ( -2.380112485275091228, 34.26557354401293765, -13.29211986648399524 ) ) ;
#2810=CARTESIAN_POINT ( 'NONE',  ( 13.32771338909670611, 75.35456652835816271, 2.149902385128953597 ) ) ;
#2813=CARTESIAN_POINT ( 'NONE',  ( -7.499999999999992895, 88.93000000000000682, -9.367496997597603681 ) ) ;
#2814=CARTESIAN_POINT ( 'NONE',  ( -4.151018824075187297, 41.53077687151799324, 12.84636745817926773 ) ) ;
#2816=CARTESIAN_POINT ( 'NONE',  ( -5.763218716402632502, 58.38963670260850591, -12.20800189707574113 ) ) ;
#2819=PLANE ( 'NONE',  #11564 ) ;
#2820=CARTESIAN_POINT ( 'NONE',  ( -8.343458848123582072, 58.38000000000000966, 11.48378591275253768 ) ) ;
#2821=CARTESIAN_POINT ( 'NONE',  ( -13.47670514672201492, 49.90263017273650092, -0.7938299215749298199 ) ) ;
#2822=CARTESIAN_POINT ( 'NONE',  ( 13.40301953286001257, 63.37151237674334681, 1.680986317143484232 ) ) ;
#2823=CARTESIAN_POINT ( 'NONE',  ( 11.28856919156083904, 42.15232267161604796, 7.408146303404825161 ) ) ;
#2824=CARTESIAN_POINT ( 'NONE',  ( 1.785599194582236620E-06, 38.68004968046676595, 13.49999999999976374 ) ) ;
#2825=ORIENTED_EDGE ( 'NONE', *, *, #2906, .F. ) ;
#2830=CARTESIAN_POINT ( 'NONE',  ( -3.553968802922996773, 43.30778666167008595, -13.03033527728538310 ) ) ;
#2831=CARTESIAN_POINT ( 'NONE',  ( -7.499999999999998224, 108.1058439696177516, 5.080312676971231234 ) ) ;
#2832=CARTESIAN_POINT ( 'NONE',  ( 13.01319014679174479, 60.55827135456127053, -3.592833797878408841 ) ) ;
#2835=CARTESIAN_POINT ( 'NONE',  ( 13.41802420445356425, 66.48176821741365927, -1.487227729902038220 ) ) ;
#2836=CARTESIAN_POINT ( 'NONE',  ( 3.222688025018089597, 56.79589291944066787, 13.10971560064693620 ) ) ;
#2837=CARTESIAN_POINT ( 'NONE',  ( -11.76794919243112325, 59.77999999999998693, -3.823638476888998827 ) ) ;
#2838=CARTESIAN_POINT ( 'NONE',  ( -3.636496289402153081, 65.32999999999999829, -11.19198476289190936 ) ) ;
#2839=CARTESIAN_POINT ( 'NONE',  ( -11.28838743354254959, 47.20770152966969846, 7.404409973131605760 ) ) ;
#2840=CARTESIAN_POINT ( 'NONE',  ( 5.558388671817832360, 45.97832039020661199, -12.30261423939740162 ) ) ;
#2841=DIRECTION ( 'NONE',  ( 0.000000000000000000, 0.000000000000000000, -1.000000000000000000 ) ) ;
#2843=CARTESIAN_POINT ( 'NONE',  ( -3.677005786994592906, 56.54778140968930700, 12.98976059619792522 ) ) ;
#2845=CARTESIAN_POINT ( 'NONE',  ( -2.138189944381236884, 39.25688142232026223, -13.50000000000000000 ) ) ;
#2846=CARTESIAN_POINT ( 'NONE',  ( 10.42437936642323137, 33.75805611468842926, -8.578056805215203084 ) ) ;
#2850=CARTESIAN_POINT ( 'NONE',  ( -0.6030540269933777342, 62.65833043166017546, 13.50000000000103562 ) ) ;
#2852=CARTESIAN_POINT ( 'NONE',  ( -13.47581441816511116, 40.90212384545007751, -0.8079750235031136762 ) ) ;
#2854=CARTESIAN_POINT ( 'NONE',  ( -13.47719069686192839, 43.95707978810331440, 0.7844768294817338061 ) ) ;
#2856=VECTOR ( 'NONE', #4357, 1000.000000000000000 ) ;
#2858=CARTESIAN_POINT ( 'NONE',  ( -13.50000000000000000, 40.92999999999999261, -3.306546357697853733E-15 ) ) ;
#2859=CARTESIAN_POINT ( 'NONE',  ( -4.171729424061787483, 45.33000000000000540, -12.83926296998457417 ) ) ;
#2860=CARTESIAN_POINT ( 'NONE',  ( -12.67307004936112413, 71.09835393786092084, 4.654973291148522208 ) ) ;
#2862=CARTESIAN_POINT ( 'NONE',  ( -9.811400904590312777, 67.56937204541171127, -9.274875428382246767 ) ) ;
#2865=CARTESIAN_POINT ( 'NONE',  ( 13.49994682080826713, 54.43208894843145629, -0.06111802256781772441 ) ) ;
#2866=B_SPLINE_CURVE_WITH_KNOTS ( 'NONE', 3,
 ( #17179, #6508, #10483, #10568, #2144, #15844, #11890, #3838, #9252, #2485, #7919, #17435, #10999, #13458, #4009, #14949, #12058, #5348, #2575, #9510, #6674, #16015, #16183, #13373, #120, #13543, #12139, #5526, #17354, #14688, #10735, #4095, #12319, #16099, #9424, #5267, #16367, #9338, #28, #1433, #5432, #14773, #212, #1523, #2749, #5617, #6760, #6593, #1182, #8094, #10910, #2663, #4185, #8007, #10821, #14855, #1345, #15035, #8181, #2839, #6851, #12228, #16279, #11973, #10652, #9597, #3921, #1263, #8357, #8271, #13631, #6940, #4275, #2927, #9685, #296, #16721, #12408, #4628, #15469, #7374, #471, #3109, #5790, #1785, #6052, #12583, #7030, #5705, #1949, #3016, #13715, #8447, #13800, #16460, #16637, #1614, #7283, #11434, #3379, #11175, #4362, #15383, #9948, #5880, #11088, #9772, #12752, #1699, #15117, #7113, #12499, #385, #4543, #16549, #12666, #16806, #4455, #9862, #555, #15211, #15297, #8536, #13973, #13886, #7196, #11259, #3199, #4713, #8619, #1868, #5965, #11346, #10035, #641, #3290, #8705, #14065, #10116, #8815, #1971, #316, #13907, #7304, #10139, #1802, #1633, #14085, #15141, #11196, #8641, #16741, #5725, #12430, #11107, #3219, #7396, #16480, #7133, #4384, #16831, #9968, #12521, #3038, #9883, #13819, #12776, #8469, #4649, #13994, #15233, #9794, #1720, #10055, #4735, #3402, #4562, #4477, #405, #15407, #11455, #1889, #492, #5812, #8554, #15316, #6075, #12688, #577, #16571, #5898, #5987 ),
 .UNSPECIFIED., .F., .F.,
 ( 4, 2, 2, 1, 1, 2, 2, 2, 2, 2, 1, 2, 2, 1, 2, 2, 2, 2, 1, 1, 2, 2, 1, 2, 2, 2, 2, 2, 2, 2, 1, 1, 1, 2, 2, 2, 2, 1, 1, 1, 2, 2, 2, 2, 2, 2, 2, 2, 2, 1, 2, 2, 1, 1, 1, 2, 2, 2, 2, 2, 1, 2, 2, 2, 2, 2, 1, 1, 1, 2, 2, 2, 2, 1, 1, 2, 2, 1, 1, 2, 2, 2, 2, 1, 2, 2, 1, 1, 1, 2, 2, 2, 2, 1, 1, 1, 2, 2, 2, 2, 2, 2, 2, 2, 2, 2, 2, 2, 1, 1, 1, 1, 2, 4 ),
 ( 0.6520416950275925716, 0.6521563145716774423, 0.6521849694576987710, 0.6522136243437199887, 0.6522709341157624241, 0.6525001732039322766, 0.6529586513802718706, 0.6538756077329512806, 0.6543340859092908746, 0.6545633249974607271, 0.6546206347695031624, 0.6546492896555243801, 0.6546636170985350445, 0.6546779445415457088, 0.6547925640856305796, 0.6557095204383098785, 0.6566264767909891775, 0.6570849549673287715, 0.6571422647393712069, 0.6571565921823818712, 0.6571637559038872034, 0.6571709196253924246, 0.6571995745114136422, 0.6573141940554986240, 0.6575434331436683655, 0.6584603894963475534, 0.6593773458490268524, 0.6596065849371965939, 0.6596638947092390293, 0.6596782221522496936, 0.6596925495952603580, 0.6597212044812815757, 0.6598358240253664464, 0.6602943022017061514, 0.6612112585543855614, 0.6613258780984705432, 0.6613402055414812075, 0.6613545329844917608, 0.6613831878705129785, 0.6614404976425554139, 0.6616697367307252664, 0.6621282149070649714, 0.6625866930834045654, 0.6628159321715744179, 0.6630451712597442704, 0.6639621276124235694, 0.6648790839651028683, 0.6657960403177821673, 0.6662545184941217613, 0.6663118282661641967, 0.6663404831521855254, 0.6663476468736907465, 0.6663548105951960787, 0.6663691380382067431, 0.6664837575822916138, 0.6667129966704614663, 0.6676299530231408763, 0.6680884311994804703, 0.6682030507435654521, 0.6682603605156078874, 0.6683176702876503228, 0.6685469093758201753, 0.6694638657284994743, 0.6699223439048391793, 0.6701515829930090318, 0.6701659104360195851, 0.6701802378790302495, 0.6702088927650514671, 0.6702662025370939025, 0.6703808220811788843, 0.6712977784338580722, 0.6717562566101977772, 0.6719854956983676297, 0.6720428054704100651, 0.6720571329134206184, 0.6720607147741732845, 0.6720642966349259506, 0.6720714603564312828, 0.6721001152424525005, 0.6722147347865373712, 0.6731316911392165592, 0.6735901693155561532, 0.6738194084037260057, 0.6739340279478108764, 0.6739626828338320941, 0.6739698465553374263, 0.6739770102768426474, 0.6739913377198533118, 0.6740486474918957471, 0.6758825601972537900, 0.6767995165499328669, 0.6768138439929434202, 0.6768281714359540846, 0.6768568263219753023, 0.6769141360940176266, 0.6770287556381024974, 0.6772579947262722389, 0.6777164729026114998, 0.6781749510789508717, 0.6784041901671206132, 0.6786334292552902436, 0.6795503856079689875, 0.6796650051520537472, 0.6797796246961386180, 0.6800088637843082484, 0.6804673419606476203, 0.6809258201369869923, 0.6811550592251567338, 0.6812696787692414935, 0.6813269885412839288, 0.6813556434273051465, 0.6813699708703158109, 0.6813771345918210320, 0.6813842983133263642 ),
 .UNSPECIFIED. ) ;
#2867=CARTESIAN_POINT ( 'NONE',  ( -13.49850325917753935, 64.94645159456099748, 0.4826294637078544225 ) ) ;
#2869=CARTESIAN_POINT ( 'NONE',  ( -13.34768415857563895, 35.00084492118001123, 2.022211493481883338 ) ) ;
#2870=ORIENTED_EDGE ( 'NONE', *, *, #7896, .F. ) ;
#2871=CARTESIAN_POINT ( 'NONE',  ( 12.57096588966968476, 78.25114472168620239, 4.928957368016985363 ) ) ;
#2873=EDGE_CURVE ( 'NONE', #13703, #10105, #16524, .T. ) ;
#2874=CARTESIAN_POINT ( 'NONE',  ( -11.71377142868683308, 31.68060524350620710, -6.712565316410540106 ) ) ;
#2875=CARTESIAN_POINT ( 'NONE',  ( 10.57277106256930743, 72.74993520006962910, -8.398181679965585289 ) ) ;
#2877=CARTESIAN_POINT ( 'NONE',  ( 13.49999999999999822, 69.27999999999997272, 4.386415899144237684 ) ) ;
#2878=CARTESIAN_POINT ( 'NONE',  ( -13.44352697023783882, 52.97286464824527741, 1.235290049340939333 ) ) ;
#2880=CARTESIAN_POINT ( 'NONE',  ( 3.636496289402157078, 44.03000000000000114, -11.19198476289190936 ) ) ;
#2881=CARTESIAN_POINT ( 'NONE',  ( -10.92172942406179104, 67.23000000000000398, 7.935100905948387684 ) ) ;
#2883=CARTESIAN_POINT ( 'NONE',  ( 11.79460588130421250, 69.18643917531105103, 6.568504325302008340 ) ) ;
#2885=CARTESIAN_POINT ( 'NONE',  ( 1.346677795875271366, 35.72842155251986895, 13.43267107845611896 ) ) ;
#2887=CARTESIAN_POINT ( 'NONE',  ( -12.02303369154052426, 74.15637003178895270, 6.139850934852907116 ) ) ;
#2888=CARTESIAN_POINT ( 'NONE',  ( -13.49205587446478027, 76.94592520882854103, 0.4631159351518623901 ) ) ;
#2889=AXIS2_PLACEMENT_3D ( 'NONE', #8915, #3500, #3678 ) ;
#2894=CARTESIAN_POINT ( 'NONE',  ( 11.76794919243112325, 49.42999999999999972, 1.441158131103945434E-15 ) ) ;
#2896=CARTESIAN_POINT ( 'NONE',  ( 2.138189944381242213, 36.10311857767973720, -13.49999999999999822 ) ) ;
#2897=CARTESIAN_POINT ( 'NONE',  ( 12.36199458607823054, 75.23191100907908435, 5.426195953618915269 ) ) ;
#2899=CARTESIAN_POINT ( 'NONE',  ( 2.272985001014427788E-15, 35.17999999999998550, -12.37355403259654985 ) ) ;
#2900=CARTESIAN_POINT ( 'NONE',  ( -11.99741742274050793, 41.15884529835775396, 6.204743281297112389 ) ) ;
#2901=CARTESIAN_POINT ( 'NONE',  ( 2.445080149700053643E-15, 66.18000000000000682, -13.50000000000000000 ) ) ;
#2902=CARTESIAN_POINT ( 'NONE',  ( 2.399255109878465575, 44.76621471937859553, 13.28788051155532912 ) ) ;
#2903=B_SPLINE_CURVE_WITH_KNOTS ( 'NONE', 3,
 ( #12973, #3511, #14456, #11570, #1036, #8925, #14284, #6104, #14201, #2169, #12890, #13147, #2083, #15780, #7682, #7595, #16860, #4846, #778, #10250, #9190, #10169, #15517, #855, #8845, #17030, #943, #4935, #6185, #13061, #6444, #2425, #6354, #11739, #16944, #10335, #7775, #3690, #7508, #15690, #15604, #6266, #3596, #11653, #14539, #9009, #2343, #14366, #7858, #10421, #17117, #11486, #2254, #5022, #3429, #9103, #11829, #17207, #5117, #10509, #15871, #692, #17291, #17461, #9624, #13316, #9449, #10594, #6701, #9276, #7943, #13570, #14975, #3862, #6534, #11913, #1461, #2514, #14798, #1208, #5204, #16304, #5462, #2689, #1121, #15955, #8120, #14629, #6617, #2867, #16212, #2601, #11997, #17379, #13233, #12168, #5294, #4124, #10676, #9537, #16041, #3949, #12080, #9363, #14713, #6881, #8031, #13398, #1287, #5374, #12253, #10761, #13486, #16124, #4035, #1374, #6788, #148, #59, #10845, #14882, #2778, #8208, #5554, #10938, #4212, #14000, #4388, #9799, #1637, #7139, #16747, #6967, #15238, #4300, #12346, #15145, #12695, #13913, #7055, #1807, #4654, #582, #8646, #11200, #7221, #5730, #9975, #13824, #7309, #9712, #10062, #13739, #2956, #11112, #5992, #16484, #12435, #11375, #3042, #8474, #321, #1549, #1724, #238, #3226, #16576, #5644, #5817, #8384, #12608, #3135, #12525, #497, #11026, #409, #15412, #8297, #16397, #15056, #4481, #5904, #11283, #13654, #9890, #8560, #4567, #16660 ),
 .UNSPECIFIED., .F., .F.,
 ( 4, 2, 2, 2, 1, 1, 2, 2, 1, 2, 1, 2, 2, 1, 1, 2, 2, 2, 2, 1, 2, 2, 2, 2, 2, 2, 2, 2, 1, 1, 2, 2, 1, 1, 2, 2, 1, 1, 2, 2, 2, 2, 2, 1, 1, 2, 2, 2, 1, 2, 2, 1, 2, 2, 1, 1, 1, 2, 2, 1, 2, 2, 2, 2, 2, 2, 2, 2, 2, 2, 2, 1, 1, 1, 1, 2, 2, 1, 2, 2, 1, 1, 2, 2, 2, 2, 2, 2, 2, 2, 1, 2, 2, 1, 1, 2, 2, 2, 2, 2, 1, 1, 2, 2, 2, 2, 2, 2, 1, 2, 4 ),
 ( 0.2989785326016397571, 0.2998994589697745461, 0.3003599221538418851, 0.3005901537458756101, 0.3007052695418924171, 0.3007628274399008483, 0.3007772169144029561, 0.3007916063889050640, 0.3008203853379092796, 0.3026622380741786911, 0.3027197959721871223, 0.3027341854466892301, 0.3027413801839403118, 0.3027485749211913379, 0.3027773538701955536, 0.3028924696662123051, 0.3031227012582458635, 0.3035831644423129805, 0.3045040908104472699, 0.3046192066064640214, 0.3046767645044724526, 0.3047343224024808284, 0.3049645539945143868, 0.3054250171785815038, 0.3063459435467157932, 0.3065761751387493517, 0.3066337330367577274, 0.3066625119857619430, 0.3066912909347661587, 0.3068064067307829101, 0.3072668699148500826, 0.3081877962829843720, 0.3084180278750179860, 0.3085331436710347375, 0.3085907015690431687, 0.3086050910435452210, 0.3086194805180473288, 0.3086482594670515445, 0.3091087226511187169, 0.3100296490192530618, 0.3104901122033202343, 0.3105188911523243944, 0.3105476701013286100, 0.3106052279993369858, 0.3107203437953537928, 0.3109505753873874068, 0.3118715017555217517, 0.3123319649395889241, 0.3124470807356057311, 0.3124758596846099468, 0.3125046386336141624, 0.3125621965316225381, 0.3127924281236560966, 0.3137133544917904415, 0.3141738176758576140, 0.3144040492678912280, 0.3144328282168954436, 0.3144472176913974959, 0.3144616071658996037, 0.3145191650639080350, 0.3146342808599247864, 0.3155552072280591314, 0.3160156704121263038, 0.3162459020041598623, 0.3163610178001766693, 0.3164185756981850450, 0.3164761335961934763, 0.3173970599643277657, 0.3183179863324621106, 0.3183467652814663262, 0.3183611547559684340, 0.3183755442304705419, 0.3184331021284789176, 0.3185482179244957246, 0.3187784495165293386, 0.3192389127005965666, 0.3201598390687310225, 0.3202749548647478295, 0.3203037338137519896, 0.3203181232882540974, 0.3203325127627562052, 0.3203900706607645810, 0.3206203022527980839, 0.3210807654368651454, 0.3220016918049992127, 0.3222319233970327157, 0.3224621549890662742, 0.3229226181731332801, 0.3238435445412673475, 0.3240737761333008504, 0.3241888919293176574, 0.3242176708783218175, 0.3242320603528239253, 0.3242464498273260332, 0.3243040077253344089, 0.3247644709094015258, 0.3256853972775357042, 0.3261458604616027657, 0.3261602499361048735, 0.3261746394106069813, 0.3262034183596111969, 0.3262609762576195727, 0.3263760920536363241, 0.3266063236456698826, 0.3275272500138040055, 0.3279877131978710669, 0.3281028289938878184, 0.3281316079428920340, 0.3281603868918961942, 0.3282179447899046254, 0.3284481763819381284 ),
 .UNSPECIFIED. ) ;
#2904=CARTESIAN_POINT ( 'NONE',  ( 8.343458848123580296, 58.98000000000000398, 11.48378591275253768 ) ) ;
#2906=EDGE_CURVE ( 'NONE', #17443, #16027, #15981, .T. ) ;
#2907=CARTESIAN_POINT ( 'NONE',  ( 6.767892274116773521, 80.93000000001259764, -11.68099457092376348 ) ) ;
#2908=CARTESIAN_POINT ( 'NONE',  ( -10.12981325033382340, 49.58606605476560247, -8.923950245100398249 ) ) ;
#2909=CARTESIAN_POINT ( 'NONE',  ( 11.56754221458070298, 63.17051984811690346, 6.960026861118096875 ) ) ;
#2910=CARTESIAN_POINT ( 'NONE',  ( 12.83702738905192398, 42.27686750378746439, 4.271642589196766870 ) ) ;
#2911=CARTESIAN_POINT ( 'NONE',  ( 5.936052360656044691, 48.96357924273701911, -12.12490342414647593 ) ) ;
#2913=CARTESIAN_POINT ( 'NONE',  ( -3.636496289402155746, 75.53000000000000114, 11.19198476289190936 ) ) ;
#2917=VERTEX_POINT ( 'NONE', #84 ) ;
#2918=CARTESIAN_POINT ( 'NONE',  ( -8.698957838002245424, 43.51485979879910815, -10.32366908839676078 ) ) ;
#2919=CYLINDRICAL_SURFACE ( 'NONE', #16696, 13.50000000000000000 ) ;
#2920=CARTESIAN_POINT ( 'NONE',  ( 11.66807071203169777, 60.68264838426821939, -6.791431104833153043 ) ) ;
#2923=CARTESIAN_POINT ( 'NONE',  ( 13.44884314945179682, 66.38927782166076952, 1.174156769367327824 ) ) ;
#2924=CARTESIAN_POINT ( 'NONE',  ( 3.171349303842611711, 56.79407181424019768, 13.12227985861226109 ) ) ;
#2925=CARTESIAN_POINT ( 'NONE',  ( -7.272992578804307939, 56.47999999999998977, -10.01041549318726886 ) ) ;
#2926=CARTESIAN_POINT ( 'NONE',  ( -9.520470885617717371, 63.23000000000001108, 6.917026985038133624 ) ) ;
#2927=CARTESIAN_POINT ( 'NONE',  ( -12.25285257643324321, 47.13773527728996271, 5.669290189831918347 ) ) ;
#2930=CARTESIAN_POINT ( 'NONE',  ( 8.257394697130328254, 30.86552653227584742, -10.68051812031342251 ) ) ;
#2931=ADVANCED_FACE ( 'NONE', ( #1491 ), #6725, .T. ) ;
#2932=CARTESIAN_POINT ( 'NONE',  ( -2.134337778213805326, 56.60326167549609266, 13.33023129177848887 ) ) ;
#2936=CARTESIAN_POINT ( 'NONE',  ( 13.29699880966072278, 33.34798608968654321, 2.332353922266759305 ) ) ;
#2938=CARTESIAN_POINT ( 'NONE',  ( 0.1174797757853172780, 40.17577724366387315, -13.49956142739842058 ) ) ;
#2941=CARTESIAN_POINT ( 'NONE',  ( -2.239153631970620673, 62.59948832305353505, 13.31301680066964543 ) ) ;
#2943=CARTESIAN_POINT ( 'NONE',  ( -13.45392095391353671, 40.96936140205911414, 1.136027132915432114 ) ) ;
#2946=CARTESIAN_POINT ( 'NONE',  ( -11.20488271874176078, 44.21300015732045097, 7.529980452644597477 ) ) ;
#2947=B_SPLINE_CURVE_WITH_KNOTS ( 'NONE', 3,
 ( #4802, #2379, #7814, #10204, #3551, #895, #15557, #5067, #7548, #13187, #7637, #11780, #9052, #13098, #6222, #8882, #14406, #3468, #10289, #984, #12926 ),
 .UNSPECIFIED., .F., .F.,
 ( 4, 2, 2, 2, 1, 2, 2, 2, 2, 1, 1, 4 ),
 ( 0.000000000000000000, 0.001230814438799202265, 0.001846221658198803290, 0.002000073463048703763, 0.002153925267898604452, 0.002461628877598403230, 0.003692443316397600508, 0.003846295121247500330, 0.003923221023672450458, 0.004000146926097401454, 0.004307850535797202833, 0.004923257755196806459 ),
 .UNSPECIFIED. ) ;
#2948=DIRECTION ( 'NONE',  ( 0.000000000000000000, -1.000000000000000000, 0.000000000000000000 ) ) ;
#2949=CARTESIAN_POINT ( 'NONE',  ( 10.92172942406179104, 30.72999999999999332, -7.935100905948385908 ) ) ;
#2952=ADVANCED_FACE ( 'NONE', ( #9560 ), #14910, .T. ) ;
#2953=CARTESIAN_POINT ( 'NONE',  ( -10.07108133119379012, 67.58295566904861573, -8.990215881721550062 ) ) ;
#2955=CARTESIAN_POINT ( 'NONE',  ( 11.54962138675810479, 54.69070229437127750, -6.989731339562734291 ) ) ;
#2956=CARTESIAN_POINT ( 'NONE',  ( -5.888583767921062417, 64.39455096188707728, -12.14803002262569720 ) ) ;
#2958=CARTESIAN_POINT ( 'NONE',  ( -12.72183143979101416, 35.09323451362223523, 4.520332688420920952 ) ) ;
#2960=CARTESIAN_POINT ( 'NONE',  ( 13.25352574315592058, 78.33850325101057877, 2.596262599255617420 ) ) ;
#2963=CARTESIAN_POINT ( 'NONE',  ( 5.943805720458234632, 72.96327358916208539, -12.12110495732162541 ) ) ;
#2964=CARTESIAN_POINT ( 'NONE',  ( 12.01373065778716231, 78.65715868066507710, -6.159954580827336379 ) ) ;
#2966=VECTOR ( 'NONE', #14736, 1000.000000000000000 ) ;
#2967=CARTESIAN_POINT ( 'NONE',  ( 8.343458848123578520, 65.97999999999997556, 11.48378591275254124 ) ) ;
#2968=CARTESIAN_POINT ( 'NONE',  ( -13.49277924355403613, 52.91293775321170756, -0.4922678860690162250 ) ) ;
#2969=CARTESIAN_POINT ( 'NONE',  ( -3.636496289402155746, 42.53000000000000114, 11.19198476289190936 ) ) ;
#2970=CARTESIAN_POINT ( 'NONE',  ( -13.49999999999999822, 61.07999999999999119, 4.386415899144235908 ) ) ;
#2972=CARTESIAN_POINT ( 'NONE',  ( 3.530559298853932049, 68.80696058099172774, 13.03017551344940550 ) ) ;
#2975=CARTESIAN_POINT ( 'NONE',  ( 2.000520122481862502E-14, 73.67999999999999261, 13.50000000000000000 ) ) ;
#2977=CARTESIAN_POINT ( 'NONE',  ( -8.440553202013695966, 74.35714477797125710, 10.53601240182882037 ) ) ;
#2978=CARTESIAN_POINT ( 'NONE',  ( -9.366007952159224104, 76.54695510398188674, -9.722646867579905816 ) ) ;
#2983=CARTESIAN_POINT ( 'NONE',  ( 9.520470885617717371, 46.73000000000000398, -6.917026985038131848 ) ) ;
#2985=CARTESIAN_POINT ( 'NONE',  ( -2.056889372791192105, 32.60599326084160765, 13.34339756607785965 ) ) ;
#2986=CARTESIAN_POINT ( 'NONE',  ( 13.06624678191117894, 75.55090238563390415, -3.394585794078206487 ) ) ;
#2988=VECTOR ( 'NONE', #13123, 1000.000000000000000 ) ;
#2989=CARTESIAN_POINT ( 'NONE',  ( -12.47701956898900910, 41.11767325390844263, 5.155734636392532266 ) ) ;
#2990=CARTESIAN_POINT ( 'NONE',  ( 6.930981503973903557, 51.92345320045085799, -11.59790771992309821 ) ) ;
#2991=CARTESIAN_POINT ( 'NONE',  ( 0.000000000000000000, 80.93000000000000682, -13.50000000000000000 ) ) ;
#2994=CARTESIAN_POINT ( 'NONE',  ( 1.653273178848926472E-15, 80.93000000000000682, 13.50000000000000000 ) ) ;
#2995=LINE ( 'NONE', #9842, #16830 ) ;
#2996=CARTESIAN_POINT ( 'NONE',  ( 8.859641085343996636, 63.02212108781364464, 10.19330108810972924 ) ) ;
#2997=CARTESIAN_POINT ( 'NONE',  ( 10.69513479019918911, 42.11700743034955252, 8.237987836516895257 ) ) ;
#3000=ORIENTED_EDGE ( 'NONE', *, *, #11955, .T. ) ;
#3001=CARTESIAN_POINT ( 'NONE',  ( 11.76794919243112680, 73.58000000000001251, -3.823638476888993942 ) ) ;
#3006=CARTESIAN_POINT ( 'NONE',  ( -4.007469125189920156, 43.32409381421197025, -12.89150143208222765 ) ) ;
#3007=CARTESIAN_POINT ( 'NONE',  ( -7.499999999999997335, 104.6873333394686796, 9.035253535952435300 ) ) ;
#3008=CARTESIAN_POINT ( 'NONE',  ( 12.99308620456710806, 60.56095136765374320, -3.664675452714382775 ) ) ;
#3011=CARTESIAN_POINT ( 'NONE',  ( 3.786209671971815016, 65.81577437060603586, 12.96002889484262965 ) ) ;
#3012=CARTESIAN_POINT ( 'NONE',  ( 10.28852882370732935, 57.09439556068322474, 8.746997244907646518 ) ) ;
#3013=CARTESIAN_POINT ( 'NONE',  ( -7.576616670048093940E-16, 60.67999999999998550, 12.37355403259654985 ) ) ;
#3014=CARTESIAN_POINT ( 'NONE',  ( 10.92172942406179104, 35.72999999999999687, -7.935100905948385908 ) ) ;
#3015=CARTESIAN_POINT ( 'NONE',  ( -7.576616670048093940E-16, 66.67999999999997840, 12.37355403259654985 ) ) ;
#3016=CARTESIAN_POINT ( 'NONE',  ( -13.49258962402246098, 46.94538227618738091, 0.4474236191536023477 ) ) ;
#3017=CARTESIAN_POINT ( 'NONE',  ( 7.545661582016999880, 45.89709249710414696, -11.19442553811792251 ) ) ;
#3018=CYLINDRICAL_SURFACE ( 'NONE', #9684, 13.50000000000000000 ) ;
#3020=CARTESIAN_POINT ( 'NONE',  ( 3.634147496961807722, 31.04944686732046222, -13.02236486152032491 ) ) ;
#3023=CARTESIAN_POINT ( 'NONE',  ( -4.171729424061787483, 39.32999999999999829, -12.83926296998457417 ) ) ;
#3024=CARTESIAN_POINT ( 'NONE',  ( 3.999863251508507744, 32.82381939080141819, 12.89392482267520634 ) ) ;
#3026=CARTESIAN_POINT ( 'NONE',  ( 2.003101852233307056, 40.10816637432754561, -13.35920704381847557 ) ) ;
#3029=CARTESIAN_POINT ( 'NONE',  ( -11.98320029393328490, 62.16226028446121887, 6.301581060576362248 ) ) ;
#3030=ORIENTED_EDGE ( 'NONE', *, *, #2316, .F. ) ;
#3033=CARTESIAN_POINT ( 'NONE',  ( -10.82450696210587360, 44.23580785916440306, 8.068722966871488822 ) ) ;
#3036=CARTESIAN_POINT ( 'NONE',  ( 6.750017152462248760, 29.92926152634062475, 11.69133304809444773 ) ) ;
#3037=CARTESIAN_POINT ( 'NONE',  ( -8.691771469529815392E-16, 46.67999999999999972, 14.19474002721660355 ) ) ;
#3038=CARTESIAN_POINT ( 'NONE',  ( -5.043317043880707118, 46.36194157942755112, -12.52473711853716409 ) ) ;
#3039=CARTESIAN_POINT ( 'NONE',  ( -3.069954153749930637, 67.29026836399954448, -13.14679252126118492 ) ) ;
#3042=CARTESIAN_POINT ( 'NONE',  ( -5.372399846363435927, 64.37448310051588862, -12.38690699972042530 ) ) ;
#3044=VERTEX_POINT ( 'NONE', #522 ) ;
#3046=CARTESIAN_POINT ( 'NONE',  ( -11.71399375460170766, 34.68062007852038420, -6.712177567382903831 ) ) ;
#3048=CIRCLE ( 'NONE', #8726, 13.50000000000000000 ) ;
#3050=CARTESIAN_POINT ( 'NONE',  ( 12.20032402202371991, 78.21732329587429433, 5.797904856266742790 ) ) ;
#3053=CARTESIAN_POINT ( 'NONE',  ( 13.40079223352167759, 72.37267490479835885, 1.638534314007722870 ) ) ;
#3054=CARTESIAN_POINT ( 'NONE',  ( 4.952149856071437206, 79.00137556925825777, -12.55891152037733249 ) ) ;
#3057=CARTESIAN_POINT ( 'NONE',  ( -10.92172942406179104, 65.22999999999998977, 7.935100905948387684 ) ) ;
#3058=CARTESIAN_POINT ( 'NONE',  ( -13.47878953293021631, 52.90389950247480044, -0.7564620949284726059 ) ) ;
#3059=CARTESIAN_POINT ( 'NONE',  ( 11.76794919243112680, 37.57999999999999829, -3.823638476888993942 ) ) ;
#3061=CARTESIAN_POINT ( 'NONE',  ( -13.49999999999999822, 58.07999999999999119, 4.386415899144235908 ) ) ;
#3064=CARTESIAN_POINT ( 'NONE',  ( 11.17437184405764228, 69.14511185220105460, 7.575987940921537600 ) ) ;
#3066=CARTESIAN_POINT ( 'NONE',  ( 0.000000000000000000, 80.93000000000000682, 0.000000000000000000 ) ) ;
#3068=CARTESIAN_POINT ( 'NONE',  ( -12.80823760898952024, 73.77596097351039361, -4.279531554935352311 ) ) ;
#3070=CARTESIAN_POINT ( 'NONE',  ( -9.417894190836991086, 76.54953966738506210, -9.672294700079755003 ) ) ;
#3073=LINE ( 'NONE', #15081, #16145 ) ;
#3076=CARTESIAN_POINT ( 'NONE',  ( -3.636496289402155746, 36.53000000000000114, 11.19198476289190936 ) ) ;
#3079=CARTESIAN_POINT ( 'NONE',  ( 13.31658272420281364, 75.35211548525167302, 2.217973532653136459 ) ) ;
#3081=EDGE_CURVE ( 'NONE', #1976, #12212, #1291, .T. ) ;
#3083=CARTESIAN_POINT ( 'NONE',  ( 7.272992578804308828, 33.97999999999999687, 10.01041549318726709 ) ) ;
#3084=CARTESIAN_POINT ( 'NONE',  ( 13.49999999999999822, 80.28000000000000114, 4.386415899144237684 ) ) ;
#3085=CARTESIAN_POINT ( 'NONE',  ( 10.02787169999155736, 51.77931855093511615, -9.038355711608794252 ) ) ;
#3089=CARTESIAN_POINT ( 'NONE',  ( -4.299010319042174011, 49.33458915034209724, -12.79749347232116996 ) ) ;
#3090=CARTESIAN_POINT ( 'NONE',  ( 12.57254746066391604, 63.25130592606551261, 4.925209957174280007 ) ) ;
#3091=CARTESIAN_POINT ( 'NONE',  ( 11.89700905113649476, 42.19366528341078038, 6.391313303333308937 ) ) ;
#3095=CARTESIAN_POINT ( 'NONE',  ( -11.76794919243112325, 68.93000000000000682, -2.882316262207890869E-15 ) ) ;
#3100=CARTESIAN_POINT ( 'NONE',  ( -2.149914682908597996, 43.25730255030944704, -13.32784165166224888 ) ) ;
#3105=CARTESIAN_POINT ( 'NONE',  ( 12.71198514923275447, 66.26577351268545613, 4.546884237145273566 ) ) ;
#3106=CARTESIAN_POINT ( 'NONE',  ( 2.933928304667394293, 56.78557572382650420, 13.17766192809576964 ) ) ;
#3107=CARTESIAN_POINT ( 'NONE',  ( -11.76794919243112325, 62.78000000000000114, -3.823638476888998827 ) ) ;
#3108=CARTESIAN_POINT ( 'NONE',  ( -7.272992578804310604, 69.38000000000000966, 10.01041549318726709 ) ) ;
#3109=CARTESIAN_POINT ( 'NONE',  ( -13.48021004250667865, 46.95565286317663833, 0.7426006389843816669 ) ) ;
#3110=CARTESIAN_POINT ( 'NONE',  ( 5.768599500741140140, 45.97025363302860512, -12.20601842401291570 ) ) ;
#3111=CARTESIAN_POINT ( 'NONE',  ( -8.891200544363830713E-16, 40.67999999999999261, 13.50000000000000000 ) ) ;
#3112=CARTESIAN_POINT ( 'NONE',  ( 8.525265987162489623, 30.85325237774112139, -10.46836572103978824 ) ) ;
#3113=CARTESIAN_POINT ( 'NONE',  ( -8.600387584108450056, 56.34974602370840557, 10.40593404801639643 ) ) ;
#3114=CARTESIAN_POINT ( 'NONE',  ( -2.124524872238272355, 50.60360011980247208, 13.33178569217110265 ) ) ;
#3116=CARTESIAN_POINT ( 'NONE',  ( 11.10072675311360513, 33.14059506802435351, 7.683623606355369340 ) ) ;
#3118=CARTESIAN_POINT ( 'NONE',  ( 0.2341561698673940428, 40.17158518995367444, -13.49825591440075634 ) ) ;
#3120=VERTEX_POINT ( 'NONE', #4896 ) ;
#3121=CARTESIAN_POINT ( 'NONE',  ( -13.47617400855946990, 61.90230964142129011, -0.8017361068469278651 ) ) ;
#3125=CARTESIAN_POINT ( 'NONE',  ( -12.71700884497776585, 43.76636331146021774, -4.530782870517315430 ) ) ;
#3127=CARTESIAN_POINT ( 'NONE',  ( -10.92172942406179104, 38.22999999999999687, 7.935100905948387684 ) ) ;
#3128=CARTESIAN_POINT ( 'NONE',  ( -8.343458848123582072, 43.38000000000000256, 11.48378591275254124 ) ) ;
#3130=CARTESIAN_POINT ( 'NONE',  ( -11.71173941027563359, 67.68051595497325934, -6.714564204021516325 ) ) ;
#3132=CARTESIAN_POINT ( 'NONE',  ( 9.353841725489496994, 54.04636460753637550, 9.734530468470028453 ) ) ;
#3133=EDGE_CURVE ( 'NONE', #6584, #5101, #903, .T. ) ;
#3135=CARTESIAN_POINT ( 'NONE',  ( -3.150082944707692345, 64.29333076386686230, -13.12737227364866754 ) ) ;
#3137=CARTESIAN_POINT ( 'NONE',  ( 5.329280581304804976, 66.98711426715624384, -12.40357932740702651 ) ) ;
#3138=CARTESIAN_POINT ( 'NONE',  ( -3.734330915784458860, 34.31427195287466247, -12.97492155557369031 ) ) ;
#3140=CARTESIAN_POINT ( 'NONE',  ( 13.07034587478314336, 78.55031594048543298, -3.378768405177414280 ) ) ;
#3142=CARTESIAN_POINT ( 'NONE',  ( -4.171729424061787483, 36.32999999999999829, -12.83926296998457417 ) ) ;
#3143=CARTESIAN_POINT ( 'NONE',  ( 13.17844283097761426, 72.32374584911075033, 3.001318119765830073 ) ) ;
#3145=CARTESIAN_POINT ( 'NONE',  ( -10.92172942406179104, 62.23000000000000398, 7.935100905948387684 ) ) ;
#3146=CARTESIAN_POINT ( 'NONE',  ( -2.598996600649929878, 52.27344996586455750, -13.24758870017709711 ) ) ;
#3147=CARTESIAN_POINT ( 'NONE',  ( -3.636496289402155746, 39.52999999999999403, 11.19198476289190936 ) ) ;
#3148=CARTESIAN_POINT ( 'NONE',  ( -13.50000000000000000, 60.92999999999999972, -3.306546357697853733E-15 ) ) ;
#3149=CIRCLE ( 'NONE', #11349, 5.000000000000000000 ) ;
#3152=CARTESIAN_POINT ( 'NONE',  ( 8.324673628499295930, 68.99745231419136360, 10.63169888693616372 ) ) ;
#3153=CARTESIAN_POINT ( 'NONE',  ( -2.736472667029865136, 37.27839283157365458, -13.21980555905066623 ) ) ;
#3155=CARTESIAN_POINT ( 'NONE',  ( -11.30478939258968296, 73.65323615164170690, -7.380050224699195915 ) ) ;
#3156=CARTESIAN_POINT ( 'NONE',  ( -0.5937140765048870561, 76.20134776794657228, -13.49999999999999645 ) ) ;
#3159=DIRECTION ( 'NONE',  ( 0.000000000000000000, 0.000000000000000000, -1.000000000000000000 ) ) ;
#3162=CARTESIAN_POINT ( 'NONE',  ( 3.636496289402154414, 39.82999999999999829, 11.19198476289190936 ) ) ;
#3165=CARTESIAN_POINT ( 'NONE',  ( -11.20853034038327856, 32.21278346977177165, 7.524684492930465041 ) ) ;
#3166=CARTESIAN_POINT ( 'NONE',  ( 1.204043358265280084, 74.72328260670963118, 13.44640036567524355 ) ) ;
#3169=CARTESIAN_POINT ( 'NONE',  ( -11.76794919243112325, 32.92999999999999972, -2.882316262207890869E-15 ) ) ;
#3170=CARTESIAN_POINT ( 'NONE',  ( -1.731132465502642548, 58.24222653993336252, -13.39023422218494197 ) ) ;
#3171=( BOUNDED_CURVE ( )  B_SPLINE_CURVE ( 2, ( #10598, #948, #12895, #3695, #15960, #2348, #8850, #14204, #10679, #6621, #245, #14980, #2784 ),
 .UNSPECIFIED., .F., .F. ) 
 B_SPLINE_CURVE_WITH_KNOTS ( ( 3, 2, 2, 2, 2, 2, 3 ),
 ( 0.6250000000000000000, 0.6277777777777777679, 0.6333333333333333037, 0.6388888888888888395, 0.6444444444444444864, 0.6500000000000000222, 0.6527777777777777901 ),
 .UNSPECIFIED. ) 
 CURVE ( )  GEOMETRIC_REPRESENTATION_ITEM ( )  RATIONAL_B_SPLINE_CURVE ( ( 0.9755282581475768211, 0.9755282581475768211, 1.000000000000000000, 0.9510565162951535312, 1.000000000000000000, 0.9510565162951535312, 1.000000000000000000, 0.9510565162951535312, 1.000000000000000000, 0.9510565162951535312, 1.000000000000000000, 0.9755282581475768211, 0.9755282581475768211 ) ) 
 REPRESENTATION_ITEM ( '' )  );
#3172=CARTESIAN_POINT ( 'NONE',  ( -4.334019030006316164, 38.52414229972498561, 12.78541219897794790 ) ) ;
#3174=CARTESIAN_POINT ( 'NONE',  ( 0.1389302926457151033, 37.17500468106219103, -13.49929213118588223 ) ) ;
#3176=CARTESIAN_POINT ( 'NONE',  ( -10.92172942406179104, 70.23000000000000398, 7.935100905948387684 ) ) ;
#3179=CARTESIAN_POINT ( 'NONE',  ( 2.636466003486186427, 62.77480020505506531, 13.24005480980223659 ) ) ;
#3180=CARTESIAN_POINT ( 'NONE',  ( 7.801031699874362957, 41.97399651719818792, 11.02225216533711283 ) ) ;
#3181=CARTESIAN_POINT ( 'NONE',  ( 10.80204579108763774, 48.73690422266599853, -8.097748324130661146 ) ) ;
#3183=ORIENTED_EDGE ( 'NONE', *, *, #10372, .T. ) ;
#3184=CARTESIAN_POINT ( 'NONE',  ( -7.576616670048093940E-16, 69.68000000000000682, 12.37355403259654807 ) ) ;
#3189=CARTESIAN_POINT ( 'NONE',  ( -1.644898173497524319, 43.23913777945310954, -13.40128083404708903 ) ) ;
#3190=CARTESIAN_POINT ( 'NONE',  ( -10.16154112307833302, 80.93000000000002103, -6.935345943057503959 ) ) ;
#3192=DIRECTION ( 'NONE',  ( 0.000000000000000000, 0.000000000000000000, 1.000000000000000000 ) ) ;
#3194=CARTESIAN_POINT ( 'NONE',  ( 6.054972155430796477, 65.90111290053462767, 12.06729893293001510 ) ) ;
#3195=CARTESIAN_POINT ( 'NONE',  ( 10.03637343360090561, 57.08084545600886628, 9.039336760165353368 ) ) ;
#3196=CARTESIAN_POINT ( 'NONE',  ( 2.272985001014427788E-15, 62.17999999999999972, -12.37355403259654985 ) ) ;
#3197=CARTESIAN_POINT ( 'NONE',  ( -13.50000000000000000, 33.92999999999999972, -3.306546357697853733E-15 ) ) ;
#3198=CARTESIAN_POINT ( 'NONE',  ( -11.76794919243112325, 69.08000000000001251, 3.823638476888994386 ) ) ;
#3199=CARTESIAN_POINT ( 'NONE',  ( -11.32567959555823833, 46.65459798133181124, -7.347039100656743038 ) ) ;
#3200=CARTESIAN_POINT ( 'NONE',  ( 9.958918772552300069, 45.78319215442776624, -9.126329330056044853 ) ) ;
#3201=CARTESIAN_POINT ( 'NONE',  ( 6.668229702898669231, 69.93442387800766369, -11.75383367542387525 ) ) ;
#3204=CARTESIAN_POINT ( 'NONE',  ( 0.1136162170211922895, 31.17591480126643688, -13.49958623107663236 ) ) ;
#3205=CARTESIAN_POINT ( 'NONE',  ( -13.23950142262943785, 56.02442396258347657, 2.673273018928831846 ) ) ;
#3207=CARTESIAN_POINT ( 'NONE',  ( -0.8894439718356197400, 50.64828125085173838, 13.47800680310904475 ) ) ;
#3208=CARTESIAN_POINT ( 'NONE',  ( 5.597103228875909053, 32.88291356958394829, 12.29308424054071658 ) ) ;
#3210=CARTESIAN_POINT ( 'NONE',  ( 9.391517042431177131, 39.81199946441067539, -9.706920749962888451 ) ) ;
#3211=VERTEX_POINT ( 'NONE', #2041 ) ;
#3212=CARTESIAN_POINT ( 'NONE',  ( -13.49217480359717491, 61.94797010018912431, 0.5234354021173442950 ) ) ;
#3216=CARTESIAN_POINT ( 'NONE',  ( 2.445080149700053643E-15, 66.18000000000000682, -13.50000000000000000 ) ) ;
#3217=CARTESIAN_POINT ( 'NONE',  ( -10.92172942406178926, 31.62999999999999901, -7.935100905948389460 ) ) ;
#3218=CARTESIAN_POINT ( 'NONE',  ( -8.343458848123576743, 39.48000000000000398, -11.48378591275254301 ) ) ;
#3219=CARTESIAN_POINT ( 'NONE',  ( -6.307303722844142868, 46.41121506314294010, -11.93599373864252478 ) ) ;
#3220=CARTESIAN_POINT ( 'NONE',  ( -2.609388387809556953, 67.27396147325951858, -13.24715127702997997 ) ) ;
#3223=CARTESIAN_POINT ( 'NONE',  ( 10.68409364263760963, 54.11638383922162632, 8.252282988383353057 ) ) ;
#3225=ORIENTED_EDGE ( 'NONE', *, *, #14449, .F. ) ;
#3226=CARTESIAN_POINT ( 'NONE',  ( -3.283445202252278428, 64.29804246037801363, -13.09461853665598774 ) ) ;
#3227=ORIENTED_EDGE ( 'NONE', *, *, #237, .T. ) ;
#3229=CARTESIAN_POINT ( 'NONE',  ( -8.075662332356120743, 34.48627614415578080, -10.81823397106624363 ) ) ;
#3231=CARTESIAN_POINT ( 'NONE',  ( 4.135038185100354369, 77.82866846073966371, 12.85155843290215394 ) ) ;
#3232=CARTESIAN_POINT ( 'NONE',  ( 4.171729424061791924, 48.02999999999999403, -12.83926296998457239 ) ) ;
#3233=DIRECTION ( 'NONE',  ( 0.000000000000000000, 1.000000000000000000, 0.000000000000000000 ) ) ;
#3235=CARTESIAN_POINT ( 'NONE',  ( 11.47066830352881439, 72.16402218860807238, 7.118558593351406394 ) ) ;
#3237=CARTESIAN_POINT ( 'NONE',  ( -13.49999999999999822, 61.77999999999998693, -4.386415899144240349 ) ) ;
#3238=CARTESIAN_POINT ( 'NONE',  ( -8.798805876808101445, 52.51956008151021393, -10.23871025406966062 ) ) ;
#3239=CARTESIAN_POINT ( 'NONE',  ( 8.343458848123578520, 61.97999999999998977, 11.48378591275254124 ) ) ;
#3242=CARTESIAN_POINT ( 'NONE',  ( 10.88591283206684857, 69.12792091989102516, 7.984178984618108821 ) ) ;
#3244=CARTESIAN_POINT ( 'NONE',  ( 8.343458848123580296, 70.98000000000000398, 11.48378591275253768 ) ) ;
#3246=CARTESIAN_POINT ( 'NONE',  ( -10.59251559326346559, 73.61123193496310080, -8.369515937429383712 ) ) ;
#3248=CARTESIAN_POINT ( 'NONE',  ( -4.702552466601850334, 79.34928690549976693, -12.65703117179169546 ) ) ;
#3252=CARTESIAN_POINT ( 'NONE',  ( -7.272992578804310604, 39.37999999999999545, 10.01041549318726886 ) ) ;
#3253=AXIS2_PLACEMENT_3D ( 'NONE', #7880, #1398, #2540 ) ;
#3254=UNCERTAINTY_MEASURE_WITH_UNIT (LENGTH_MEASURE( 1.000000000000000082E-05 ), #14174, 'distance_accuracy_value', 'NONE');
#3257=CARTESIAN_POINT ( 'NONE',  ( -1.735113556039163285, 32.61758944806980764, 13.38823632957157983 ) ) ;
#3258=CARTESIAN_POINT ( 'NONE',  ( 3.688403295120684433, 74.81262137495812681, 12.98636652492995580 ) ) ;
#3263=CARTESIAN_POINT ( 'NONE',  ( 8.343458848123583849, 83.87999999999998124, -11.48378591275253768 ) ) ;
#3264=CARTESIAN_POINT ( 'NONE',  ( 9.810655436414416286, 51.79065996878712497, -9.275473329678410650 ) ) ;
#3266=CARTESIAN_POINT ( 'NONE',  ( -6.694392717615978761, 38.43308941745874563, 11.72613373514175095 ) ) ;
#3267=DIRECTION ( 'NONE',  ( 0.000000000000000000, 1.000000000000000000, 0.000000000000000000 ) ) ;
#3268=FACE_OUTER_BOUND ( 'NONE', #4170, .T. ) ;
#3269=DIRECTION ( 'NONE',  ( 0.000000000000000000, -1.000000000000000000, 0.000000000000000000 ) ) ;
#3270=CARTESIAN_POINT ( 'NONE',  ( 9.614817975872671951, 63.05940465635595160, 9.476564584252601620 ) ) ;
#3272=CARTESIAN_POINT ( 'NONE',  ( 13.20987146810338686, 48.52847080726490248, -2.784488331728600663 ) ) ;
#3275=CARTESIAN_POINT ( 'NONE',  ( 3.636496289402157078, 65.03000000000000114, -11.19198476289190936 ) ) ;
#3284=CARTESIAN_POINT ( 'NONE',  ( 8.411964441243910073, 66.00153322346682216, 10.55915802395268344 ) ) ;
#3288=CARTESIAN_POINT ( 'NONE',  ( 11.76794919243112680, 49.57999999999999119, -3.823638476888993942 ) ) ;
#3289=CARTESIAN_POINT ( 'NONE',  ( -7.576616670048093940E-16, 57.67999999999999261, 12.37355403259654985 ) ) ;
#3290=CARTESIAN_POINT ( 'NONE',  ( -10.30583073249865045, 46.59490174438735721, -8.728845011251372910 ) ) ;
#3291=CARTESIAN_POINT ( 'NONE',  ( 7.506318827951740325, 45.89879490785331484, -11.22085109350133614 ) ) ;
#3292=CARTESIAN_POINT ( 'NONE',  ( 5.745986813403028748, 69.97110941641926729, -12.21637056639575292 ) ) ;
#3295=CARTESIAN_POINT ( 'NONE',  ( 0.2317842287749069252, 31.17166591792411978, -13.49801495282379094 ) ) ;
#3296=CARTESIAN_POINT ( 'NONE',  ( -13.49470243760989696, 55.91483651601082983, -0.4366705576521556220 ) ) ;
#3297=VECTOR ( 'NONE', #6335, 1000.000000000000000 ) ;
#3299=CARTESIAN_POINT ( 'NONE',  ( 0.5562443415044789896, 32.70003642497442797, 13.49174744467049258 ) ) ;
#3300=CARTESIAN_POINT ( 'NONE',  ( 2.804204357426235195, 43.07917734367891427, -13.20558232696900980 ) ) ;
#3301=CARTESIAN_POINT ( 'NONE',  ( 6.372342379802677925, 39.94615721271951969, -11.90962055736550518 ) ) ;
#3302=EDGE_LOOP ( 'NONE', ( #7735, #9347, #14761, #9523, #1552, #7644 ) ) ;
#3303=CARTESIAN_POINT ( 'NONE',  ( -10.74856790587859479, 62.24021944068277179, 8.173410186847442915 ) ) ;
#3308=CARTESIAN_POINT ( 'NONE',  ( 11.19043610557870494, 48.14612993255676088, 7.554903771323779438 ) ) ;
#3309=CARTESIAN_POINT ( 'NONE',  ( 2.450181162087849529, 58.09190187880095380, -13.27579793785504059 ) ) ;
#3310=CARTESIAN_POINT ( 'NONE',  ( -13.49999999999999822, 32.07999999999999829, 4.386415899144235908 ) ) ;
#3314=CARTESIAN_POINT ( 'NONE',  ( 0.000000000000000000, 75.00000000000000000, 0.000000000000000000 ) ) ;
#3316=CARTESIAN_POINT ( 'NONE',  ( 5.022062556576507575, 53.86124677859262277, 12.53116408511900381 ) ) ;
#3317=ORIENTED_EDGE ( 'NONE', *, *, #12615, .T. ) ;
#3318=DIRECTION ( 'NONE',  ( -0.000000000000000000, -1.000000000000000000, -0.000000000000000000 ) ) ;
#3320=CARTESIAN_POINT ( 'NONE',  ( 5.639642118617593347, 66.97529727505714447, -12.26620933673328473 ) ) ;
#3321=CARTESIAN_POINT ( 'NONE',  ( -4.034686368860703531, 34.32507233461874563, -12.88341026651710486 ) ) ;
#3324=CARTESIAN_POINT ( 'NONE',  ( 4.285061171620013099, 77.83408588564444130, 12.80199298906653382 ) ) ;
#3325=CARTESIAN_POINT ( 'NONE',  ( -8.891200544363830713E-16, 46.67999999999999972, 13.50000000000000000 ) ) ;
#3328=CARTESIAN_POINT ( 'NONE',  ( 12.93105386136839563, 72.56893679360238991, -3.878076313447386791 ) ) ;
#3329=CARTESIAN_POINT ( 'NONE',  ( 7.586958922275961470, 66.89532775841007606, -11.16783085649728591 ) ) ;
#3331=CARTESIAN_POINT ( 'NONE',  ( -8.691771469529815392E-16, 65.68000000000000682, 14.19474002721660355 ) ) ;
#3332=CARTESIAN_POINT ( 'NONE',  ( -10.59755759974650680, 52.60935872665269386, -8.433183405451526227 ) ) ;
#3334=CARTESIAN_POINT ( 'NONE',  ( 11.76794919243112680, 34.57999999999999829, -3.823638476888993942 ) ) ;
#3336=CARTESIAN_POINT ( 'NONE',  ( -13.49999999999999822, 55.08000000000000540, 4.386415899144235908 ) ) ;
#3339=CARTESIAN_POINT ( 'NONE',  ( -4.376496056507735766, 68.52259899468778315, 12.77091595960407489 ) ) ;
#3342=AXIS2_PLACEMENT_3D ( 'NONE', #12452, #15164, #8489 ) ;
#3344=CARTESIAN_POINT ( 'NONE',  ( -13.37666621905920650, 73.99562545368686983, 1.878105658975215420 ) ) ;
#3347=DIRECTION ( 'NONE',  ( 0.000000000000000000, 0.000000000000000000, -1.000000000000000000 ) ) ;
#3348=CARTESIAN_POINT ( 'NONE',  ( 9.520470885617715595, 34.13000000000000256, 6.917026985038134512 ) ) ;
#3349=DIRECTION ( 'NONE',  ( 0.000000000000000000, 0.000000000000000000, -1.000000000000000000 ) ) ;
#3350=CARTESIAN_POINT ( 'NONE',  ( -1.471122160089594955, 32.62715143919767513, 13.41980678565153795 ) ) ;
#3352=CARTESIAN_POINT ( 'NONE',  ( 2.138189944381259977, 61.75688142232026934, 13.49999999999999289 ) ) ;
#3354=CARTESIAN_POINT ( 'NONE',  ( -13.49999999999999822, 79.07999999999999829, 4.386415899144235908 ) ) ;
#3355=CARTESIAN_POINT ( 'NONE',  ( 12.48859630623820038, 51.61660746006936762, -5.128397564142412435 ) ) ;
#3356=CARTESIAN_POINT ( 'NONE',  ( -7.028416087530689360, 38.41914928954428632, 11.52616306344620689 ) ) ;
#3357=DIRECTION ( 'NONE',  ( 0.000000000000000000, 1.000000000000000000, 0.000000000000000000 ) ) ;
#3360=FACE_OUTER_BOUND ( 'NONE', #8104, .T. ) ;
#3361=CARTESIAN_POINT ( 'NONE',  ( 0.07515814835109146941, 62.68270335294189266, 13.49999999999987033 ) ) ;
#3362=CARTESIAN_POINT ( 'NONE',  ( 3.518843866200051185, 41.80622085848303016, 13.03652279665081615 ) ) ;
#3363=CARTESIAN_POINT ( 'NONE',  ( 10.73149705005626409, 48.74093281793692256, -8.190661608126919901 ) ) ;
#3366=EDGE_CURVE ( 'NONE', #8302, #12894, #4887, .T. ) ;
#3368=CARTESIAN_POINT ( 'NONE',  ( -3.636496289402155746, 63.53000000000000114, 11.19198476289190936 ) ) ;
#3373=CARTESIAN_POINT ( 'NONE',  ( -7.321446643551189126, 80.93000000000003524, -10.20755442052239026 ) ) ;
#3375=CARTESIAN_POINT ( 'NONE',  ( 11.72063973829996009, 66.18111146641619769, 6.700015991577908281 ) ) ;
#3377=CARTESIAN_POINT ( 'NONE',  ( -7.272992578804310604, 51.37999999999998835, 10.01041549318726709 ) ) ;
#3378=CARTESIAN_POINT ( 'NONE',  ( -8.343458848123576743, 33.47999999999999687, -11.48378591275254301 ) ) ;
#3379=CARTESIAN_POINT ( 'NONE',  ( -13.32459686664603282, 46.85386381616618223, -2.169380165940829386 ) ) ;
#3381=CARTESIAN_POINT ( 'NONE',  ( 9.153033843582718987, 45.82346993534611812, -9.923304509235496340 ) ) ;
#3382=CARTESIAN_POINT ( 'NONE',  ( 9.813981802417188760, 69.79049870256335453, -9.272224570126397225 ) ) ;
#3384=CARTESIAN_POINT ( 'NONE',  ( 12.22840589594397542, 30.63979685967524347, -5.723655948989013531 ) ) ;
#3385=CARTESIAN_POINT ( 'NONE',  ( -12.00723429333529779, 56.16046608847325672, 6.256725284067366388 ) ) ;
#3386=CARTESIAN_POINT ( 'NONE',  ( 8.343458848123583849, 53.87999999999999545, -11.48378591275253768 ) ) ;
#3387=CARTESIAN_POINT ( 'NONE',  ( 9.174595195680133486, 33.03757788585047450, 9.903405154293709600 ) ) ;
#3388=CARTESIAN_POINT ( 'NONE',  ( 4.913930544642371778, 43.00284194709907126, -12.57587111961252191 ) ) ;
#3389=CARTESIAN_POINT ( 'NONE',  ( 11.94294432412099916, 39.66253801985712357, -6.294138039312064059 ) ) ;
#3391=CARTESIAN_POINT ( 'NONE',  ( -13.24494331279968762, 61.83784905754306038, -2.611875526739312559 ) ) ;
#3396=CARTESIAN_POINT ( 'NONE',  ( 9.793712905158246329, 48.06848970801387111, 9.292869918114371686 ) ) ;
#3397=CARTESIAN_POINT ( 'NONE',  ( 0.5920084214834188119, 58.15871356119428270, -13.50000000000000711 ) ) ;
#3398=CARTESIAN_POINT ( 'NONE',  ( 7.095737324529082457, 78.91631958237633171, -11.48492378435084404 ) ) ;
#3399=CARTESIAN_POINT ( 'NONE',  ( 9.520470885617715595, 79.13000000000000966, 6.917026985038134512 ) ) ;
#3400=CARTESIAN_POINT ( 'NONE',  ( 13.50000000000000355, 38.57999999999999829, -4.386415899144233244 ) ) ;
#3402=CARTESIAN_POINT ( 'NONE',  ( -2.279876193866607892, 46.26197366689496704, -13.30632321474556434 ) ) ;
#3405=CARTESIAN_POINT ( 'NONE',  ( 10.47640949927847842, 54.10478805614472719, 8.515037930683744705 ) ) ;
#3408=EDGE_CURVE ( 'NONE', #10105, #13489, #2294, .T. ) ;
#3410=CARTESIAN_POINT ( 'NONE',  ( 5.323009095788314937, 66.98734768220822389, -12.40627203521292721 ) ) ;
#3411=CARTESIAN_POINT ( 'NONE',  ( -5.541662318619955840, 34.38103254278009757, -12.31017199372226223 ) ) ;
#3414=CARTESIAN_POINT ( 'NONE',  ( -3.609344227228918900, 59.55023083539120421, 13.00886259437187142 ) ) ;
#3417=CARTESIAN_POINT ( 'NONE',  ( 13.37466002425821188, 72.36584947057816919, 1.835341461556227127 ) ) ;
#3418=CARTESIAN_POINT ( 'NONE',  ( 8.048570524534548909, 66.87494734074847713, -10.83862139358550003 ) ) ;
#3420=CARTESIAN_POINT ( 'NONE',  ( -4.171729424061787483, 55.32999999999999829, -12.83926296998457417 ) ) ;
#3421=CARTESIAN_POINT ( 'NONE',  ( -5.775258882854464204, 52.39010693232381755, -12.20232514914052402 ) ) ;
#3422=CARTESIAN_POINT ( 'NONE',  ( -13.50000000000000000, 51.93000000000000682, -3.306546357697853733E-15 ) ) ;
#3423=CARTESIAN_POINT ( 'NONE',  ( 13.50000000000000355, 77.57999999999999829, -4.386415899144233244 ) ) ;
#3425=CARTESIAN_POINT ( 'NONE',  ( -1.650043268377658690, 68.62054052734106335, 13.40390642837740565 ) ) ;
#3429=CARTESIAN_POINT ( 'NONE',  ( -11.25052354211586270, 65.20990605257976824, 7.462422595341770659 ) ) ;
#3433=CARTESIAN_POINT ( 'NONE',  ( -11.76794919243112325, 38.77999999999999403, -3.823638476888998827 ) ) ;
#3435=CARTESIAN_POINT ( 'NONE',  ( -4.741376437275918398, 40.35074587188617556, -12.64175464265864157 ) ) ;
#3436=CARTESIAN_POINT ( 'NONE',  ( -12.96199357294905674, 31.79498504800923442, -3.773402922091955602 ) ) ;
#3437=CARTESIAN_POINT ( 'NONE',  ( 5.450067102490391946, 74.87759374410906332, 12.35271490370261027 ) ) ;
#3438=CARTESIAN_POINT ( 'NONE',  ( 10.92172942406178926, 62.13000000000000256, 7.935100905948387684 ) ) ;
#3441=CARTESIAN_POINT ( 'NONE',  ( -5.491332954668864730, 30.39042612893359419, 16.75890910139807843 ) ) ;
#3442=CARTESIAN_POINT ( 'NONE',  ( 11.68331733722775034, 51.68148845516454060, -6.763944398493564769 ) ) ;
#3443=CARTESIAN_POINT ( 'NONE',  ( -13.32055366127931961, 38.00703768986679165, 2.194235484290746552 ) ) ;
#3444=CARTESIAN_POINT ( 'NONE',  ( 11.94661826698584939, 36.66226039872729814, -6.287206104090115488 ) ) ;
#3447=CARTESIAN_POINT ( 'NONE',  ( -10.85718845775721064, 77.23369997451160884, 8.023478501512466110 ) ) ;
#3451=CARTESIAN_POINT ( 'NONE',  ( 5.478462649124859141, 41.87859710647594369, 12.33842961194233290 ) ) ;
#3452=CARTESIAN_POINT ( 'NONE',  ( 13.49272709919642566, 48.41445879050284873, 0.4520991473949109163 ) ) ;
#3454=ORIENTED_EDGE ( 'NONE', *, *, #15559, .T. ) ;
#3455=CARTESIAN_POINT ( 'NONE',  ( -9.520470885617715595, 62.63000000000000256, -6.917026985038136289 ) ) ;
#3460=CARTESIAN_POINT ( 'NONE',  ( -8.380961239556755871, 80.92999999999997840, -9.227099233233150954 ) ) ;
#3463=CARTESIAN_POINT ( 'NONE',  ( 9.520470885617715595, 49.13000000000000256, 6.917026985038134512 ) ) ;
#3465=CARTESIAN_POINT ( 'NONE',  ( -13.46528334221770251, 58.96347564477174075, 0.9676412435863588346 ) ) ;
#3466=CARTESIAN_POINT ( 'NONE',  ( 12.90801733370770954, 45.28818780823190338, 3.954641600816362956 ) ) ;
#3467=CARTESIAN_POINT ( 'NONE',  ( 10.14775816985478230, 69.77298195707258799, -8.903540694107199727 ) ) ;
#3468=CARTESIAN_POINT ( 'NONE',  ( 1.227614123976220384, 80.72414343316154373, 13.44515162415854803 ) ) ;
#3469=CARTESIAN_POINT ( 'NONE',  ( 13.48837557053283831, 30.44930113163437824, -0.5606353105131218761 ) ) ;
#3470=CARTESIAN_POINT ( 'NONE',  ( -13.49205171756009847, 55.94874241206034071, 0.5458872085021070353 ) ) ;
#3471=CARTESIAN_POINT ( 'NONE',  ( -4.556504444975026047, 50.51610007432194749, 12.72330644818372214 ) ) ;
#3472=DIRECTION ( 'NONE',  ( 0.000000000000000000, -1.000000000000000000, 0.000000000000000000 ) ) ;
#3473=CARTESIAN_POINT ( 'NONE',  ( 0.2926259582140912641, 43.16951355705446502, -13.49726570074850152 ) ) ;
#3474=CARTESIAN_POINT ( 'NONE',  ( 6.806927860051751544, 39.92851749465472722, -11.67113343977014672 ) ) ;
#3475=EDGE_LOOP ( 'NONE', ( #8992, #1711, #8082, #15058 ) ) ;
#3476=CARTESIAN_POINT ( 'NONE',  ( -10.77335659271368762, 61.62127811166998015, -8.136614450085879469 ) ) ;
#3478=VERTEX_POINT ( 'NONE', #11692 ) ;
#3481=CARTESIAN_POINT ( 'NONE',  ( 12.97866832662360537, 48.29713054261845429, 3.716351513807763407 ) ) ;
#3482=CARTESIAN_POINT ( 'NONE',  ( 11.37239215724911112, 57.70229078515689025, -7.275958244018569943 ) ) ;
#3483=CARTESIAN_POINT ( 'NONE',  ( 6.873487081399273002, 78.92563002817296081, -11.61942495236515249 ) ) ;
#3484=CARTESIAN_POINT ( 'NONE',  ( 9.520470885617717371, 79.72999999999998977, -6.917026985038131848 ) ) ;
#3486=EDGE_CURVE ( 'NONE', #10721, #6584, #2947, .T. ) ;
#3488=FACE_OUTER_BOUND ( 'NONE', #15893, .T. ) ;
#3491=CARTESIAN_POINT ( 'NONE',  ( 6.074345959363277814, 33.95809426174932355, -12.05647970507914302 ) ) ;
#3492=ORIENTED_EDGE ( 'NONE', *, *, #7896, .T. ) ;
#3493=PLANE ( 'NONE',  #14007 ) ;
#3494=ORIENTED_EDGE ( 'NONE', *, *, #11716, .T. ) ;
#3498=CARTESIAN_POINT ( 'NONE',  ( -7.075555937736629275, 59.41716819547789186, 11.49737106684309751 ) ) ;
#3500=DIRECTION ( 'NONE',  ( 1.000000000000000000, 0.000000000000000000, 0.000000000000000000 ) ) ;
#3501=CARTESIAN_POINT ( 'NONE',  ( 7.829317792819562527, 71.97528757275648559, 10.99897765872064781 ) ) ;
#3502=CARTESIAN_POINT ( 'NONE',  ( -8.343458848123576743, 52.47999999999999687, -11.48378591275254301 ) ) ;
#3503=CARTESIAN_POINT ( 'NONE',  ( -6.381350698036120761, 52.41419776773467731, -11.90580418029937526 ) ) ;
#3505=CARTESIAN_POINT ( 'NONE',  ( 10.92172942406178926, 77.13000000000000966, 7.935100905948387684 ) ) ;
#3507=CARTESIAN_POINT ( 'NONE',  ( -8.574308837607619083, 68.35095914637041403, 10.42743186381050968 ) ) ;
#3509=DIRECTION ( 'NONE',  ( 0.000000000000000000, -1.000000000000000000, 0.000000000000000000 ) ) ;
#3511=CARTESIAN_POINT ( 'NONE',  ( -0.6046803220343888174, 65.65828050903189705, 13.49999999993799982 ) ) ;
#3512=CARTESIAN_POINT ( 'NONE',  ( 0.000000000000000000, 0.000000000000000000, 9.500000000000021316 ) ) ;
#3516=CARTESIAN_POINT ( 'NONE',  ( 11.76794919243112325, 31.27999999999998693, 3.823638476888997051 ) ) ;
#3517=CARTESIAN_POINT ( 'NONE',  ( -4.273851079481598703, 40.33368115456159586, -12.80566632602802102 ) ) ;
#3518=CARTESIAN_POINT ( 'NONE',  ( -13.41444007591816678, 31.98338318546857550, 1.533229712954465196 ) ) ;
#3520=CARTESIAN_POINT ( 'NONE',  ( 13.06329500387617770, 60.30866768971296921, 3.406192448351748503 ) ) ;
#3522=CARTESIAN_POINT ( 'NONE',  ( -4.171729424061787483, 78.32999999999999829, -12.83926296998457417 ) ) ;
#3524=CARTESIAN_POINT ( 'NONE',  ( 13.49059967034253305, 51.44733065808145511, -0.5037421684802066979 ) ) ;
#3525=CARTESIAN_POINT ( 'NONE',  ( -13.48070957841285278, 37.90502422016587047, -0.7223451569848480247 ) ) ;
#3526=CARTESIAN_POINT ( 'NONE',  ( 11.22475465503331371, 36.71175793279847710, -7.500328621267835061 ) ) ;
#3529=DIRECTION ( 'NONE',  ( -1.734723475976807094E-16, 1.000000000000000000, 0.000000000000000000 ) ) ;
#3530=CARTESIAN_POINT ( 'NONE',  ( -1.551070049701340103, 80.62418276194892997, 13.41104721329206839 ) ) ;
#3531=CARTESIAN_POINT ( 'NONE',  ( 5.633694881767536522, 41.88459927968532526, 12.26853111873423252 ) ) ;
#3532=CARTESIAN_POINT ( 'NONE',  ( 13.46307399052660259, 48.39473455737326901, 1.018718451003600478 ) ) ;
#3534=VERTEX_POINT ( 'NONE', #17069 ) ;
#3535=CARTESIAN_POINT ( 'NONE',  ( -7.576616670048093940E-16, 60.67999999999999261, 12.37355403259654807 ) ) ;
#3541=CARTESIAN_POINT ( 'NONE',  ( 0.5390086576906194527, 76.16062051171672920, -13.49046569834956877 ) ) ;
#3543=CARTESIAN_POINT ( 'NONE',  ( 13.50000000000000000, 81.43000000000000682, 1.653273178848926867E-15 ) ) ;
#3545=CARTESIAN_POINT ( 'NONE',  ( -9.520470885617717371, 51.22999999999999687, 6.917026985038133624 ) ) ;
#3546=DIRECTION ( 'NONE',  ( 0.8660221325896413358, 0.000000000000000000, -0.5000056658327882708 ) ) ;
#3547=EDGE_CURVE ( 'NONE', #10228, #6792, #12433, .T. ) ;
#3548=CARTESIAN_POINT ( 'NONE',  ( -13.47664760107280735, 58.90259797499196281, -0.7937112629172573541 ) ) ;
#3549=CARTESIAN_POINT ( 'NONE',  ( 10.82628732869974719, 45.12415098472465758, 8.070053677659583258 ) ) ;
#3550=CARTESIAN_POINT ( 'NONE',  ( 13.09907156312732290, 69.54612857034256024, -3.265651416783837746 ) ) ;
#3551=CARTESIAN_POINT ( 'NONE',  ( 4.572122312880307682, 80.84449485487320430, 12.70468199279591559 ) ) ;
#3552=CARTESIAN_POINT ( 'NONE',  ( 13.06123906118353517, 30.55161712359772253, -3.413860246534342835 ) ) ;
#3553=CARTESIAN_POINT ( 'NONE',  ( -13.45979128135589420, 55.89390028866353788, -1.044999607113579643 ) ) ;
#3554=CARTESIAN_POINT ( 'NONE',  ( -13.49470981577344375, 49.91485972376758440, -0.4364497393623030241 ) ) ;
#3555=FACE_OUTER_BOUND ( 'NONE', #581, .T. ) ;
#3557=CARTESIAN_POINT ( 'NONE',  ( 13.41230998493642623, 39.48517279672220326, -1.584139233609136665 ) ) ;
#3559=CARTESIAN_POINT ( 'NONE',  ( -5.845759849409800424, 61.39277117633377401, -12.17771138739238701 ) ) ;
#3565=CARTESIAN_POINT ( 'NONE',  ( 6.813825994921812068, 47.93197876211288389, 11.65439317571491706 ) ) ;
#3566=CARTESIAN_POINT ( 'NONE',  ( 10.68081498587143408, 57.74381789421609312, -8.257788020075247815 ) ) ;
#3567=CARTESIAN_POINT ( 'NONE',  ( 0.7009303126130895789, 79.15481186450742257, -13.48240536218643193 ) ) ;
#3568=CARTESIAN_POINT ( 'NONE',  ( -11.76794919243112325, 75.08000000000001251, 3.823638476888994386 ) ) ;
#3569=CARTESIAN_POINT ( 'NONE',  ( 11.76794919243112325, 82.43000000000000682, 1.441158131103945434E-15 ) ) ;
#3571=CIRCLE ( 'NONE', #10639, 13.50000000000000000 ) ;
#3575=CARTESIAN_POINT ( 'NONE',  ( 8.343458848123580296, 43.97999999999999687, 11.48378591275253768 ) ) ;
#3578=FACE_OUTER_BOUND ( 'NONE', #3654, .T. ) ;
#3579=ORIENTED_EDGE ( 'NONE', *, *, #1090, .T. ) ;
#3582=CARTESIAN_POINT ( 'NONE',  ( 0.4449454661118308341, 77.69610243158906826, 13.49999999997334044 ) ) ;
#3583=CARTESIAN_POINT ( 'NONE',  ( -1.328659818498353332E-07, 59.67999629905246195, 13.49999999999999822 ) ) ;
#3587=CARTESIAN_POINT ( 'NONE',  ( 10.92172942406179104, 48.72999999999999687, -7.935100905948385908 ) ) ;
#3588=CARTESIAN_POINT ( 'NONE',  ( -4.378381081909518358, 71.52253779549604928, 12.77041120775835026 ) ) ;
#3590=CARTESIAN_POINT ( 'NONE',  ( 2.000520122481862502E-14, 76.67999999999999261, 13.50000000000000000 ) ) ;
#3592=CARTESIAN_POINT ( 'NONE',  ( -0.9445818373508010346, 68.64612565221730733, 13.46771734312773638 ) ) ;
#3594=CARTESIAN_POINT ( 'NONE',  ( 3.280605613281809330, 55.06204156931236326, -13.09532926545062814 ) ) ;
#3596=CARTESIAN_POINT ( 'NONE',  ( -9.675226902770793558, 65.29754703176814701, 9.415198896858003152 ) ) ;
#3598=CARTESIAN_POINT ( 'NONE',  ( -4.672525169807293821, 35.51179140871166595, 12.66707033060281518 ) ) ;
#3604=CARTESIAN_POINT ( 'NONE',  ( 2.138189944381238661, 79.75688142232024802, 13.50000000000000000 ) ) ;
#3605=CARTESIAN_POINT ( 'NONE',  ( -13.46812497729234259, 31.89793320150942435, -0.9275556759729549627 ) ) ;
#3607=CARTESIAN_POINT ( 'NONE',  ( 13.50000640706135613, 60.42933411119164333, 0.01923106255287391694 ) ) ;
#3609=CARTESIAN_POINT ( 'NONE',  ( -9.925458028546751521, 53.28467197136558298, 9.150698730621169119 ) ) ;
#3610=CARTESIAN_POINT ( 'NONE',  ( -7.576616670048093940E-16, 60.67999999999998550, 12.37355403259654985 ) ) ;
#3611=CARTESIAN_POINT ( 'NONE',  ( 13.41279326728364651, 51.37661727247101595, 1.532238328333574096 ) ) ;
#3612=CARTESIAN_POINT ( 'NONE',  ( -12.57861966457431002, 38.10786478379095854, 4.901884260589575604 ) ) ;
#3613=CARTESIAN_POINT ( 'NONE',  ( 13.47639277022257964, 36.45819009604027627, -0.8166540340939039133 ) ) ;
#3616=CARTESIAN_POINT ( 'NONE',  ( -10.66312149623454530, 77.24479860351357274, 8.279365195195687477 ) ) ;
#3617=CARTESIAN_POINT ( 'NONE',  ( -4.905989025644352353, 80.50308446184858724, 12.57886947468737482 ) ) ;
#3618=CARTESIAN_POINT ( 'NONE',  ( 7.500000000000000000, 105.3828822090421227, -8.693347190813733860 ) ) ;
#3622=CARTESIAN_POINT ( 'NONE',  ( -11.76794919243112325, 56.77999999999998693, -3.823638476888998827 ) ) ;
#3627=CARTESIAN_POINT ( 'NONE',  ( 10.51572120785151654, 75.75302732738094846, -8.465820318027104108 ) ) ;
#3628=CARTESIAN_POINT ( 'NONE',  ( -3.636496289402155746, 33.52999999999999403, 11.19198476289190936 ) ) ;
#3629=VECTOR ( 'NONE', #16184, 1000.000000000000000 ) ;
#3631=CARTESIAN_POINT ( 'NONE',  ( 3.112499768079701745, 65.79190412735221116, 13.13630053735090542 ) ) ;
#3632=CARTESIAN_POINT ( 'NONE',  ( -10.92172942406179104, 71.23000000000000398, 7.935100905948387684 ) ) ;
#3633=CARTESIAN_POINT ( 'NONE',  ( -11.76794919243112325, 47.92999999999999972, -2.882316262207890869E-15 ) ) ;
#3635=CARTESIAN_POINT ( 'NONE',  ( -13.46720615212894501, 58.96252600434252145, 0.9405017376672494267 ) ) ;
#3636=CARTESIAN_POINT ( 'NONE',  ( 11.47344028360550006, 45.16420593273019080, 7.114091049973444214 ) ) ;
#3637=CARTESIAN_POINT ( 'NONE',  ( 11.01362784260440542, 69.72461688776509448, -7.807153119340634717 ) ) ;
#3639=CARTESIAN_POINT ( 'NONE',  ( 13.48964992093387849, 30.44819364669021766, -0.5286683032485781641 ) ) ;
#3640=AXIS2_PLACEMENT_3D ( 'NONE', #13459, #10911, #4096 ) ;
#3641=CARTESIAN_POINT ( 'NONE',  ( -11.04618422503944686, 55.63728354584706182, -7.761965573417075603 ) ) ;
#3642=CARTESIAN_POINT ( 'NONE',  ( -9.907659367957414531, 50.28597023960409018, 9.180989528200973027 ) ) ;
#3643=CARTESIAN_POINT ( 'NONE',  ( 5.351965053708911846, 63.98625261907654505, -12.39380797406724710 ) ) ;
#3645=CARTESIAN_POINT ( 'NONE',  ( 13.31289339363439517, 39.35132640896662082, 2.239837115172842896 ) ) ;
#3647=CARTESIAN_POINT ( 'NONE',  ( -9.584052401572662916, 70.55787012011465720, -9.510499048535340449 ) ) ;
#3648=CARTESIAN_POINT ( 'NONE',  ( -10.86637700757906622, 61.62663672810896998, -8.012531335975232594 ) ) ;
#3649=( BOUNDED_CURVE ( )  B_SPLINE_CURVE ( 2, ( #13265, #9223, #10623, #16158, #2548, #13179, #11863, #17238, #5148, #9395, #7978, #14575, #16074 ),
 .UNSPECIFIED., .F., .F. ) 
 B_SPLINE_CURVE_WITH_KNOTS ( ( 3, 2, 2, 2, 2, 2, 3 ),
 ( 0.2916666666666666297, 0.2944444444444444531, 0.2999999999999999889, 0.3055555555555555802, 0.3111111111111111160, 0.3166666666666666519, 0.3194444444444444198 ),
 .UNSPECIFIED. ) 
 CURVE ( )  GEOMETRIC_REPRESENTATION_ITEM ( )  RATIONAL_B_SPLINE_CURVE ( ( 0.9755282581475768211, 0.9755282581475765991, 1.000000000000000000, 0.9510565162951535312, 1.000000000000000000, 0.9510565162951535312, 1.000000000000000000, 0.9510565162951535312, 1.000000000000000000, 0.9510565162951535312, 1.000000000000000000, 0.9755282581475770431, 0.9755282581475768211 ) ) 
 REPRESENTATION_ITEM ( '' )  );
#3652=EDGE_CURVE ( 'NONE', #3044, #16628, #16079, .T. ) ;
#3653=CARTESIAN_POINT ( 'NONE',  ( -11.54462091828690440, 40.66874641531683210, -7.004015811786465484 ) ) ;
#3654=EDGE_LOOP ( 'NONE', ( #670, #11374, #7882 ) ) ;
#3657=CARTESIAN_POINT ( 'NONE',  ( 2.254128362010559439, 47.76103611355556211, 13.31951350158262315 ) ) ;
#3658=CARTESIAN_POINT ( 'NONE',  ( 1.938283894950695974, 58.11032032463412378, -13.36127657765577759 ) ) ;
#3659=CARTESIAN_POINT ( 'NONE',  ( 12.18688363209133030, 78.64319475361247669, -5.807748549134894134 ) ) ;
#3660=AXIS2_PLACEMENT_3D ( 'NONE', #14202, #6017, #16772 ) ;
#3661=CARTESIAN_POINT ( 'NONE',  ( 2.272985001014427788E-15, 74.17999999999997840, -12.37355403259654985 ) ) ;
#3662=CARTESIAN_POINT ( 'NONE',  ( 3.636496289402154414, 81.82999999999999829, 11.19198476289190936 ) ) ;
#3665=CARTESIAN_POINT ( 'NONE',  ( -0.1635035910697570927, 67.18587897178171886, -13.49901470174091855 ) ) ;
#3668=CARTESIAN_POINT ( 'NONE',  ( 3.496867611406847764, 34.05434841121682155, -13.04155495172319768 ) ) ;
#3669=CARTESIAN_POINT ( 'NONE',  ( -13.48700498846246276, 73.90959446758982665, -0.5924077624709760403 ) ) ;
#3673=ORIENTED_EDGE ( 'NONE', *, *, #14015, .T. ) ;
#3675=CARTESIAN_POINT ( 'NONE',  ( -3.426950242872616847, 44.55682256194640445, 13.06444397049863504 ) ) ;
#3676=CARTESIAN_POINT ( 'NONE',  ( -7.506691621707916262, 59.39882663589411749, 11.22238440737102749 ) ) ;
#3677=DIRECTION ( 'NONE',  ( 8.673617379884035472E-17, -1.000000000000000000, 0.000000000000000000 ) ) ;
#3678=DIRECTION ( 'NONE',  ( 0.000000000000000000, 0.000000000000000000, -1.000000000000000000 ) ) ;
#3679=CARTESIAN_POINT ( 'NONE',  ( -8.343458848123576743, 55.47999999999998977, -11.48378591275254301 ) ) ;
#3680=CARTESIAN_POINT ( 'NONE',  ( -7.866213445538476456, 71.38314426818901381, 10.97589501671720491 ) ) ;
#3682=CARTESIAN_POINT ( 'NONE',  ( -9.432230830578065550, 59.31010286422545619, 9.668454110407326496 ) ) ;
#3684=ADVANCED_FACE ( 'NONE', ( #12118 ), #16346, .T. ) ;
#3685=CARTESIAN_POINT ( 'NONE',  ( 6.123233995736765296E-16, 75.00000000000000000, -5.000000000000000000 ) ) ;
#3687=CARTESIAN_POINT ( 'NONE',  ( 6.762232371920031682, 54.93041419438679185, -11.69278108536045302 ) ) ;
#3690=CARTESIAN_POINT ( 'NONE',  ( -7.991773808256851019, 65.37750511056809444, 10.88130972677807229 ) ) ;
#3692=CARTESIAN_POINT ( 'NONE',  ( -1.717771643151318361, 35.61820511656272004, 13.39054620278180430 ) ) ;
#3695=CARTESIAN_POINT ( 'NONE',  ( 8.343458848123583849, 50.87999999999999545, -11.48378591275253768 ) ) ;
#3696=CARTESIAN_POINT ( 'NONE',  ( -12.69323189075679359, 32.09621662746886983, 4.598406620704597714 ) ) ;
#3697=CARTESIAN_POINT ( 'NONE',  ( -3.737279461696752201E-15, 73.17999999999999261, -13.50000000000000000 ) ) ;
#3698=CARTESIAN_POINT ( 'NONE',  ( 9.443557525633938354, 60.05081174560719859, 9.647429353757006609 ) ) ;
#3700=CARTESIAN_POINT ( 'NONE',  ( -11.98718778898151349, 53.15915301820461281, 6.209526914751407389 ) ) ;
#3701=CARTESIAN_POINT ( 'NONE',  ( -9.520470885617717371, 60.22999999999999687, 6.917026985038133624 ) ) ;
#3702=CARTESIAN_POINT ( 'NONE',  ( 13.37713670579460157, 51.36639808551130670, 1.819116265251073283 ) ) ;
#3703=CARTESIAN_POINT ( 'NONE',  ( -13.47376594344626177, 37.90094777547172811, -0.8416043350724276007 ) ) ;
#3704=CARTESIAN_POINT ( 'NONE',  ( 11.25768462558175287, 36.70972676642409027, -7.450841025583892829 ) ) ;
#3706=CARTESIAN_POINT ( 'NONE',  ( -4.145437653765961628, 74.53085911066104075, 12.85327900485357233 ) ) ;
#3707=CARTESIAN_POINT ( 'NONE',  ( -8.225025902617534967, 77.36731451037184115, 10.71433264759214588 ) ) ;
#3708=CARTESIAN_POINT ( 'NONE',  ( -6.694905124455936551, 80.43301383616126543, 11.72313240434259463 ) ) ;
#3709=DIRECTION ( 'NONE',  ( 0.000000000000000000, 0.000000000000000000, 1.000000000000000000 ) ) ;
#3710=ORIENTED_EDGE ( 'NONE', *, *, #9973, .T. ) ;
#3712=EDGE_LOOP ( 'NONE', ( #13957, #7098, #10577, #7311 ) ) ;
#3713=CARTESIAN_POINT ( 'NONE',  ( 11.76794919243112325, 55.27999999999998693, 3.823638476888997051 ) ) ;
#3717=AXIS2_PLACEMENT_3D ( 'NONE', #14310, #13002, #9220 ) ;
#3718=CARTESIAN_POINT ( 'NONE',  ( 6.226471401687747154, 75.95203426803303159, -11.97835911601103120 ) ) ;
#3719=CARTESIAN_POINT ( 'NONE',  ( 9.235079662642815990, 32.03187319105528985, 10.25657514373247992 ) ) ;
#3720=CARTESIAN_POINT ( 'NONE',  ( 8.343458848123583849, 75.87999999999998124, -11.48378591275253768 ) ) ;
#3721=CARTESIAN_POINT ( 'NONE',  ( 9.520470885617715595, 43.13000000000000256, 6.917026985038134512 ) ) ;
#3723=CARTESIAN_POINT ( 'NONE',  ( -13.39844892242865626, 58.87026394863372758, -1.714548835752056632 ) ) ;
#3724=EDGE_CURVE ( 'NONE', #10745, #3120, #12992, .T. ) ;
#3725=CARTESIAN_POINT ( 'NONE',  ( 9.182243949852553655, 45.03795070569126580, 9.896291786696478354 ) ) ;
#3726=CARTESIAN_POINT ( 'NONE',  ( 13.12018455494123081, 69.54296377198190271, -3.179949692328717159 ) ) ;
#3728=CARTESIAN_POINT ( 'NONE',  ( 11.84345469503521464, 30.18954924114118299, 6.489769361157302185 ) ) ;
#3729=CARTESIAN_POINT ( 'NONE',  ( -11.52415037849118384, 55.66688209782287089, -7.052009664402310030 ) ) ;
#3730=CARTESIAN_POINT ( 'NONE',  ( -12.01105834539781902, 50.16019076819019773, 6.249781159449053547 ) ) ;
#3731=CARTESIAN_POINT ( 'NONE',  ( 3.705909840006434752, 64.04664249640974560, -12.98321921109010191 ) ) ;
#3732=CARTESIAN_POINT ( 'NONE',  ( 10.34708690891700478, 42.76227428168909483, -8.671260026376653940 ) ) ;
#3733=CARTESIAN_POINT ( 'NONE',  ( 13.48088785067486128, 39.39742276772284413, 0.9325739214256087983 ) ) ;
#3734=ORIENTED_EDGE ( 'NONE', *, *, #16517, .T. ) ;
#3736=CARTESIAN_POINT ( 'NONE',  ( -7.781309575702445969, 70.47319914026155629, -11.03183906678731141 ) ) ;
#3737=CARTESIAN_POINT ( 'NONE',  ( -4.127570232279888174, 61.32841266336937025, -12.85361106895534355 ) ) ;
#3740=CARTESIAN_POINT ( 'NONE',  ( -5.847339916432642504, 40.39291978250835768, -12.16879597960247494 ) ) ;
#3744=CARTESIAN_POINT ( 'NONE',  ( 1.121066298875345035, 61.13973486878198571, -13.46140389959024120 ) ) ;
#3746=CARTESIAN_POINT ( 'NONE',  ( 12.46100838988894388, 57.24085334314524687, 5.193585410646714529 ) ) ;
#3747=CARTESIAN_POINT ( 'NONE',  ( 7.272992578804311492, 79.87999999999999545, -10.01041549318726709 ) ) ;
#3748=CARTESIAN_POINT ( 'NONE',  ( -13.49999999999999822, 36.78000000000000114, -4.386415899144240349 ) ) ;
#3749=CARTESIAN_POINT ( 'NONE',  ( -11.76794919243112325, 81.07999999999998408, 3.823638476888994386 ) ) ;
#3755=( BOUNDED_CURVE ( )  B_SPLINE_CURVE ( 2, ( #13951, #4781, #4694, #12645, #3176, #10099, #7261, #11587, #15275, #16963, #10014, #15362, #4865 ),
 .UNSPECIFIED., .F., .F. ) 
 B_SPLINE_CURVE_WITH_KNOTS ( ( 3, 2, 2, 2, 2, 2, 3 ),
 ( 0.2638888888888888951, 0.2666666666666666630, 0.2722222222222221988, 0.2777777777777777901, 0.2833333333333333259, 0.2888888888888888618, 0.2916666666666666297 ),
 .UNSPECIFIED. ) 
 CURVE ( )  GEOMETRIC_REPRESENTATION_ITEM ( )  RATIONAL_B_SPLINE_CURVE ( ( 0.9755282581475768211, 0.9755282581475768211, 1.000000000000000000, 0.9510565162951535312, 1.000000000000000000, 0.9510565162951535312, 1.000000000000000000, 0.9510565162951535312, 1.000000000000000000, 0.9510565162951535312, 1.000000000000000000, 0.9755282581475770431, 0.9755282581475768211 ) ) 
 REPRESENTATION_ITEM ( '' )  );
#3756=AXIS2_PLACEMENT_3D ( 'NONE', #10322, #15769, #678 ) ;
#3757=CARTESIAN_POINT ( 'NONE',  ( 8.343458848123583849, 44.87999999999998835, -11.48378591275253768 ) ) ;
#3758=CARTESIAN_POINT ( 'NONE',  ( 2.435307549839813124, 34.09246322853890376, -13.28282044714515031 ) ) ;
#3759=CARTESIAN_POINT ( 'NONE',  ( -7.465912594396658442, 73.45946290405333912, -11.24767626733296133 ) ) ;
#3762=CARTESIAN_POINT ( 'NONE',  ( -7.272992578804310604, 75.37999999999999545, 10.01041549318726886 ) ) ;
#3766=CARTESIAN_POINT ( 'NONE',  ( -7.682391541889500353, 44.39115312923465950, 11.10122368241315449 ) ) ;
#3768=CARTESIAN_POINT ( 'NONE',  ( 12.53368164500171389, 66.61264531847000114, -5.027186995046044160 ) ) ;
#3769=CARTESIAN_POINT ( 'NONE',  ( -13.50000000000000000, 49.92999999999999972, -3.306546357697853733E-15 ) ) ;
#3770=CARTESIAN_POINT ( 'NONE',  ( -3.162095574282764776, 71.56630276718368577, 13.12444876022228435 ) ) ;
#3773=CARTESIAN_POINT ( 'NONE',  ( -13.32309267394441221, 68.00683485648823989, 2.188465561525937186 ) ) ;
#3775=CARTESIAN_POINT ( 'NONE',  ( 4.857942641284302532, 55.00488871956680725, -12.59565032908122006 ) ) ;
#3779=CARTESIAN_POINT ( 'NONE',  ( -1.104890279304959755, 62.64030871745742957, 13.46071023764019259 ) ) ;
#3780=CARTESIAN_POINT ( 'NONE',  ( -9.362710248175982741, 35.31320775059099049, 9.725773573732148236 ) ) ;
#3781=VERTEX_POINT ( 'NONE', #3898 ) ;
#3782=DIRECTION ( 'NONE',  ( 0.000000000000000000, 0.000000000000000000, 1.000000000000000000 ) ) ;
#3783=CARTESIAN_POINT ( 'NONE',  ( -13.49475676771158383, 31.91478873253841186, -0.4353569615216364985 ) ) ;
#3786=CARTESIAN_POINT ( 'NONE',  ( 9.203170713077465592, 60.03895907460095316, 9.877926015694953321 ) ) ;
#3788=CARTESIAN_POINT ( 'NONE',  ( -9.925890167077604076, 53.28464950770988651, 9.150231210120352898 ) ) ;
#3789=CARTESIAN_POINT ( 'NONE',  ( -11.76794919243112325, 53.92999999999999972, -2.882316262207890869E-15 ) ) ;
#3791=CARTESIAN_POINT ( 'NONE',  ( 5.363543519840087370, 50.87413298173109411, 12.39218804481266645 ) ) ;
#3792=CARTESIAN_POINT ( 'NONE',  ( -13.47203084398158524, 37.90000543725030724, -0.8690430185918386341 ) ) ;
#3794=CARTESIAN_POINT ( 'NONE',  ( 11.73271526642915141, 36.67822783863627478, -6.684209631556711884 ) ) ;
#3796=CARTESIAN_POINT ( 'NONE',  ( -0.7060178253421292016, 74.65461446910167354, 13.48159923038322638 ) ) ;
#3798=CARTESIAN_POINT ( 'NONE',  ( -12.64011703651372187, 77.10247514769642407, 4.761869442916747630 ) ) ;
#3799=CARTESIAN_POINT ( 'NONE',  ( -13.32733280186987024, 80.00689698629075508, 2.196482157303579985 ) ) ;
#3800=DIRECTION ( 'NONE',  ( 1.000000000000000000, 0.000000000000000000, 0.000000000000000000 ) ) ;
#3801=VERTEX_POINT ( 'NONE', #1590 ) ;
#3805=CARTESIAN_POINT ( 'NONE',  ( -9.520470885617717371, 54.23000000000000398, 6.917026985038133624 ) ) ;
#3807=FACE_OUTER_BOUND ( 'NONE', #12680, .T. ) ;
#3809=CARTESIAN_POINT ( 'NONE',  ( 6.186989602441420821, 75.95361305086539971, -11.99880612961145587 ) ) ;
#3811=CARTESIAN_POINT ( 'NONE',  ( 10.92172942406178926, 72.12999999999999545, 7.935100905948387684 ) ) ;
#3812=CARTESIAN_POINT ( 'NONE',  ( 7.272992578804311492, 43.87999999999999545, -10.01041549318726709 ) ) ;
#3814=CARTESIAN_POINT ( 'NONE',  ( -11.53975138069232109, 58.66770748737323515, -7.033342735042283245 ) ) ;
#3815=CARTESIAN_POINT ( 'NONE',  ( 7.168473922838755286, 44.94694224986446329, 11.44171851688767916 ) ) ;
#3816=CARTESIAN_POINT ( 'NONE',  ( 11.08577043759925118, 69.72028810587863745, -7.704379851462255679 ) ) ;
#3817=CARTESIAN_POINT ( 'NONE',  ( -10.92172942406178926, 66.62999999999999545, -7.935100905948389460 ) ) ;
#3819=CARTESIAN_POINT ( 'NONE',  ( -1.977116238977308482, 55.25103791471835279, -13.36401229022775361 ) ) ;
#3820=CARTESIAN_POINT ( 'NONE',  ( -5.519339117068075673, 50.47982862213257249, 12.32018707268373703 ) ) ;
#3821=CARTESIAN_POINT ( 'NONE',  ( 9.703181444203755390, 63.79612580964563762, -9.386421454467969383 ) ) ;
#3822=CARTESIAN_POINT ( 'NONE',  ( 11.92514546446363788, 42.66388649755253226, -6.327788414984513388 ) ) ;
#3823=CARTESIAN_POINT ( 'NONE',  ( 12.51531601377990022, 39.24597988571901652, 5.061315126527163422 ) ) ;
#3825=CARTESIAN_POINT ( 'NONE',  ( -13.39686745019108294, 70.87189925962454140, -1.665516949025961368 ) ) ;
#3826=CARTESIAN_POINT ( 'NONE',  ( -12.18511954038002365, 61.71674294599442590, -5.811709024524145839 ) ) ;
#3833=CARTESIAN_POINT ( 'NONE',  ( 3.086401082262576256, 61.06902437418678176, -13.14245697113578437 ) ) ;
#3835=CARTESIAN_POINT ( 'NONE',  ( 12.35346123165463617, 57.62892738134787862, -5.444651084883814995 ) ) ;
#3836=CARTESIAN_POINT ( 'NONE',  ( 3.636496289402157078, 68.03000000000000114, -11.19198476289190936 ) ) ;
#3837=CARTESIAN_POINT ( 'NONE',  ( 11.76794919243112680, 76.57999999999998408, -3.823638476888993942 ) ) ;
#3838=CARTESIAN_POINT ( 'NONE',  ( -0.5808156989666466430, 47.65911991592597730, 13.48844809475130369 ) ) ;
#3843=CARTESIAN_POINT ( 'NONE',  ( -5.073760196756867735, 73.36319280854625902, -12.51029294622204446 ) ) ;
#3844=ORIENTED_EDGE ( 'NONE', *, *, #4416, .F. ) ;
#3845=ORIENTED_EDGE ( 'NONE', *, *, #75, .F. ) ;
#3846=CARTESIAN_POINT ( 'NONE',  ( -11.76794919243112325, 77.92999999999999261, -2.882316262207890869E-15 ) ) ;
#3849=CARTESIAN_POINT ( 'NONE',  ( -0.5815368319779855577, 44.65908970977663017, 13.48758275782939542 ) ) ;
#3852=CARTESIAN_POINT ( 'NONE',  ( 13.39960944229175333, 66.48731185255626031, -1.643332913497620451 ) ) ;
#3854=CARTESIAN_POINT ( 'NONE',  ( -8.691771469529815392E-16, 44.67999999999999972, 14.19474002721660355 ) ) ;
#3855=CARTESIAN_POINT ( 'NONE',  ( -8.293551300264768500, 71.36388038614214224, 10.65233661047543556 ) ) ;
#3857=CARTESIAN_POINT ( 'NONE',  ( -13.42158662539458192, 67.87941032537437991, -1.453869035909064467 ) ) ;
#3859=CARTESIAN_POINT ( 'NONE',  ( 7.145042507201743831, 54.91449063741976744, -11.46286542413573173 ) ) ;
#3862=CARTESIAN_POINT ( 'NONE',  ( -12.77386615626469535, 65.08747835186800046, 4.369140299076793355 ) ) ;
#3863=CARTESIAN_POINT ( 'NONE',  ( -5.432056264447402860, 35.48329878629467515, 12.36543368378323748 ) ) ;
#3866=EDGE_CURVE ( 'NONE', #13443, #743, #9296, .T. ) ;
#3868=CARTESIAN_POINT ( 'NONE',  ( -3.785303478180469305, 31.31610501778620659, -12.96062533801228689 ) ) ;
#3869=DIRECTION ( 'NONE',  ( 0.000000000000000000, -1.000000000000000000, 0.000000000000000000 ) ) ;
#3870=CARTESIAN_POINT ( 'NONE',  ( 12.93954261948424111, 60.29192777250819546, 3.855782101392678740 ) ) ;
#3871=CARTESIAN_POINT ( 'NONE',  ( -8.374943186797883854, 53.36072342052383988, 10.60918593187694192 ) ) ;
#3872=CARTESIAN_POINT ( 'NONE',  ( 11.76794919243112680, 46.57999999999999829, -3.823638476888993942 ) ) ;
#3874=CARTESIAN_POINT ( 'NONE',  ( -13.49999999999999822, 69.78000000000000114, -4.386415899144240349 ) ) ;
#3875=CARTESIAN_POINT ( 'NONE',  ( 8.243599928797097576, 50.99384897302891062, 10.69102843549329940 ) ) ;
#3876=CARTESIAN_POINT ( 'NONE',  ( -11.88435525982994889, 37.69305171285699174, -6.404073035000328318 ) ) ;
#3877=CARTESIAN_POINT ( 'NONE',  ( 10.51734625305970461, 36.10681963769080483, 8.466829602298034274 ) ) ;
#3879=CARTESIAN_POINT ( 'NONE',  ( -6.050054063620305733, 74.45907014989788308, 12.06844880531143360 ) ) ;
#3880=CARTESIAN_POINT ( 'NONE',  ( -13.50069008547208860, 76.92950476662907988, -0.01155620547472042438 ) ) ;
#3881=CARTESIAN_POINT ( 'NONE',  ( -10.15564728739121669, 80.27272457646746773, 8.905508388590966717 ) ) ;
#3883=CARTESIAN_POINT ( 'NONE',  ( 7.500000000000001776, 105.3920397463311218, 8.709571264514705646 ) ) ;
#3884=CARTESIAN_POINT ( 'NONE',  ( -7.499999999999998224, 108.9300000000000068, -9.367496997597600128 ) ) ;
#3886=CARTESIAN_POINT ( 'NONE',  ( 9.520470885617717371, 52.72999999999999687, -6.917026985038131848 ) ) ;
#3891=CARTESIAN_POINT ( 'NONE',  ( 3.905267433998111493, 76.03955353119496863, -12.92325076002208206 ) ) ;
#3893=CARTESIAN_POINT ( 'NONE',  ( -11.76794919243112325, 38.77999999999999403, -3.823638476888998827 ) ) ;
#3895=CARTESIAN_POINT ( 'NONE',  ( -13.14170631426251212, 58.81803730528373819, -3.156520166358864010 ) ) ;
#3896=CARTESIAN_POINT ( 'NONE',  ( 2.884611534850368475, 44.78371962230355052, 13.18822724452614459 ) ) ;
#3897=CARTESIAN_POINT ( 'NONE',  ( 12.37795243579363635, 69.62700217947723047, -5.400564600271921201 ) ) ;
#3898=CARTESIAN_POINT ( 'NONE',  ( 2.445080149700053643E-15, 33.17999999999999261, -13.50000000000000000 ) ) ;
#3899=CARTESIAN_POINT ( 'NONE',  ( 8.719434965209991617, 30.01580748498589202, 10.30804611199927301 ) ) ;
#3900=EDGE_CURVE ( 'NONE', #3211, #16090, #6391, .T. ) ;
#3901=CARTESIAN_POINT ( 'NONE',  ( -10.11073118668884874, 55.58505174064411136, -8.945568110028689901 ) ) ;
#3902=CARTESIAN_POINT ( 'NONE',  ( -5.538802633866588110, 50.47907763144620930, 12.31144910959687877 ) ) ;
#3903=CARTESIAN_POINT ( 'NONE',  ( 11.51750660560541561, 63.69287151518827983, -7.042528692690322778 ) ) ;
#3904=CARTESIAN_POINT ( 'NONE',  ( 13.05580366346349841, 42.55242448848036929, -3.435679632562075980 ) ) ;
#3905=CARTESIAN_POINT ( 'NONE',  ( 9.165837416579254437, 39.03714869363280116, 9.911684281184246714 ) ) ;
#3908=CARTESIAN_POINT ( 'NONE',  ( -9.881012300872606957, 70.57302064171045686, -9.198673637768660427 ) ) ;
#3911=ORIENTED_EDGE ( 'NONE', *, *, #8030, .F. ) ;
#3915=CARTESIAN_POINT ( 'NONE',  ( -1.005545769327274827E-13, 52.18000000000000682, -13.50000000000000000 ) ) ;
#3917=CARTESIAN_POINT ( 'NONE',  ( 8.310874194162975570, 71.99679895926327333, 10.64270930270453341 ) ) ;
#3918=CARTESIAN_POINT ( 'NONE',  ( 13.06949918658192367, 57.55469024356798258, -3.496992391659727417 ) ) ;
#3919=CARTESIAN_POINT ( 'NONE',  ( -7.272992578804307939, 65.48000000000000398, -10.01041549318726886 ) ) ;
#3920=CARTESIAN_POINT ( 'NONE',  ( 7.272992578804311492, 76.88000000000000966, -10.01041549318726709 ) ) ;
#3921=CARTESIAN_POINT ( 'NONE',  ( -11.42340091696314630, 47.19916785071956156, 7.194499597321170725 ) ) ;
#3927=DIRECTION ( 'NONE',  ( 0.000000000000000000, -1.000000000000000000, 0.000000000000000000 ) ) ;
#3928=CARTESIAN_POINT ( 'NONE',  ( 11.99720772546109693, 33.65837649682584498, -6.190075193952552901 ) ) ;
#3929=CARTESIAN_POINT ( 'NONE',  ( -7.006031218443153463, 73.43963910418750629, -11.55271937892839063 ) ) ;
#3930=ORIENTED_EDGE ( 'NONE', *, *, #6778, .F. ) ;
#3932=CARTESIAN_POINT ( 'NONE',  ( -3.636496289402153081, 77.32999999999999829, -11.19198476289190936 ) ) ;
#3934=CARTESIAN_POINT ( 'NONE',  ( -13.31322428518614309, 41.00862424342748369, 2.238198738180153136 ) ) ;
#3937=CARTESIAN_POINT ( 'NONE',  ( -10.19438961638010177, 44.27054227623447247, 8.850209172380360201 ) ) ;
#3940=CARTESIAN_POINT ( 'NONE',  ( -10.92172942406179104, 41.22999999999999687, 7.935100905948387684 ) ) ;
#3941=CARTESIAN_POINT ( 'NONE',  ( -6.957400787806288456, 71.42232733259757538, 11.58147395634350296 ) ) ;
#3943=CARTESIAN_POINT ( 'NONE',  ( -12.92540607541860886, 68.06966242483530038, 3.897284986388191097 ) ) ;
#3946=CARTESIAN_POINT ( 'NONE',  ( 10.46984184081570568, 54.75555934975864858, -8.522531150578997128 ) ) ;
#3949=CARTESIAN_POINT ( 'NONE',  ( -13.39894528404028406, 64.87027492873734502, -1.716493634713462724 ) ) ;
#3950=B_SPLINE_CURVE_WITH_KNOTS ( 'NONE', 3,
 ( #15374, #11512, #3541, #7456, #4620, #10026, #14057, #8955, #886, #1944, #723, #12836, #6132, #12919, #7626, #16887, #4794, #10195, #2112, #14313, #2199, #6298, #10621, #15813, #14573, #3891, #10455, #7806, #16073, #12111, #8065, #1151, #6563, #13428, #3809, #9308, #3718, #1, #15900, #11943, #15721, #15987, #9222, #11770, #14659, #13090, #2547, #13177, #9135, #6475, #7712, #1235, #14395, #2457, #6732, #14484, #7976, #3627, #7887, #17237, #2371, #12028, #1063, #6387, #11861, #6647, #1317, #5147, #17323, #13345, #10538, #2284, #13264, #3980, #5235, #17407, #17147, #5056, #975, #5322, #10706, #9394, #14744, #2634, #10368, #9043, #6912, #1670, #2986, #9567, #16519, #1759, #8242, #15087, #8417, #9655, #8506, #12376, #12555, #5759, #15179, #5677, #4245, #92, #12288, #8329, #9834, #269, #11057, #10878, #15006, #16430, #5497, #2810, #11143, #7169, #3079, #13684, #1582, #13855, #16338, #7084, #2897, #5407, #13768, #4333, #12468, #9742, #10969, #6822, #353, #8150, #4425, #13602, #4155, #1497, #2722, #10792, #9482, #7000, #16157, #4066, #14828, #14917, #13514, #1406, #12200, #16249, #182, #5590, #15354, #8853, #8933, #526, #2009, #702, #1925, #4512, #14037, #6192, #4688, #7603, #10007, #16867, #9919, #8592, #16954, #11316, #15527, #7346, #14207, #14292, #12727, #2091, #3437, #4600, #11579, #2177, #3258, #10177, #7518, #16693, #12898, #785, #10091, #16779, #16607, #613, #6112, #441, #6024, #5850, #4856, #13943, #8678, #7435, #10259, #15269, #11232, #3166, #12814, #11408, #15611, #15442 ),
 .UNSPECIFIED., .F., .F.,
 ( 4, 2, 2, 2, 2, 1, 1, 1, 2, 2, 2, 2, 2, 1, 1, 1, 2, 2, 2, 2, 2, 2, 2, 2, 2, 2, 1, 1, 1, 2, 2, 1, 2, 2, 1, 2, 2, 1, 2, 2, 2, 2, 1, 2, 2, 2, 2, 2, 2, 2, 2, 1, 1, 1, 2, 2, 2, 1, 1, 1, 2, 2, 2, 2, 2, 2, 2, 2, 1, 1, 2, 2, 2, 2, 1, 2, 2, 2, 2, 2, 1, 1, 2, 2, 2, 1, 2, 2, 2, 2, 2, 2, 2, 2, 2, 2, 1, 2, 2, 2, 2, 2, 2, 1, 1, 1, 1, 2, 2, 2, 1, 2, 2, 1, 1, 1, 2, 2, 4 ),
 ( 0.09315741062983846910, 0.09361976615167078020, 0.09373535503212884756, 0.09374980364218611639, 0.09375702794721474387, 0.09376425225224337134, 0.09379314947235789512, 0.09385094391258694269, 0.09408212167350313293, 0.09500683271716785228, 0.09546918823900021889, 0.09570036599991640913, 0.09571481460997366408, 0.09572926322003093291, 0.09575816044014544282, 0.09581595488037449038, 0.09593154376083258550, 0.09685625480449729097, 0.09731861032632964370, 0.09754978808724582007, 0.09760758252747486763, 0.09766537696770391519, 0.09778096584816199643, 0.09870567689182659088, 0.09916803241365888810, 0.09939921017457503671, 0.09951479905503310408, 0.09957259349526213776, 0.09960149071537666154, 0.09960871502040528902, 0.09961593932543391650, 0.09963038793549117145, 0.1005550989791556965, 0.1014798100228202216, 0.1015376044630492552, 0.1015520530731065102, 0.1015665016831637651, 0.1015953989032782889, 0.1017109877837363424, 0.1019421655446524494, 0.1024045210664846772, 0.1033292321101491468, 0.1034448209906072003, 0.1035026154308362339, 0.1035604098710652538, 0.1037915876319813885, 0.1042539431538136718, 0.1051786541974782246, 0.1054098319583943594, 0.1054676263986233931, 0.1054748507036520205, 0.1054820750086806480, 0.1054965236187379168, 0.1055254208388524267, 0.1056410097193104802, 0.1061033652411427081, 0.1070280762848071499, 0.1072592540457232568, 0.1073748429261813103, 0.1074037401462958341, 0.1074181887563530891, 0.1074326373664103440, 0.1074904318066393638, 0.1079527873284715639, 0.1088774983721359502, 0.1093398538939681364, 0.1093687511140826463, 0.1093976483341971701, 0.1094554427744262037, 0.1095710316548842572, 0.1098022094158003781, 0.1116516315031293033, 0.1118828092640454241, 0.1119406037042744440, 0.1119983981445034776, 0.1121139870249615311, 0.1125763425467937590, 0.1130386980686259868, 0.1131542869490840403, 0.1132120813893130601, 0.1132698758295420938, 0.1135010535904582007, 0.1144257646341226564, 0.1144546618542371802, 0.1144835590743516901, 0.1145413535145807377, 0.1146569423950388467, 0.1148881201559550369, 0.1153504756777874452, 0.1162751867214522616, 0.1163329811616813092, 0.1163907756019103706, 0.1165063644823684796, 0.1167375422432846838, 0.1171998977651171059, 0.1181246088087819501, 0.1182401976892400591, 0.1182979921294691067, 0.1183557865696981681, 0.1185869643306143723, 0.1190493198524467944, 0.1199740308961116525, 0.1199884795061689213, 0.1200029281162261763, 0.1200318253363407139, 0.1200896197765697615, 0.1202052086570278844, 0.1204363864179441301, 0.1208987419397766078, 0.1213610974616090854, 0.1215922752225253312, 0.1216500696627543926, 0.1216572939677830201, 0.1216645182728116614, 0.1216789668828689303, 0.1217078641029834679, 0.1218234529834416047, 0.1222858085052741794, 0.1227481640271067542 ),
 .UNSPECIFIED. ) ;
#3951=CARTESIAN_POINT ( 'NONE',  ( -9.257384347542936709, 35.31844601351780710, 9.826854653260157946 ) ) ;
#3954=CARTESIAN_POINT ( 'NONE',  ( -9.610466609222978462, 31.55914188783036423, -9.486719919042664984 ) ) ;
#3960=CARTESIAN_POINT ( 'NONE',  ( -9.845067486581010385, 53.28885231408968082, 9.237281070633853730 ) ) ;
#3961=CARTESIAN_POINT ( 'NONE',  ( 3.636496289402154414, 48.82999999999999829, 11.19198476289190936 ) ) ;
#3963=CARTESIAN_POINT ( 'NONE',  ( 13.50000000000000355, 68.57999999999998408, -4.386415899144233244 ) ) ;
#3964=CARTESIAN_POINT ( 'NONE',  ( 10.03500853364407064, 51.08076950763429380, 9.041007138082409966 ) ) ;
#3965=CARTESIAN_POINT ( 'NONE',  ( -10.23891164854874702, 37.59188044157124864, -8.798564376260818776 ) ) ;
#3966=EDGE_CURVE ( 'NONE', #10490, #7293, #4519, .T. ) ;
#3967=CARTESIAN_POINT ( 'NONE',  ( 10.97156431219244510, 36.13285426820748114, 7.867357652818380842 ) ) ;
#3969=CARTESIAN_POINT ( 'NONE',  ( -0.9212313319806377798, 74.64687916296506387, 13.46868817401126606 ) ) ;
#3970=CARTESIAN_POINT ( 'NONE',  ( -13.30102111233071760, 76.84881920128778177, -2.309297776588126627 ) ) ;
#3971=CARTESIAN_POINT ( 'NONE',  ( -9.859355752153115660, 80.28820049829310790, 9.232342221173379215 ) ) ;
#3972=CARTESIAN_POINT ( 'NONE',  ( 7.500000000000000000, 103.1860286984271795, -9.367496997597600128 ) ) ;
#3975=CARTESIAN_POINT ( 'NONE',  ( 11.76794919243112680, 49.57999999999999119, -3.823638476888993942 ) ) ;
#3979=CARTESIAN_POINT ( 'NONE',  ( -2.854184389239543762, 34.28262590607400995, -13.19500222631561037 ) ) ;
#3980=CARTESIAN_POINT ( 'NONE',  ( 12.05584393367779406, 75.65379272059647064, -6.075093657815592074 ) ) ;
#3981=CARTESIAN_POINT ( 'NONE',  ( 1.653273178848926472E-15, 80.93000000000000682, 13.50000000000000000 ) ) ;
#3982=CARTESIAN_POINT ( 'NONE',  ( -7.576616670048093940E-16, 36.67999999999999972, 12.37355403259654985 ) ) ;
#3983=CARTESIAN_POINT ( 'NONE',  ( -4.765598480478985266, 41.50834662332702862, 12.63248701834810639 ) ) ;
#3984=CARTESIAN_POINT ( 'NONE',  ( -5.773622420134949529, 58.39004374645310946, -12.20308674553266925 ) ) ;
#3985=CARTESIAN_POINT ( 'NONE',  ( 2.941637194391252041, 44.78576598995574898, 13.17562406899208405 ) ) ;
#3986=EDGE_CURVE ( 'NONE', #13703, #13982, #15361, .T. ) ;
#3987=DIRECTION ( 'NONE',  ( 0.000000000000000000, -1.000000000000000000, 0.000000000000000000 ) ) ;
#3988=DIRECTION ( 'NONE',  ( 0.000000000000000000, 0.000000000000000000, 1.000000000000000000 ) ) ;
#3989=CARTESIAN_POINT ( 'NONE',  ( -7.389574489282211722, 55.45617881592348652, -11.29799270601480288 ) ) ;
#3990=CARTESIAN_POINT ( 'NONE',  ( -13.26124712707118825, 49.84090803523835689, -2.527720896449040744 ) ) ;
#3991=CARTESIAN_POINT ( 'NONE',  ( 12.75440868670226813, 63.58958983645529628, -4.424554037362297798 ) ) ;
#3992=CARTESIAN_POINT ( 'NONE',  ( 11.18391117983416372, 42.71430389940879735, -7.561094431090153556 ) ) ;
#3993=CARTESIAN_POINT ( 'NONE',  ( 13.48029845638929558, 39.45517033420289010, -0.7296389357882047122 ) ) ;
#3994=ORIENTED_EDGE ( 'NONE', *, *, #13862, .F. ) ;
#3995=CARTESIAN_POINT ( 'NONE',  ( -12.63529163522881227, 70.75760609934009437, -4.760530200637639098 ) ) ;
#3996=CARTESIAN_POINT ( 'NONE',  ( -8.343458848123578520, 48.48000000000000398, -11.48378591275254124 ) ) ;
#3997=VERTEX_POINT ( 'NONE', #15093 ) ;
#3998=ORIENTED_EDGE ( 'NONE', *, *, #14625, .T. ) ;
#4001=CARTESIAN_POINT ( 'NONE',  ( 6.523056816745746112, 47.91989408141689921, 11.81980764766238501 ) ) ;
#4003=CARTESIAN_POINT ( 'NONE',  ( 10.67056894037764359, 72.11562701491169491, 8.269762857265360978 ) ) ;
#4004=CARTESIAN_POINT ( 'NONE',  ( 12.37411402100152458, 57.62708032287364546, -5.397352088785305924 ) ) ;
#4005=CARTESIAN_POINT ( 'NONE',  ( 11.76794919243112680, 64.57999999999999829, -3.823638476888993942 ) ) ;
#4006=CARTESIAN_POINT ( 'NONE',  ( 4.171729424061789260, 34.82999999999999829, 12.83926296998457417 ) ) ;
#4007=CARTESIAN_POINT ( 'NONE',  ( -11.76794919243112325, 80.93000000000000682, -2.882316262207890869E-15 ) ) ;
#4009=CARTESIAN_POINT ( 'NONE',  ( -3.320277394660133385, 47.56063789249560614, 13.08648027329329544 ) ) ;
#4013=DIRECTION ( 'NONE',  ( 1.000000000000000000, -1.156482317317871133E-15, 0.000000000000000000 ) ) ;
#4016=CARTESIAN_POINT ( 'NONE',  ( 13.48828357174217807, 33.44935985554970870, -0.5623287429662219283 ) ) ;
#4017=CARTESIAN_POINT ( 'NONE',  ( -7.790051440343440881, 73.47356962630189514, -11.02593981657268607 ) ) ;
#4020=CARTESIAN_POINT ( 'NONE',  ( -11.76794919243112325, 78.07999999999999829, 3.823638476888994830 ) ) ;
#4021=ORIENTED_EDGE ( 'NONE', *, *, #15801, .F. ) ;
#4022=CIRCLE ( 'NONE', #11087, 4.000000000000004441 ) ;
#4024=CARTESIAN_POINT ( 'NONE',  ( -6.570750217010064453, 44.43812314528702245, 11.79549799968171264 ) ) ;
#4026=CARTESIAN_POINT ( 'NONE',  ( -10.92172942406178926, 40.63000000000000256, -7.935100905948389460 ) ) ;
#4027=CARTESIAN_POINT ( 'NONE',  ( -13.49970439451574400, 70.94072343917298440, 0.3103739863738418370 ) ) ;
#4030=CARTESIAN_POINT ( 'NONE',  ( -13.35263207532700669, 67.86002430682577824, -1.997692355781490292 ) ) ;
#4032=CARTESIAN_POINT ( 'NONE',  ( 11.55530260182779401, 54.69032320486194010, -6.980335635328147603 ) ) ;
#4035=CARTESIAN_POINT ( 'NONE',  ( -12.17476046333273842, 64.71527778992695801, -5.849856061721414591 ) ) ;
#4036=CARTESIAN_POINT ( 'NONE',  ( -13.34634384165835286, 35.00116161489640376, 2.031037000000563530 ) ) ;
#4039=CARTESIAN_POINT ( 'NONE',  ( -1.091948754393482712, 31.21923308297253286, -13.45827295822001091 ) ) ;
#4040=CARTESIAN_POINT ( 'NONE',  ( 3.141418519012163291, 73.06704652263337607, -13.13050367329915602 ) ) ;
#4043=EDGE_CURVE ( 'NONE', #12592, #13217, #1861, .T. ) ;
#4045=CARTESIAN_POINT ( 'NONE',  ( -11.99931260044677472, 53.15821574507319269, 6.186054099126281791 ) ) ;
#4046=CARTESIAN_POINT ( 'NONE',  ( -11.76794919243112325, 44.92999999999999972, -2.882316262207890869E-15 ) ) ;
#4047=PRODUCT_CONTEXT ( 'NONE', #13204, 'mechanical' ) ;
#4048=CARTESIAN_POINT ( 'NONE',  ( 13.49999999999999822, 65.28000000000000114, 4.386415899144237684 ) ) ;
#4049=CARTESIAN_POINT ( 'NONE',  ( 4.993261676203598398, 50.86016716623841916, 12.54262158262842597 ) ) ;
#4050=CARTESIAN_POINT ( 'NONE',  ( -11.34510250317683600, 37.65566839993009296, -7.320287091699782422 ) ) ;
#4051=CARTESIAN_POINT ( 'NONE',  ( 4.208051776087926577, 35.83130703551096019, 12.82741174251338023 ) ) ;
#4053=CARTESIAN_POINT ( 'NONE',  ( -12.95509469782950873, 74.06591892939171373, 3.797696039018899405 ) ) ;
#4054=CARTESIAN_POINT ( 'NONE',  ( -12.95329468731883260, 76.79322173300190002, -3.819660872089479575 ) ) ;
#4055=CARTESIAN_POINT ( 'NONE',  ( -11.14889335015297966, 80.21642165902807164, 7.613376886237952057 ) ) ;
#4056=CARTESIAN_POINT ( 'NONE',  ( -2.648919002463483441, 80.93000000000000682, 12.65678160791643592 ) ) ;
#4059=CARTESIAN_POINT ( 'NONE',  ( -7.272992578804307939, 47.47999999999999687, -10.01041549318727064 ) ) ;
#4064=CARTESIAN_POINT ( 'NONE',  ( -9.612436902512136783, 40.55921212120037467, -9.485869169573415860 ) ) ;
#4066=CARTESIAN_POINT ( 'NONE',  ( 10.31463346427486982, 75.09593381292602032, 8.709679962864647962 ) ) ;
#4069=CARTESIAN_POINT ( 'NONE',  ( 11.76794919243112680, 40.57999999999999829, -3.823638476888993942 ) ) ;
#4070=CARTESIAN_POINT ( 'NONE',  ( -11.18770039063602262, 41.21406332147840601, 7.555487409198383908 ) ) ;
#4071=CARTESIAN_POINT ( 'NONE',  ( -11.07316193868316390, 58.63892660121854306, -7.722844086540342268 ) ) ;
#4076=CARTESIAN_POINT ( 'NONE',  ( -6.405441672365779660, 49.41516637713032623, -11.88598892033222398 ) ) ;
#4077=CARTESIAN_POINT ( 'NONE',  ( 13.50050750903061747, 63.42343654352898596, 0.1847079823050248870 ) ) ;
#4078=CARTESIAN_POINT ( 'NONE',  ( 10.28321627186559262, 42.76572808278937998, -8.746763802038561408 ) ) ;
#4079=CARTESIAN_POINT ( 'NONE',  ( 4.245544141064997667, 38.83265899993158854, 12.81504996667835883 ) ) ;
#4080=ORIENTED_EDGE ( 'NONE', *, *, #17466, .T. ) ;
#4081=CARTESIAN_POINT ( 'NONE',  ( 2.445080149700053643E-15, 75.17999999999999261, -13.50000000000000000 ) ) ;
#4085=CARTESIAN_POINT ( 'NONE',  ( -5.834127350457870342, 43.39242430467762546, -12.17494074988466224 ) ) ;
#4087=CARTESIAN_POINT ( 'NONE',  ( 9.331600089522767760, 60.81473193213921036, -9.755580554834571316 ) ) ;
#4091=CARTESIAN_POINT ( 'NONE',  ( -1.010931998681471075E-07, 71.67999718330101189, 13.49999999999999822 ) ) ;
#4092=CARTESIAN_POINT ( 'NONE',  ( 11.62061665277031075, 57.68594776230959553, -6.871996344357341080 ) ) ;
#4093=CARTESIAN_POINT ( 'NONE',  ( -3.636496289402155746, 72.53000000000000114, 11.19198476289190936 ) ) ;
#4094=CARTESIAN_POINT ( 'NONE',  ( -7.272992578804307939, 77.48000000000000398, -10.01041549318726886 ) ) ;
#4095=CARTESIAN_POINT ( 'NONE',  ( -7.033908694595895739, 47.41891739858513688, 11.52279350434594285 ) ) ;
#4096=DIRECTION ( 'NONE',  ( 0.000000000000000000, 0.000000000000000000, -1.000000000000000000 ) ) ;
#4098=CARTESIAN_POINT ( 'NONE',  ( 2.107853069822502790E-14, 31.18000000000000682, -13.50000000000000000 ) ) ;
#4099=CARTESIAN_POINT ( 'NONE',  ( -5.620581134510726606, 56.47591212409395922, 12.27434859643074994 ) ) ;
#4102=CARTESIAN_POINT ( 'NONE',  ( 10.71824045277809923, 33.74192371909632016, -8.219471766505868970 ) ) ;
#4103=CARTESIAN_POINT ( 'NONE',  ( -3.211247102494231953, 73.29552755700889577, -13.11374676138101947 ) ) ;
#4107=CARTESIAN_POINT ( 'NONE',  ( -4.830293611773615048, 62.50587364081614083, 12.60858922533637205 ) ) ;
#4109=ORIENTED_EDGE ( 'NONE', *, *, #4375, .T. ) ;
#4110=CARTESIAN_POINT ( 'NONE',  ( -13.47828624137987497, 40.90358342329059127, -0.7654979494148171915 ) ) ;
#4112=CARTESIAN_POINT ( 'NONE',  ( -11.20659543516484469, 44.21289395307379522, 7.527431242496333219 ) ) ;
#4114=CARTESIAN_POINT ( 'NONE',  ( 10.92172942406178926, 45.12999999999999545, 7.935100905948387684 ) ) ;
#4115=CARTESIAN_POINT ( 'NONE',  ( 8.343458848123583849, 44.87999999999998835, -11.48378591275253768 ) ) ;
#4116=CARTESIAN_POINT ( 'NONE',  ( -12.93889380315461501, 71.06794844313003523, 3.851678986249745140 ) ) ;
#4117=AXIS2_PLACEMENT_3D ( 'NONE', #7077, #12280, #16422 ) ;
#4119=CARTESIAN_POINT ( 'NONE',  ( -13.43488328562637513, 67.88398595381684686, -1.324420451639741092 ) ) ;
#4121=CARTESIAN_POINT ( 'NONE',  ( 11.39185320920821809, 54.70104879577822743, -7.245458119857994816 ) ) ;
#4123=EDGE_CURVE ( 'NONE', #4640, #8734, #10328, .T. ) ;
#4124=CARTESIAN_POINT ( 'NONE',  ( -13.46072377650594376, 64.89438511582379476, -1.029100581260686376 ) ) ;
#4126=CARTESIAN_POINT ( 'NONE',  ( -13.49476282772579694, 34.91482293905653478, -0.4351865453969105402 ) ) ;
#4128=ORIENTED_EDGE ( 'NONE', *, *, #4596, .F. ) ;
#4129=DIRECTION ( 'NONE',  ( 0.000000000000000000, 0.000000000000000000, -1.000000000000000000 ) ) ;
#4131=CARTESIAN_POINT ( 'NONE',  ( 7.696945099050856776, 72.89056765019519446, -11.09520446863491827 ) ) ;
#4133=CARTESIAN_POINT ( 'NONE',  ( 0.07359788859287424989, 79.17735392238709835, -13.49981184443148408 ) ) ;
#4135=CARTESIAN_POINT ( 'NONE',  ( -8.343458848123576743, 76.48000000000001819, -11.48378591275254301 ) ) ;
#4136=CARTESIAN_POINT ( 'NONE',  ( -12.16582101725930265, 52.71440321287756348, -5.873394938063603021 ) ) ;
#4137=CARTESIAN_POINT ( 'NONE',  ( -11.76794919243112325, 47.92999999999999972, -2.882316262207890869E-15 ) ) ;
#4138=CARTESIAN_POINT ( 'NONE',  ( 12.50102360570146942, 51.24461652421468472, 5.096535108048335871 ) ) ;
#4139=CARTESIAN_POINT ( 'NONE',  ( -5.545884925436540769, 37.38119561285134296, -12.30826441516979664 ) ) ;
#4140=CARTESIAN_POINT ( 'NONE',  ( 4.003383602335978786, 35.82394118477286327, 12.89283635254156835 ) ) ;
#4142=CARTESIAN_POINT ( 'NONE',  ( -12.11092945869762438, 74.14939596029618940, 5.964972250005902588 ) ) ;
#4143=CARTESIAN_POINT ( 'NONE',  ( -11.21515498128762900, 76.64763740971592654, -7.514674283766924923 ) ) ;
#4144=CARTESIAN_POINT ( 'NONE',  ( -10.57611007270270065, 80.24971877258465724, 8.393134611178751925 ) ) ;
#4148=DIRECTION ( 'NONE',  ( 0.000000000000000000, 0.000000000000000000, -1.000000000000000000 ) ) ;
#4150=CARTESIAN_POINT ( 'NONE',  ( 11.76794919243112325, 46.27999999999999403, 3.823638476888997051 ) ) ;
#4153=CARTESIAN_POINT ( 'NONE',  ( -10.37886156279672889, 40.59931919632202124, -8.633337318100664959 ) ) ;
#4154=CARTESIAN_POINT ( 'NONE',  ( 6.750022862106050958, 30.59592842876635643, 11.69132975161703492 ) ) ;
#4155=CARTESIAN_POINT ( 'NONE',  ( 11.44075521902680670, 75.16203548088178366, 7.166853402732320077 ) ) ;
#4157=CARTESIAN_POINT ( 'NONE',  ( 3.636496289402157078, 35.03000000000000114, -11.19198476289190936 ) ) ;
#4158=CARTESIAN_POINT ( 'NONE',  ( -3.648845442435871611, 41.54898592542676283, 13.00161767624870457 ) ) ;
#4159=CARTESIAN_POINT ( 'NONE',  ( -5.854979236895436756, 58.39324858652572914, -12.16430431366758569 ) ) ;
#4164=CARTESIAN_POINT ( 'NONE',  ( -0.1475770875894988898, 55.18530632762605848, -13.50000000041324100 ) ) ;
#4166=CARTESIAN_POINT ( 'NONE',  ( -10.18460302888335534, 49.58894042909286526, -8.861442684701360761 ) ) ;
#4167=CARTESIAN_POINT ( 'NONE',  ( 13.25541523722283266, 63.33835930678574755, 2.600118167593814977 ) ) ;
#4168=CARTESIAN_POINT ( 'NONE',  ( 13.45911878322305277, 42.46696013891686050, -1.067321996712556897 ) ) ;
#4169=CARTESIAN_POINT ( 'NONE',  ( 7.123418755682585868, 38.94487885092864587, 11.46980419701936249 ) ) ;
#4170=EDGE_LOOP ( 'NONE', ( #2151, #1354, #2779, #11010 ) ) ;
#4172=CARTESIAN_POINT ( 'NONE',  ( -2.138189944381236884, 48.25688142232026223, -13.50000000000000000 ) ) ;
#4175=B_SPLINE_CURVE_WITH_KNOTS ( 'NONE', 3,
 ( #4689, #13944, #703, #8680, #10092, #8768, #11494, #13158, #6455, #2610, #1044, #2354, #13408, #15880, #11840, #17389, #14465, #7786, #5036, #11922, #9113, #2526, #5127, #13325, #10770, #1132, #7955, #2265, #9201, #17127, #17216, #6543, #14722, #13071, #956, #14639, #1217, #11751, #2436, #3871, #7868, #10517, #8041, #3960, #5215, #1297, #14552, #9021, #3609, #3788, #6628, #13243, #10434, #5385, #6712, #15793, #17302, #17472, #10603, #5304, #15968, #9287, #12007, #14377, #10686, #16052, #9372, #7692, #6368, #12089, #3700, #4045, #164, #4223, #16317, #16499, #1650, #14807, #7066, #16410, #9637, #12535, #5829, #12448, #5568, #9459, #10950, #14986, #2878, #4403, #333, #2701, #5742, #421, #9813, #14897, #7150, #11124, #2968, #15159, #8222, #8129, #13495, #3058, #5476, #8486, #1562, #1384, #8397, #2791, #6801, #10857, #1737, #16133, #13583, #15068, #12179, #13751, #13837, #70, #12357, #16225, #4136, #9548, #1476, #6893, #5656, #12266, #8311, #13666, #6982, #4311, #251, #11038, #9723, #12882, #3332, #10074, #9901, #6005, #16851, #16760, #10242, #7233, #4580, #11475, #3238, #14014, #15596, #8659, #9987, #3503, #11387, #1906, #7501, #15335, #7323, #12620, #1989, #16674, #16936, #12707, #3421, #847, #8747, #15509, #15248, #4667, #508, #594, #14104, #4839, #3146, #8571, #4753, #8835, #1818, #15425, #10159, #7414, #5916, #8918, #11561, #12796, #14276 ),
 .UNSPECIFIED., .F., .F.,
 ( 4, 2, 2, 1, 1, 2, 2, 2, 2, 1, 2, 2, 1, 1, 2, 2, 2, 1, 1, 2, 2, 1, 2, 2, 2, 2, 2, 1, 2, 2, 1, 2, 2, 2, 1, 1, 2, 2, 1, 2, 2, 2, 2, 1, 1, 2, 2, 1, 2, 2, 1, 2, 2, 1, 2, 2, 1, 1, 1, 1, 2, 2, 2, 1, 1, 1, 1, 2, 2, 2, 2, 2, 1, 2, 2, 2, 2, 2, 1, 1, 1, 2, 2, 1, 2, 2, 1, 1, 2, 2, 1, 2, 2, 2, 2, 1, 1, 2, 2, 1, 1, 1, 2, 2, 2, 2, 1, 2, 2, 1, 2, 2, 4 ),
 ( 0.5344080644574688010, 0.5345226381220460343, 0.5345512815381903149, 0.5345799249543345955, 0.5346372117866232676, 0.5348663591157777342, 0.5353246537740865563, 0.5362412430907044225, 0.5366995377490133556, 0.5369286850781678222, 0.5370432587427450555, 0.5370719021588893360, 0.5371005455750336166, 0.5371578324073221777, 0.5380744217239400440, 0.5389910110405577992, 0.5394493056988667323, 0.5395065925311554045, 0.5395352359472996850, 0.5395495576553718253, 0.5395567185094078955, 0.5395638793634439656, 0.5396784530280211989, 0.5399076003571755544, 0.5408241896737931986, 0.5417407789904108428, 0.5419699263195651984, 0.5420272131518538705, 0.5420415348599260108, 0.5420558565679981511, 0.5420844999841424317, 0.5421990736487196649, 0.5426573683070287091, 0.5431156629653376422, 0.5432302366299148755, 0.5432875234622035476, 0.5433018451702756879, 0.5433161668783478282, 0.5433448102944922198, 0.5435739576236466863, 0.5444905469402646636, 0.5445478337725533358, 0.5446051206048420079, 0.5447196942694192412, 0.5449488415985737078, 0.5454071362568827519, 0.5463237255735007292, 0.5467820202318096623, 0.5470111675609642399, 0.5470684543932528010, 0.5471257412255414732, 0.5472403148901187064, 0.5481569042067366837, 0.5482714778713139170, 0.5483001212874583086, 0.5483144429955304489, 0.5483287647036025891, 0.5483860515358911503, 0.5486151988650457278, 0.5490734935233547720, 0.5495317881816637051, 0.5495604315978080967, 0.5495675924518441668, 0.5495747533058802370, 0.5495890750139523773, 0.5496463618462410494, 0.5497609355108182827, 0.5499900828399727493, 0.5509066721565909486, 0.5518232614732090369, 0.5520524088023635034, 0.5521096956346521756, 0.5521669824669407367, 0.5522815561315180810, 0.5527398507898271252, 0.5536564401064452134, 0.5541147347647542576, 0.5543438820939088352, 0.5544584557584860685, 0.5545157425907747406, 0.5545443860069190212, 0.5545587077149911615, 0.5545658685690272316, 0.5545730294230633017, 0.5564062080562987012, 0.5568645027146076343, 0.5569790763791848676, 0.5570363632114734287, 0.5570650066276177093, 0.5570793283356898495, 0.5570936500437619898, 0.5573227973729164564, 0.5582393866895342116, 0.5591559760061519668, 0.5593851233353063224, 0.5594996969998835556, 0.5595569838321722278, 0.5595641446862082979, 0.5595713055402443681, 0.5595856272483165084, 0.5596142706644607889, 0.5600725653227697221, 0.5605308599810786552, 0.5607600073102330107, 0.5609891546393874773, 0.5619057439560052325, 0.5620203176205824658, 0.5620489610367268574, 0.5620776044528711379, 0.5621348912851596991, 0.5623640386143141656, 0.5628223332726230987, 0.5637389225892408540 ),
 .UNSPECIFIED. ) ;
#4176=CARTESIAN_POINT ( 'NONE',  ( -4.364754663317498284, 43.33701438703417352, -12.77552687514723928 ) ) ;
#4177=CARTESIAN_POINT ( 'NONE',  ( -7.500000000000000000, 108.7270211387039183, -1.010069558262743028 ) ) ;
#4178=CARTESIAN_POINT ( 'NONE',  ( 12.99687134794458920, 60.56044921522202884, -3.651220384438404576 ) ) ;
#4181=CARTESIAN_POINT ( 'NONE',  ( 13.40455306696748927, 66.48586035906389213, -1.602499198163928273 ) ) ;
#4182=CARTESIAN_POINT ( 'NONE',  ( 3.256375548821571542, 56.79708330500473323, 13.10137511577798719 ) ) ;
#4183=CARTESIAN_POINT ( 'NONE',  ( -11.76794919243112325, 59.92999999999999972, -2.882316262207890869E-15 ) ) ;
#4184=CARTESIAN_POINT ( 'NONE',  ( 7.272992578804311492, 64.87999999999999545, -10.01041549318726709 ) ) ;
#4185=CARTESIAN_POINT ( 'NONE',  ( -9.912099458519779915, 47.28536638360703392, 9.165169439464738943 ) ) ;
#4186=CARTESIAN_POINT ( 'NONE',  ( 5.537792478938636798, 45.97909885940507024, -12.31190230144335906 ) ) ;
#4187=CARTESIAN_POINT ( 'NONE',  ( 0.000000000000000000, 80.93000000000000682, 0.000000000000000000 ) ) ;
#4192=EDGE_CURVE ( 'NONE', #12894, #14883, #16604, .T. ) ;
#4193=CYLINDRICAL_SURFACE ( 'NONE', #10084, 4.000000000000003553 ) ;
#4194=CARTESIAN_POINT ( 'NONE',  ( 13.35406747998390564, 33.36045359896084506, 1.984711021133432896 ) ) ;
#4197=ORIENTED_EDGE ( 'NONE', *, *, #11562, .T. ) ;
#4198=CARTESIAN_POINT ( 'NONE',  ( -8.343458848123582072, 43.38000000000000256, 11.48378591275253768 ) ) ;
#4200=CARTESIAN_POINT ( 'NONE',  ( -13.47061399229918344, 40.89918744336559797, -0.8931361110388874591 ) ) ;
#4203=CARTESIAN_POINT ( 'NONE',  ( -12.08847575587519074, 44.15120909323470499, 6.010142657089093454 ) ) ;
#4205=CARTESIAN_POINT ( 'NONE',  ( -8.343458848123582072, 41.38000000000000256, 11.48378591275254124 ) ) ;
#4206=CARTESIAN_POINT ( 'NONE',  ( -13.42488017928338628, 70.88049257656408031, -1.423317239027405590 ) ) ;
#4208=CARTESIAN_POINT ( 'NONE',  ( -1.260278075713701318, 67.22531399419105469, -13.44469158219603422 ) ) ;
#4210=CARTESIAN_POINT ( 'NONE',  ( 13.49413416657210085, 54.44402071019561618, -0.4078984894991014576 ) ) ;
#4212=CARTESIAN_POINT ( 'NONE',  ( -11.35960375279439738, 64.65661637531263750, -7.297776375780255620 ) ) ;
#4213=VERTEX_POINT ( 'NONE', #16506 ) ;
#4214=CARTESIAN_POINT ( 'NONE',  ( -12.66168252233810421, 35.09958735483692749, 4.686808648749069661 ) ) ;
#4215=ORIENTED_EDGE ( 'NONE', *, *, #617, .T. ) ;
#4216=CARTESIAN_POINT ( 'NONE',  ( 12.87051123520935825, 78.28367826617611058, 4.074318883512994205 ) ) ;
#4218=CARTESIAN_POINT ( 'NONE',  ( -7.845105219487623849, 31.47600457549274466, -10.98698378474273696 ) ) ;
#4219=CARTESIAN_POINT ( 'NONE',  ( 8.220432041259709166, 72.86719779332030100, -10.70875809315417548 ) ) ;
#4222=CARTESIAN_POINT ( 'NONE',  ( 8.343458848123578520, 71.98000000000000398, 11.48378591275254124 ) ) ;
#4223=CARTESIAN_POINT ( 'NONE',  ( -12.11224912280836108, 53.14936213474186388, 5.963634143833839829 ) ) ;
#4226=CARTESIAN_POINT ( 'NONE',  ( 11.76794919243112680, 52.57999999999999119, -3.823638476888993942 ) ) ;
#4227=CARTESIAN_POINT ( 'NONE',  ( -8.691771469529815392E-16, 64.68000000000000682, 14.19474002721660355 ) ) ;
#4229=CARTESIAN_POINT ( 'NONE',  ( 4.953436321318733349, 68.85867169319138270, 12.55852084432367732 ) ) ;
#4230=CARTESIAN_POINT ( 'NONE',  ( -4.183764169839751190, 37.33043068766654926, -12.83544830047670082 ) ) ;
#4232=CARTESIAN_POINT ( 'NONE',  ( 5.574118405682551014, 35.88201004368047364, 12.30340700596329917 ) ) ;
#4234=CARTESIAN_POINT ( 'NONE',  ( -12.73921229380289155, 74.09290750163174266, 4.517609494197782460 ) ) ;
#4236=CARTESIAN_POINT ( 'NONE',  ( -12.05845239338915320, 76.70338954954424082, -6.158670844540059974 ) ) ;
#4237=CARTESIAN_POINT ( 'NONE',  ( -4.342137793289712278, 79.33615335351939279, -12.78264298514469210 ) ) ;
#4242=CARTESIAN_POINT ( 'NONE',  ( 2.272985001014427393E-15, 47.17999999999999972, -12.37355403259654807 ) ) ;
#4244=CARTESIAN_POINT ( 'NONE',  ( -1.111710639975107329, 34.21993612021496745, -13.46167583268210244 ) ) ;
#4245=CARTESIAN_POINT ( 'NONE',  ( 13.48545920529975284, 75.45158341798384072, -0.6264344526569241012 ) ) ;
#4248=CARTESIAN_POINT ( 'NONE',  ( -7.272992578804307939, 35.47999999999999687, -10.01041549318726886 ) ) ;
#4249=CARTESIAN_POINT ( 'NONE',  ( -11.16896011296937985, 41.21521864355013065, 7.583167778474193987 ) ) ;
#4250=CIRCLE ( 'NONE', #10474, 8.999999999999998224 ) ;
#4251=CARTESIAN_POINT ( 'NONE',  ( 10.97408553220991578, 51.72700490979467958, -7.865491942308953988 ) ) ;
#4252=CARTESIAN_POINT ( 'NONE',  ( 5.900366410768304704, 44.89475997489012826, 12.14732960817785390 ) ) ;
#4253=CARTESIAN_POINT ( 'NONE',  ( 13.50000000000000000, 59.42999999999999972, 1.653273178848926867E-15 ) ) ;
#4255=CARTESIAN_POINT ( 'NONE',  ( -2.138189944381279073, 57.25688142232026223, -13.49999999999998579 ) ) ;
#4256=CARTESIAN_POINT ( 'NONE',  ( -13.07794080639409273, 49.80669500938279270, -3.469076081897399799 ) ) ;
#4257=CARTESIAN_POINT ( 'NONE',  ( 13.14224245847790584, 63.31794964476952714, 3.160171244385233447 ) ) ;
#4258=CARTESIAN_POINT ( 'NONE',  ( 13.48432407896599727, 42.40750944205898065, 0.6513807325604739074 ) ) ;
#4259=CARTESIAN_POINT ( 'NONE',  ( 2.495622557441647960, 38.76969659664788992, 13.26920102393307133 ) ) ;
#4260=EDGE_LOOP ( 'NONE', ( #6579, #5444 ) ) ;
#4261=CARTESIAN_POINT ( 'NONE',  ( -2.501400086087330887, 70.26993977764597332, -13.26633446808875405 ) ) ;
#4262=CARTESIAN_POINT ( 'NONE',  ( -8.891200544363830713E-16, 55.67999999999999972, 13.50000000000000000 ) ) ;
#4264=EDGE_LOOP ( 'NONE', ( #10641, #17272, #12349, #9847 ) ) ;
#4265=CARTESIAN_POINT ( 'NONE',  ( -8.671810352671009525, 43.51358743475483237, -10.34650997788421378 ) ) ;
#4266=CARTESIAN_POINT ( 'NONE',  ( -7.500000000000000000, 107.5003227710673315, -6.479247348114220983 ) ) ;
#4267=CARTESIAN_POINT ( 'NONE',  ( 13.42672319008129733, 60.48085777008815711, -1.461561770537686655 ) ) ;
#4269=CARTESIAN_POINT ( 'NONE',  ( 0.000000000000000000, 75.00000000000000000, 0.000000000000000000 ) ) ;
#4270=CARTESIAN_POINT ( 'NONE',  ( 13.47174093492468572, 66.39920212035603697, 0.8849161873603186290 ) ) ;
#4271=CARTESIAN_POINT ( 'NONE',  ( 3.251687347492562274, 56.79691776447067042, 13.10253915792208090 ) ) ;
#4272=EDGE_CURVE ( 'NONE', #14369, #10721, #3571, .T. ) ;
#4273=CARTESIAN_POINT ( 'NONE',  ( 3.636496289402154414, 57.82999999999999829, 11.19198476289190936 ) ) ;
#4274=CARTESIAN_POINT ( 'NONE',  ( 9.520470885617717371, 64.72999999999998977, -6.917026985038131848 ) ) ;
#4275=CARTESIAN_POINT ( 'NONE',  ( -12.19111560182831688, 47.14291408922787951, 5.800482751556255145 ) ) ;
#4278=CARTESIAN_POINT ( 'NONE',  ( 10.50560174212768239, 30.75358953031270204, -8.478557939404936405 ) ) ;
#4279=CARTESIAN_POINT ( 'NONE',  ( -1.773934221698072244, 56.61635730958409596, 13.38478979355031662 ) ) ;
#4282=CARTESIAN_POINT ( 'NONE',  ( 13.32051220209429054, 33.35292530209495965, 2.195222926766236871 ) ) ;
#4291=CARTESIAN_POINT ( 'NONE',  ( -13.47250643389561731, 43.90011943282842566, -0.8628561982218695414 ) ) ;
#4293=CARTESIAN_POINT ( 'NONE',  ( -13.50000000000000000, 34.92999999999999261, -3.306546357697853733E-15 ) ) ;
#4294=EDGE_CURVE ( 'NONE', #5101, #13300, #2700, .T. ) ;
#4296=CARTESIAN_POINT ( 'NONE',  ( -10.73144679257710443, 67.61893913152461266, -8.194928624396487393 ) ) ;
#4298=AXIS2_PLACEMENT_3D ( 'NONE', #3314, #6162, #13038 ) ;
#4299=CARTESIAN_POINT ( 'NONE',  ( 13.19823589370220418, 54.32922229573070894, 2.848376102529405873 ) ) ;
#4300=CARTESIAN_POINT ( 'NONE',  ( -10.30332649398041589, 64.59537434288125723, -8.723052715348487141 ) ) ;
#4302=CARTESIAN_POINT ( 'NONE',  ( -13.33433074695494902, 35.00395194388527642, 2.108614894658309868 ) ) ;
#4304=CARTESIAN_POINT ( 'NONE',  ( 13.40182142610995264, 78.37333532350689325, 1.625185903533163501 ) ) ;
#4306=CARTESIAN_POINT ( 'NONE',  ( -10.92172942406179104, 37.22999999999999687, 7.935100905948387684 ) ) ;
#4307=CARTESIAN_POINT ( 'NONE',  ( 9.054673339175000280, 72.82854102722255618, -10.02701106865682945 ) ) ;
#4308=CARTESIAN_POINT ( 'NONE',  ( 6.571298569607622042, 59.92192712267667076, 11.79271934300702895 ) ) ;
#4310=CARTESIAN_POINT ( 'NONE',  ( -8.343458848123576743, 61.47999999999999687, -11.48378591275254301 ) ) ;
#4311=CARTESIAN_POINT ( 'NONE',  ( -11.22131014912690539, 52.64801998336128008, -7.505488620872328376 ) ) ;
#4314=CARTESIAN_POINT ( 'NONE',  ( -9.520470885617715595, 35.62999999999999545, -6.917026985038136289 ) ) ;
#4315=CARTESIAN_POINT ( 'NONE',  ( 13.50000000000000000, 62.42999999999999972, 1.653273178848926867E-15 ) ) ;
#4316=CARTESIAN_POINT ( 'NONE',  ( 1.538791601217685434, 50.73532928937410702, 13.41201501813375785 ) ) ;
#4317=CARTESIAN_POINT ( 'NONE',  ( 10.73231909348931623, 69.11905621171094083, 8.192208697413700946 ) ) ;
#4318=CARTESIAN_POINT ( 'NONE',  ( -3.763716488224063461, 37.31531146090827633, -12.96716657343995927 ) ) ;
#4321=CARTESIAN_POINT ( 'NONE',  ( -13.25722080889316956, 74.02023315977538687, 2.559143689761975704 ) ) ;
#4323=CARTESIAN_POINT ( 'NONE',  ( -4.728261339063823065, 76.35029506892772133, -12.64499010195072515 ) ) ;
#4327=CARTESIAN_POINT ( 'NONE',  ( -10.98210873310329028, 80.93000000000000682, 5.183560256204878591 ) ) ;
#4330=CARTESIAN_POINT ( 'NONE',  ( -3.636496289402155746, 45.53000000000000114, 11.19198476289190936 ) ) ;
#4333=CARTESIAN_POINT ( 'NONE',  ( 12.24585265403194256, 75.22174939294195894, 5.682387988859129102 ) ) ;
#4335=DIRECTION ( 'NONE',  ( 0.000000000000000000, 0.000000000000000000, 1.000000000000000000 ) ) ;
#4336=CARTESIAN_POINT ( 'NONE',  ( -12.55122207835515447, 41.11055379480070826, 4.971617317440445660 ) ) ;
#4337=CARTESIAN_POINT ( 'NONE',  ( 4.734980970745145790, 52.00945447310526504, -12.64239079011760403 ) ) ;
#4338=CARTESIAN_POINT ( 'NONE',  ( -2.901612525891934080, 38.57569620751132788, 13.19105549594109306 ) ) ;
#4342=CARTESIAN_POINT ( 'NONE',  ( -7.375934228542610605, 49.45559395763999078, -11.30689537173397596 ) ) ;
#4343=CARTESIAN_POINT ( 'NONE',  ( 9.615610945565020273, 63.05944476093819162, 9.475759931419338145 ) ) ;
#4344=CARTESIAN_POINT ( 'NONE',  ( 13.47794799030919677, 42.40337696373789811, 0.7719109943771497173 ) ) ;
#4346=EDGE_CURVE ( 'NONE', #4960, #2740, #13211, .T. ) ;
#4348=CARTESIAN_POINT ( 'NONE',  ( -3.636496289402155746, 78.53000000000000114, 11.19198476289190936 ) ) ;
#4353=CARTESIAN_POINT ( 'NONE',  ( -8.581213741271680462, 43.50935130007908924, -10.42230493472992414 ) ) ;
#4354=CARTESIAN_POINT ( 'NONE',  ( -7.499999999999999112, 108.1112172271399885, -5.064597142177449385 ) ) ;
#4355=CARTESIAN_POINT ( 'NONE',  ( 10.53104951465778072, 60.75217764884847327, -8.446732320805995897 ) ) ;
#4357=DIRECTION ( 'NONE',  ( 0.000000000000000000, -1.000000000000000000, 0.000000000000000000 ) ) ;
#4358=CARTESIAN_POINT ( 'NONE',  ( 11.56614369255154884, 66.68953821447213670, -6.962363570687350567 ) ) ;
#4359=CARTESIAN_POINT ( 'NONE',  ( 0.9172422442983635404, 56.71299257732687948, 13.47663206627262866 ) ) ;
#4360=CARTESIAN_POINT ( 'NONE',  ( 3.636496289402154414, 54.83000000000000540, 11.19198476289190936 ) ) ;
#4361=CARTESIAN_POINT ( 'NONE',  ( -7.576616670048093940E-16, 63.67999999999997840, 12.37355403259654985 ) ) ;
#4362=CARTESIAN_POINT ( 'NONE',  ( -13.31335613090667636, 46.85142544004738596, -2.237095574266806164 ) ) ;
#4364=CARTESIAN_POINT ( 'NONE',  ( 13.11257284244564758, 45.54411236249859485, -3.211077615855648659 ) ) ;
#4365=DIRECTION ( 'NONE',  ( 0.000000000000000000, -1.000000000000000000, 0.000000000000000000 ) ) ;
#4367=CARTESIAN_POINT ( 'NONE',  ( 11.52463669016155023, 30.69249958188942173, -7.032419985331740619 ) ) ;
#4368=CARTESIAN_POINT ( 'NONE',  ( -8.872232410392204116, 56.33699134164967859, 10.17624346630946164 ) ) ;
#4370=FACE_OUTER_BOUND ( 'NONE', #6840, .T. ) ;
#4372=CARTESIAN_POINT ( 'NONE',  ( 4.044151295397504953, 32.82541237245334997, 12.88009870303249649 ) ) ;
#4374=CARTESIAN_POINT ( 'NONE',  ( 4.326427921100060026, 40.02441582939385256, -12.78796848161989530 ) ) ;
#4375=EDGE_CURVE ( 'NONE', #13131, #6792, #923, .T. ) ;
#4376=ORIENTED_EDGE ( 'NONE', *, *, #16117, .T. ) ;
#4377=CARTESIAN_POINT ( 'NONE',  ( -3.904307695423253843, 62.53961551243608596, 12.92310544161152208 ) ) ;
#4381=CARTESIAN_POINT ( 'NONE',  ( -13.39575438633939974, 43.86970701691569730, -1.729825961451170180 ) ) ;
#4383=CARTESIAN_POINT ( 'NONE',  ( 13.50000000000000000, 30.42999999999999972, 1.653273178848926867E-15 ) ) ;
#4384=CARTESIAN_POINT ( 'NONE',  ( -6.062686308920030243, 46.40130649435582910, -12.06266578976461368 ) ) ;
#4385=CARTESIAN_POINT ( 'NONE',  ( -5.384922564330007155, 67.37499116741884109, -12.38015867815493820 ) ) ;
#4387=CARTESIAN_POINT ( 'NONE',  ( 12.98213763223733430, 54.56239296006683759, -3.703273827960795295 ) ) ;
#4388=CARTESIAN_POINT ( 'NONE',  ( -10.73392024359467278, 64.61856367689141223, -8.199116172563279292 ) ) ;
#4392=CARTESIAN_POINT ( 'NONE',  ( -13.11532218737669275, 34.81618246207430900, -3.203318699896558375 ) ) ;
#4395=CARTESIAN_POINT ( 'NONE',  ( 13.06826610077310669, 78.55061381712845048, -3.386803558175533357 ) ) ;
#4398=CARTESIAN_POINT ( 'NONE',  ( 10.22275275003651807, 72.76898976254949503, -8.817758165833254225 ) ) ;
#4399=CARTESIAN_POINT ( 'NONE',  ( 4.773719326841550092, 79.00791013106511684, -12.62843301006502195 ) ) ;
#4402=CARTESIAN_POINT ( 'NONE',  ( 8.343458848123578520, 59.97999999999998977, 11.48378591275254124 ) ) ;
#4403=CARTESIAN_POINT ( 'NONE',  ( -13.45103708625743977, 52.96991811583343690, 1.151443694251493843 ) ) ;
#4404=CARTESIAN_POINT ( 'NONE',  ( 7.272992578804308828, 42.97999999999998977, 10.01041549318726709 ) ) ;
#4406=CARTESIAN_POINT ( 'NONE',  ( -13.50000000000000000, 57.92999999999999972, -3.306546357697853733E-15 ) ) ;
#4407=DIRECTION ( 'NONE',  ( 0.000000000000000000, 1.000000000000000000, 0.000000000000000000 ) ) ;
#4409=CARTESIAN_POINT ( 'NONE',  ( 5.415421185760910028, 68.87609980712950630, 12.37010947186780463 ) ) ;
#4413=CARTESIAN_POINT ( 'NONE',  ( -12.19220406405763590, 73.71653302039153743, -5.818182159799721198 ) ) ;
#4415=CARTESIAN_POINT ( 'NONE',  ( -4.565779138216930377, 76.34430483734830375, -12.70460796047683694 ) ) ;
#4416=EDGE_CURVE ( 'NONE', #10663, #11531, #6347, .T. ) ;
#4417=CARTESIAN_POINT ( 'NONE',  ( -12.50000000000000000, 98.93000000000002103, 1.224646799147353059E-15 ) ) ;
#4419=CARTESIAN_POINT ( 'NONE',  ( 2.150159292860174709, 80.93000000000003524, 13.03677673010521687 ) ) ;
#4422=CARTESIAN_POINT ( 'NONE',  ( 2.272985001014427393E-15, 41.17999999999999972, -12.37355403259654807 ) ) ;
#4424=CARTESIAN_POINT ( 'NONE',  ( -1.609251342409827590, 32.62215026715757205, 13.40374960566758311 ) ) ;
#4425=CARTESIAN_POINT ( 'NONE',  ( 11.64814124600084000, 75.17585265429842423, 6.829356019357755159 ) ) ;
#4429=CARTESIAN_POINT ( 'NONE',  ( 8.343458848123583849, 80.88000000000000966, -11.48378591275253768 ) ) ;
#4430=CARTESIAN_POINT ( 'NONE',  ( 7.976956726953756238, 51.87815718135391307, -10.89215259667266622 ) ) ;
#4431=( BOUNDED_CURVE ( )  B_SPLINE_CURVE ( 2, ( #8865, #14217, #6379, #11762, #2190, #8945, #14133, #4868, #15713, #6466, #10271, #12825, #5047 ),
 .UNSPECIFIED., .F., .F. ) 
 B_SPLINE_CURVE_WITH_KNOTS ( ( 3, 2, 2, 2, 2, 2, 3 ),
 ( 0.4305555555555555247, 0.4333333333333333481, 0.4388888888888888840, 0.4444444444444444198, 0.4500000000000000111, 0.4555555555555555469, 0.4583333333333333148 ),
 .UNSPECIFIED. ) 
 CURVE ( )  GEOMETRIC_REPRESENTATION_ITEM ( )  RATIONAL_B_SPLINE_CURVE ( ( 0.9755282581475768211, 0.9755282581475765991, 1.000000000000000000, 0.9510565162951535312, 1.000000000000000000, 0.9510565162951535312, 1.000000000000000000, 0.9510565162951535312, 1.000000000000000000, 0.9510565162951535312, 1.000000000000000000, 0.9755282581475770431, 0.9755282581475768211 ) ) 
 REPRESENTATION_ITEM ( '' )  );
#4433=CARTESIAN_POINT ( 'NONE',  ( 5.716269257680778537, 36.97215740540831064, -12.23006940680748933 ) ) ;
#4434=CARTESIAN_POINT ( 'NONE',  ( -10.92172942406179104, 58.23000000000000398, 7.935100905948387684 ) ) ;
#4435=CARTESIAN_POINT ( 'NONE',  ( -1.376415865686975826, 49.22940551379771534, -13.43194262913766579 ) ) ;
#4436=CARTESIAN_POINT ( 'NONE',  ( 11.18930872728590842, 63.14597851813704210, 7.560098781496484399 ) ) ;
#4437=CARTESIAN_POINT ( 'NONE',  ( 13.48225451615983772, 42.40611353782374948, 0.6920966954215841405 ) ) ;
#4438=CARTESIAN_POINT ( 'NONE',  ( 7.427339947964860301, 48.90222951860057066, -11.27838517315750799 ) ) ;
#4441=CARTESIAN_POINT ( 'NONE',  ( -11.76794919243112325, 69.07999999999999829, 3.823638476888994830 ) ) ;
#4446=CARTESIAN_POINT ( 'NONE',  ( -4.805598482947267769, 43.35318775884549325, -12.61785274320682149 ) ) ;
#4447=CARTESIAN_POINT ( 'NONE',  ( -7.499999999999998224, 108.7391404411723244, 0.5315352956498785586 ) ) ;
#4448=CARTESIAN_POINT ( 'NONE',  ( 8.246934402308351508, 60.86644310941438363, -10.69753009404646704 ) ) ;
#4451=CARTESIAN_POINT ( 'NONE',  ( 9.297651317836157503, 66.04322071083470291, 9.806469248494018132 ) ) ;
#4452=CARTESIAN_POINT ( 'NONE',  ( 5.359754162089569007, 56.87398751003383524, 12.39402400664639003 ) ) ;
#4453=CARTESIAN_POINT ( 'NONE',  ( 9.520470885617717371, 61.72999999999999687, -6.917026985038131848 ) ) ;
#4454=CARTESIAN_POINT ( 'NONE',  ( 3.636496289402154414, 69.82999999999999829, 11.19198476289190936 ) ) ;
#4455=CARTESIAN_POINT ( 'NONE',  ( -12.45694272784634471, 46.74046472961560994, -5.203717773247669598 ) ) ;
#4457=CARTESIAN_POINT ( 'NONE',  ( 10.24454763814321190, 45.76800118563600250, -8.800910918144792205 ) ) ;
#4460=CARTESIAN_POINT ( 'NONE',  ( 8.403316352008756596, 30.85885728073062140, -10.56577960906128055 ) ) ;
#4461=CARTESIAN_POINT ( 'NONE',  ( -8.574071495653086572, 56.35097050867326374, 10.42766517367652312 ) ) ;
#4464=CARTESIAN_POINT ( 'NONE',  ( 12.13288869186091645, 33.20991524044760013, 5.984383512105693192 ) ) ;
#4466=CARTESIAN_POINT ( 'NONE',  ( 4.433426395804998421, 40.02052604634783251, -12.75131370640142059 ) ) ;
#4468=ORIENTED_EDGE ( 'NONE', *, *, #10645, .T. ) ;
#4469=CARTESIAN_POINT ( 'NONE',  ( -12.73589991630869100, 62.09160515021331861, 4.477510439207101456 ) ) ;
#4473=CARTESIAN_POINT ( 'NONE',  ( -12.73615524967575574, 43.76842681669471347, -4.476659004287373733 ) ) ;
#4475=CARTESIAN_POINT ( 'NONE',  ( -4.171729424061787483, 34.32999999999999829, -12.83926296998457417 ) ) ;
#4476=CARTESIAN_POINT ( 'NONE',  ( -8.343458848123582072, 46.37999999999999545, 11.48378591275254124 ) ) ;
#4477=CARTESIAN_POINT ( 'NONE',  ( -1.937690227285938205, 46.24965744208711982, -13.36137179930980778 ) ) ;
#4478=CARTESIAN_POINT ( 'NONE',  ( -2.917897579637011241, 67.28493650261737002, -13.18089723172849403 ) ) ;
#4480=CARTESIAN_POINT ( 'NONE',  ( 10.76214398255494586, 54.12080488597943173, 8.150716040728196887 ) ) ;
#4481=CARTESIAN_POINT ( 'NONE',  ( -0.4982172014182387754, 64.19791404813746283, -13.49082082228690638 ) ) ;
#4483=CARTESIAN_POINT ( 'NONE',  ( -10.04923048958269405, 34.58189789653238932, -9.015230755480622804 ) ) ;
#4485=CARTESIAN_POINT ( 'NONE',  ( 13.40746492369621556, 78.48656952345000093, -1.623796509401284283 ) ) ;
#4488=CARTESIAN_POINT ( 'NONE',  ( 12.96587728178895738, 72.56450825003899752, -3.759848239116166280 ) ) ;
#4490=CARTESIAN_POINT ( 'NONE',  ( -10.92172942406179104, 59.22999999999999687, 7.935100905948387684 ) ) ;
#4491=CARTESIAN_POINT ( 'NONE',  ( -1.175964444707957579, 71.63773400114577328, 13.45120314782261772 ) ) ;
#4492=EDGE_CURVE ( 'NONE', #17443, #12574, #12063, .T. ) ;
#4493=CARTESIAN_POINT ( 'NONE',  ( -11.76794919243112325, 35.92999999999999972, -2.882316262207890869E-15 ) ) ;
#4494=CARTESIAN_POINT ( 'NONE',  ( -8.343458848123576743, 54.48000000000000398, -11.48378591275254301 ) ) ;
#4495=EDGE_CURVE ( 'NONE', #6493, #13300, #16020, .T. ) ;
#4497=STYLED_ITEM('',(#17519),#8814);
#4499=CARTESIAN_POINT ( 'NONE',  ( 10.86192711411459122, 69.12653421500604622, 8.016776366340984339 ) ) ;
#4501=CARTESIAN_POINT ( 'NONE',  ( -2.138189944381230223, 73.60311857767972299, 13.50000000000000178 ) ) ;
#4503=CARTESIAN_POINT ( 'NONE',  ( -11.39092472967678837, 73.65879597142989610, -7.245477644767023939 ) ) ;
#4504=CARTESIAN_POINT ( 'NONE',  ( -2.389462197225028728, 76.26591624804247260, -13.28685410492694530 ) ) ;
#4510=CARTESIAN_POINT ( 'NONE',  ( -3.636496289402153081, 35.32999999999999829, -11.19198476289190936 ) ) ;
#4512=CARTESIAN_POINT ( 'NONE',  ( 8.311262620771346477, 74.99693123154169427, 10.63835658022000707 ) ) ;
#4514=CARTESIAN_POINT ( 'NONE',  ( 9.520470885617717371, 34.72999999999999687, -6.917026985038131848 ) ) ;
#4515=CARTESIAN_POINT ( 'NONE',  ( -9.520470885617715595, 32.63000000000000256, -6.917026985038136289 ) ) ;
#4516=EDGE_CURVE ( 'NONE', #14499, #16836, #6691, .T. ) ;
#4517=CARTESIAN_POINT ( 'NONE',  ( 4.761726286637288474, 52.00846422156020310, -12.63236328405458408 ) ) ;
#4518=CARTESIAN_POINT ( 'NONE',  ( -1.596087918524577542, 38.62259808071801359, 13.40533364316977760 ) ) ;
#4519=LINE ( 'NONE', #5943, #17106 ) ;
#4521=CARTESIAN_POINT ( 'NONE',  ( -2.559407043143859806, 49.27189254790160788, -13.26134293993454705 ) ) ;
#4522=CARTESIAN_POINT ( 'NONE',  ( 4.408271315188386552, 62.83777092602397829, 12.79017921344417097 ) ) ;
#4523=CARTESIAN_POINT ( 'NONE',  ( 13.32680416487845321, 42.35436111799107550, 2.155617169667197963 ) ) ;
#4524=CARTESIAN_POINT ( 'NONE',  ( 8.550215766970532982, 48.85207767227580433, -10.44719490448041022 ) ) ;
#4527=CARTESIAN_POINT ( 'NONE',  ( -3.636496289402153081, 68.32999999999999829, -11.19198476289190936 ) ) ;
#4532=CARTESIAN_POINT ( 'NONE',  ( -0.006952547203360656333, 43.18024923986452279, -13.49999999219945934 ) ) ;
#4536=CARTESIAN_POINT ( 'NONE',  ( 11.81479127198460155, 66.18791984854836130, 6.531537704173645764 ) ) ;
#4538=CARTESIAN_POINT ( 'NONE',  ( 8.254427490791934829, 56.99432593801493852, 10.68333636219931293 ) ) ;
#4539=CARTESIAN_POINT ( 'NONE',  ( -11.76794919243112325, 63.07999999999999119, 3.823638476888994386 ) ) ;
#4540=CARTESIAN_POINT ( 'NONE',  ( 8.343458848123583849, 32.88000000000000256, -11.48378591275253768 ) ) ;
#4541=CARTESIAN_POINT ( 'NONE',  ( -3.636496289402155746, 69.53000000000001535, 11.19198476289190936 ) ) ;
#4543=CARTESIAN_POINT ( 'NONE',  ( -12.56761561834811403, 46.75105081705815735, -4.930021005048375926 ) ) ;
#4544=CARTESIAN_POINT ( 'NONE',  ( 9.264981600666393646, 45.81801372893175284, -9.819209257909990995 ) ) ;
#4547=CARTESIAN_POINT ( 'NONE',  ( 0.6446146492995459276, 31.15683549778061234, -13.48678750428668494 ) ) ;
#4548=CARTESIAN_POINT ( 'NONE',  ( -10.17582679281236935, 56.27190818227264657, 8.882075982020387173 ) ) ;
#4549=DIRECTION ( 'NONE',  ( -3.552713678800500929E-15, 0.000000000000000000, 1.000000000000000000 ) ) ;
#4550=CARTESIAN_POINT ( 'NONE',  ( 0.9449016496340574278, 32.71398372948575428, 13.46769545381985012 ) ) ;
#4552=CARTESIAN_POINT ( 'NONE',  ( 10.54603764524003040, 39.75142172891366954, -8.431702247120188787 ) ) ;
#4555=CARTESIAN_POINT ( 'NONE',  ( -13.46566103132326297, 61.96328914063155224, 0.9623097876522905825 ) ) ;
#4556=VERTEX_POINT ( 'NONE', #11806 ) ;
#4558=CARTESIAN_POINT ( 'NONE',  ( 10.70843530424569856, 48.11775999830372541, 8.220672230353347487 ) ) ;
#4559=CARTESIAN_POINT ( 'NONE',  ( -8.891200544363830713E-16, 64.67999999999999261, 13.50000000000000000 ) ) ;
#4560=CARTESIAN_POINT ( 'NONE',  ( -10.92172942406178926, 34.62999999999999545, -7.935100905948389460 ) ) ;
#4561=CARTESIAN_POINT ( 'NONE',  ( -10.92172942406179104, 40.23000000000000398, 7.935100905948387684 ) ) ;
#4562=CARTESIAN_POINT ( 'NONE',  ( -2.198120649712783869, 46.25903117140494203, -13.32013477985053918 ) ) ;
#4563=CARTESIAN_POINT ( 'NONE',  ( -2.264496491277277812, 67.26149511457354890, -13.31769803748488279 ) ) ;
#4565=CARTESIAN_POINT ( 'NONE',  ( 6.801677017248844770, 53.93148548877682202, 11.66148778661555951 ) ) ;
#4566=VERTEX_POINT ( 'NONE', #1098 ) ;
#4567=CARTESIAN_POINT ( 'NONE',  ( -0.1481528981132104184, 64.18532703164794384, -13.49999999999999645 ) ) ;
#4571=CARTESIAN_POINT ( 'NONE',  ( -9.956290844395114803, 34.57701004435445924, -9.118751552402068583 ) ) ;
#4573=CARTESIAN_POINT ( 'NONE',  ( 13.07345783715813603, 78.54986944972205265, -3.366722508972363581 ) ) ;
#4577=CARTESIAN_POINT ( 'NONE',  ( 13.35802549108727000, 72.36165858179914778, 1.953960687672332108 ) ) ;
#4579=CARTESIAN_POINT ( 'NONE',  ( -4.171729424061791036, 65.53000000000000114, 12.83926296998457239 ) ) ;
#4580=CARTESIAN_POINT ( 'NONE',  ( -8.831087761643750866, 52.52108727616624151, -10.21087246435311435 ) ) ;
#4581=CARTESIAN_POINT ( 'NONE',  ( -3.636496289402153081, 35.32999999999999829, -11.19198476289190936 ) ) ;
#4582=CARTESIAN_POINT ( 'NONE',  ( -13.50000000000000000, 54.92999999999999972, -3.306546357697853733E-15 ) ) ;
#4584=PLANE ( 'NONE',  #3342 ) ;
#4586=CARTESIAN_POINT ( 'NONE',  ( 10.00340607087883349, 69.07939772179537385, 9.065424430625297347 ) ) ;
#4587=FACE_OUTER_BOUND ( 'NONE', #13999, .T. ) ;
#4590=CARTESIAN_POINT ( 'NONE',  ( -10.86631776481396905, 73.62653164792240545, -8.015947894086419723 ) ) ;
#4591=CARTESIAN_POINT ( 'NONE',  ( -7.225584998327790665, 76.44917738724952017, -11.40355617289543844 ) ) ;
#4596=EDGE_CURVE ( 'NONE', #19, #902, #5002, .T. ) ;
#4597=CARTESIAN_POINT ( 'NONE',  ( -11.76794919243112325, 38.92999999999999972, -2.882316262207890869E-15 ) ) ;
#4599=CARTESIAN_POINT ( 'NONE',  ( -7.124089981346021005, 32.41512088030167149, 11.46724091227400955 ) ) ;
#4600=CARTESIAN_POINT ( 'NONE',  ( 4.878482463424276716, 74.85599699807477236, 12.59450660046991999 ) ) ;
#4601=CARTESIAN_POINT ( 'NONE',  ( 8.343458848123580296, 61.97999999999999687, 11.48378591275253768 ) ) ;
#4603=CARTESIAN_POINT ( 'NONE',  ( -10.92172942406179104, 82.23000000000000398, 7.935100905948387684 ) ) ;
#4604=CARTESIAN_POINT ( 'NONE',  ( 10.04308425913412250, 51.77851858841606969, -9.021445512424994817 ) ) ;
#4605=CARTESIAN_POINT ( 'NONE',  ( -6.476206340861387467, 38.44199689924342778, 11.84763527750397394 ) ) ;
#4606=CARTESIAN_POINT ( 'NONE',  ( 8.074219154787348529, 36.87380170060612983, -10.82003361857776547 ) ) ;
#4608=CARTESIAN_POINT ( 'NONE',  ( -4.136362903238101296, 49.32872232693532055, -12.85098559761272874 ) ) ;
#4609=CARTESIAN_POINT ( 'NONE',  ( 2.690935862572700010, 62.77670372775656915, 13.22909870504613927 ) ) ;
#4610=CARTESIAN_POINT ( 'NONE',  ( -11.76794919243112325, 80.92999999999767624, -5.919446256302011733E-11 ) ) ;
#4611=CARTESIAN_POINT ( 'NONE',  ( 12.99504019031924962, 48.56107377554576487, -3.664513708583787110 ) ) ;
#4614=CARTESIAN_POINT ( 'NONE',  ( -3.636496289402153081, 65.32999999999999829, -11.19198476289190936 ) ) ;
#4618=ADVANCED_FACE ( 'NONE', ( #5095 ), #10487, .T. ) ;
#4619=CARTESIAN_POINT ( 'NONE',  ( -1.849123144677635722, 43.24648372408316277, -13.37408686090705956 ) ) ;
#4620=CARTESIAN_POINT ( 'NONE',  ( 0.8082646707930503105, 76.15093783529552240, -13.47583662643777913 ) ) ;
#4623=CARTESIAN_POINT ( 'NONE',  ( 5.725467330485540352, 65.88816334722764623, 12.22575439232458727 ) ) ;
#4624=CARTESIAN_POINT ( 'NONE',  ( -13.50000000000000000, 82.93000000000000682, -3.306546357697853733E-15 ) ) ;
#4625=CARTESIAN_POINT ( 'NONE',  ( -11.76794919243112325, 54.07999999999999119, 3.823638476888994386 ) ) ;
#4626=CARTESIAN_POINT ( 'NONE',  ( 2.607531440858944223E-15, 33.17999999999999261, -14.19474002721660355 ) ) ;
#4627=CARTESIAN_POINT ( 'NONE',  ( -11.76794919243112325, 57.07999999999999829, 3.823638476888994386 ) ) ;
#4628=CARTESIAN_POINT ( 'NONE',  ( -13.22621774997404920, 47.02780800035617403, 2.761248823199535796 ) ) ;
#4629=CARTESIAN_POINT ( 'NONE',  ( 9.091354351312018522, 45.82646639924907106, -9.980085113653212048 ) ) ;
#4630=CARTESIAN_POINT ( 'NONE',  ( 8.426818388819521388, 69.85781622895851228, -10.54854181807195879 ) ) ;
#4632=CARTESIAN_POINT ( 'NONE',  ( 10.37303206245883302, 30.76086691204845991, -8.640359589916528193 ) ) ;
#4633=CARTESIAN_POINT ( 'NONE',  ( -12.38444555254770485, 55.73389167458477544, -5.378193122225002121 ) ) ;
#4634=CARTESIAN_POINT ( 'NONE',  ( 2.138189944381242213, 54.10311857767973009, -13.49999999999999822 ) ) ;
#4635=CARTESIAN_POINT ( 'NONE',  ( 7.123395093792429300, 32.94489533744902587, 11.46981911532503240 ) ) ;
#4636=CARTESIAN_POINT ( 'NONE',  ( 2.911951681939318970, 43.07529696608821723, -13.18220571944093500 ) ) ;
#4637=CARTESIAN_POINT ( 'NONE',  ( 11.19045305759900089, 39.71388240225230959, -7.551420157137952671 ) ) ;
#4639=CARTESIAN_POINT ( 'NONE',  ( -13.22913111164857192, 61.83496861166081260, -2.690993549969627807 ) ) ;
#4640=VERTEX_POINT ( 'NONE', #2580 ) ;
#4641=ADVANCED_FACE ( 'NONE', ( #4370 ), #4193, .F. ) ;
#4644=( BOUNDED_CURVE ( )  B_SPLINE_CURVE ( 2, ( #14119, #4941, #16865, #700, #2175, #10342, #6110, #6363, #4770, #3604, #9453 ),
 .UNSPECIFIED., .F., .F. ) 
 B_SPLINE_CURVE_WITH_KNOTS ( ( 3, 2, 2, 2, 2, 3 ),
 ( 0.07409432434525202449, 0.07777777777777777901, 0.08333333333333332871, 0.08888888888888889228, 0.09444444444444444198, 0.09722222222222222376 ),
 .UNSPECIFIED. ) 
 CURVE ( )  GEOMETRIC_REPRESENTATION_ITEM ( )  RATIONAL_B_SPLINE_CURVE ( ( 0.9781297068810623774, 0.9675494122505707839, 1.000000000000000000, 0.9510565162951535312, 1.000000000000000000, 0.9510565162951535312, 1.000000000000000000, 0.9510565162951535312, 1.000000000000000000, 0.9755282581475768211, 0.9755282581475768211 ) ) 
 REPRESENTATION_ITEM ( '' )  );
#4645=CARTESIAN_POINT ( 'NONE',  ( 2.636941296682203006, 58.08524355054738209, -13.24082347101475321 ) ) ;
#4646=CARTESIAN_POINT ( 'NONE',  ( -4.171729424061787483, 37.32999999999999829, -12.83926296998457417 ) ) ;
#4647=CARTESIAN_POINT ( 'NONE',  ( 0.2690821827029589719, 65.68967525039607835, 13.49733241026649821 ) ) ;
#4649=CARTESIAN_POINT ( 'NONE',  ( -3.930507969928632939, 46.32123624867764278, -12.91573196151841074 ) ) ;
#4650=DIRECTION ( 'NONE',  ( 0.000000000000000000, -1.000000000000000000, 0.000000000000000000 ) ) ;
#4652=CARTESIAN_POINT ( 'NONE',  ( 11.21398382682447448, 54.14760983389460591, 7.519816583474207228 ) ) ;
#4654=CARTESIAN_POINT ( 'NONE',  ( -8.608562527083625682, 64.51060847542233034, -10.40036578628359010 ) ) ;
#4656=CARTESIAN_POINT ( 'NONE',  ( 2.710823146150888707, 67.08252889310698208, -13.22504384347605288 ) ) ;
#4657=CARTESIAN_POINT ( 'NONE',  ( -10.97982169273876707, 34.63276478775296141, -7.866720829704087592 ) ) ;
#4660=CARTESIAN_POINT ( 'NONE',  ( 7.867868983202085609, 77.97688993890311338, 10.97928513584511911 ) ) ;
#4661=CARTESIAN_POINT ( 'NONE',  ( 2.445080149700053643E-15, 48.17999999999999972, -13.50000000000000000 ) ) ;
#4664=CARTESIAN_POINT ( 'NONE',  ( 12.95808625703547001, 72.29434740553908512, 3.790096261879717598 ) ) ;
#4666=CARTESIAN_POINT ( 'NONE',  ( -13.49999999999999822, 58.77999999999998693, -4.386415899144240349 ) ) ;
#4667=CARTESIAN_POINT ( 'NONE',  ( -4.319839466158835073, 52.33534458003789780, -12.79062298228854822 ) ) ;
#4668=CARTESIAN_POINT ( 'NONE',  ( -11.76794919243112325, 38.77999999999999403, -3.823638476888998827 ) ) ;
#4670=CARTESIAN_POINT ( 'NONE',  ( 8.343458848123578520, 58.98000000000000398, 11.48378591275254124 ) ) ;
#4674=CARTESIAN_POINT ( 'NONE',  ( -0.7780706695535477557, 68.65214339747750216, 13.47801817613818187 ) ) ;
#4678=CARTESIAN_POINT ( 'NONE',  ( -13.47543018545582072, 73.95811523521949482, 0.8141832615170856435 ) ) ;
#4679=CARTESIAN_POINT ( 'NONE',  ( -2.366530682011494413, 76.26509166571406695, -13.29096256660020536 ) ) ;
#4684=CARTESIAN_POINT ( 'NONE',  ( -11.76794919243112325, 36.07999999999999829, 3.823638476888994830 ) ) ;
#4687=CARTESIAN_POINT ( 'NONE',  ( -3.895040229899401574, 32.54007840815446428, 12.92655551793117752 ) ) ;
#4688=CARTESIAN_POINT ( 'NONE',  ( 7.957144986088850125, 74.98096353892839261, 10.90684177774465624 ) ) ;
#4689=CARTESIAN_POINT ( 'NONE',  ( -1.003760800223034469E-07, 53.67999720368429450, 13.49999999999999822 ) ) ;
#4690=CARTESIAN_POINT ( 'NONE',  ( 9.520470885617717371, 31.72999999999999332, -6.917026985038131848 ) ) ;
#4691=CARTESIAN_POINT ( 'NONE',  ( 11.77278396783205494, 51.67514776089146267, -6.607601308730693290 ) ) ;
#4693=CARTESIAN_POINT ( 'NONE',  ( 1.203083463835363736E-13, 37.18000000000000682, -13.50000000000000000 ) ) ;
#4694=CARTESIAN_POINT ( 'NONE',  ( -4.171729424061791036, 70.53000000000001535, 12.83926296998457239 ) ) ;
#4696=CARTESIAN_POINT ( 'NONE',  ( 11.57644837279713634, 63.17112552278116056, 6.945208394352803793 ) ) ;
#4697=CARTESIAN_POINT ( 'NONE',  ( 0.5720401143641312691, 41.70056841707977924, 13.48815436162953496 ) ) ;
#4698=CARTESIAN_POINT ( 'NONE',  ( 8.474790154542958476, 48.85557007193735046, -10.50863980086850624 ) ) ;
#4700=ORIENTED_EDGE ( 'NONE', *, *, #10545, .F. ) ;
#4701=CARTESIAN_POINT ( 'NONE',  ( 7.272992578804311492, 64.87999999999999545, -10.01041549318726886 ) ) ;
#4705=CARTESIAN_POINT ( 'NONE',  ( -0.4211686846404315565, 43.19514363978697702, -13.49345797000271752 ) ) ;
#4706=CARTESIAN_POINT ( 'NONE',  ( -9.639429313053440751, 80.92999999999996419, -7.743379967852192181 ) ) ;
#4709=CARTESIAN_POINT ( 'NONE',  ( 5.326996769190816217, 65.87277302910042920, 12.40504085361147801 ) ) ;
#4711=CARTESIAN_POINT ( 'NONE',  ( -7.576616670048093940E-16, 45.67999999999999261, 12.37355403259654985 ) ) ;
#4713=CARTESIAN_POINT ( 'NONE',  ( -11.32419978475406097, 46.65450354790017684, -7.349319770073909908 ) ) ;
#4714=CARTESIAN_POINT ( 'NONE',  ( 12.93101617915861468, 45.56904160174139662, -3.882179959006170744 ) ) ;
#4715=CARTESIAN_POINT ( 'NONE',  ( 0.1326703767182750571, 70.17522967471386153, -13.49941531153568519 ) ) ;
#4718=CARTESIAN_POINT ( 'NONE',  ( 11.82890730580016481, 30.67109828621973477, -6.507028451830479732 ) ) ;
#4719=CARTESIAN_POINT ( 'NONE',  ( -11.12375258374542852, 56.21798818910362172, 7.649515620900761093 ) ) ;
#4721=CARTESIAN_POINT ( 'NONE',  ( -1.553272499165753162, 50.62433072722591731, 13.41218807779914357 ) ) ;
#4722=CARTESIAN_POINT ( 'NONE',  ( 10.75527420406746160, 33.12017030730734746, 8.165193978116038309 ) ) ;
#4724=CARTESIAN_POINT ( 'NONE',  ( 10.78095112019851243, 39.73819790818856745, -8.130464480974270103 ) ) ;
#4726=CARTESIAN_POINT ( 'NONE',  ( -13.47535547316411275, 61.90184251200314947, -0.8153781735254963525 ) ) ;
#4727=ORIENTED_EDGE ( 'NONE', *, *, #9840, .F. ) ;
#4731=CARTESIAN_POINT ( 'NONE',  ( 12.90756584819196284, 48.28806130775965499, 3.958932217318702929 ) ) ;
#4733=CARTESIAN_POINT ( 'NONE',  ( 9.395478811695362253, 78.81154358623695089, -9.694686115291968775 ) ) ;
#4734=CARTESIAN_POINT ( 'NONE',  ( 7.272992578804308828, 75.98000000000001819, 10.01041549318726709 ) ) ;
#4735=CARTESIAN_POINT ( 'NONE',  ( -2.394975141653304274, 46.26611428870612741, -13.28591781961343621 ) ) ;
#4736=DIRECTION ( 'NONE',  ( 0.000000000000000000, -0.000000000000000000, -1.000000000000000000 ) ) ;
#4738=CARTESIAN_POINT ( 'NONE',  ( 3.038735707072813153, 53.78933652538139398, 13.15431546165133447 ) ) ;
#4742=ORIENTED_EDGE ( 'NONE', *, *, #8030, .T. ) ;
#4744=CARTESIAN_POINT ( 'NONE',  ( -7.562439852726942746, 34.46358584180068618, -11.18616918020162920 ) ) ;
#4746=CARTESIAN_POINT ( 'NONE',  ( 8.833285895147833244, 78.02118567081015499, 10.20927156115941692 ) ) ;
#4747=CYLINDRICAL_SURFACE ( 'NONE', #14341, 13.50000000000000000 ) ;
#4750=CARTESIAN_POINT ( 'NONE',  ( 12.73193533167149383, 72.59359374908758866, -4.534872268809349904 ) ) ;
#4752=CARTESIAN_POINT ( 'NONE',  ( 10.92172942406179104, 54.73000000000000398, -7.935100905948385908 ) ) ;
#4753=CARTESIAN_POINT ( 'NONE',  ( -2.454226844576152811, 52.26824491471117540, -13.27505143425381640 ) ) ;
#4755=CARTESIAN_POINT ( 'NONE',  ( -4.171729424061791036, 52.53000000000000114, 12.83926296998457239 ) ) ;
#4759=CARTESIAN_POINT ( 'NONE',  ( -9.390739836095129078, 68.31192509387784639, 9.701155184843470280 ) ) ;
#4765=CARTESIAN_POINT ( 'NONE',  ( 12.00000000000000533, 102.9300000000000210, 1.714505518806294638E-15 ) ) ;
#4769=CARTESIAN_POINT ( 'NONE',  ( -7.576616670048093940E-16, 33.67999999999999972, 12.37355403259654807 ) ) ;
#4770=CARTESIAN_POINT ( 'NONE',  ( 4.171729424061789260, 79.82999999999999829, 12.83926296998457417 ) ) ;
#4771=CARTESIAN_POINT ( 'NONE',  ( -12.59586300201226905, 32.10615256030042275, 4.857418912420909507 ) ) ;
#4776=CARTESIAN_POINT ( 'NONE',  ( 11.76794919243112680, 31.57999999999999119, -3.823638476888993942 ) ) ;
#4777=CARTESIAN_POINT ( 'NONE',  ( 12.59636570365032604, 51.60610490905947501, -4.856197627295611774 ) ) ;
#4778=CARTESIAN_POINT ( 'NONE',  ( -12.04821575658347399, 38.15737380506738674, 6.178014121549161075 ) ) ;
#4779=CARTESIAN_POINT ( 'NONE',  ( 11.44150878627701218, 36.69798984994930180, -7.166082743125198995 ) ) ;
#4781=CARTESIAN_POINT ( 'NONE',  ( -2.138189944381240881, 70.60311857767972299, 13.49999999999999822 ) ) ;
#4783=CARTESIAN_POINT ( 'NONE',  ( -4.175698386514455684, 80.52985464586872411, 12.83807197239628195 ) ) ;
#4785=CARTESIAN_POINT ( 'NONE',  ( 13.49548971893528915, 48.41801641569664127, 0.3489674621406130828 ) ) ;
#4786=( GEOMETRIC_REPRESENTATION_CONTEXT ( 3 ) GLOBAL_UNCERTAINTY_ASSIGNED_CONTEXT ( ( #3254 ) ) GLOBAL_UNIT_ASSIGNED_CONTEXT ( ( #14174, #17181, #6420 ) ) REPRESENTATION_CONTEXT ( 'NONE', 'WORKASPACE' ) );
#4788=ORIENTED_EDGE ( 'NONE', *, *, #7738, .T. ) ;
#4789=CARTESIAN_POINT ( 'NONE',  ( 11.76794919243112325, 64.27999999999998693, 3.823638476888997051 ) ) ;
#4791=CARTESIAN_POINT ( 'NONE',  ( 4.171729424061791924, 57.02999999999999403, -12.83926296998457239 ) ) ;
#4794=CARTESIAN_POINT ( 'NONE',  ( 2.991272544791215182, 76.07245980423030574, -13.16609516694613013 ) ) ;
#4796=CARTESIAN_POINT ( 'NONE',  ( 7.827816212328980505, 65.97516117987781570, 11.00319993222369774 ) ) ;
#4797=CARTESIAN_POINT ( 'NONE',  ( 13.49999999999999822, 78.28000000000000114, 4.386415899144237684 ) ) ;
#4798=CARTESIAN_POINT ( 'NONE',  ( 7.272992578804311492, 52.87999999999998835, -10.01041549318726709 ) ) ;
#4799=CARTESIAN_POINT ( 'NONE',  ( -9.857808185263392531, 59.28819691158693672, 9.223707725319705730 ) ) ;
#4800=CARTESIAN_POINT ( 'NONE',  ( 13.47549715633743972, 45.40126855624355784, 0.8316350769568319201 ) ) ;
#4801=CARTESIAN_POINT ( 'NONE',  ( 5.637257242016931791, 69.97526884685950677, -12.26667565995465559 ) ) ;
#4802=CARTESIAN_POINT ( 'NONE',  ( 6.767892274421971166, 80.93000000000000682, 11.68099457074693603 ) ) ;
#4803=CARTESIAN_POINT ( 'NONE',  ( 13.46162618359535479, 30.46568736832789526, -1.030778076480221239 ) ) ;
#4804=CARTESIAN_POINT ( 'NONE',  ( -9.881254368068633553, 56.28734683505406622, 9.209166116772257382 ) ) ;
#4805=CYLINDRICAL_SURFACE ( 'NONE', #6974, 13.50000000000000000 ) ;
#4806=CARTESIAN_POINT ( 'NONE',  ( 2.751218558133481817, 64.08107632749974414, -13.21668710184735929 ) ) ;
#4807=CARTESIAN_POINT ( 'NONE',  ( 0.1477893832224585757, 43.17470362251723515, -13.49930464728724289 ) ) ;
#4808=CARTESIAN_POINT ( 'NONE',  ( 11.00470575586250810, 39.72507583716802060, -7.820951810514976010 ) ) ;
#4809=ORIENTED_EDGE ( 'NONE', *, *, #7493, .F. ) ;
#4810=CARTESIAN_POINT ( 'NONE',  ( -13.48302807339056741, 61.90651663121243331, -0.6789273804275641755 ) ) ;
#4812=ORIENTED_EDGE ( 'NONE', *, *, #13733, .T. ) ;
#4815=EDGE_CURVE ( 'NONE', #13318, #16628, #8155, .T. ) ;
#4816=CARTESIAN_POINT ( 'NONE',  ( 13.06962153774350632, 48.30957997059271491, 3.381577084613068163 ) ) ;
#4817=CARTESIAN_POINT ( 'NONE',  ( 7.964522300346896344, 57.87871040425520874, -10.90125341165491157 ) ) ;
#4818=CARTESIAN_POINT ( 'NONE',  ( 1.955722316818022888, 79.10969806729961817, -13.35880382187874282 ) ) ;
#4819=CARTESIAN_POINT ( 'NONE',  ( -3.636496289402153081, 80.32999999999999829, -11.19198476289190936 ) ) ;
#4820=CARTESIAN_POINT ( 'NONE',  ( 4.171729424061789260, 40.82999999999999829, 12.83926296998457417 ) ) ;
#4822=CARTESIAN_POINT ( 'NONE',  ( 13.50000000000000355, 41.57999999999999119, -4.386415899144233244 ) ) ;
#4824=CARTESIAN_POINT ( 'NONE',  ( -10.92172942406178926, 72.62999999999999545, -7.935100905948389460 ) ) ;
#4825=CARTESIAN_POINT ( 'NONE',  ( 10.29729702274682701, 33.76497182664475361, -8.730269506234060728 ) ) ;
#4829=CARTESIAN_POINT ( 'NONE',  ( 3.016341264242877962, 67.07153834722653585, -13.15950437981546628 ) ) ;
#4831=DIRECTION ( 'NONE',  ( 0.000000000000000000, -1.000000000000000000, 0.000000000000000000 ) ) ;
#4832=CARTESIAN_POINT ( 'NONE',  ( -5.673995304191476130, 59.47382727098472088, 12.25757816507847942 ) ) ;
#4833=DIRECTION ( 'NONE',  ( 0.000000000000000000, 1.000000000000000000, 0.000000000000000000 ) ) ;
#4834=EDGE_CURVE ( 'NONE', #2392, #7733, #9971, .T. ) ;
#4835=PLANE ( 'NONE',  #2889 ) ;
#4836=CARTESIAN_POINT ( 'NONE',  ( 11.65143199204702640, 72.68378159801741845, -6.819995948022331334 ) ) ;
#4838=CARTESIAN_POINT ( 'NONE',  ( -8.691771469529815392E-16, 53.67999999999999972, 14.19474002721660355 ) ) ;
#4839=CARTESIAN_POINT ( 'NONE',  ( -3.112744993334869648, 52.29192044083434610, -13.14449540143910511 ) ) ;
#4842=CARTESIAN_POINT ( 'NONE',  ( -8.605926364152821861, 68.34948858320100840, 10.40136348367510521 ) ) ;
#4846=CARTESIAN_POINT ( 'NONE',  ( -5.145432190156538077, 65.49406957235127891, 12.48100614422567567 ) ) ;
#4850=ORIENTED_EDGE ( 'NONE', *, *, #16834, .F. ) ;
#4851=CARTESIAN_POINT ( 'NONE',  ( 7.272992578804311492, 31.87999999999999190, -10.01041549318726886 ) ) ;
#4853=FACE_OUTER_BOUND ( 'NONE', #11810, .T. ) ;
#4855=CARTESIAN_POINT ( 'NONE',  ( -13.35352338939232908, 31.99944910354191663, 1.983290760110415496 ) ) ;
#4856=CARTESIAN_POINT ( 'NONE',  ( 1.328818477845309154, 74.72777941065712071, 13.43444295586212966 ) ) ;
#4857=CARTESIAN_POINT ( 'NONE',  ( 13.00822605418956179, 60.30103388586579882, 3.611571338210629811 ) ) ;
#4858=CARTESIAN_POINT ( 'NONE',  ( 0.000000000000000000, 80.93000000000000682, -13.50000000000000000 ) ) ;
#4860=CARTESIAN_POINT ( 'NONE',  ( 4.171729424061789260, 76.83000000000001251, 12.83926296998457417 ) ) ;
#4861=CARTESIAN_POINT ( 'NONE',  ( 13.48501078242496654, 51.39964884254468558, 0.8735145204809163788 ) ) ;
#4862=CARTESIAN_POINT ( 'NONE',  ( -8.224415399157907203, 38.36732905943534888, 10.71480048592647272 ) ) ;
#4863=CARTESIAN_POINT ( 'NONE',  ( 9.386110757463605125, 36.81227025756452775, -9.712354000322354963 ) ) ;
#4865=CARTESIAN_POINT ( 'NONE',  ( -4.023268246324633536E-14, 69.18000000000000682, -13.50000000000000000 ) ) ;
#4866=CARTESIAN_POINT ( 'NONE',  ( -3.068676428938670764, 77.56962524474758425, 13.14846988648537973 ) ) ;
#4868=CARTESIAN_POINT ( 'NONE',  ( -13.49999999999999822, 60.78000000000000114, -4.386415899144240349 ) ) ;
#4869=CARTESIAN_POINT ( 'NONE',  ( 7.499999999999998224, 88.93000000000000682, 9.367496997597600128 ) ) ;
#4870=CARTESIAN_POINT ( 'NONE',  ( 10.68025330336615042, 48.74383335475763346, -8.257267871943595239 ) ) ;
#4872=VERTEX_POINT ( 'NONE', #14862 ) ;
#4873=CARTESIAN_POINT ( 'NONE',  ( 9.520470885617715595, 61.13000000000000256, 6.917026985038134512 ) ) ;
#4875=CARTESIAN_POINT ( 'NONE',  ( 8.343458848123583849, 56.88000000000000256, -11.48378591275253768 ) ) ;
#4881=CARTESIAN_POINT ( 'NONE',  ( -9.520470885617717371, 48.23000000000000398, 6.917026985038133624 ) ) ;
#4883=AXIS2_PLACEMENT_3D ( 'NONE', #16773, #5843, #16600 ) ;
#4884=CARTESIAN_POINT ( 'NONE',  ( -13.47580627843815293, 58.90211067187865979, -0.8079450873288145374 ) ) ;
#4885=CARTESIAN_POINT ( 'NONE',  ( 13.49590972726846694, 45.41858991162752091, 0.3323335590089481761 ) ) ;
#4887=LINE ( 'NONE', #6572, #5549 ) ;
#4888=CARTESIAN_POINT ( 'NONE',  ( 13.07359181035909046, 30.54984980636906045, -3.366191560203806610 ) ) ;
#4889=EDGE_CURVE ( 'NONE', #3120, #2392, #13556, .T. ) ;
#4890=CARTESIAN_POINT ( 'NONE',  ( -13.42161547619133088, 55.98153511078791666, 1.480727477277027360 ) ) ;
#4891=CARTESIAN_POINT ( 'NONE',  ( -13.45714999850223670, 49.96723316153270389, 1.074876126443667701 ) ) ;
#4893=CARTESIAN_POINT ( 'NONE',  ( 2.889960586727556624, 43.07608798778890247, -13.18705226990277168 ) ) ;
#4894=CARTESIAN_POINT ( 'NONE',  ( 13.22552129195517523, 39.52604716363583037, -2.718968166365361760 ) ) ;
#4896=CARTESIAN_POINT ( 'NONE',  ( 2.445080149700053643E-15, 54.17999999999999972, -13.50000000000000000 ) ) ;
#4897=CARTESIAN_POINT ( 'NONE',  ( -11.22690699968129202, 61.64836490642452560, -7.497176070716886187 ) ) ;
#4899=ORIENTED_EDGE ( 'NONE', *, *, #12334, .F. ) ;
#4903=CARTESIAN_POINT ( 'NONE',  ( 13.34781774912188546, 48.35712733598928281, 2.080601422126210576 ) ) ;
#4904=CARTESIAN_POINT ( 'NONE',  ( 2.420781169875645400, 58.09295764678753926, -13.28118368607770172 ) ) ;
#4905=CARTESIAN_POINT ( 'NONE',  ( 11.42824258410874982, 78.69914800313584635, -7.198334943051281520 ) ) ;
#4906=CARTESIAN_POINT ( 'NONE',  ( 7.272992578804308828, 78.97999999999998977, 10.01041549318726709 ) ) ;
#4907=CARTESIAN_POINT ( 'NONE',  ( 10.92172942406179104, 41.72999999999999687, -7.935100905948385908 ) ) ;
#4908=CARTESIAN_POINT ( 'NONE',  ( 9.520470885617717371, 82.73000000000000398, -6.917026985038131848 ) ) ;
#4909=CARTESIAN_POINT ( 'NONE',  ( 1.653273178848926472E-15, 80.93000000000000682, 13.50000000000000000 ) ) ;
#4910=CARTESIAN_POINT ( 'NONE',  ( 0.000000000000000000, 80.93000000000000682, 0.000000000000000000 ) ) ;
#4914=CARTESIAN_POINT ( 'NONE',  ( 1.442428843286516438, 35.73186409263165331, 13.42278470930840939 ) ) ;
#4915=CARTESIAN_POINT ( 'NONE',  ( 4.389406115141700759, 34.02213224516504653, -12.76650137279820107 ) ) ;
#4916=ORIENTED_EDGE ( 'NONE', *, *, #9795, .F. ) ;
#4919=CARTESIAN_POINT ( 'NONE',  ( 5.197337872768928335, 66.99201906321724209, -12.45956099938747208 ) ) ;
#4921=CARTESIAN_POINT ( 'NONE',  ( 1.774688460779562327, 77.74381030479406718, 13.38330506251782204 ) ) ;
#4922=CARTESIAN_POINT ( 'NONE',  ( 0.000000000000000000, 80.93000000000000682, 0.000000000000000000 ) ) ;
#4924=FACE_BOUND ( 'NONE', #11960, .T. ) ;
#4926=CARTESIAN_POINT ( 'NONE',  ( 4.171729424061789260, 56.82999999999999829, 12.83926296998457417 ) ) ;
#4927=CARTESIAN_POINT ( 'NONE',  ( -3.201505495297523041, 71.56488954480640530, 13.11491780500991311 ) ) ;
#4930=CARTESIAN_POINT ( 'NONE',  ( -8.642976562267744356, 68.34776206137323129, 10.37064509888684682 ) ) ;
#4933=CARTESIAN_POINT ( 'NONE',  ( 9.287700127114062454, 54.81689961847566650, -9.797388458301975689 ) ) ;
#4935=CARTESIAN_POINT ( 'NONE',  ( -5.577144119655765842, 65.47773180331512322, 12.29492813050585731 ) ) ;
#4938=CARTESIAN_POINT ( 'NONE',  ( -1.812176205795150041, 35.61479768570823978, 13.37810765195845519 ) ) ;
#4939=ORIENTED_EDGE ( 'NONE', *, *, #1090, .F. ) ;
#4941=CARTESIAN_POINT ( 'NONE',  ( 9.241419651377785982, 80.82775795770034222, -10.24784889786167774 ) ) ;
#4942=CARTESIAN_POINT ( 'NONE',  ( -12.61531847087750258, 32.10420026677966376, 4.806648137471639437 ) ) ;
#4944=CARTESIAN_POINT ( 'NONE',  ( 10.68453665737815150, 60.11640859769380540, 8.251753631019978386 ) ) ;
#4946=DIRECTION ( 'NONE',  ( 0.000000000000000000, -1.000000000000000000, 0.000000000000000000 ) ) ;
#4947=CARTESIAN_POINT ( 'NONE',  ( 3.636496289402157078, 56.02999999999999403, -11.19198476289190936 ) ) ;
#4949=CARTESIAN_POINT ( 'NONE',  ( 13.48945982917662789, 51.44836422055956859, -0.5335955830629390828 ) ) ;
#4950=CARTESIAN_POINT ( 'NONE',  ( -11.05767084123177035, 38.22202780657029564, 7.745299231847412536 ) ) ;
#4952=CARTESIAN_POINT ( 'NONE',  ( 11.99492941862966333, 36.65855328830576809, -6.194533839644177142 ) ) ;
#4954=CARTESIAN_POINT ( 'NONE',  ( -5.233730858707171585, 74.49075943819711654, 12.44419822032766376 ) ) ;
#4955=CARTESIAN_POINT ( 'NONE',  ( -6.367807814168689795, 77.44634757438805650, 11.90382492994284114 ) ) ;
#4956=CARTESIAN_POINT ( 'NONE',  ( -3.495764761518072916, 80.55428792539511562, 13.04705504019511864 ) ) ;
#4957=CARTESIAN_POINT ( 'NONE',  ( 7.500000000000000000, 106.2138518220599650, 8.084116494856623092 ) ) ;
#4960=VERTEX_POINT ( 'NONE', #16727 ) ;
#4961=CARTESIAN_POINT ( 'NONE',  ( -11.76794919243112325, 57.07999999999999829, 3.823638476888994830 ) ) ;
#4964=CARTESIAN_POINT ( 'NONE',  ( -3.565931047808069021, 80.92999999999999261, -12.36697741789391536 ) ) ;
#4966=CARTESIAN_POINT ( 'NONE',  ( -8.691771469529815392E-16, 80.68000000000000682, 14.19474002721660355 ) ) ;
#4968=CARTESIAN_POINT ( 'NONE',  ( -7.576616670048093940E-16, 54.67999999999999261, 12.37355403259654985 ) ) ;
#4970=CARTESIAN_POINT ( 'NONE',  ( -12.32963178104218294, 59.13122713586460577, 5.502663897909060076 ) ) ;
#4971=CARTESIAN_POINT ( 'NONE',  ( 13.49933328929112264, 45.42501111118324530, 0.1461406261329739054 ) ) ;
#4972=CARTESIAN_POINT ( 'NONE',  ( 13.41605565035905201, 69.37766445847722707, 1.503147272406539336 ) ) ;
#4973=CARTESIAN_POINT ( 'NONE',  ( -2.138189944381219565, 67.60311857767970878, 13.50000000000000355 ) ) ;
#4974=CARTESIAN_POINT ( 'NONE',  ( 13.28617369785314928, 30.34578285407915033, 2.393266104260259208 ) ) ;
#4975=CARTESIAN_POINT ( 'NONE',  ( -11.18631900104275978, 55.64585107649359941, -7.557541126061750880 ) ) ;
#4976=CARTESIAN_POINT ( 'NONE',  ( -13.14190856829288379, 50.04143232289781196, 3.139569975885453168 ) ) ;
#4977=CARTESIAN_POINT ( 'NONE',  ( 4.745372806345461214, 64.00876641970079106, -12.64604413371457525 ) ) ;
#4978=CARTESIAN_POINT ( 'NONE',  ( 4.325681857567722943, 43.02444320334033989, -12.78825713985152213 ) ) ;
#4979=CARTESIAN_POINT ( 'NONE',  ( 13.36748020402493964, 39.36365328056236024, 1.894345376098481415 ) ) ;
#4980=ORIENTED_EDGE ( 'NONE', *, *, #3133, .T. ) ;
#4981=CARTESIAN_POINT ( 'NONE',  ( -8.014660668667909604, 70.48352739142377743, -10.86416305456324416 ) ) ;
#4982=CARTESIAN_POINT ( 'NONE',  ( -10.37380102186887321, 61.59903092850272799, -8.640656467602703117 ) ) ;
#4983=VECTOR ( 'NONE', #9145, 1000.000000000000000 ) ;
#4986=CARTESIAN_POINT ( 'NONE',  ( -12.95148698083498218, 40.79361840698238240, -3.809996331347294873 ) ) ;
#4990=CARTESIAN_POINT ( 'NONE',  ( 5.597690550215550509, 47.88292748343059202, 12.29688404133074009 ) ) ;
#4991=CARTESIAN_POINT ( 'NONE',  ( 4.778181653748105440, 58.00785439407665223, -12.62614106855890483 ) ) ;
#4992=CARTESIAN_POINT ( 'NONE',  ( 11.93212341947577926, 78.66338650403393729, -6.315679433880966975 ) ) ;
#4993=ADVANCED_FACE ( 'NONE', ( #10041 ), #16557, .T. ) ;
#4994=CARTESIAN_POINT ( 'NONE',  ( 11.76794919243112325, 82.27999999999998693, 3.823638476888996607 ) ) ;
#4995=CARTESIAN_POINT ( 'NONE',  ( -10.92172942406179104, 37.22999999999999687, 7.935100905948387684 ) ) ;
#4998=CARTESIAN_POINT ( 'NONE',  ( 2.138189944381238661, 40.75688142232026934, 13.50000000000000000 ) ) ;
#5001=( BOUNDED_CURVE ( )  B_SPLINE_CURVE ( 2, ( #16280, #5435, #2576, #13375, #213, #12410, #14689, #121, #29, #10737, #5618, #1615, #6675 ),
 .UNSPECIFIED., .F., .F. ) 
 B_SPLINE_CURVE_WITH_KNOTS ( ( 3, 2, 2, 2, 2, 2, 3 ),
 ( 0.7083333333333333703, 0.7111111111111111382, 0.7166666666666666741, 0.7222222222222222099, 0.7277777777777777457, 0.7333333333333332815, 0.7361111111111110494 ),
 .UNSPECIFIED. ) 
 CURVE ( )  GEOMETRIC_REPRESENTATION_ITEM ( )  RATIONAL_B_SPLINE_CURVE ( ( 0.9755282581475768211, 0.9755282581475768211, 1.000000000000000000, 0.9510565162951535312, 1.000000000000000000, 0.9510565162951535312, 1.000000000000000000, 0.9510565162951535312, 1.000000000000000000, 0.9510565162951535312, 1.000000000000000000, 0.9755282581475772652, 0.9755282581475768211 ) ) 
 REPRESENTATION_ITEM ( '' )  );
#5002=LINE ( 'NONE', #9080, #8956 ) ;
#5003=CARTESIAN_POINT ( 'NONE',  ( 8.296534642002788118, 33.86373860633018751, -10.64977992570600662 ) ) ;
#5004=CARTESIAN_POINT ( 'NONE',  ( -13.36016819754640750, 73.86216746102554964, -1.938184205018641082 ) ) ;
#5006=DIRECTION ( 'NONE',  ( 0.000000000000000000, -1.000000000000000000, 0.000000000000000000 ) ) ;
#5009=CARTESIAN_POINT ( 'NONE',  ( -4.023268246324633536E-14, 69.18000000000000682, -13.50000000000000000 ) ) ;
#5010=CARTESIAN_POINT ( 'NONE',  ( -3.985033859854695937, 59.53671145982129786, 12.89854622073393031 ) ) ;
#5011=PLANE ( 'NONE',  #15949 ) ;
#5013=CARTESIAN_POINT ( 'NONE',  ( -13.49999999999999822, 49.78000000000000114, -4.386415899144240349 ) ) ;
#5014=CARTESIAN_POINT ( 'NONE',  ( -7.628114507008727507, 71.39355340672105399, 11.14151516845310219 ) ) ;
#5017=CARTESIAN_POINT ( 'NONE',  ( 0.4448257041681634716, 68.69614250464667293, 13.49999999991288213 ) ) ;
#5019=CARTESIAN_POINT ( 'NONE',  ( 6.352825135554033942, 54.94695263489539627, -11.91183081968598501 ) ) ;
#5022=CARTESIAN_POINT ( 'NONE',  ( -10.94367429142997850, 65.22875971052661725, 7.916974700845242907 ) ) ;
#5023=CARTESIAN_POINT ( 'NONE',  ( -11.80607357642263544, 80.93000000000000682, -0.5610838546640731783 ) ) ;
#5024=CARTESIAN_POINT ( 'NONE',  ( -1.612532095345881933, 35.62201661823903009, 13.40334904042095943 ) ) ;
#5028=DIRECTION ( 'NONE',  ( 0.000000000000000000, -1.000000000000000000, 0.000000000000000000 ) ) ;
#5029=CARTESIAN_POINT ( 'NONE',  ( -4.296388646608581219, 40.33449593194379190, -12.79811344974312881 ) ) ;
#5030=CARTESIAN_POINT ( 'NONE',  ( -13.46762570571352846, 31.89769696204961846, -0.9344603740635033517 ) ) ;
#5032=CARTESIAN_POINT ( 'NONE',  ( 13.20086187186735671, 60.32965506492238461, 2.836544637259669877 ) ) ;
#5033=EDGE_CURVE ( 'NONE', #6381, #10449, #2145, .T. ) ;
#5036=CARTESIAN_POINT ( 'NONE',  ( -3.877293585379739227, 53.54058681617228643, 12.93122935937666185 ) ) ;
#5037=CARTESIAN_POINT ( 'NONE',  ( 9.520470885617715595, 55.12999999999999545, 6.917026985038134512 ) ) ;
#5039=CARTESIAN_POINT ( 'NONE',  ( 8.343458848123578520, 73.97999999999998977, 11.48378591275254124 ) ) ;
#5040=CARTESIAN_POINT ( 'NONE',  ( 13.40136960300497826, 51.37320127860066066, 1.628906160047896012 ) ) ;
#5041=VECTOR ( 'NONE', #1290, 1000.000000000000000 ) ;
#5042=CARTESIAN_POINT ( 'NONE',  ( -13.31211181591337578, 38.00888502146048609, 2.245302585987761557 ) ) ;
#5043=CARTESIAN_POINT ( 'NONE',  ( 11.97434507244688184, 36.66013894208906265, -6.234185302249787064 ) ) ;
#5045=CARTESIAN_POINT ( 'NONE',  ( -3.458677200775941429, 74.55563874354560028, 13.04943159450400003 ) ) ;
#5046=CARTESIAN_POINT ( 'NONE',  ( -6.523521772619733206, 77.44003651811182465, 11.81943641442651760 ) ) ;
#5047=CARTESIAN_POINT ( 'NONE',  ( -4.023268246324633536E-14, 60.18000000000000682, -13.50000000000000000 ) ) ;
#5048=CARTESIAN_POINT ( 'NONE',  ( 7.500000000000001776, 103.4461236652718696, -9.346045933502386660 ) ) ;
#5049=ORIENTED_EDGE ( 'NONE', *, *, #12715, .T. ) ;
#5052=CARTESIAN_POINT ( 'NONE',  ( 9.520470885617715595, 58.13000000000000256, 6.917026985038134512 ) ) ;
#5056=CARTESIAN_POINT ( 'NONE',  ( 12.10419440643161515, 75.64994209057574892, -5.978384200320835618 ) ) ;
#5058=ADVANCED_FACE ( 'NONE', ( #6146 ), #4805, .T. ) ;
#5059=LINE ( 'NONE', #3981, #5994 ) ;
#5060=CARTESIAN_POINT ( 'NONE',  ( 2.684808531364387907, 65.77668069368513670, 13.23259810234951672 ) ) ;
#5061=CARTESIAN_POINT ( 'NONE',  ( -13.50000000000000000, 67.93000000000000682, -3.306546357697853733E-15 ) ) ;
#5062=CARTESIAN_POINT ( 'NONE',  ( 11.76794919243112325, 43.28000000000000114, 3.823638476888996607 ) ) ;
#5064=CARTESIAN_POINT ( 'NONE',  ( -13.38719676025015204, 58.99337602412490611, 1.818195643690203145 ) ) ;
#5065=CARTESIAN_POINT ( 'NONE',  ( 9.190356918478798320, 45.03834564354057335, 9.888769335142141514 ) ) ;
#5066=CARTESIAN_POINT ( 'NONE',  ( 11.11381991456607921, 69.71858770960906782, -7.663787684871768313 ) ) ;
#5067=CARTESIAN_POINT ( 'NONE',  ( 4.092636507115654965, 80.82714932348959280, 12.86485741472674249 ) ) ;
#5068=CARTESIAN_POINT ( 'NONE',  ( 13.27325193621214972, 30.51706269903375102, -2.471716390437845412 ) ) ;
#5069=VECTOR ( 'NONE', #7744, 1000.000000000000000 ) ;
#5070=CARTESIAN_POINT ( 'NONE',  ( -11.98088293444550523, 55.70025900529297758, -6.222366544694983403 ) ) ;
#5071=CARTESIAN_POINT ( 'NONE',  ( -13.46016075455064254, 49.96588609214764887, 1.036464527647057432 ) ) ;
#5072=CARTESIAN_POINT ( 'NONE',  ( 7.792390880217984872, 63.88631323827352304, -11.02401972263586494 ) ) ;
#5073=CARTESIAN_POINT ( 'NONE',  ( 11.91798314216262256, 42.66442715076532011, -6.341270923659345193 ) ) ;
#5074=CARTESIAN_POINT ( 'NONE',  ( 12.50959235204128284, 39.24543322991454630, 5.075441208484069655 ) ) ;
#5076=CARTESIAN_POINT ( 'NONE',  ( -10.27595300512552612, 70.59341302248357408, -8.758023051731081310 ) ) ;
#5077=CARTESIAN_POINT ( 'NONE',  ( -9.315893856011628671, 61.54410272838872942, -9.782409614841228063 ) ) ;
#5080=CARTESIAN_POINT ( 'NONE',  ( -7.793068910463410326, 40.47363171592833453, -11.02779009344588346 ) ) ;
#5084=CARTESIAN_POINT ( 'NONE',  ( 3.176854332491030775, 47.79429613678128419, 13.12122346607776890 ) ) ;
#5085=EDGE_CURVE ( 'NONE', #10490, #10985, #10951, .T. ) ;
#5086=CARTESIAN_POINT ( 'NONE',  ( 13.23136294834424653, 57.33332165125162305, 2.733612023197712571 ) ) ;
#5087=CARTESIAN_POINT ( 'NONE',  ( 12.85467642924241183, 78.57828243993452588, -4.127473429646537184 ) ) ;
#5089=CARTESIAN_POINT ( 'NONE',  ( 9.520470885617715595, 82.13000000000000966, 6.917026985038134512 ) ) ;
#5090=CARTESIAN_POINT ( 'NONE',  ( -3.636496289402155746, 81.53000000000000114, 11.19198476289190936 ) ) ;
#5093=CARTESIAN_POINT ( 'NONE',  ( 0.000000000000000000, 88.93000000000000682, 0.000000000000000000 ) ) ;
#5095=FACE_OUTER_BOUND ( 'NONE', #10831, .T. ) ;
#5096=CARTESIAN_POINT ( 'NONE',  ( 3.075030622404754777, 34.06943319545086979, -13.14513346880981715 ) ) ;
#5097=CARTESIAN_POINT ( 'NONE',  ( -3.472868589956898955, 73.30492623780139638, -13.04596869824614025 ) ) ;
#5100=CARTESIAN_POINT ( 'NONE',  ( 2.000520122481862502E-14, 76.67999999999999261, 13.50000000000000000 ) ) ;
#5101=VERTEX_POINT ( 'NONE', #13778 ) ;
#5102=CARTESIAN_POINT ( 'NONE',  ( -12.87952649464229005, 41.07582668764707989, 4.061290009118315503 ) ) ;
#5104=CARTESIAN_POINT ( 'NONE',  ( -2.167233541823554877, 44.60213075612084310, 13.33398610478137769 ) ) ;
#5106=CARTESIAN_POINT ( 'NONE',  ( 11.59055319155406139, 66.68791535026535655, -6.921638745017356875 ) ) ;
#5107=CARTESIAN_POINT ( 'NONE',  ( -10.92172942406179104, 56.23000000000000398, 7.935100905948387684 ) ) ;
#5108=CARTESIAN_POINT ( 'NONE',  ( -4.501388629725658674, 71.51804696647752735, 12.72743260569431456 ) ) ;
#5111=CARTESIAN_POINT ( 'NONE',  ( -12.83831444568583002, 68.08011178376837336, 4.174688847921135704 ) ) ;
#5113=CARTESIAN_POINT ( 'NONE',  ( 3.292662364912134709, 55.06160801123378690, -13.09230389691793306 ) ) ;
#5116=EDGE_CURVE ( 'NONE', #16836, #10403, #2995, .T. ) ;
#5117=CARTESIAN_POINT ( 'NONE',  ( -11.50465976997115547, 65.19371892221600717, 7.063487139731847719 ) ) ;
#5118=CARTESIAN_POINT ( 'NONE',  ( 4.299690572160308814E-08, 62.68000119825558869, 13.49999999999999822 ) ) ;
#5119=CARTESIAN_POINT ( 'NONE',  ( -11.22894223272487046, 35.21150567205079085, 7.494087460015308011 ) ) ;
#5123=CARTESIAN_POINT ( 'NONE',  ( -13.47177724509586483, 31.89980168472233402, -0.8729076666594210998 ) ) ;
#5125=CARTESIAN_POINT ( 'NONE',  ( 7.219420632988450492, 59.94908418118669147, 11.40963323477301472 ) ) ;
#5127=CARTESIAN_POINT ( 'NONE',  ( -4.436382084028307915, 53.52041252290905504, 12.75888727614251650 ) ) ;
#5128=CARTESIAN_POINT ( 'NONE',  ( -7.272992578804307939, 59.48000000000000398, -10.01041549318726886 ) ) ;
#5129=CARTESIAN_POINT ( 'NONE',  ( -13.50000000000000000, 72.92999999999999261, -3.306546357697853733E-15 ) ) ;
#5130=CARTESIAN_POINT ( 'NONE',  ( 12.48710485657553804, 51.24329990980355376, 5.130518657651855996 ) ) ;
#5131=CARTESIAN_POINT ( 'NONE',  ( -9.337699186879977020, 38.31443680239338789, 9.749747033323940215 ) ) ;
#5132=CARTESIAN_POINT ( 'NONE',  ( 11.23610652242876107, 36.71105984972950864, -7.483311881068123839 ) ) ;
#5135=DIRECTION ( 'NONE',  ( 1.000000000000000000, 0.000000000000000000, 0.000000000000000000 ) ) ;
#5136=CARTESIAN_POINT ( 'NONE',  ( -12.16888219137197602, 77.14468546548981465, 5.845481969467562600 ) ) ;
#5137=CARTESIAN_POINT ( 'NONE',  ( -7.123498274578269118, 79.44487204299775840, -11.46975519674731459 ) ) ;
#5138=CARTESIAN_POINT ( 'NONE',  ( 7.499999999999998224, 104.9408589258552098, 8.949127168380908159 ) ) ;
#5139=ORIENTED_EDGE ( 'NONE', *, *, #744, .T. ) ;
#5142=CARTESIAN_POINT ( 'NONE',  ( -7.576616670048093940E-16, 54.67999999999999261, 12.37355403259654807 ) ) ;
#5147=CARTESIAN_POINT ( 'NONE',  ( 11.21289274167025773, 75.71237501678724868, -7.524009696738541031 ) ) ;
#5148=CARTESIAN_POINT ( 'NONE',  ( 10.92172942406178926, 68.12999999999999545, 7.935100905948387684 ) ) ;
#5149=CARTESIAN_POINT ( 'NONE',  ( 1.574810205816248532, 65.73663956441438927, 13.41017204387538442 ) ) ;
#5150=CARTESIAN_POINT ( 'NONE',  ( 13.50000000000000000, 72.42999999999999261, 1.653273178848926867E-15 ) ) ;
#5151=CARTESIAN_POINT ( 'NONE',  ( 11.76794919243112680, 37.57999999999999829, -3.823638476888993942 ) ) ;
#5152=CARTESIAN_POINT ( 'NONE',  ( -13.25214052457024216, 58.83776751653361714, -2.615125762588000224 ) ) ;
#5153=CARTESIAN_POINT ( 'NONE',  ( 11.39928639567819424, 45.15932595380822079, 7.232671352425048994 ) ) ;
#5154=CARTESIAN_POINT ( 'NONE',  ( 11.03746613180151215, 69.72319289778489804, -7.773423729612433775 ) ) ;
#5158=CARTESIAN_POINT ( 'NONE',  ( -4.835225515329382162, 55.35429197270953239, -12.60603724776291656 ) ) ;
#5160=CARTESIAN_POINT ( 'NONE',  ( -6.619156144680720999, 50.43619166903473428, 11.77703965849789292 ) ) ;
#5161=CARTESIAN_POINT ( 'NONE',  ( 6.310916549568529099, 63.94882138232988211, -11.94029056665552702 ) ) ;
#5162=CARTESIAN_POINT ( 'NONE',  ( 10.98041672999455365, 42.72652285908267089, -7.855008297392397587 ) ) ;
#5163=CARTESIAN_POINT ( 'NONE',  ( 9.762871203696802169, 39.06670793169961797, 9.331473753957455486 ) ) ;
#5165=CARTESIAN_POINT ( 'NONE',  ( -12.86325130802400096, 70.78271567125864294, -4.099968533946731775 ) ) ;
#5166=CARTESIAN_POINT ( 'NONE',  ( -5.442442773936573275, 61.37717677536036121, -12.36136841408004372 ) ) ;
#5168=VERTEX_POINT ( 'NONE', #622 ) ;
#5169=ORIENTED_EDGE ( 'NONE', *, *, #14361, .T. ) ;
#5172=CARTESIAN_POINT ( 'NONE',  ( 3.042243549217453769, 61.07061215346910643, -13.15276014662998172 ) ) ;
#5173=CARTESIAN_POINT ( 'NONE',  ( 12.18771478896523064, 57.64319249440018922, -5.807660356779048350 ) ) ;
#5174=CARTESIAN_POINT ( 'NONE',  ( 7.272992578804311492, 73.88000000000000966, -10.01041549318726709 ) ) ;
#5175=CARTESIAN_POINT ( 'NONE',  ( -8.343458848123576743, 36.47999999999998977, -11.48378591275254301 ) ) ;
#5176=CARTESIAN_POINT ( 'NONE',  ( -9.520470885617717371, 81.22999999999998977, 6.917026985038133624 ) ) ;
#5182=EDGE_CURVE ( 'NONE', #9540, #11531, #14045, .T. ) ;
#5183=CARTESIAN_POINT ( 'NONE',  ( -7.499999999999996447, 88.93000000000000682, -12.00000000000000178 ) ) ;
#5184=CARTESIAN_POINT ( 'NONE',  ( 8.086404608413186423, 33.87324810585550239, -10.81069809738593790 ) ) ;
#5185=CARTESIAN_POINT ( 'NONE',  ( -3.769655809539932179, 73.31549332748073766, -12.96321091462792552 ) ) ;
#5186=VERTEX_POINT ( 'NONE', #1677 ) ;
#5188=CARTESIAN_POINT ( 'NONE',  ( 3.636496289402157078, 77.03000000000000114, -11.19198476289190936 ) ) ;
#5189=ORIENTED_EDGE ( 'NONE', *, *, #14625, .F. ) ;
#5191=CARTESIAN_POINT ( 'NONE',  ( -12.96917948489248040, 41.06450665792823429, 3.758514619347866237 ) ) ;
#5193=CARTESIAN_POINT ( 'NONE',  ( -2.614575715703594483, 44.58605660440404961, 13.25095008111780359 ) ) ;
#5195=CARTESIAN_POINT ( 'NONE',  ( 11.58370557121411260, 66.68837149964352307, -6.933095401133553715 ) ) ;
#5196=CARTESIAN_POINT ( 'NONE',  ( 10.92172942406178926, 48.13000000000000256, 7.935100905948387684 ) ) ;
#5197=CARTESIAN_POINT ( 'NONE',  ( -5.807920978506090570, 71.46861498452221895, 12.18681003659212259 ) ) ;
#5199=CARTESIAN_POINT ( 'NONE',  ( -11.68323218641632977, 68.18151092926409262, 6.764040740981662303 ) ) ;
#5201=CARTESIAN_POINT ( 'NONE',  ( 3.933372914426268352, 55.03853806791980929, -12.91984279767183885 ) ) ;
#5204=CARTESIAN_POINT ( 'NONE',  ( -13.36843182285373643, 64.99577036403836416, 1.880491479935817445 ) ) ;
#5205=CARTESIAN_POINT ( 'NONE',  ( -4.441721580454757401, 35.52022541264950206, 12.74838867243934715 ) ) ;
#5207=ORIENTED_EDGE ( 'NONE', *, *, #1788, .T. ) ;
#5210=CARTESIAN_POINT ( 'NONE',  ( -5.068380164899249252, 31.36292906761380195, -12.51566991174745702 ) ) ;
#5211=CARTESIAN_POINT ( 'NONE',  ( 1.228569358179881110, 73.13583881254791663, -13.44621423555252449 ) ) ;
#5212=CARTESIAN_POINT ( 'NONE',  ( 13.04260590495897532, 60.30576534669085476, 3.484349753159051932 ) ) ;
#5215=CARTESIAN_POINT ( 'NONE',  ( -9.875734236714132308, 53.28725852313749556, 9.204417485957288037 ) ) ;
#5216=EDGE_CURVE ( 'NONE', #15567, #3801, #7262, .T. ) ;
#5218=CARTESIAN_POINT ( 'NONE',  ( 9.428902991474831907, 51.04980280169728246, 9.671452565076423369 ) ) ;
#5219=CARTESIAN_POINT ( 'NONE',  ( -10.40656815491510123, 37.60077104023546468, -8.599786994842322230 ) ) ;
#5221=CARTESIAN_POINT ( 'NONE',  ( 9.351852784421879505, 36.04625061253739915, 9.736770932323047134 ) ) ;
#5223=CARTESIAN_POINT ( 'NONE',  ( -3.715995504620742462, 74.54638359986023488, 12.98043278505261178 ) ) ;
#5225=CARTESIAN_POINT ( 'NONE',  ( -3.825492553879640933, 77.54244891512146864, 12.94665650124274947 ) ) ;
#5226=CARTESIAN_POINT ( 'NONE',  ( -11.44555968023306214, 80.19798584157584287, 7.171502794116832114 ) ) ;
#5228=CARTESIAN_POINT ( 'NONE',  ( 7.500000000000000000, 108.7270211387039325, 1.010069558262741918 ) ) ;
#5231=CARTESIAN_POINT ( 'NONE',  ( 3.636496289402157078, 53.03000000000000114, -11.19198476289190936 ) ) ;
#5235=CARTESIAN_POINT ( 'NONE',  ( 12.06631813232368344, 75.65296445888444055, -6.054263178453977545 ) ) ;
#5236=CARTESIAN_POINT ( 'NONE',  ( 4.171729424061791924, 33.02999999999999403, -12.83926296998457239 ) ) ;
#5237=CARTESIAN_POINT ( 'NONE',  ( 0.3979337702179393532, 65.69430812332862502, 13.49420666704868843 ) ) ;
#5238=CARTESIAN_POINT ( 'NONE',  ( 3.636496289402154414, 42.82999999999999829, 11.19198476289190936 ) ) ;
#5240=CARTESIAN_POINT ( 'NONE',  ( -10.94460162584092622, 58.63120264642423507, -7.905306038853614048 ) ) ;
#5241=CARTESIAN_POINT ( 'NONE',  ( 2.918937870619084496, 44.78495419697207325, 13.18066017063958384 ) ) ;
#5242=CARTESIAN_POINT ( 'NONE',  ( 10.21818166811046780, 69.76923834543529779, -8.822804023081456393 ) ) ;
#5244=CARTESIAN_POINT ( 'NONE',  ( 11.11471058409703083, 30.14144794081360601, 7.663010259766935839 ) ) ;
#5245=CARTESIAN_POINT ( 'NONE',  ( -0.6196186009307830256, 55.20227918106063925, -13.48581699895939678 ) ) ;
#5246=CARTESIAN_POINT ( 'NONE',  ( -11.13026847521628504, 50.21760025236010705, 7.640326842646127048 ) ) ;
#5247=CARTESIAN_POINT ( 'NONE',  ( 12.71605810479952758, 63.26620497749446770, 4.535529403342682286 ) ) ;
#5248=CARTESIAN_POINT ( 'NONE',  ( 8.421811294184292862, 42.85802858309214258, -10.55187809311721558 ) ) ;
#5249=CARTESIAN_POINT ( 'NONE',  ( 13.50175417813731471, 39.43989184164867368, -0.2898738848101085619 ) ) ;
#5251=CARTESIAN_POINT ( 'NONE',  ( -5.799651830195980295, 70.39105055476129280, -12.19207057802755401 ) ) ;
#5252=CARTESIAN_POINT ( 'NONE',  ( -7.317172661068146233, 61.45307890462790112, -11.34501891446300448 ) ) ;
#5255=B_SPLINE_CURVE_WITH_KNOTS ( 'NONE', 3,
 ( #3697, #14462, #6452, #13155, #9110, #2351, #7783, #11836, #9198, #14549, #7866, #17298, #5211, #10601, #9719, #66, #4040, #5471, #16406, #16493, #8125, #10946, #1293, #247, #6797, #6708, #14803, #11119, #15155, #10852, #6977, #12085, #16129, #7062, #1380, #17468, #5381, #10767, #9633, #2963, #9455, #12175, #16219, #2696, #16312, #13492, #13746, #4131, #12444, #9543, #4219, #1646, #6889, #14892, #2786, #8217, #4307, #5738, #9809, #14982, #13578, #4398, #1470, #12261, #8307, #157, #5563, #2875, #13662, #329, #1557, #12353, #5652, #11034, #15065, #8393, #8037, #13405, #4836, #767, #11384, #12617, #16933, #505, #16847, #14010, #10239, #12793, #1985, #4750, #3328, #8655, #4488, #8744, #5825, #7411, #5913, #1815, #16670, #418, #11471, #6091, #1733, #10156, #3053, #14188, #7229, #11557, #15506, #679, #3417, #11292, #16583, #4577, #8831, #8482, #3143, #4664, #14101, #9984, #7146, #13833, #9897, #6175, #12532, #15332, #2073, #11209, #15245, #7498, #13921, #12878, #3235, #8568, #1903, #7320, #12704, #591, #6001, #16756, #10071, #15422, #4003, #14601, #2481, #12135, #24, #8003, #14683, #14273, #10648, #9420, #6845, #16011, #5521, #10817, #11643, #7914, #5344, #13453, #14768, #15593, #3917, #12053, #3501, #13289, #1178, #2659, #12223, #8916, #1339, #5262, #2160, #17350, #9334, #2571, #16179, #6756, #7584, #5427, #115, #12963, #13369, #1258, #6589, #6670, #8175, #17431, #845, #6256, #4091 ),
 .UNSPECIFIED., .F., .F.,
 ( 4, 2, 2, 2, 2, 1, 1, 2, 2, 2, 2, 1, 1, 1, 2, 2, 2, 1, 2, 2, 2, 2, 2, 1, 1, 1, 2, 2, 2, 1, 1, 2, 2, 2, 2, 2, 2, 2, 2, 1, 1, 1, 2, 2, 2, 2, 2, 1, 1, 2, 2, 1, 2, 2, 1, 2, 2, 1, 1, 2, 2, 2, 1, 1, 2, 2, 1, 1, 2, 2, 2, 2, 1, 2, 2, 2, 2, 2, 2, 2, 1, 1, 1, 1, 2, 2, 1, 1, 1, 2, 2, 1, 1, 1, 2, 2, 1, 2, 2, 2, 2, 1, 2, 2, 1, 2, 2, 2, 2, 2, 1, 2, 2, 2, 4 ),
 ( 0.1519801020625093646, 0.1522107000347949768, 0.1523259990209377968, 0.1523404113942056215, 0.1523548237674734740, 0.1523836485140091790, 0.1524412980070805890, 0.1529024939516518133, 0.1538248858407942621, 0.1542860817853654865, 0.1543437312784368964, 0.1544013807715083064, 0.1545166797576510986, 0.1547472777299367386, 0.1552084736745079629, 0.1552661231675793452, 0.1552949479141150502, 0.1553237726606507552, 0.1554390716467935751, 0.1556696696190791873, 0.1561308655636504672, 0.1562461645497932594, 0.1562605769230611119, 0.1562749892963289644, 0.1563038140428646694, 0.1563614635359360794, 0.1565920615082216638, 0.1575144533973640293, 0.1579756493419352259, 0.1580909483280780181, 0.1581485978211494281, 0.1581774225676851331, 0.1582062473142208103, 0.1584368452865064225, 0.1593592371756488157, 0.1598204331202200124, 0.1600510310925056245, 0.1601086805855770068, 0.1601663300786484168, 0.1602816290647912090, 0.1607428250093624056, 0.1609734229816479900, 0.1610887219677907822, 0.1611463714608621922, 0.1612040209539335744, 0.1616652168985047433, 0.1618958148707903277, 0.1620111138569331199, 0.1620687633500045022, 0.1620975880965402072, 0.1621120004698080597, 0.1621264128430759122, 0.1630488047322183331, 0.1639711966213607541, 0.1640288461144321364, 0.1640576708609678414, 0.1640864956075035463, 0.1642017945936463386, 0.1644323925659319507, 0.1648935885105031751, 0.1667383722887880171, 0.1676607641779304658, 0.1678913621502160503, 0.1679490116432874602, 0.1679634240165553127, 0.1679706302031892251, 0.1679778363898231652, 0.1680066611363588702, 0.1681219601225017457, 0.1685831560670731921, 0.1695055479562161127, 0.1697361459285018359, 0.1698514449146447114, 0.1699090944077161214, 0.1699667439007875591, 0.1704279398453590333, 0.1713503317345019539, 0.1718115276790734280, 0.1718691771721448658, 0.1718980019186805708, 0.1719268266652163035, 0.1720421256513591790, 0.1722727236236449300, 0.1727339195682164041, 0.1728492185543592796, 0.1728636309276271321, 0.1728780433008949846, 0.1729068680474307174, 0.1729645175405021273, 0.1731951155127878228, 0.1736563114573592137, 0.1737716104435020614, 0.1738004351900377942, 0.1738148475633056467, 0.1738220537499395590, 0.1738292599365734992, 0.1738869094296449092, 0.1741175074019306046, 0.1750398992910733587, 0.1755010952356447218, 0.1757316932079304173, 0.1757605179544661222, 0.1757749303277339747, 0.1757893427010018272, 0.1758469921940732650, 0.1759622911802161127, 0.1778070749585018984, 0.1796518587367876840, 0.1796806834833233890, 0.1797095082298591218, 0.1797671577229305317, 0.1798824567090734072, 0.1801130546813591304, 0.1805742506259305491, 0.1814966425150734142 ),
 .UNSPECIFIED. ) ;
#5259=CARTESIAN_POINT ( 'NONE',  ( 4.607920928993483933, 61.01406224977615267, -12.68936818568986169 ) ) ;
#5262=CARTESIAN_POINT ( 'NONE',  ( 7.510597098088380719, 71.96138830267196340, 11.21812259324408600 ) ) ;
#5263=CARTESIAN_POINT ( 'NONE',  ( 12.38525507082440846, 57.62608040142962551, -5.371732038651033214 ) ) ;
#5264=CARTESIAN_POINT ( 'NONE',  ( 9.520470885617717371, 70.73000000000000398, -6.917026985038131848 ) ) ;
#5265=CARTESIAN_POINT ( 'NONE',  ( 7.272992578804311492, 73.88000000000000966, -10.01041549318726709 ) ) ;
#5267=CARTESIAN_POINT ( 'NONE',  ( -7.103768928370617353, 47.41597804696614560, 11.47982913313177100 ) ) ;
#5270=CARTESIAN_POINT ( 'NONE',  ( -10.92172942406179104, 76.23000000000000398, 7.935100905948387684 ) ) ;
#5273=CARTESIAN_POINT ( 'NONE',  ( 0.000000000000000000, 80.93000000000000682, -13.50000000000000000 ) ) ;
#5274=CARTESIAN_POINT ( 'NONE',  ( 13.41211784917930672, 33.48531139465221429, -1.588086113499469709 ) ) ;
#5275=CARTESIAN_POINT ( 'NONE',  ( -8.646567327866257813, 73.51228972662816830, -10.37015323812492795 ) ) ;
#5277=ORIENTED_EDGE ( 'NONE', *, *, #4123, .F. ) ;
#5278=CARTESIAN_POINT ( 'NONE',  ( -11.76794919243112325, 77.77999999999998693, -3.823638476888998827 ) ) ;
#5279=ORIENTED_EDGE ( 'NONE', *, *, #11955, .F. ) ;
#5280=CARTESIAN_POINT ( 'NONE',  ( -13.25459942044035522, 41.02077662930307156, 2.572929991539389949 ) ) ;
#5282=CARTESIAN_POINT ( 'NONE',  ( -10.13651174585746517, 44.27358713097766696, 8.916350804182590295 ) ) ;
#5285=CARTESIAN_POINT ( 'NONE',  ( -4.171729424061791036, 47.52999999999999403, 12.83926296998457239 ) ) ;
#5286=CARTESIAN_POINT ( 'NONE',  ( -3.154529238787930456, 71.56657476481365165, 13.12627027073374997 ) ) ;
#5289=CARTESIAN_POINT ( 'NONE',  ( -13.41193127300099341, 67.98364253050446848, 1.540011178302385098 ) ) ;
#5291=CARTESIAN_POINT ( 'NONE',  ( 10.53126001476443641, 54.75216587731950568, -8.446463747446077974 ) ) ;
#5294=CARTESIAN_POINT ( 'NONE',  ( -13.46180875895859863, 64.89487663202089607, -1.014747862443932114 ) ) ;
#5295=CARTESIAN_POINT ( 'NONE',  ( -2.260798837967500585, 35.59867054265404107, 13.31089883379040195 ) ) ;
#5299=CARTESIAN_POINT ( 'NONE',  ( -10.12002213127730599, 31.58559136480824847, -8.935086232216313817 ) ) ;
#5302=CARTESIAN_POINT ( 'NONE',  ( 6.398260148579073103, 59.91481284056136758, 11.88785343304075504 ) ) ;
#5304=CARTESIAN_POINT ( 'NONE',  ( -11.01659837438729639, 53.22442766106070167, 7.802951671792171418 ) ) ;
#5306=CARTESIAN_POINT ( 'NONE',  ( 11.76794919243112680, 49.57999999999999119, -3.823638476888993942 ) ) ;
#5307=CARTESIAN_POINT ( 'NONE',  ( -10.92172942406178926, 66.62999999999999545, -7.935100905948389460 ) ) ;
#5308=CARTESIAN_POINT ( 'NONE',  ( 12.17517545768429876, 51.21400524570869095, 5.885944979336298566 ) ) ;
#5309=CARTESIAN_POINT ( 'NONE',  ( -8.156909919353799054, 37.48992992535880120, -10.75717574548666988 ) ) ;
#5310=CARTESIAN_POINT ( 'NONE',  ( 12.55356676875865851, 36.24955043834909674, 4.970527845185399585 ) ) ;
#5312=CARTESIAN_POINT ( 'NONE',  ( 12.50000000000000000, 98.93000000000002103, 1.224646799147353059E-15 ) ) ;
#5313=CARTESIAN_POINT ( 'NONE',  ( -12.79026727553113574, 77.08651115985230717, 4.342467306496795132 ) ) ;
#5314=CARTESIAN_POINT ( 'NONE',  ( -6.837099079481030017, 79.43283332879646252, -11.64115347217222585 ) ) ;
#5317=CARTESIAN_POINT ( 'NONE',  ( -9.520470885617715595, 50.62999999999999545, -6.917026985038136289 ) ) ;
#5322=CARTESIAN_POINT ( 'NONE',  ( 12.23302105539664630, 75.63938679806872756, -5.712831750750090087 ) ) ;
#5324=CARTESIAN_POINT ( 'NONE',  ( 8.343458848123583849, 50.87999999999999545, -11.48378591275253768 ) ) ;
#5325=CARTESIAN_POINT ( 'NONE',  ( -11.76794919243112325, 35.92999999999999972, -2.882316262207890869E-15 ) ) ;
#5326=CARTESIAN_POINT ( 'NONE',  ( -4.326023945792585756, 41.52443083497766452, 12.78812056084685445 ) ) ;
#5327=CARTESIAN_POINT ( 'NONE',  ( -11.16450694584518821, 58.64450753011422535, -7.589733078635504171 ) ) ;
#5328=CARTESIAN_POINT ( 'NONE',  ( 3.163029786985204428, 44.79363501894889055, 13.12593006502653381 ) ) ;
#5331=CARTESIAN_POINT ( 'NONE',  ( -5.403018934253463357, 55.37564755616709533, -12.37835651047473462 ) ) ;
#5332=CARTESIAN_POINT ( 'NONE',  ( -13.28966059072577544, 49.84642827815817867, -2.375547661775054831 ) ) ;
#5333=CARTESIAN_POINT ( 'NONE',  ( 11.89192460612368230, 63.66677491408763245, -6.398269676534774852 ) ) ;
#5334=CARTESIAN_POINT ( 'NONE',  ( 11.89692274447344822, 42.66601371750947891, -6.380819027429124546 ) ) ;
#5335=CARTESIAN_POINT ( 'NONE',  ( 11.15118288380620193, 39.14369104754556616, 7.609292751937021038 ) ) ;
#5336=ORIENTED_EDGE ( 'NONE', *, *, #4495, .F. ) ;
#5337=CARTESIAN_POINT ( 'NONE',  ( -5.975539096150562557, 70.39796680391430073, -12.10731297254534233 ) ) ;
#5338=CARTESIAN_POINT ( 'NONE',  ( -1.118605446415761540, 61.22016070313634373, -13.45630796219644232 ) ) ;
#5344=CARTESIAN_POINT ( 'NONE',  ( 9.642912583273176352, 72.06081399527650433, 9.448274979317345057 ) ) ;
#5345=CARTESIAN_POINT ( 'NONE',  ( 13.41714116088561504, 57.48201277496755068, -1.496883884248394470 ) ) ;
#5346=CARTESIAN_POINT ( 'NONE',  ( -9.520470885617715595, 65.62999999999999545, -6.917026985038136289 ) ) ;
#5347=CARTESIAN_POINT ( 'NONE',  ( 9.520470885617717371, 76.73000000000000398, -6.917026985038131848 ) ) ;
#5348=CARTESIAN_POINT ( 'NONE',  ( -3.750474274136188058, 47.54514764475112543, 12.96859104554123832 ) ) ;
#5349=AXIS2_PLACEMENT_3D ( 'NONE', #14923, #12034, #11950 ) ;
#5355=CARTESIAN_POINT ( 'NONE',  ( 12.63363789258784919, 33.60376611986286122, -4.802290623392311275 ) ) ;
#5356=CARTESIAN_POINT ( 'NONE',  ( -8.104139024512610590, 73.48750659267841456, -10.79785279560148048 ) ) ;
#5358=ADVANCED_FACE ( 'NONE', ( #3360, #8776 ), #2018, .F. ) ;
#5360=CARTESIAN_POINT ( 'NONE',  ( -7.576616670048093940E-16, 78.67999999999999261, 12.37355403259654807 ) ) ;
#5364=CARTESIAN_POINT ( 'NONE',  ( -0.5192945675772188130, 44.66132637824818374, 13.49007153335960929 ) ) ;
#5366=CARTESIAN_POINT ( 'NONE',  ( -13.49999999999999822, 46.77999999999998693, -4.386415899144240349 ) ) ;
#5367=CARTESIAN_POINT ( 'NONE',  ( -13.45458289502007787, 70.96834162828989179, 1.106455849619511156 ) ) ;
#5369=CARTESIAN_POINT ( 'NONE',  ( -13.49991414957460734, 67.93186668194280742, 0.05455920092559319451 ) ) ;
#5371=CARTESIAN_POINT ( 'NONE',  ( 11.64104852335463569, 54.17556994306837481, 6.836414762659024369 ) ) ;
#5374=CARTESIAN_POINT ( 'NONE',  ( -12.96223390259766184, 64.79501674517034360, -3.772551170016495981 ) ) ;
#5375=EDGE_CURVE ( 'NONE', #2917, #3478, #14924, .T. ) ;
#5377=CARTESIAN_POINT ( 'NONE',  ( -13.07700142429071200, 34.81050193234469958, -3.356985455952382402 ) ) ;
#5378=ORIENTED_EDGE ( 'NONE', *, *, #13862, .T. ) ;
#5380=CARTESIAN_POINT ( 'NONE',  ( -1.999421349371006906, 31.25185859380078668, -13.35861204086333309 ) ) ;
#5381=CARTESIAN_POINT ( 'NONE',  ( 5.857397934039831000, 72.96667994176048921, -12.16334209717476433 ) ) ;
#5383=CARTESIAN_POINT ( 'NONE',  ( 4.844150578424402553, 59.85459317586593642, 12.60107945964768561 ) ) ;
#5385=CARTESIAN_POINT ( 'NONE',  ( -10.15663687072385635, 53.27256531316408683, 8.895185726361642509 ) ) ;
#5386=CARTESIAN_POINT ( 'NONE',  ( -7.272992578804310604, 48.38000000000000256, 10.01041549318726709 ) ) ;
#5388=CARTESIAN_POINT ( 'NONE',  ( 13.50000000000000000, 65.43000000000000682, 1.653273178848926867E-15 ) ) ;
#5389=CARTESIAN_POINT ( 'NONE',  ( 7.529356974007705539, 50.96216477632258091, 11.20855974609861683 ) ) ;
#5390=CARTESIAN_POINT ( 'NONE',  ( -8.055337278822385372, 37.48536512197566850, -10.83337006914397449 ) ) ;
#5392=CARTESIAN_POINT ( 'NONE',  ( 7.123395036261381819, 35.94488704657532452, 11.46981905184369133 ) ) ;
#5394=CARTESIAN_POINT ( 'NONE',  ( -11.99030647170363828, 74.15890988944590845, 6.203430717540079797 ) ) ;
#5395=CARTESIAN_POINT ( 'NONE',  ( -10.92538970018559752, 76.63004364216227771, -7.932434916078520359 ) ) ;
#5397=CARTESIAN_POINT ( 'NONE',  ( -12.63983531847754627, 79.75770905865978477, -4.762627132487758708 ) ) ;
#5399=CARTESIAN_POINT ( 'NONE',  ( -1.218708134006305066, 80.93000000000000682, 12.93996086231513409 ) ) ;
#5401=CARTESIAN_POINT ( 'NONE',  ( -7.272992578804307939, 44.47999999999999687, -10.01041549318727064 ) ) ;
#5405=CARTESIAN_POINT ( 'NONE',  ( -12.92793998791257337, 40.79065489648220222, -3.889074535841753999 ) ) ;
#5407=CARTESIAN_POINT ( 'NONE',  ( 12.31660755751379632, 75.22787210861035589, 5.528443808838319207 ) ) ;
#5408=CARTESIAN_POINT ( 'NONE',  ( -7.272992578804310604, 39.38000000000000256, 10.01041549318726709 ) ) ;
#5409=CARTESIAN_POINT ( 'NONE',  ( -7.190695991324615122, 41.41232216974482583, 11.42629593928715792 ) ) ;
#5410=CARTESIAN_POINT ( 'NONE',  ( -10.01477406080996424, 58.57944998338118126, -9.064625782096852546 ) ) ;
#5411=CARTESIAN_POINT ( 'NONE',  ( 4.266835968733136752, 44.83337071590181466, 12.80827659740992175 ) ) ;
#5412=CARTESIAN_POINT ( 'NONE',  ( 8.343458848123583849, 59.87999999999999545, -11.48378591275253768 ) ) ;
#5413=DIRECTION ( 'NONE',  ( 0.000000000000000000, -1.000000000000000000, 0.000000000000000000 ) ) ;
#5415=CARTESIAN_POINT ( 'NONE',  ( -7.484330937750101498, 49.46025488201969722, -11.23552342734818055 ) ) ;
#5416=CARTESIAN_POINT ( 'NONE',  ( 13.42206755560985698, 63.48053927388662743, -1.452603711471143866 ) ) ;
#5417=CARTESIAN_POINT ( 'NONE',  ( 12.89381267789188534, 42.57361400711115351, -4.003013936710616782 ) ) ;
#5418=CARTESIAN_POINT ( 'NONE',  ( 1.923701266133974741, 38.74915784931967977, 13.36274881015140359 ) ) ;
#5419=ORIENTED_EDGE ( 'NONE', *, *, #7512, .F. ) ;
#5423=CARTESIAN_POINT ( 'NONE',  ( -5.667801726729744694, 43.38591874923557867, -12.25259268504242804 ) ) ;
#5425=CARTESIAN_POINT ( 'NONE',  ( 9.320893742113016245, 60.81526611863908727, -9.765814572247236924 ) ) ;
#5427=CARTESIAN_POINT ( 'NONE',  ( 2.452834738616162191, 71.76819877488479449, 13.27530762632762773 ) ) ;
#5428=CARTESIAN_POINT ( 'NONE',  ( 13.36384259635446803, 57.49692427815710971, -1.912564800906976448 ) ) ;
#5429=CARTESIAN_POINT ( 'NONE',  ( 3.636496289402154414, 72.83000000000001251, 11.19198476289190936 ) ) ;
#5430=CARTESIAN_POINT ( 'NONE',  ( -9.520470885617717371, 78.23000000000000398, 6.917026985038133624 ) ) ;
#5432=CARTESIAN_POINT ( 'NONE',  ( -7.565627924516670433, 47.39628028002687188, 11.18235063458430467 ) ) ;
#5433=B_SPLINE_CURVE_WITH_KNOTS ( 'NONE', 3,
 ( #3583, #842, #15675, #12875, #6253, #15502, #8913, #8996, #14443, #14270, #11468, #17103, #764, #16929, #14354, #13049, #3414, #8827, #6172, #2242, #5010, #931, #11554, #4832, #10236, #17018, #15591, #3498, #2157, #11639, #10410, #7670, #6341, #11727, #15767, #3676, #9090, #2330, #16844, #3682, #16981, #4799, #6394, #1069, #6139, #2038, #12843, #7545, #7811, #9142, #10373, #2376, #14318, #14148, #10286, #15905, #14489, #2206, #11776, #10201, #7632, #981, #6482, #13010, #7719, #14234, #8791, #891, #4970, #7462, #731, #13184, #6304, #11518, #15638, #16895, #11867, #11689, #17153, #15553, #17066, #5064, #17242, #15727, #13095, #2119, #3465, #3635, #9049, #8879, #12923, #14401, #807, #6219, #11605, #10459, #3548, #4884, #8962, #10544, #15819, #2290, #3723, #5152, #3895, #5, #1158, #14749, #17328, #13350, #9400, #13606, #2638, #14581, #2462, #9572, #10625, #3814, #15991, #9313, #6568, #13519, #5327, #14663, #4071, #5240, #2552, #11949, #5502, #5410, #7981, #9486, #10711, #16077, #1239, #8069, #12293, #7893, #10797, #6651, #13270, #12033, #1410, #6825, #17412, #1501, #188, #8245, #4159, #6737, #2726, #3984, #10884, #13433, #2816, #1321, #12116, #14832, #16161, #8154, #6915, #12203, #96, #16254, #14922, #5594, #10974, #9227, #14041, #1928, #7351, #11235, #13687, #13859, #11061, #15272, #16612, #9838, #3170, #15010, #12381, #7258 ),
 .UNSPECIFIED., .F., .F.,
 ( 4, 1, 2, 2, 1, 1, 2, 2, 2, 2, 1, 2, 2, 2, 2, 2, 1, 2, 2, 1, 1, 1, 2, 2, 2, 2, 1, 1, 2, 2, 2, 2, 2, 1, 1, 2, 2, 1, 2, 2, 2, 2, 2, 1, 1, 2, 2, 2, 2, 1, 2, 2, 1, 1, 1, 2, 1, 2, 2, 1, 1, 2, 2, 2, 2, 2, 2, 1, 2, 2, 2, 2, 2, 1, 1, 1, 2, 2, 2, 2, 2, 2, 1, 1, 1, 1, 2, 2, 2, 2, 1, 1, 1, 2, 2, 1, 1, 2, 2, 2, 2, 2, 1, 1, 2, 2, 1, 2, 2, 4 ),
 ( 0.4167745338196714999, 0.4168890612373624127, 0.4169176930917851687, 0.4169320090189965189, 0.4169463249462078691, 0.4170035886550533255, 0.4172326434904351511, 0.4176907531611988578, 0.4186069725027261601, 0.4190650821734898668, 0.4192941370088716924, 0.4194086644265626052, 0.4195231918442535179, 0.4204394111857808758, 0.4213556305273082336, 0.4218137401980718848, 0.4219282676157627976, 0.4219354255793684727, 0.4219425835429741478, 0.4219568994701855535, 0.4219855313246083095, 0.4220427950334537659, 0.4222718498688357025, 0.4231880692103633934, 0.4241042885518910843, 0.4243333433872730209, 0.4243906070961184773, 0.4244192389505412333, 0.4244335548777526390, 0.4244478708049639892, 0.4245623982226550130, 0.4250205078934190528, 0.4254786175641831480, 0.4255931449818741719, 0.4256504086907196838, 0.4256790405451423842, 0.4256933564723537899, 0.4257076723995651957, 0.4259367272349471878, 0.4268529465764753228, 0.4273110562472394180, 0.4277691659180034578, 0.4286853852595315928, 0.4291434949302956881, 0.4293725497656777357, 0.4294298134745232476, 0.4294870771833687595, 0.4296016046010597278, 0.4305178239425879183, 0.4306323513602789421, 0.4306896150691243985, 0.4307182469235471545, 0.4307468787779699104, 0.4309759336133519581, 0.4314340432841160533, 0.4318921529548800931, 0.4319207848093028490, 0.4319351007365142547, 0.4319494166637256050, 0.4320066803725711169, 0.4321212077902621407, 0.4323502626256441883, 0.4332664819671723788, 0.4341827013087005138, 0.4344117561440825614, 0.4344403879985053174, 0.4344690198529280734, 0.4345262835617735853, 0.4346408109794646091, 0.4350989206502287043, 0.4369313593332849743, 0.4369456752604963801, 0.4369599911877077303, 0.4369886230421305418, 0.4370458867509760537, 0.4371604141686670775, 0.4373894690040492361, 0.4378475786748134424, 0.4387637980163419105, 0.4392219076871061167, 0.4394509625224882199, 0.4394581204860938950, 0.4394652784496996256, 0.4394795943769110314, 0.4395082262313337873, 0.4395654899401793547, 0.4396800173578704340, 0.4405962366993994017, 0.4415124560409283139, 0.4417415108763105280, 0.4418560382940016074, 0.4419133020028471748, 0.4419419338572699862, 0.4419490918208756614, 0.4419562497844813365, 0.4419705657116927422, 0.4424286753824571705, 0.4428867850532216544, 0.4431158398886038685, 0.4432303673062950033, 0.4433448947239861382, 0.4442611140655150503, 0.4443756414832061297, 0.4444329051920516971, 0.4444472211192631028, 0.4444615370464744530, 0.4444901689008972645, 0.4447192237362794787, 0.4451773334070439625, 0.4460935527485729302 ),
 .UNSPECIFIED. ) ;
#5435=CARTESIAN_POINT ( 'NONE',  ( -2.138189944381240881, 46.60311857767973009, 13.49999999999999822 ) ) ;
#5436=CARTESIAN_POINT ( 'NONE',  ( 8.343458848123580296, 73.97999999999998977, 11.48378591275253768 ) ) ;
#5437=CARTESIAN_POINT ( 'NONE',  ( 10.92172942406179104, 38.73000000000000398, -7.935100905948385908 ) ) ;
#5438=CARTESIAN_POINT ( 'NONE',  ( -4.171729424061791036, 34.53000000000000114, 12.83926296998457239 ) ) ;
#5440=CARTESIAN_POINT ( 'NONE',  ( -8.343458848123582072, 40.37999999999999545, 11.48378591275253768 ) ) ;
#5441=CARTESIAN_POINT ( 'NONE',  ( 13.44669328521645113, 33.38616000105633219, 1.256905049340288683 ) ) ;
#5442=CARTESIAN_POINT ( 'NONE',  ( -10.21952983404348458, 73.59082116183350308, -8.824648151853521583 ) ) ;
#5444=ORIENTED_EDGE ( 'NONE', *, *, #10059, .T. ) ;
#5446=CARTESIAN_POINT ( 'NONE',  ( -2.192110700418634206, 62.60117977606283546, 13.32083775572103512 ) ) ;
#5449=CARTESIAN_POINT ( 'NONE',  ( -13.50304319313545065, 40.92847950508530630, -0.04090659003252928444 ) ) ;
#5451=CARTESIAN_POINT ( 'NONE',  ( -11.16075802225499025, 44.21572617453895759, 7.595305378214631808 ) ) ;
#5452=DIRECTION ( 'NONE',  ( 0.000000000000000000, 0.000000000000000000, -1.000000000000000000 ) ) ;
#5453=CARTESIAN_POINT ( 'NONE',  ( -4.171729424061787483, 43.32999999999999829, -12.83926296998457417 ) ) ;
#5454=CARTESIAN_POINT ( 'NONE',  ( -12.93008338321562256, 71.06905249602031915, 3.881103319701416421 ) ) ;
#5458=CARTESIAN_POINT ( 'NONE',  ( -12.51906270480975714, 68.11402849159634343, 5.063022440180297679 ) ) ;
#5460=CARTESIAN_POINT ( 'NONE',  ( 13.05816527381254666, 54.30794901924826235, 3.425548258310757710 ) ) ;
#5462=CARTESIAN_POINT ( 'NONE',  ( -13.37946240819375632, 64.99289358431782659, 1.800012917707035420 ) ) ;
#5463=ORIENTED_EDGE ( 'NONE', *, *, #8679, .T. ) ;
#5465=CARTESIAN_POINT ( 'NONE',  ( -13.34870812582085264, 35.00060202485487793, 2.015441165875480944 ) ) ;
#5470=CARTESIAN_POINT ( 'NONE',  ( -5.976125424403057274, 31.39799419942340819, -12.10679337452015503 ) ) ;
#5471=CARTESIAN_POINT ( 'NONE',  ( 3.326001417435852758, 73.06040922954841221, -13.08388940738754158 ) ) ;
#5475=CARTESIAN_POINT ( 'NONE',  ( -10.92172942406179104, 74.23000000000000398, 7.935100905948387684 ) ) ;
#5476=CARTESIAN_POINT ( 'NONE',  ( -13.47854047285069790, 52.90374775157414433, -0.7608956181714418010 ) ) ;
#5477=CARTESIAN_POINT ( 'NONE',  ( 7.272992578804308828, 51.97999999999998977, 10.01041549318726709 ) ) ;
#5479=CARTESIAN_POINT ( 'NONE',  ( 3.182817155287316346, 50.79451344581282513, 13.11991552520243154 ) ) ;
#5480=CARTESIAN_POINT ( 'NONE',  ( -5.657249770757468710, 37.38550904903456029, -12.25752513883166017 ) ) ;
#5481=CARTESIAN_POINT ( 'NONE',  ( 13.26418904884840977, 36.34139017399488836, 2.514688632223297748 ) ) ;
#5483=CARTESIAN_POINT ( 'NONE',  ( -11.97893996698503116, 74.15978608494305035, 6.225358771720943984 ) ) ;
#5484=CARTESIAN_POINT ( 'NONE',  ( -13.32578297425849811, 76.85407912984071288, -2.163276995893335997 ) ) ;
#5485=CARTESIAN_POINT ( 'NONE',  ( -10.71227016036927715, 80.24208485109964784, 8.218659176430634261 ) ) ;
#5491=CARTESIAN_POINT ( 'NONE',  ( 11.76794919243112325, 49.28000000000000114, 3.823638476888997051 ) ) ;
#5495=CARTESIAN_POINT ( 'NONE',  ( -5.651595557928720481, 40.38528827607240856, -12.26012243411721414 ) ) ;
#5496=CARTESIAN_POINT ( 'NONE',  ( 8.343458848123583849, 35.87999999999999545, -11.48378591275253768 ) ) ;
#5497=CARTESIAN_POINT ( 'NONE',  ( 13.32852092168753444, 75.35474669015187033, 2.144890943754141688 ) ) ;
#5499=CARTESIAN_POINT ( 'NONE',  ( -11.76794919243112325, 32.77999999999999403, -3.823638476888998827 ) ) ;
#5500=CARTESIAN_POINT ( 'NONE',  ( -9.311494743582063194, 41.31572317635779257, 9.774769270546801891 ) ) ;
#5501=EDGE_CURVE ( 'NONE', #5168, #4872, #2903, .T. ) ;
#5502=CARTESIAN_POINT ( 'NONE',  ( -10.46166914714195251, 58.60362355544496182, -8.535617357307549113 ) ) ;
#5503=CARTESIAN_POINT ( 'NONE',  ( 0.000000000000000000, 3.999999999999961808, -13.50000000000000000 ) ) ;
#5505=CARTESIAN_POINT ( 'NONE',  ( 9.265344266068700207, 30.04200008453489090, 9.818925412339686076 ) ) ;
#5507=CARTESIAN_POINT ( 'NONE',  ( -11.19025799215657990, 49.64609340414283878, -7.551709246331172132 ) ) ;
#5508=CARTESIAN_POINT ( 'NONE',  ( 13.46290329342287961, 63.39539363581478426, 1.002166455802397937 ) ) ;
#5509=CARTESIAN_POINT ( 'NONE',  ( 11.14094309903787661, 42.14309538808735311, 7.629476624620709302 ) ) ;
#5513=CARTESIAN_POINT ( 'NONE',  ( 2.107853069822502790E-14, 31.18000000000000682, -13.50000000000000000 ) ) ;
#5515=VERTEX_POINT ( 'NONE', #15322 ) ;
#5516=AXIS2_PLACEMENT_3D ( 'NONE', #11576, #5028, #2088 ) ;
#5517=CARTESIAN_POINT ( 'NONE',  ( -10.96290148446646739, 43.63233836037143476, -7.879540134695893983 ) ) ;
#5518=CARTESIAN_POINT ( 'NONE',  ( -7.499999999999998224, 104.9266221009243907, 8.932545650451682917 ) ) ;
#5519=CARTESIAN_POINT ( 'NONE',  ( 11.39486570637464524, 60.70084465595979140, -7.240720970025911640 ) ) ;
#5521=CARTESIAN_POINT ( 'NONE',  ( 9.772396245993814290, 72.06742462017868434, 9.313983778355371612 ) ) ;
#5522=CARTESIAN_POINT ( 'NONE',  ( 13.21191709738701547, 66.52910010606868241, -2.802833979466235359 ) ) ;
#5523=CARTESIAN_POINT ( 'NONE',  ( 4.938667887072522689, 56.85812260315885425, 12.56421927770909441 ) ) ;
#5524=CARTESIAN_POINT ( 'NONE',  ( 9.520470885617715595, 73.12999999999999545, 6.917026985038134512 ) ) ;
#5525=CARTESIAN_POINT ( 'NONE',  ( 3.636496289402154414, 63.82999999999999829, 11.19198476289190936 ) ) ;
#5526=CARTESIAN_POINT ( 'NONE',  ( -5.721591114156050928, 47.47194874911851770, 12.23566511108304944 ) ) ;
#5527=DIRECTION ( 'NONE',  ( 0.000000000000000000, 1.000000000000000000, 0.000000000000000000 ) ) ;
#5528=CARTESIAN_POINT ( 'NONE',  ( 13.50000000000000000, 74.42999999999999261, 1.653273178848926867E-15 ) ) ;
#5530=CARTESIAN_POINT ( 'NONE',  ( -4.950837632938861255, 56.50144079815311215, 12.56439702090226795 ) ) ;
#5532=CARTESIAN_POINT ( 'NONE',  ( -2.138189944381240881, 52.60311857767972299, 13.49999999999999822 ) ) ;
#5533=CARTESIAN_POINT ( 'NONE',  ( 11.30035725208420416, 33.70704868103326390, -7.386062474298981329 ) ) ;
#5535=CARTESIAN_POINT ( 'NONE',  ( -8.891200544363830713E-16, 70.68000000000000682, 13.50000000000000000 ) ) ;
#5538=CARTESIAN_POINT ( 'NONE',  ( -5.383880044892523031, 62.48502448089114125, 12.38026817833133464 ) ) ;
#5540=CARTESIAN_POINT ( 'NONE',  ( -13.48341350937561245, 40.95312764241855774, 0.6709278542534650169 ) ) ;
#5544=CARTESIAN_POINT ( 'NONE',  ( -13.25475736232484536, 44.02032189088402703, 2.561673765456097929 ) ) ;
#5546=CARTESIAN_POINT ( 'NONE',  ( 13.50000000000000000, 42.42999999999999261, 1.653273178848926867E-15 ) ) ;
#5547=CARTESIAN_POINT ( 'NONE',  ( -10.92172942406178926, 48.63000000000000256, -7.935100905948389460 ) ) ;
#5548=CARTESIAN_POINT ( 'NONE',  ( -13.45742039876322593, 70.96712778246572384, 1.071852073170212583 ) ) ;
#5549=VECTOR ( 'NONE', #2122, 1000.000000000000000 ) ;
#5551=CARTESIAN_POINT ( 'NONE',  ( -6.904622430831049762, 67.43546043278743696, -11.61287708378492844 ) ) ;
#5553=CARTESIAN_POINT ( 'NONE',  ( 13.07586280307878646, 54.31047242261610819, 3.357496143552672230 ) ) ;
#5554=CARTESIAN_POINT ( 'NONE',  ( -11.72818448617283060, 64.68162745856044182, -6.687357485148088365 ) ) ;
#5557=CARTESIAN_POINT ( 'NONE',  ( -11.99508897926147633, 34.70129772595861795, -6.199144905531880134 ) ) ;
#5558=ORIENTED_EDGE ( 'NONE', *, *, #13733, .F. ) ;
#5559=CARTESIAN_POINT ( 'NONE',  ( 13.47351438217874353, 78.45921297451653231, -0.8456703420030140528 ) ) ;
#5562=CARTESIAN_POINT ( 'NONE',  ( -8.613042784256499829, 31.51074471318071701, -10.39969252900315588 ) ) ;
#5563=CARTESIAN_POINT ( 'NONE',  ( 10.39863764822032799, 72.75946676389163770, -8.609374654801005278 ) ) ;
#5567=CARTESIAN_POINT ( 'NONE',  ( -8.343458848123576743, 70.48000000000000398, -11.48378591275254301 ) ) ;
#5568=CARTESIAN_POINT ( 'NONE',  ( -13.22220161272585415, 53.02624049857811883, 2.725156051118921674 ) ) ;
#5569=CARTESIAN_POINT ( 'NONE',  ( -3.636496289402153081, 44.32999999999999829, -11.19198476289190936 ) ) ;
#5570=CARTESIAN_POINT ( 'NONE',  ( 13.49999999999999822, 68.28000000000001535, 4.386415899144237684 ) ) ;
#5572=CARTESIAN_POINT ( 'NONE',  ( 12.08458693532313077, 69.65149262053893153, -6.018661980718448490 ) ) ;
#5574=CARTESIAN_POINT ( 'NONE',  ( -4.329460928816934562, 37.33568557241510177, -12.78734651434877279 ) ) ;
#5575=CARTESIAN_POINT ( 'NONE',  ( 3.187467471045011269, 35.79457724241678562, 13.12592493638926605 ) ) ;
#5577=CARTESIAN_POINT ( 'NONE',  ( -10.42895341926080732, 74.25780691452938242, 8.572557870554565085 ) ) ;
#5578=( BOUNDED_CURVE ( )  B_SPLINE_CURVE ( 1, ( #5922, #11132 ),
 .UNSPECIFIED., .F., .F. ) 
 B_SPLINE_CURVE_WITH_KNOTS ( ( 2, 2 ),
 ( 0.000000000000000000, 1.000000000000000000 ),
 .UNSPECIFIED. ) 
 CURVE ( )  GEOMETRIC_REPRESENTATION_ITEM ( )  RATIONAL_B_SPLINE_CURVE ( ( 0.9782075447827165426, 0.9782075447827165426 ) ) 
 REPRESENTATION_ITEM ( '' )  );
#5579=CARTESIAN_POINT ( 'NONE',  ( -12.98389310290256837, 77.06248361752962239, 3.703783162427040754 ) ) ;
#5582=CARTESIAN_POINT ( 'NONE',  ( -8.711848673609697613, 80.93000000000002103, 8.870066681586113333 ) ) ;
#5586=CARTESIAN_POINT ( 'NONE',  ( 9.520470885617715595, 49.13000000000000256, 6.917026985038134512 ) ) ;
#5588=CARTESIAN_POINT ( 'NONE',  ( -11.89602199667058535, 40.69392324594991805, -6.382374777626396600 ) ) ;
#5590=CARTESIAN_POINT ( 'NONE',  ( 10.10331317266893336, 75.08473884772422480, 8.954271362371356346 ) ) ;
#5592=CARTESIAN_POINT ( 'NONE',  ( -3.636496289402153081, 35.32999999999999829, -11.19198476289190936 ) ) ;
#5593=CARTESIAN_POINT ( 'NONE',  ( -7.024337696613344839, 41.41931987901391921, 11.52861112765396889 ) ) ;
#5594=CARTESIAN_POINT ( 'NONE',  ( -3.973104663489275712, 58.32285798913706287, -12.90221010763657361 ) ) ;
#5596=DIRECTION ( 'NONE',  ( 0.000000000000000000, 0.000000000000000000, -1.000000000000000000 ) ) ;
#5597=CARTESIAN_POINT ( 'NONE',  ( -10.92172942406178926, 57.63000000000000256, -7.935100905948389460 ) ) ;
#5598=CARTESIAN_POINT ( 'NONE',  ( -13.26588416208786647, 49.84179529059223768, -2.503281531231600798 ) ) ;
#5599=CARTESIAN_POINT ( 'NONE',  ( 13.49885676942609614, 63.44608529167037858, -0.4713237517850633052 ) ) ;
#5600=CARTESIAN_POINT ( 'NONE',  ( 10.07256217038269064, 42.08276731119590153, 8.999075269577950564 ) ) ;
#5601=CARTESIAN_POINT ( 'NONE',  ( 1.747925173837019175, 38.74284411846687703, 13.38730336300498536 ) ) ;
#5603=CARTESIAN_POINT ( 'NONE',  ( -4.225622128461934857, 70.33197010581022823, -12.82179701616371226 ) ) ;
#5608=CARTESIAN_POINT ( 'NONE',  ( -6.508780211867530419, 43.41933150643208705, -11.83743217236817102 ) ) ;
#5609=CARTESIAN_POINT ( 'NONE',  ( -7.499999999999999112, 108.6686507028258717, -2.034160311361953966 ) ) ;
#5610=CARTESIAN_POINT ( 'NONE',  ( 10.70400462187975776, 60.74250492953063230, -8.227714730520327535 ) ) ;
#5613=CARTESIAN_POINT ( 'NONE',  ( 13.49854170867679493, 66.44634207941858506, -0.4798613340506648894 ) ) ;
#5614=CARTESIAN_POINT ( 'NONE',  ( 6.439080603729475882, 56.91648054290170222, 11.87284769991120648 ) ) ;
#5615=CARTESIAN_POINT ( 'NONE',  ( -9.520470885617715595, 59.63000000000000256, -6.917026985038136289 ) ) ;
#5616=CARTESIAN_POINT ( 'NONE',  ( 3.636496289402157078, 68.03000000000000114, -11.19198476289190936 ) ) ;
#5617=CARTESIAN_POINT ( 'NONE',  ( -9.668289202133056648, 47.29798508749041019, 9.423919283597269825 ) ) ;
#5618=CARTESIAN_POINT ( 'NONE',  ( -4.171729424061787483, 45.33000000000000540, -12.83926296998457417 ) ) ;
#5619=DIRECTION ( 'NONE',  ( 0.000000000000000000, -1.000000000000000000, 0.000000000000000000 ) ) ;
#5625=CARTESIAN_POINT ( 'NONE',  ( 13.01499335373094013, 33.55803638891549667, -3.586594114771764374 ) ) ;
#5627=DIRECTION ( 'NONE',  ( 0.000000000000000000, -1.000000000000000000, 0.000000000000000000 ) ) ;
#5633=CARTESIAN_POINT ( 'NONE',  ( -13.47827025046990990, 43.95642512897427423, 0.7656873746960646265 ) ) ;
#5636=CARTESIAN_POINT ( 'NONE',  ( -8.343458848123582072, 38.37999999999998835, 11.48378591275254124 ) ) ;
#5637=CARTESIAN_POINT ( 'NONE',  ( -4.171729424061791036, 46.53000000000000114, 12.83926296998457239 ) ) ;
#5638=CARTESIAN_POINT ( 'NONE',  ( -12.81710173804216346, 71.08258523398228590, 4.240278988823360962 ) ) ;
#5640=CARTESIAN_POINT ( 'NONE',  ( -11.73022876284554883, 67.68182808645379112, -6.682201463345557535 ) ) ;
#5642=CARTESIAN_POINT ( 'NONE',  ( 11.67482575541059475, 54.17791662511717732, 6.778571967042572588 ) ) ;
#5644=CARTESIAN_POINT ( 'NONE',  ( -3.261899838592319689, 64.29728490861971579, -13.10000070067140321 ) ) ;
#5645=ORIENTED_EDGE ( 'NONE', *, *, #4272, .F. ) ;
#5646=CARTESIAN_POINT ( 'NONE',  ( -13.49999999999999822, 64.07999999999999829, 4.386415899144235020 ) ) ;
#5647=CARTESIAN_POINT ( 'NONE',  ( -12.51102511793943961, 34.74498775374014059, -5.090906052585752128 ) ) ;
#5649=CARTESIAN_POINT ( 'NONE',  ( 13.49994509081106386, 78.41450604159769000, 0.4393232071407982553 ) ) ;
#5652=CARTESIAN_POINT ( 'NONE',  ( 11.18757194939378330, 72.71406989031071078, -7.555694557022631486 ) ) ;
#5655=CARTESIAN_POINT ( 'NONE',  ( 13.50000000000000000, 75.42999999999999261, 1.653273178848926867E-15 ) ) ;
#5656=CARTESIAN_POINT ( 'NONE',  ( -11.42382290241512521, 52.66093731307155679, -7.194032250886600366 ) ) ;
#5657=CARTESIAN_POINT ( 'NONE',  ( 11.76794919243112680, 43.57999999999999119, -3.823638476888993942 ) ) ;
#5658=CARTESIAN_POINT ( 'NONE',  ( -8.691771469529815392E-16, 70.67999999999999261, 14.19474002721660355 ) ) ;
#5660=B_SPLINE_CURVE_WITH_KNOTS ( 'NONE', 3,
 ( #5765, #11149, #8422, #15273, #16525, #13775, #15185, #1674, #4518, #15447, #16436, #13949, #9839, #4338, #1764, #11413, #12643, #8512, #532, #3172, #7259, #7353, #1846, #16700, #7173, #8683, #447, #16785, #4605, #3266, #14042, #1930, #3356, #8772, #7006, #9748, #15092, #14298, #4862, #15797, #12904, #17221, #5131, #10522, #14381, #16873, #17045, #14212, #960, #2271, #12988, #6372, #707, #15532, #11584, #4950, #13162, #788, #10265, #6117, #15885, #11846, #4778, #12820, #11497, #6198, #1048, #2358, #3612, #6461, #7612, #7440, #2013, #8940, #11756, #15616, #5042, #3443, #871, #10354, #16960, #6282, #17132, #7524, #9205, #11670, #15708, #10181, #8858, #9026, #2097, #3525, #2184, #10439, #7697, #13074, #3703, #3792, #9120, #14470, #7791, #10956, #14644, #10775, #11926, #8045, #10606, #6633, #2616, #6898, #13413, #7872, #13249, #2796, #3876, #14557, #9292, #2532, #17307, #17477, #2440, #12183, #4050, #15973, #7960, #5219, #16230, #16140, #13330, #14811, #3965, #16058, #1221, #12013, #9463, #74, #1136, #6547, #17393, #2706, #9552, #10861, #5309, #10692, #9378, #5390, #14727, #1303, #6717, #12095, #14902, #8135, #5480, #13500, #1390, #6805, #4139, #8227, #12272, #16324, #13588, #1482, #169, #5574, #4230, #9907, #8492, #4318, #16505, #12542, #14023, #16592, #15254, #15074, #13843, #3153, #9728, #7071, #15343, #8404, #12362, #7157, #1656 ),
 .UNSPECIFIED., .F., .F.,
 ( 4, 2, 1, 2, 2, 1, 2, 2, 2, 2, 1, 1, 2, 2, 1, 2, 2, 2, 2, 2, 1, 2, 2, 1, 1, 2, 2, 1, 2, 2, 2, 2, 1, 1, 1, 2, 2, 2, 1, 1, 2, 2, 1, 2, 2, 2, 2, 1, 2, 2, 1, 2, 2, 2, 1, 1, 2, 2, 2, 2, 2, 2, 2, 2, 2, 2, 2, 2, 2, 1, 1, 1, 2, 2, 1, 1, 1, 2, 2, 2, 2, 2, 2, 1, 2, 2, 1, 2, 2, 2, 1, 2, 2, 1, 2, 2, 2, 2, 1, 1, 1, 1, 2, 2, 2, 2, 2, 4 ),
 ( 0.8284411291432991487, 0.8293602319378399201, 0.8294751197871574888, 0.8295038417494868810, 0.8295325637118162732, 0.8295900076364750575, 0.8298197833351103059, 0.8302793347323806916, 0.8311984375269214631, 0.8314282132255567115, 0.8314856571502154958, 0.8315143791125448880, 0.8315287400937095841, 0.8315431010748742802, 0.8316579889241918488, 0.8321175403214622346, 0.8330366431160030061, 0.8334961945132733918, 0.8335536384379321762, 0.8336110823625909605, 0.8337259702119086402, 0.8339557459105437776, 0.8348748487050845490, 0.8353344001023548238, 0.8355641758009900721, 0.8355928977633194643, 0.8356216197256488565, 0.8356790636503076408, 0.8357939514996252095, 0.8367130542941659810, 0.8371726056914362557, 0.8374023813900715041, 0.8375172692393890728, 0.8375747131640478571, 0.8376034351263772493, 0.8376177961075419454, 0.8376321570887066414, 0.8394703626777877403, 0.8395852505271053090, 0.8396426944517640933, 0.8396570554329287894, 0.8396714164140934855, 0.8397001383764228777, 0.8399299140750580150, 0.8403894654723281787, 0.8413085682668687282, 0.8415383439655038655, 0.8416532318148214342, 0.8416819537771508264, 0.8417106757394802186, 0.8417681196641390029, 0.8422276710614091666, 0.8431467738559497160, 0.8436063252532199908, 0.8436637691778787751, 0.8436924911402081673, 0.8437068521213728634, 0.8437212131025375594, 0.8438361009518551281, 0.8440658766504902655, 0.8449849794450308149, 0.8454445308423010896, 0.8456743065409362270, 0.8457891943902537957, 0.8459040822395713644, 0.8468231850341118028, 0.8477422878286523522, 0.8477710097909817444, 0.8477997317533111366, 0.8478571756779699209, 0.8479720635272874896, 0.8482018392259226269, 0.8486613906231930127, 0.8495804934177335621, 0.8496953812670511308, 0.8497528251917099151, 0.8497815471540393073, 0.8497959081352040034, 0.8498102691163686995, 0.8500400448150039479, 0.8504995962122743336, 0.8514186990068152161, 0.8516484747054503535, 0.8517633625547680332, 0.8518208064794268175, 0.8518495284417562097, 0.8518782504040856018, 0.8523378018013559876, 0.8532569045958968701, 0.8537164559931672558, 0.8538313438424848245, 0.8538600658048142167, 0.8538887877671437199, 0.8539462316918025042, 0.8541760073904376416, 0.8546355587877080273, 0.8548653344863431647, 0.8549802223356608444, 0.8550951101849784131, 0.8555546615822487988, 0.8557844372808839362, 0.8558418812055427205, 0.8558706031678721127, 0.8558993251302015048, 0.8560142129795191845, 0.8569333157740598450, 0.8573928671713302307, 0.8578524185686006165 ),
 .UNSPECIFIED. ) ;
#5662=CARTESIAN_POINT ( 'NONE',  ( 3.582496635403904062, 68.80879950270664835, 13.01598647554185639 ) ) ;
#5664=AXIS2_PLACEMENT_3D ( 'NONE', #7318, #2158, #11382 ) ;
#5667=CARTESIAN_POINT ( 'NONE',  ( -11.99020945619393075, 74.15891743954519200, 6.203620012955681773 ) ) ;
#5668=CARTESIAN_POINT ( 'NONE',  ( -5.437383120998211972, 76.37690954485367456, -12.36259108923011674 ) ) ;
#5670=LINE ( 'NONE', #345, #10058 ) ;
#5672=DIRECTION ( 'NONE',  ( 0.000000000000000000, 0.000000000000000000, -1.000000000000000000 ) ) ;
#5674=CARTESIAN_POINT ( 'NONE',  ( 11.76794919243112680, 46.57999999999999829, -3.823638476888993942 ) ) ;
#5676=CARTESIAN_POINT ( 'NONE',  ( -10.40732797419851963, 32.25961365229549926, 8.610261354245384524 ) ) ;
#5677=CARTESIAN_POINT ( 'NONE',  ( 13.48494557894230539, 75.45196395580148874, -0.6373953516020099963 ) ) ;
#5679=CARTESIAN_POINT ( 'NONE',  ( -11.76794919243112325, 33.07999999999998408, 3.823638476888994386 ) ) ;
#5680=CARTESIAN_POINT ( 'NONE',  ( -12.53918026858758061, 41.11172392978211576, 5.001923395695291319 ) ) ;
#5681=( GEOMETRIC_REPRESENTATION_CONTEXT ( 3 ) GLOBAL_UNCERTAINTY_ASSIGNED_CONTEXT ( ( #10004 ) ) GLOBAL_UNIT_ASSIGNED_CONTEXT ( ( #15008, #12290, #16433 ) ) REPRESENTATION_CONTEXT ( 'NONE', 'WORKASPACE' ) );
#5682=CARTESIAN_POINT ( 'NONE',  ( 4.861248255796603246, 52.00477046739004550, -12.59468897525855624 ) ) ;
#5683=ADVANCED_FACE ( 'NONE', ( #3578 ), #3493, .T. ) ;
#5685=CARTESIAN_POINT ( 'NONE',  ( 8.293271311656841505, 36.86388732214020081, -10.65232149131729855 ) ) ;
#5687=CARTESIAN_POINT ( 'NONE',  ( -13.36307422868558703, 49.86276556841097118, -1.922284815108510792 ) ) ;
#5688=CARTESIAN_POINT ( 'NONE',  ( 10.61938128423869365, 63.11274346617898345, 8.335457914628065623 ) ) ;
#5689=CARTESIAN_POINT ( 'NONE',  ( 8.359408846421068517, 41.99913092812320059, 10.60054140072220008 ) ) ;
#5690=CARTESIAN_POINT ( 'NONE',  ( 4.140633560867821750, 38.82887436838161932, 12.84970033327834926 ) ) ;
#5692=CARTESIAN_POINT ( 'NONE',  ( -9.520470885617717371, 72.23000000000000398, 6.917026985038133624 ) ) ;
#5695=VERTEX_POINT ( 'NONE', #5100 ) ;
#5696=CARTESIAN_POINT ( 'NONE',  ( -2.258558314520655141, 43.26120942166914318, -13.30973117251418358 ) ) ;
#5698=CARTESIAN_POINT ( 'NONE',  ( 11.18658721041314763, 60.71407845817507365, -7.562691393858058220 ) ) ;
#5701=CARTESIAN_POINT ( 'NONE',  ( 13.39967370095669352, 66.37080031235018396, 1.701620727286339285 ) ) ;
#5702=CARTESIAN_POINT ( 'NONE',  ( 1.442593713695419444, 56.73187045217319735, 13.42270898593407935 ) ) ;
#5703=CARTESIAN_POINT ( 'NONE',  ( 9.520470885617715595, 55.12999999999999545, 6.917026985038134512 ) ) ;
#5704=CARTESIAN_POINT ( 'NONE',  ( -7.576616670048093940E-16, 69.68000000000000682, 12.37355403259654985 ) ) ;
#5705=CARTESIAN_POINT ( 'NONE',  ( -13.49176311494470681, 46.94621656216333605, 0.4715414884418810404 ) ) ;
#5707=CARTESIAN_POINT ( 'NONE',  ( 2.000520122481862502E-14, 73.67999999999999261, 13.50000000000000000 ) ) ;
#5709=CARTESIAN_POINT ( 'NONE',  ( 8.331761120487128025, 30.86213173433371182, -10.62223457817614225 ) ) ;
#5710=CARTESIAN_POINT ( 'NONE',  ( -5.728624354601031143, 56.47170591170164045, 12.22464376188452206 ) ) ;
#5712=CARTESIAN_POINT ( 'NONE',  ( -4.171729424061787483, 51.32999999999999829, -12.83926296998457417 ) ) ;
#5713=CARTESIAN_POINT ( 'NONE',  ( 9.450540653006603620, 33.05113386618337756, 9.640956752933217189 ) ) ;
#5715=CARTESIAN_POINT ( 'NONE',  ( 4.192885926659680962, 40.02925677665264459, -12.83275633162273976 ) ) ;
#5716=ORIENTED_EDGE ( 'NONE', *, *, #8002, .T. ) ;
#5717=CARTESIAN_POINT ( 'NONE',  ( -6.180644893164205733, 62.45382428835798549, 12.00516588008592045 ) ) ;
#5720=CARTESIAN_POINT ( 'NONE',  ( -13.42920886623006105, 43.88144049818974679, -1.399576480510955401 ) ) ;
#5723=CARTESIAN_POINT ( 'NONE',  ( 13.49999999999999822, 30.27999999999999403, 4.386415899144237684 ) ) ;
#5725=CARTESIAN_POINT ( 'NONE',  ( -6.333153400715997527, 46.41227267698536707, -11.92229910835860096 ) ) ;
#5726=CARTESIAN_POINT ( 'NONE',  ( -7.633650000891075038, 67.46670873368714183, -11.13611842294216814 ) ) ;
#5729=CARTESIAN_POINT ( 'NONE',  ( 13.47366810957596073, 54.45994921630894225, -0.8662603028162058072 ) ) ;
#5730=CARTESIAN_POINT ( 'NONE',  ( -7.473959287627094383, 64.45978679042782744, -11.24528175482741688 ) ) ;
#5731=ORIENTED_EDGE ( 'NONE', *, *, #16652, .F. ) ;
#5733=CARTESIAN_POINT ( 'NONE',  ( -11.84936134568200750, 34.69045658404807142, -6.468588641860953281 ) ) ;
#5735=CARTESIAN_POINT ( 'NONE',  ( 11.80121533525529998, 78.18692176761594226, 6.556313531099895897 ) ) ;
#5736=CARTESIAN_POINT ( 'NONE',  ( 13.49999999999999822, 47.28000000000000114, 4.386415899144236796 ) ) ;
#5738=CARTESIAN_POINT ( 'NONE',  ( 9.400174290359263551, 72.81156905856246908, -9.698804889119921668 ) ) ;
#5739=CARTESIAN_POINT ( 'NONE',  ( 2.473603416425627088, 79.09105862451949065, -13.27151636866100404 ) ) ;
#5741=CARTESIAN_POINT ( 'NONE',  ( 2.607531440858944223E-15, 61.17999999999998550, -14.19474002721660355 ) ) ;
#5742=CARTESIAN_POINT ( 'NONE',  ( -13.46057364109657151, 52.96569535534638362, 1.031020640244758368 ) ) ;
#5743=CARTESIAN_POINT ( 'NONE',  ( -7.576616670048093940E-16, 39.67999999999999261, 12.37355403259654985 ) ) ;
#5745=CARTESIAN_POINT ( 'NONE',  ( 4.171729424061789260, 58.82999999999999829, 12.83926296998457417 ) ) ;
#5746=CARTESIAN_POINT ( 'NONE',  ( 0.000000000000000000, 3.999999999999961808, 0.000000000000000000 ) ) ;
#5747=CARTESIAN_POINT ( 'NONE',  ( 12.20035770258772878, 69.21726674062897189, 5.799875816967380082 ) ) ;
#5751=CARTESIAN_POINT ( 'NONE',  ( -11.28504704467765407, 74.20798629947016423, 7.409300117848043321 ) ) ;
#5752=CARTESIAN_POINT ( 'NONE',  ( -9.412723707183822341, 76.54928254877205518, -9.677326817764578593 ) ) ;
#5756=CARTESIAN_POINT ( 'NONE',  ( -3.636496289402153081, 41.32999999999999829, -11.19198476289190936 ) ) ;
#5758=CARTESIAN_POINT ( 'NONE',  ( -4.700843871787972361, 32.51074219333796833, 12.65638779739501629 ) ) ;
#5759=CARTESIAN_POINT ( 'NONE',  ( 13.48116795019819847, 75.45464721144679743, -0.7146242057943285042 ) ) ;
#5760=EDGE_CURVE ( 'NONE', #5168, #15852, #13129, .T. ) ;
#5762=CARTESIAN_POINT ( 'NONE',  ( 3.636496289402154414, 33.82999999999999829, 11.19198476289190936 ) ) ;
#5763=CARTESIAN_POINT ( 'NONE',  ( 13.50000000000000355, 83.57999999999999829, -4.386415899144233244 ) ) ;
#5764=CARTESIAN_POINT ( 'NONE',  ( -1.005545769327274827E-13, 52.18000000000000682, -13.50000000000000000 ) ) ;
#5765=CARTESIAN_POINT ( 'NONE',  ( 1.785599194582236620E-06, 38.68004968046676595, 13.49999999999976374 ) ) ;
#5766=CARTESIAN_POINT ( 'NONE',  ( 0.1182731081639512155, 37.17574734598938591, -13.49948365268883776 ) ) ;
#5768=CARTESIAN_POINT ( 'NONE',  ( -0.5736229098616415500, 49.20060530840606816, -13.48854776642249576 ) ) ;
#5769=CARTESIAN_POINT ( 'NONE',  ( 7.569887829306680693, 62.96389870297073088, 11.17971963918203393 ) ) ;
#5770=CARTESIAN_POINT ( 'NONE',  ( 12.34753929015662521, 42.23053449865343367, 5.457913282602898875 ) ) ;
#5771=CARTESIAN_POINT ( 'NONE',  ( 6.202863237649241412, 48.95301221118648272, -11.99187382583002126 ) ) ;
#5773=ORIENTED_EDGE ( 'NONE', *, *, #6605, .T. ) ;
#5774=CARTESIAN_POINT ( 'NONE',  ( -9.520470885617715595, 77.63000000000000966, -6.917026985038136289 ) ) ;
#5779=CARTESIAN_POINT ( 'NONE',  ( -5.664207996239682963, 43.38577903074708075, -12.25425443241694090 ) ) ;
#5780=CARTESIAN_POINT ( 'NONE',  ( -7.499999999999999112, 102.9299999999999073, -9.367496997597655195 ) ) ;
#5781=CARTESIAN_POINT ( 'NONE',  ( 7.332788481940905712, 60.90639710865967515, -11.33710643711476251 ) ) ;
#5784=DIRECTION ( 'NONE',  ( 1.776356839400250465E-15, 0.000000000000000000, 1.000000000000000000 ) ) ;
#5785=CARTESIAN_POINT ( 'NONE',  ( 9.629085971571848646, 66.06008022608338592, 9.468271534833982983 ) ) ;
#5786=CARTESIAN_POINT ( 'NONE',  ( 10.66232145652183760, 57.11515599909031238, 8.280407745028306010 ) ) ;
#5787=CARTESIAN_POINT ( 'NONE',  ( -3.636496289402155746, 57.53000000000000114, 11.19198476289190936 ) ) ;
#5788=CARTESIAN_POINT ( 'NONE',  ( 8.343458848123578520, 34.97999999999999687, 11.48378591275254124 ) ) ;
#5789=CARTESIAN_POINT ( 'NONE',  ( 9.520470885617715595, 67.12999999999999545, 6.917026985038134512 ) ) ;
#5790=CARTESIAN_POINT ( 'NONE',  ( -13.48570619275009008, 46.95166055620521917, 0.6284690211920893610 ) ) ;
#5791=CARTESIAN_POINT ( 'NONE',  ( 5.912838536822658142, 45.96461575129709587, -12.13792530647693546 ) ) ;
#5794=CARTESIAN_POINT ( 'NONE',  ( 5.785475118908125047, 30.96942592604588285, -12.19750789377168232 ) ) ;
#5795=CARTESIAN_POINT ( 'NONE',  ( -5.595416803014888529, 56.47688909101474053, 12.28583926748330590 ) ) ;
#5799=CARTESIAN_POINT ( 'NONE',  ( 12.55310634897202959, 33.24964244554870163, 4.968087426967330522 ) ) ;
#5801=CARTESIAN_POINT ( 'NONE',  ( 0.000000000000000000, 80.93000000000000682, -13.50000000000000000 ) ) ;
#5803=CARTESIAN_POINT ( 'NONE',  ( -13.50527712561470040, 61.93091922064468946, 0.03146696456400008973 ) ) ;
#5806=EDGE_CURVE ( 'NONE', #4640, #7799, #669, .T. ) ;
#5807=CARTESIAN_POINT ( 'NONE',  ( -11.26318954741650735, 44.20936586529614232, 7.442652888113295617 ) ) ;
#5810=CARTESIAN_POINT ( 'NONE',  ( 10.92172942406179104, 36.72999999999999687, -7.935100905948385908 ) ) ;
#5811=CARTESIAN_POINT ( 'NONE',  ( 2.607531440858944223E-15, 48.17999999999999261, -14.19474002721660355 ) ) ;
#5812=CARTESIAN_POINT ( 'NONE',  ( -0.3591556296474884835, 46.19290918421699388, -13.49539728357718182 ) ) ;
#5813=CARTESIAN_POINT ( 'NONE',  ( -2.933613647220042697, 67.28548860721471669, -13.17740267288178480 ) ) ;
#5816=CARTESIAN_POINT ( 'NONE',  ( 10.66717994462818453, 54.11542978231774725, 8.274144942030686067 ) ) ;
#5817=CARTESIAN_POINT ( 'NONE',  ( -3.253207560246772267, 64.29697931017841483, -13.10216303624528678 ) ) ;
#5819=CARTESIAN_POINT ( 'NONE',  ( -5.519522428242297885, 34.38017859743614935, -12.32010052773795117 ) ) ;
#5821=CARTESIAN_POINT ( 'NONE',  ( 12.86350982126121423, 78.28284642631409440, 4.096370210139349766 ) ) ;
#5823=EDGE_CURVE ( 'NONE', #10105, #13703, #200, .T. ) ;
#5824=CARTESIAN_POINT ( 'NONE',  ( -2.138189944381240881, 37.60311857767972299, 13.49999999999999822 ) ) ;
#5825=CARTESIAN_POINT ( 'NONE',  ( 12.98023825795362285, 72.56264182897429293, -3.709933363244806159 ) ) ;
#5828=CARTESIAN_POINT ( 'NONE',  ( 4.171729424061789260, 65.82999999999999829, 12.83926296998457417 ) ) ;
#5829=CARTESIAN_POINT ( 'NONE',  ( -13.20087293324353617, 53.02997338240815139, 2.826193941060762160 ) ) ;
#5830=CARTESIAN_POINT ( 'NONE',  ( -9.520470885617717371, 36.22999999999999687, 6.917026985038133624 ) ) ;
#5831=CARTESIAN_POINT ( 'NONE',  ( -8.343458848123582072, 55.37999999999998835, 11.48378591275254124 ) ) ;
#5832=CARTESIAN_POINT ( 'NONE',  ( 2.894739436579920166E-06, 50.68008041434205069, 13.49999999999938005 ) ) ;
#5834=CARTESIAN_POINT ( 'NONE',  ( 10.87711439316070994, 69.12741176127229892, 7.996158228696909731 ) ) ;
#5836=CARTESIAN_POINT ( 'NONE',  ( -2.138189944381240881, 79.60311857767972299, 13.49999999999999822 ) ) ;
#5838=CARTESIAN_POINT ( 'NONE',  ( -13.30952709364465392, 73.85039203528728535, -2.265519377583317784 ) ) ;
#5840=CARTESIAN_POINT ( 'NONE',  ( -4.504434722200154617, 76.34205122430185497, -12.72642524997305280 ) ) ;
#5841=LINE ( 'NONE', #1829, #826 ) ;
#5843=DIRECTION ( 'NONE',  ( 1.000000000000000000, 0.000000000000000000, 0.000000000000000000 ) ) ;
#5846=CARTESIAN_POINT ( 'NONE',  ( 9.520470885617717371, 37.72999999999999687, -6.917026985038131848 ) ) ;
#5849=CARTESIAN_POINT ( 'NONE',  ( -9.445309217286480319, 32.30909206433305769, 9.645539299803775890 ) ) ;
#5850=CARTESIAN_POINT ( 'NONE',  ( 1.364733589292189020, 74.72907077985779267, 13.43087977156992707 ) ) ;
#5854=DIRECTION ( 'NONE',  ( -1.000000000000000000, -1.734723475976807094E-16, -0.000000000000000000 ) ) ;
#5855=CARTESIAN_POINT ( 'NONE',  ( -8.343458848123576743, 84.48000000000000398, -11.48378591275254301 ) ) ;
#5856=CARTESIAN_POINT ( 'NONE',  ( 10.51668321839406950, 51.75308810284574434, -8.469583928564711428 ) ) ;
#5858=CARTESIAN_POINT ( 'NONE',  ( 7.592992521937700801, 36.89513823555898142, -11.16818768155278185 ) ) ;
#5861=CARTESIAN_POINT ( 'NONE',  ( 6.020175498787003754, 62.89962116244318935, 12.09133458464389754 ) ) ;
#5862=CARTESIAN_POINT ( 'NONE',  ( 13.49678185461208990, 42.41729046651699520, 0.3662733902496916882 ) ) ;
#5863=CARTESIAN_POINT ( 'NONE',  ( 8.344294404855231662, 48.86157356941107821, -10.61324355268026842 ) ) ;
#5866=CARTESIAN_POINT ( 'NONE',  ( 11.76794919243112325, 67.28000000000000114, 3.823638476888997051 ) ) ;
#5870=VERTEX_POINT ( 'NONE', #926 ) ;
#5871=CARTESIAN_POINT ( 'NONE',  ( -0.4522785723817098757, 43.19626226204393760, -13.49242542680654644 ) ) ;
#5875=CARTESIAN_POINT ( 'NONE',  ( 12.19709600459181154, 66.21706713072794059, 5.804849116533907782 ) ) ;
#5876=CARTESIAN_POINT ( 'NONE',  ( 1.488409699040705636, 56.73351772559257711, 13.41770261815923249 ) ) ;
#5877=CARTESIAN_POINT ( 'NONE',  ( -7.272992578804307939, 62.47999999999998977, -10.01041549318726886 ) ) ;
#5878=CARTESIAN_POINT ( 'NONE',  ( -10.92172942406179104, 34.22999999999999687, 7.935100905948387684 ) ) ;
#5879=CARTESIAN_POINT ( 'NONE',  ( -3.636496289402153081, 71.32999999999999829, -11.19198476289190936 ) ) ;
#5880=CARTESIAN_POINT ( 'NONE',  ( -13.29558833726832923, 46.84766757876133880, -2.340971711627301666 ) ) ;
#5881=CARTESIAN_POINT ( 'NONE',  ( 9.154447501136807830, 45.82340124140479531, -9.922000396780600084 ) ) ;
#5882=CARTESIAN_POINT ( 'NONE',  ( 5.635477359489657445, 69.97533625320679107, -12.26749346402417373 ) ) ;
#5884=CARTESIAN_POINT ( 'NONE',  ( 10.42314640861484065, 30.75812289050851689, -8.579516016103108100 ) ) ;
#5885=CARTESIAN_POINT ( 'NONE',  ( -5.431336152102981707, 56.48321098987901223, 12.35944654956180777 ) ) ;
#5886=CARTESIAN_POINT ( 'NONE',  ( 8.343458848123580296, 52.97999999999999687, 11.48378591275253768 ) ) ;
#5887=CARTESIAN_POINT ( 'NONE',  ( 7.311496232511652593, 32.95290564063432726, 11.35083834095794408 ) ) ;
#5889=CARTESIAN_POINT ( 'NONE',  ( -1.092208315176195654, 73.21924657073326159, -13.46228893901942669 ) ) ;
#5890=CARTESIAN_POINT ( 'NONE',  ( 0.4650740877207917290, 40.16329413024163841, -13.49310518871272535 ) ) ;
#5892=CARTESIAN_POINT ( 'NONE',  ( -13.12312772325057431, 62.04431330923600996, 3.218249322805211587 ) ) ;
#5894=CARTESIAN_POINT ( 'NONE',  ( 10.58196978195695515, 48.11063103762162285, 8.383901230509726688 ) ) ;
#5895=CARTESIAN_POINT ( 'NONE',  ( 8.343458848123580296, 64.97999999999997556, 11.48378591275253768 ) ) ;
#5896=CARTESIAN_POINT ( 'NONE',  ( 4.171729424061789260, 32.82999999999999829, 12.83926296998457417 ) ) ;
#5897=CARTESIAN_POINT ( 'NONE',  ( -4.171729424061791036, 40.52999999999999403, 12.83926296998457239 ) ) ;
#5898=CARTESIAN_POINT ( 'NONE',  ( -0.003427026735675507609, 46.18012310849080393, -13.50000000215092832 ) ) ;
#5900=CARTESIAN_POINT ( 'NONE',  ( -10.55949117639465484, 67.60932008274608052, -8.413858223306061035 ) ) ;
#5902=CARTESIAN_POINT ( 'NONE',  ( 7.790142975789170698, 53.97365200280928121, 11.03460745363281426 ) ) ;
#5903=ORIENTED_EDGE ( 'NONE', *, *, #7636, .F. ) ;
#5904=CARTESIAN_POINT ( 'NONE',  ( -0.4727126854107578380, 64.19699700596120806, -13.49172460010241714 ) ) ;
#5905=VERTEX_POINT ( 'NONE', #11723 ) ;
#5907=CARTESIAN_POINT ( 'NONE',  ( -10.19441049769735130, 34.58951039502781555, -8.850085066458992955 ) ) ;
#5909=AXIS2_PLACEMENT_3D ( 'NONE', #6271, #11917, #3782 ) ;
#5910=CARTESIAN_POINT ( 'NONE',  ( 11.83416267854458326, 78.18933780232462993, 6.496366743272888655 ) ) ;
#5911=CARTESIAN_POINT ( 'NONE',  ( -1.545162525932825686E-06, 79.18000005555833809, -13.49999999999990941 ) ) ;
#5913=CARTESIAN_POINT ( 'NONE',  ( 13.04355863927429127, 72.55420972505207544, -3.483812310663820355 ) ) ;
#5915=CARTESIAN_POINT ( 'NONE',  ( -8.343458848123576743, 67.48000000000000398, -11.48378591275254301 ) ) ;
#5916=CARTESIAN_POINT ( 'NONE',  ( -1.929592546336893033, 52.24936810948035060, -13.36251507991583942 ) ) ;
#5917=CARTESIAN_POINT ( 'NONE',  ( -11.76794919243112325, 38.92999999999999972, -2.882316262207890869E-15 ) ) ;
#5918=CARTESIAN_POINT ( 'NONE',  ( -8.691771469529815392E-16, 61.67999999999999261, 14.19474002721660355 ) ) ;
#5921=CARTESIAN_POINT ( 'NONE',  ( 7.621696303231366265, 68.96619805644265000, 11.14361944240803481 ) ) ;
#5922=CARTESIAN_POINT ( 'NONE',  ( 5.883989548015875926, 30.92926152634062475, 10.19133431864935879 ) ) ;
#5923=EDGE_CURVE ( 'NONE', #15045, #11619, #14348, .T. ) ;
#5926=CARTESIAN_POINT ( 'NONE',  ( -13.42510730815057940, 73.98100147573404683, 1.466630498505447466 ) ) ;
#5927=CARTESIAN_POINT ( 'NONE',  ( -2.715950498892019116, 76.27759078984141183, -13.22580361578473251 ) ) ;
#5929=DIRECTION ( 'NONE',  ( -0.000000000000000000, -1.000000000000000000, -0.000000000000000000 ) ) ;
#5932=CARTESIAN_POINT ( 'NONE',  ( 9.520470885617715595, 40.12999999999999545, 6.917026985038134512 ) ) ;
#5934=CARTESIAN_POINT ( 'NONE',  ( -11.28038879628374502, 32.20827684399202440, 7.416391123192743962 ) ) ;
#5936=VECTOR ( 'NONE', #15436, 1000.000000000000000 ) ;
#5939=CARTESIAN_POINT ( 'NONE',  ( 2.272985001014427788E-15, 32.17999999999999972, -12.37355403259654985 ) ) ;
#5940=CARTESIAN_POINT ( 'NONE',  ( 8.534827298566797893, 51.85287959032340410, -10.46283363410773681 ) ) ;
#5941=LINE ( 'NONE', #2991, #17180 ) ;
#5942=EDGE_CURVE ( 'NONE', #4960, #3997, #12337, .T. ) ;
#5943=CARTESIAN_POINT ( 'NONE',  ( 1.653273178848926472E-15, 80.93000000000000682, 13.50000000000000000 ) ) ;
#5945=DIRECTION ( 'NONE',  ( -0.000000000000000000, -1.000000000000000000, -0.000000000000000000 ) ) ;
#5946=CARTESIAN_POINT ( 'NONE',  ( 10.64655758642687644, 63.11426932925019884, 8.300667950577015120 ) ) ;
#5947=CARTESIAN_POINT ( 'NONE',  ( 0.5030752140698526720, 41.69808937357471024, 13.49082046348348385 ) ) ;
#5948=CARTESIAN_POINT ( 'NONE',  ( 12.44133635878537625, 48.62102703855506292, -5.241715575524017012 ) ) ;
#5951=CARTESIAN_POINT ( 'NONE',  ( 9.520470885617717371, 70.73000000000000398, -6.917026985038131848 ) ) ;
#5957=CARTESIAN_POINT ( 'NONE',  ( 1.668451422296728159, 80.92999999999999261, -13.07629037559559748 ) ) ;
#5960=CARTESIAN_POINT ( 'NONE',  ( 11.54972359916251889, 66.16909762691344099, 6.995529268059574868 ) ) ;
#5961=CARTESIAN_POINT ( 'NONE',  ( 10.92172942406179104, 81.73000000000000398, -7.935100905948385908 ) ) ;
#5962=CARTESIAN_POINT ( 'NONE',  ( 9.520470885617715595, 61.13000000000000256, 6.917026985038134512 ) ) ;
#5963=CARTESIAN_POINT ( 'NONE',  ( -6.299567892059761753, 31.39042612893360484, 19.22554806868047805 ) ) ;
#5964=CARTESIAN_POINT ( 'NONE',  ( 9.520470885617715595, 58.13000000000000256, 6.917026985038134512 ) ) ;
#5965=CARTESIAN_POINT ( 'NONE',  ( -11.29930542946217109, 46.65291765115935618, -7.387593347751512773 ) ) ;
#5966=CARTESIAN_POINT ( 'NONE',  ( 11.66267797177103738, 45.68289626953719562, -6.800399157363517411 ) ) ;
#5967=CARTESIAN_POINT ( 'NONE',  ( 5.850572103796928047, 69.96703761332742033, -12.16734276622654320 ) ) ;
#5969=CARTESIAN_POINT ( 'NONE',  ( 0.1944445437207606431, 31.17300849257853201, -13.49860884749332435 ) ) ;
#5970=CARTESIAN_POINT ( 'NONE',  ( -13.45018538520116635, 55.97019992538123745, 1.159223571585510149 ) ) ;
#5972=CARTESIAN_POINT ( 'NONE',  ( 0.000000000000000000, 80.93000000000000682, 0.000000000000000000 ) ) ;
#5973=CARTESIAN_POINT ( 'NONE',  ( 0.4129281128241998888, 43.16520274255920242, -13.49391189084656162 ) ) ;
#5974=CARTESIAN_POINT ( 'NONE',  ( 12.14332122887934240, 39.64679378178001201, -5.899935319809511469 ) ) ;
#5975=ORIENTED_EDGE ( 'NONE', *, *, #7675, .F. ) ;
#5976=CARTESIAN_POINT ( 'NONE',  ( -11.08913010680831945, 62.22008114857175798, 7.699440692202677461 ) ) ;
#5977=ORIENTED_EDGE ( 'NONE', *, *, #16517, .F. ) ;
#5978=CARTESIAN_POINT ( 'NONE',  ( -13.08215237349078208, 40.81125640288357914, -3.336602680432516177 ) ) ;
#5981=CARTESIAN_POINT ( 'NONE',  ( 13.06196386905416595, 48.30848771352356863, 3.411030766945946979 ) ) ;
#5982=CARTESIAN_POINT ( 'NONE',  ( 4.478433445390353818, 58.01891974520321327, -12.73584891686745202 ) ) ;
#5983=EDGE_CURVE ( 'NONE', #5515, #10469, #15351, .T. ) ;
#5984=CARTESIAN_POINT ( 'NONE',  ( -13.50000000000000000, 37.92999999999999972, -3.306546357697853733E-15 ) ) ;
#5985=CARTESIAN_POINT ( 'NONE',  ( 2.607531440858944223E-15, 39.17999999999999972, -14.19474002721660355 ) ) ;
#5986=CARTESIAN_POINT ( 'NONE',  ( -7.576616670048093940E-16, 81.68000000000000682, 12.37355403259654985 ) ) ;
#5987=CARTESIAN_POINT ( 'NONE',  ( 8.464728390624178894E-06, 46.17999963826949994, -13.49999999999734790 ) ) ;
#5990=CARTESIAN_POINT ( 'NONE',  ( 4.344646002123737638, 53.83610922229849649, 12.78506762605347546 ) ) ;
#5992=CARTESIAN_POINT ( 'NONE',  ( -5.870390962563227788, 64.39383572203485073, -12.15683169922916917 ) ) ;
#5993=ORIENTED_EDGE ( 'NONE', *, *, #12520, .T. ) ;
#5994=VECTOR ( 'NONE', #14829, 1000.000000000000000 ) ;
#5995=CARTESIAN_POINT ( 'NONE',  ( 4.743044421334680294, 67.00886042820928878, -12.64690991240490270 ) ) ;
#5996=CARTESIAN_POINT ( 'NONE',  ( -5.508910881225164147, 34.37976951287060956, -12.32485102207323990 ) ) ;
#6001=CARTESIAN_POINT ( 'NONE',  ( 10.88156798610315512, 72.12748164754577829, 7.994026003792296109 ) ) ;
#6002=CARTESIAN_POINT ( 'NONE',  ( 7.822218710939744746, 66.88499866975831765, -11.00287478893467785 ) ) ;
#6004=CARTESIAN_POINT ( 'NONE',  ( -13.50000000000000000, 64.93000000000000682, -3.306546357697853733E-15 ) ) ;
#6005=CARTESIAN_POINT ( 'NONE',  ( -9.135817427633982746, 52.53563195485393322, -9.940718253270615534 ) ) ;
#6006=CARTESIAN_POINT ( 'NONE',  ( 7.272992578804311492, 37.87999999999999545, -10.01041549318726709 ) ) ;
#6008=CARTESIAN_POINT ( 'NONE',  ( 13.50000000000000355, 56.57999999999999119, -4.386415899144233244 ) ) ;
#6012=CARTESIAN_POINT ( 'NONE',  ( 9.918004550652394613, 69.07493629982988637, 9.158913472290203472 ) ) ;
#6013=DIRECTION ( 'NONE',  ( 0.000000000000000000, -1.000000000000000000, 0.000000000000000000 ) ) ;
#6015=CARTESIAN_POINT ( 'NONE',  ( -12.64052664110000812, 73.75835914970723195, -4.739995431488866373 ) ) ;
#6016=CARTESIAN_POINT ( 'NONE',  ( -5.827696143467630208, 76.39199596957689664, -12.18641047183595383 ) ) ;
#6017=DIRECTION ( 'NONE',  ( 0.000000000000000000, -1.000000000000000000, 0.000000000000000000 ) ) ;
#6018=CYLINDRICAL_SURFACE ( 'NONE', #14732, 12.00000000000000178 ) ;
#6020=CARTESIAN_POINT ( 'NONE',  ( 3.636496289402154414, 36.82999999999999119, 11.19198476289190936 ) ) ;
#6022=AXIS2_PLACEMENT_3D ( 'NONE', #1228, #15805, #3709 ) ;
#6023=CARTESIAN_POINT ( 'NONE',  ( -4.024261390522248405, 32.53540582810948223, 12.88699713268044889 ) ) ;
#6024=CARTESIAN_POINT ( 'NONE',  ( 1.523553703479234134, 74.73478094211517941, 13.41454831652031388 ) ) ;
#6028=CARTESIAN_POINT ( 'NONE',  ( 8.343458848123578520, 82.97999999999997556, 11.48378591275254124 ) ) ;
#6029=CARTESIAN_POINT ( 'NONE',  ( 10.05803025841681198, 51.77773163741208151, -9.004780719399368749 ) ) ;
#6030=CARTESIAN_POINT ( 'NONE',  ( 0.000000000000000000, 80.93000000000000682, -13.50000000000000000 ) ) ;
#6032=CARTESIAN_POINT ( 'NONE',  ( 5.585016930642382249, 36.97714006553758281, -12.29076469185453746 ) ) ;
#6033=CARTESIAN_POINT ( 'NONE',  ( 2.445080149700053643E-15, 75.17999999999999261, -13.50000000000000000 ) ) ;
#6034=CARTESIAN_POINT ( 'NONE',  ( -2.115617638502927722, 49.25593553345355957, -13.34243514950316190 ) ) ;
#6035=CARTESIAN_POINT ( 'NONE',  ( 9.872799149639176264, 63.07256805672663091, 9.208769869332330771 ) ) ;
#6036=CARTESIAN_POINT ( 'NONE',  ( 0.8300164950611879089, 41.70984460997175347, 13.47471283487947069 ) ) ;
#6037=CARTESIAN_POINT ( 'NONE',  ( 12.37575769567737538, 48.62700662711739596, -5.395588928150912622 ) ) ;
#6039=ORIENTED_EDGE ( 'NONE', *, *, #2551, .T. ) ;
#6040=CARTESIAN_POINT ( 'NONE',  ( -7.576616670048093940E-16, 66.67999999999999261, 12.37355403259654807 ) ) ;
#6044=FACE_OUTER_BOUND ( 'NONE', #7103, .T. ) ;
#6048=CARTESIAN_POINT ( 'NONE',  ( 5.773176358834770205, 65.89002590883258392, 12.20330810491806162 ) ) ;
#6049=CARTESIAN_POINT ( 'NONE',  ( -10.92172942406179104, 80.22999999999998977, 7.935100905948387684 ) ) ;
#6050=CARTESIAN_POINT ( 'NONE',  ( 11.76794919243112325, 46.27999999999999403, 3.823638476888996607 ) ) ;
#6052=CARTESIAN_POINT ( 'NONE',  ( -13.49064219070377746, 46.94729801505019395, 0.5027933102212878147 ) ) ;
#6053=CARTESIAN_POINT ( 'NONE',  ( 9.420796519002903935, 45.81034643145268603, -9.670816597974919659 ) ) ;
#6054=CARTESIAN_POINT ( 'NONE',  ( 8.045227603496410751, 69.87508753446272181, -10.84086963142225457 ) ) ;
#6055=CARTESIAN_POINT ( 'NONE',  ( 10.43422754191850998, 30.75751561893000741, -8.566035940238601043 ) ) ;
#6056=CARTESIAN_POINT ( 'NONE',  ( -11.06564900652519334, 56.22149449859761461, 7.733138918553730257 ) ) ;
#6058=CARTESIAN_POINT ( 'NONE',  ( 4.981677685877808237, 32.85966306824430916, 12.54919354416681188 ) ) ;
#6059=CARTESIAN_POINT ( 'NONE',  ( 0.01063419157620585156, 43.17961891178009637, -13.49999685939349625 ) ) ;
#6060=CARTESIAN_POINT ( 'NONE',  ( 12.46449749046236199, 39.61925870500666491, -5.200596085897637444 ) ) ;
#6062=CARTESIAN_POINT ( 'NONE',  ( -12.71230713429092063, 62.09414301502697953, 4.544061370062732585 ) ) ;
#6067=CARTESIAN_POINT ( 'NONE',  ( 11.74915954432862009, 48.18317559676947326, 6.649098532137857731 ) ) ;
#6068=CARTESIAN_POINT ( 'NONE',  ( 9.335235950531815854E-15, 58.17999999999999972, -13.50000000000000178 ) ) ;
#6069=CARTESIAN_POINT ( 'NONE',  ( 8.908714855037628055, 78.83534774718576443, -10.14565470230079391 ) ) ;
#6071=CARTESIAN_POINT ( 'NONE',  ( -9.520470885617717371, 78.23000000000000398, 6.917026985038133624 ) ) ;
#6073=B_SPLINE_CURVE_WITH_KNOTS ( 'NONE', 3,
 ( #14560, #2274, #1052, #7875, #14385, #11759, #7963, #16061, #10695, #3796, #9208, #3969, #7794, #13252, #7700, #14301, #6464, #2443, #2188, #6375, #5045, #6285, #11673, #5223, #3706, #17048, #15802, #11849, #14473, #14647, #10609, #4954, #15976, #10357, #13333, #963, #15711, #9295, #1139, #3879, #10442, #9030, #9123, #1225, #11930, #12365, #12275, #2619, #1659, #6720, #8050, #13416, #8138, #8407, #9731, #10959, #2977, #14905, #14730, #9381, #16233, #6808, #15077, #11135, #7074, #172, #5577, #12458, #2799, #8319, #14815, #16508, #8230, #16327, #1306, #1393, #12186, #14995, #5751, #12098, #259, #78, #13503, #5483, #17480, #5667, #5394, #13591, #10779, #9467, #2887, #16143, #1485, #4142, #10865, #6902, #342, #4234, #4053, #2709, #13759, #9555, #9645, #13674, #1571, #6990, #11047, #16419, #4321, #3344, #5926, #8582, #8758, #8495, #4678, #11398, #6332, #6425, #14114, #7752, #15759, #691, #2000, #13933, #3669, #1014, #7243, #7426, #12806, #8669, #13125, #16770, #11809, #5004, #7334, #11721, #1827, #17096, #9997, #9082, #432, #5838, #12629, #10083, #10402, #3068, #15169, #13846, #6015, #14434, #1748, #9910, #7160, #2324, #4413, #9824, #15434, #12545, #11305, #11221, #16596, #4503, #15257, #16683, #3155, #517, #4590, #15345, #3246, #14026, #1915, #12718, #604, #17271, #14611, #5442, #1441, #14864, #8014, #13381, #2758, #2494, #13467, #10659, #6859, #9431, #16107, #1353, #17442, #5275, #1100, #5356, #2405, #4017, #7925, #15936, #13298, #14519, #8102, #3759, #3929, #2670, #17186, #10829, #3843, #8190, #12148, #14780, #6769, #9258, #13213, #1189, #37, #13552, #5185, #1271, #10743, #6600, #9171, #11980, #16191, #5097, #4103, #6515, #9519, #10489, #15851, #7840, #11896, #6683, #17361, #10575, #16022, #9346, #14695, #2582, #12065, #5889, #8629, #15041 ),
 .UNSPECIFIED., .F., .F.,
 ( 4, 2, 2, 2, 1, 1, 1, 2, 2, 2, 1, 1, 2, 2, 1, 1, 1, 1, 1, 2, 2, 1, 1, 2, 2, 1, 1, 2, 2, 1, 2, 2, 2, 2, 1, 1, 2, 2, 2, 2, 2, 1, 2, 2, 1, 1, 1, 1, 1, 2, 2, 1, 2, 2, 2, 2, 1, 1, 1, 2, 2, 2, 2, 1, 2, 2, 1, 1, 2, 2, 2, 2, 2, 2, 1, 1, 1, 1, 2, 2, 2, 2, 2, 1, 1, 1, 2, 2, 2, 2, 2, 2, 2, 2, 1, 1, 2, 2, 2, 1, 2, 2, 1, 1, 1, 2, 2, 1, 1, 2, 2, 2, 1, 2, 2, 1, 1, 2, 2, 2, 2, 1, 1, 2, 2, 1, 2, 2, 1, 2, 2, 1, 1, 2, 1, 2, 2, 1, 1, 2, 2, 2, 2, 2, 1, 1, 1, 2, 2, 4 ),
 ( 0.1227481640271067542, 0.1229765385430084124, 0.1229908119502522712, 0.1229979486538742006, 0.1230050853574961162, 0.1230336321719838338, 0.1230907258009592414, 0.1232049130589100705, 0.1236616620907133590, 0.1245751601543199499, 0.1248035346702215942, 0.1249177219281724233, 0.1249748155571478309, 0.1250033623716355347, 0.1250319091861232523, 0.1254886582179265131, 0.1259454072497297739, 0.1261737817656314320, 0.1262879690235822472, 0.1262951057272041766, 0.1263022424308260783, 0.1263165158380699371, 0.1263450626525576548, 0.1264021562815330901, 0.1268589053133364897, 0.1269159989423118973, 0.1269445457567996149, 0.1269516824604215444, 0.1269588191640434738, 0.1269730925712873326, 0.1270872798292382033, 0.1273156543451399447, 0.1282291524087469103, 0.1286859014405503931, 0.1288000886985012639, 0.1288571823274766992, 0.1288857291419644169, 0.1289142759564521346, 0.1291426504723538760, 0.1300561485359607583, 0.1305128975677642134, 0.1307412720836659270, 0.1308554593416167977, 0.1308840061561045154, 0.1309125529705922053, 0.1309696465995676407, 0.1314263956313710402, 0.1316547701472727538, 0.1317689574052236245, 0.1318260510341990321, 0.1318403244414428910, 0.1318545978486867498, 0.1318831446631744675, 0.1327966427267815441, 0.1328109161340254030, 0.1328180528376473324, 0.1328251895412692618, 0.1328537363557569795, 0.1329108299847323593, 0.1330250172426831745, 0.1332533917585847771, 0.1337101407903879824, 0.1346236388539943929, 0.1347378261119452081, 0.1347520995191890392, 0.1347663729264328980, 0.1347949197409206157, 0.1348520133698959955, 0.1350803878857975981, 0.1355371369176008312, 0.1364506349812072417, 0.1366790094971088443, 0.1367075563115965620, 0.1367361031260842519, 0.1367931967550596595, 0.1369073840130104469, 0.1373641330448136522, 0.1375925075607152270, 0.1376496011896906346, 0.1377066948186660422, 0.1378208820766168297, 0.1382776311084200072, 0.1385060056243216098, 0.1386201928822723972, 0.1386487396967600871, 0.1386630131040039460, 0.1386701498076258754, 0.1386772865112477771, 0.1387343801402231847, 0.1391911291720262234, 0.1401046272356323008, 0.1405613762674353395, 0.1406184698964107194, 0.1406470167108984093, 0.1406755635253860992, 0.1407897507833368866, 0.1410181252992384060, 0.1419316233628445389, 0.1423883723946476054, 0.1425025596525983651, 0.1425596532815737449, 0.1425882000960614349, 0.1426167469105491248, 0.1428451214264506719, 0.1433018704582537661, 0.1435302449741553132, 0.1435587917886430032, 0.1435873386031306931, 0.1436444322321060729, 0.1437586194900568604, 0.1442153685218600101, 0.1444437430377615850, 0.1445008366667369648, 0.1445293834812246825, 0.1445365201848465841, 0.1445436568884685136, 0.1445579302957123446, 0.1446721175536630488, 0.1455856156172688487, 0.1460423646490717209, 0.1462707391649731847, 0.1463849264229238889, 0.1464420200518992687, 0.1464705668663869309, 0.1464848402736307897, 0.1464991136808746208, 0.1474126117444803652, 0.1483261098080860818, 0.1483832034370614339, 0.1484117502515491238, 0.1484402970660367860, 0.1485544843239875179, 0.1487828588398889540, 0.1492396078716918262, 0.1493537951296425303, 0.1494108887586178824, 0.1494251621658617413, 0.1494394355731055724, 0.1494679823875932623, 0.1496963569034947261, 0.1501531059352976538, 0.1503814804511991177, 0.1503886171548210471, 0.1503957538584429765, 0.1504100272656868076, 0.1504385740801744975, 0.1504956677091498496, 0.1506098549671005815, 0.1510666039989035092, 0.1519801020625093646 ),
 .UNSPECIFIED. ) ;
#6075=CARTESIAN_POINT ( 'NONE',  ( -0.06432022310792409603, 46.18231244616364251, -13.49986851205962424 ) ) ;
#6076=CARTESIAN_POINT ( 'NONE',  ( -0.1337557719945228207, 67.18480936409068249, -13.49933757132007628 ) ) ;
#6078=CARTESIAN_POINT ( 'NONE',  ( 6.644535271319878866, 53.92494203076220316, 11.75165990948425154 ) ) ;
#6079=ADVANCED_FACE ( 'NONE', ( #17122 ), #6460, .T. ) ;
#6085=CARTESIAN_POINT ( 'NONE',  ( -4.731689125201891777, 34.35038980843969370, -12.64542749166197844 ) ) ;
#6087=CARTESIAN_POINT ( 'NONE',  ( 3.101660632740125934, 77.79147361761071977, 13.14641033372065415 ) ) ;
#6091=CARTESIAN_POINT ( 'NONE',  ( 13.49760795208683284, 72.41181223906431796, 0.5098544550378681928 ) ) ;
#6093=CARTESIAN_POINT ( 'NONE',  ( 10.92172942406179104, 63.72999999999999687, -7.935100905948385908 ) ) ;
#6094=CARTESIAN_POINT ( 'NONE',  ( -0.3351920408089422709, 71.66794772448770345, 13.49586090856208820 ) ) ;
#6095=CARTESIAN_POINT ( 'NONE',  ( -9.520470885617715595, 38.62999999999999545, -6.917026985038136289 ) ) ;
#6097=CARTESIAN_POINT ( 'NONE',  ( -8.343458848123576743, 57.48000000000000398, -11.48378591275254301 ) ) ;
#6100=CARTESIAN_POINT ( 'NONE',  ( 3.426020828344902736, 68.80323833450283644, 13.05809747433249868 ) ) ;
#6104=CARTESIAN_POINT ( 'NONE',  ( -2.381931281991595206, 65.59435760367297519, 13.28825607429043387 ) ) ;
#6107=ORIENTED_EDGE ( 'NONE', *, *, #15386, .F. ) ;
#6108=CARTESIAN_POINT ( 'NONE',  ( -9.520470885617715595, 41.63000000000000256, -6.917026985038136289 ) ) ;
#6110=CARTESIAN_POINT ( 'NONE',  ( 10.92172942406178926, 80.13000000000000966, 7.935100905948387684 ) ) ;
#6111=CARTESIAN_POINT ( 'NONE',  ( -13.39519961485953026, 31.86913630564962929, -1.748191886245508364 ) ) ;
#6112=CARTESIAN_POINT ( 'NONE',  ( 2.042046933105797546, 74.75341727322346230, 13.34690593482024212 ) ) ;
#6114=CARTESIAN_POINT ( 'NONE',  ( -10.92172942406178926, 78.63000000000000966, -7.935100905948389460 ) ) ;
#6115=CARTESIAN_POINT ( 'NONE',  ( 12.65245305301080414, 51.60041585730986213, -4.708045043639258687 ) ) ;
#6117=CARTESIAN_POINT ( 'NONE',  ( -11.21035395369201915, 38.21266103485134380, 7.521839952431427889 ) ) ;
#6118=CARTESIAN_POINT ( 'NONE',  ( 10.32492466292448974, 36.76347586491808528, -8.697596036060231128 ) ) ;
#6122=CARTESIAN_POINT ( 'NONE',  ( 1.653273178848926472E-15, 80.93000000000000682, 13.50000000000000000 ) ) ;
#6123=CARTESIAN_POINT ( 'NONE',  ( -2.419409634026826961, 80.59289594391761113, 13.28325634299493707 ) ) ;
#6124=CARTESIAN_POINT ( 'NONE',  ( 4.457234882645010110, 41.84008533871757152, 12.75041784350807106 ) ) ;
#6125=CARTESIAN_POINT ( 'NONE',  ( 13.49762871381596874, 48.42116860337419126, 0.2575671418023918746 ) ) ;
#6128=CARTESIAN_POINT ( 'NONE',  ( 7.272992578804308828, 69.97999999999998977, 10.01041549318726886 ) ) ;
#6130=CARTESIAN_POINT ( 'NONE',  ( 8.343458848123580296, 55.97999999999999687, 11.48378591275253768 ) ) ;
#6132=CARTESIAN_POINT ( 'NONE',  ( 1.133384680211434459, 76.13924943277646662, -13.45318893631145052 ) ) ;
#6135=CARTESIAN_POINT ( 'NONE',  ( 10.16039061381173525, 66.08774085974377499, 8.889160252383520699 ) ) ;
#6136=CARTESIAN_POINT ( 'NONE',  ( 10.92172942406179104, 78.72999999999998977, -7.935100905948385908 ) ) ;
#6137=CARTESIAN_POINT ( 'NONE',  ( -3.636496289402153081, 53.33000000000000540, -11.19198476289190936 ) ) ;
#6139=CARTESIAN_POINT ( 'NONE',  ( -9.938087151227913196, 59.28401552682182540, 9.136990211801220951 ) ) ;
#6140=CARTESIAN_POINT ( 'NONE',  ( 13.16726819044754393, 45.53581346377539063, -2.986114351398691191 ) ) ;
#6141=CARTESIAN_POINT ( 'NONE',  ( 10.14020416995585983, 69.77338333202821730, -8.912142960987960549 ) ) ;
#6143=CARTESIAN_POINT ( 'NONE',  ( 13.23463183243080366, 30.52433186400915588, -2.671914872127473473 ) ) ;
#6144=CARTESIAN_POINT ( 'NONE',  ( -13.47837838110856090, 55.90363568160458385, -0.7637818885891087817 ) ) ;
#6146=FACE_OUTER_BOUND ( 'NONE', #1355, .T. ) ;
#6149=CARTESIAN_POINT ( 'NONE',  ( 12.95691110344991337, 39.56579465547967089, -3.794630013198587282 ) ) ;
#6150=ORIENTED_EDGE ( 'NONE', *, *, #5216, .F. ) ;
#6152=CARTESIAN_POINT ( 'NONE',  ( -12.99103486005599883, 61.79864889427442876, -3.678670038247435325 ) ) ;
#6153=ORIENTED_EDGE ( 'NONE', *, *, #14837, .T. ) ;
#6157=CARTESIAN_POINT ( 'NONE',  ( 6.919944324611998709, 57.92390741887160743, -11.60445687867207987 ) ) ;
#6158=CARTESIAN_POINT ( 'NONE',  ( 10.71171996125772985, 78.74211244272670740, -8.219364172421744996 ) ) ;
#6159=CARTESIAN_POINT ( 'NONE',  ( 9.520470885617717371, 82.73000000000000398, -6.917026985038131848 ) ) ;
#6160=CARTESIAN_POINT ( 'NONE',  ( -13.49999999999999822, 43.07999999999999829, 4.386415899144235908 ) ) ;
#6161=CARTESIAN_POINT ( 'NONE',  ( -11.76794919243112325, 83.78000000000001535, -3.823638476888998827 ) ) ;
#6162=DIRECTION ( 'NONE',  ( 0.000000000000000000, -1.000000000000000000, 0.000000000000000000 ) ) ;
#6165=CARTESIAN_POINT ( 'NONE',  ( 9.453713556340927582, 54.05132085550528842, 9.637327269826936771 ) ) ;
#6169=CARTESIAN_POINT ( 'NONE',  ( 1.408343819019457359E-15, 0.000000000000000000, -9.500000000000021316 ) ) ;
#6172=CARTESIAN_POINT ( 'NONE',  ( -3.851070442117878745, 59.54153006582451013, 12.93912176508445810 ) ) ;
#6173=PLANE ( 'NONE',  #17372 ) ;
#6175=CARTESIAN_POINT ( 'NONE',  ( 12.68447996868631122, 72.26291114008931515, 4.621164343339557057 ) ) ;
#6177=CARTESIAN_POINT ( 'NONE',  ( 8.343458848123583849, 48.87999999999998835, -11.48378591275253768 ) ) ;
#6178=CARTESIAN_POINT ( 'NONE',  ( -0.3911409227513171771, 71.66593604615781032, 13.49433737296981306 ) ) ;
#6179=DIRECTION ( 'NONE',  ( 0.000000000000000000, -1.000000000000000000, 0.000000000000000000 ) ) ;
#6180=CARTESIAN_POINT ( 'NONE',  ( -4.282754437214131293, 68.52600206748782341, 12.80272888647489893 ) ) ;
#6183=AXIS2_PLACEMENT_3D ( 'NONE', #17465, #9281, #4129 ) ;
#6185=CARTESIAN_POINT ( 'NONE',  ( -5.734174865113238262, 65.47163811465718197, 12.22337932611075573 ) ) ;
#6186=CARTESIAN_POINT ( 'NONE',  ( -11.80445978200331503, 80.92999999999996419, -1.125850548943733376 ) ) ;
#6187=DIRECTION ( 'NONE',  ( 0.000000000000000000, -1.000000000000000000, 0.000000000000000000 ) ) ;
#6189=CARTESIAN_POINT ( 'NONE',  ( -3.636496289402153081, 32.32999999999999829, -11.19198476289190936 ) ) ;
#6190=CARTESIAN_POINT ( 'NONE',  ( -2.883235578040820091, 40.28367049126757138, -13.18852187992278502 ) ) ;
#6191=CARTESIAN_POINT ( 'NONE',  ( -12.52052419915814063, 31.74586622497447408, -5.068148337449895457 ) ) ;
#6192=CARTESIAN_POINT ( 'NONE',  ( 8.148423059287221548, 74.98954435357713066, 10.76380695295465273 ) ) ;
#6193=CARTESIAN_POINT ( 'NONE',  ( 11.56270653563395356, 60.17021069121303611, 6.968727811706270536 ) ) ;
#6194=CARTESIAN_POINT ( 'NONE',  ( 8.343458848123583849, 62.88000000000000256, -11.48378591275253768 ) ) ;
#6195=CIRCLE ( 'NONE', #7608, 12.00000000000000178 ) ;
#6196=EDGE_CURVE ( 'NONE', #7733, #7293, #3171, .T. ) ;
#6197=CARTESIAN_POINT ( 'NONE',  ( 11.32976262874806395, 51.70524724435282593, -7.343873846068756706 ) ) ;
#6198=CARTESIAN_POINT ( 'NONE',  ( -12.55208093682576909, 38.11047456955122925, 4.969580869381986510 ) ) ;
#6199=CARTESIAN_POINT ( 'NONE',  ( 12.20992711788400520, 36.64133221546218522, -5.762380518153004338 ) ) ;
#6202=CARTESIAN_POINT ( 'NONE',  ( -3.800243545151680280, 77.54335724604808888, 12.95408144013974194 ) ) ;
#6204=CARTESIAN_POINT ( 'NONE',  ( -7.499999999999998224, 108.9300000000000068, 9.367496997597600128 ) ) ;
#6205=CARTESIAN_POINT ( 'NONE',  ( 13.47608760677475459, 48.40154206234144851, 0.8241170574654087533 ) ) ;
#6208=CARTESIAN_POINT ( 'NONE',  ( -3.636496289402155746, 60.53000000000000114, 11.19198476289190936 ) ) ;
#6213=DIRECTION ( 'NONE',  ( 0.000000000000000000, 0.000000000000000000, -1.000000000000000000 ) ) ;
#6215=CARTESIAN_POINT ( 'NONE',  ( 2.607531440858944223E-15, 82.18000000000000682, -14.19474002721660355 ) ) ;
#6216=EDGE_CURVE ( 'NONE', #11530, #13318, #6705, .T. ) ;
#6217=CARTESIAN_POINT ( 'NONE',  ( -11.76794919243112325, 48.07999999999998408, 3.823638476888994386 ) ) ;
#6219=CARTESIAN_POINT ( 'NONE',  ( -13.47905022307413603, 58.90402517245511405, -0.7520165846117183861 ) ) ;
#6220=CARTESIAN_POINT ( 'NONE',  ( 11.55642355312311942, 45.16972346798684868, 6.979809178588280538 ) ) ;
#6221=DIRECTION ( 'NONE',  ( 0.000000000000000000, -1.000000000000000000, 0.000000000000000000 ) ) ;
#6222=CARTESIAN_POINT ( 'NONE',  ( 1.529356327037144636, 80.73498994847588506, 13.41315609044504065 ) ) ;
#6223=CARTESIAN_POINT ( 'NONE',  ( 12.02353733592099161, 30.65632963770153196, -6.138774346578745877 ) ) ;
#6224=CARTESIAN_POINT ( 'NONE',  ( -13.28969977581182071, 55.84641863258806893, -2.375863902518644988 ) ) ;
#6225=CARTESIAN_POINT ( 'NONE',  ( -13.42114948243943218, 49.98161693057358690, 1.483081436913393780 ) ) ;
#6226=CARTESIAN_POINT ( 'NONE',  ( 3.017866001013571609, 64.07148374553901249, -13.15915560476493162 ) ) ;
#6228=CARTESIAN_POINT ( 'NONE',  ( 13.09506756767692082, 39.54674493898122734, -3.282300712200310944 ) ) ;
#6229=ORIENTED_EDGE ( 'NONE', *, *, #9898, .T. ) ;
#6230=CARTESIAN_POINT ( 'NONE',  ( -7.131439210029803633, 61.44517228716789248, -11.46358492120966766 ) ) ;
#6232=EDGE_LOOP ( 'NONE', ( #9106, #11703, #6929, #5336 ) ) ;
#6235=CARTESIAN_POINT ( 'NONE',  ( 13.06645423851852073, 48.30912723757910499, 3.393787163694668152 ) ) ;
#6236=LINE ( 'NONE', #16739, #12442 ) ;
#6237=CARTESIAN_POINT ( 'NONE',  ( 0.5008926393039752067, 79.16199793852693745, -13.49195660129378460 ) ) ;
#6238=CARTESIAN_POINT ( 'NONE',  ( -3.636496289402155746, 75.53000000000000114, 11.19198476289190936 ) ) ;
#6239=CARTESIAN_POINT ( 'NONE',  ( 4.171729424061791924, 39.03000000000000114, -12.83926296998457239 ) ) ;
#6241=ADVANCED_FACE ( 'NONE', ( #6973 ), #2604, .T. ) ;
#6243=CARTESIAN_POINT ( 'NONE',  ( -0.1463139935563050886, 67.18526091003258216, -13.49920831200174831 ) ) ;
#6245=CARTESIAN_POINT ( 'NONE',  ( -4.171729424061787483, 78.32999999999999829, -12.83926296998457417 ) ) ;
#6246=CARTESIAN_POINT ( 'NONE',  ( 5.770345405016722218, 33.97008500761054250, -12.20464375447771488 ) ) ;
#6250=CARTESIAN_POINT ( 'NONE',  ( 2.372771011195240920, 67.09468957437705683, -13.29338533608859585 ) ) ;
#6252=CARTESIAN_POINT ( 'NONE',  ( 4.338753566204257339, 77.83602819694414165, 12.78390686162523338 ) ) ;
#6253=CARTESIAN_POINT ( 'NONE',  ( -0.3413906785081720074, 59.66772483089536649, 13.49568742704858160 ) ) ;
#6256=CARTESIAN_POINT ( 'NONE',  ( 0.7476565982748099026, 71.70685699333597540, 13.50000000000422951 ) ) ;
#6257=CARTESIAN_POINT ( 'NONE',  ( 13.49999999999999822, 51.27999999999998693, 4.386415899144237684 ) ) ;
#6258=CARTESIAN_POINT ( 'NONE',  ( -5.788310938635475189, 71.46938236682071022, 12.19612480893602147 ) ) ;
#6262=CARTESIAN_POINT ( 'NONE',  ( -4.406206840049315510, 68.52151906854182073, 12.76072571588954929 ) ) ;
#6264=CARTESIAN_POINT ( 'NONE',  ( 2.909063323423874969, 55.07541729461457436, -13.18314304101936507 ) ) ;
#6266=CARTESIAN_POINT ( 'NONE',  ( -9.403854346568712330, 65.31129198192570584, 9.690887349900259906 ) ) ;
#6268=CARTESIAN_POINT ( 'NONE',  ( -11.24427269215573588, 35.21054676296952124, 7.471034886962134358 ) ) ;
#6270=ORIENTED_EDGE ( 'NONE', *, *, #3966, .T. ) ;
#6271=CARTESIAN_POINT ( 'NONE',  ( 0.000000000000000000, 0.000000000000000000, 0.000000000000000000 ) ) ;
#6272=CARTESIAN_POINT ( 'NONE',  ( -4.492754712431366038, 40.34163550128833009, -12.73059084564603971 ) ) ;
#6273=CARTESIAN_POINT ( 'NONE',  ( -13.43211739905840751, 31.88231842745090105, -1.376614423219626238 ) ) ;
#6275=CARTESIAN_POINT ( 'NONE',  ( 10.82852970008509708, 60.12463039269763954, 8.062284012199853578 ) ) ;
#6278=VECTOR ( 'NONE', #15613, 1000.000000000000000 ) ;
#6279=CARTESIAN_POINT ( 'NONE',  ( -9.520470885617715595, 59.63000000000000256, -6.917026985038136289 ) ) ;
#6280=CARTESIAN_POINT ( 'NONE',  ( 13.50000000000000355, 74.58000000000001251, -4.386415899144233244 ) ) ;
#6281=CARTESIAN_POINT ( 'NONE',  ( 12.96113944439583143, 51.56544759790433119, -3.784739602708540041 ) ) ;
#6282=CARTESIAN_POINT ( 'NONE',  ( -13.33882841394733987, 38.00291347817611154, 2.079824949345720597 ) ) ;
#6283=CARTESIAN_POINT ( 'NONE',  ( 13.35680911868298892, 36.50067082660722662, -2.019122932424611605 ) ) ;
#6285=CARTESIAN_POINT ( 'NONE',  ( -3.467007694106094107, 74.55533922032466876, 13.04722352598931145 ) ) ;
#6286=CARTESIAN_POINT ( 'NONE',  ( -11.20645768432849998, 77.21280782326037695, 7.531521138223463474 ) ) ;
#6288=CARTESIAN_POINT ( 'NONE',  ( 0.3932787996077972692, 62.69414064364450923, 13.49440792938528588 ) ) ;
#6289=CARTESIAN_POINT ( 'NONE',  ( 2.314350980473266706, 41.76329157920511648, 13.31043818058748585 ) ) ;
#6293=EDGE_LOOP ( 'NONE', ( #9587, #10061, #16731, #5903 ) ) ;
#6294=CARTESIAN_POINT ( 'NONE',  ( 3.636496289402157078, 59.03000000000000114, -11.19198476289190936 ) ) ;
#6296=CARTESIAN_POINT ( 'NONE',  ( 10.92172942406178926, 56.13000000000000256, 7.935100905948387684 ) ) ;
#6298=CARTESIAN_POINT ( 'NONE',  ( 3.647687574545794842, 76.04884256590771940, -12.99786464873113800 ) ) ;
#6301=CARTESIAN_POINT ( 'NONE',  ( 3.636496289402154414, 48.82999999999999829, 11.19198476289190936 ) ) ;
#6302=PLANE ( 'NONE',  #10340 ) ;
#6304=CARTESIAN_POINT ( 'NONE',  ( -13.00542838102342103, 59.05976455672130498, 3.627390584878091406 ) ) ;
#6305=CARTESIAN_POINT ( 'NONE',  ( 13.02807058628658154, 45.30366086987346819, 3.541023234573203560 ) ) ;
#6306=CARTESIAN_POINT ( 'NONE',  ( 13.40107646287879106, 69.37314970047374629, 1.632315145005664769 ) ) ;
#6308=CARTESIAN_POINT ( 'NONE',  ( 13.49017281487221709, 30.44772149245933335, -0.5150320868971011157 ) ) ;
#6309=CARTESIAN_POINT ( 'NONE',  ( -11.05190432090530095, 56.22231890020226075, 7.752779392575588346 ) ) ;
#6310=CARTESIAN_POINT ( 'NONE',  ( -8.000342243122073427, 50.37758064104690447, 10.89743709494727675 ) ) ;
#6311=CYLINDRICAL_SURFACE ( 'NONE', #14927, 13.50000000000000000 ) ;
#6312=CARTESIAN_POINT ( 'NONE',  ( 3.419293449951197772, 43.05708390336630487, -13.06129965743578225 ) ) ;
#6313=CARTESIAN_POINT ( 'NONE',  ( 7.866618816620490229, 38.97691562748362770, 10.98017853868179827 ) ) ;
#6315=CARTESIAN_POINT ( 'NONE',  ( -4.064505406101394769, 61.32614459997894585, -12.87361187749841207 ) ) ;
#6318=CARTESIAN_POINT ( 'NONE',  ( -11.90455661557854405, 40.69456295689673908, -6.366441307886505641 ) ) ;
#6319=EDGE_LOOP ( 'NONE', ( #4376, #2449 ) ) ;
#6322=CARTESIAN_POINT ( 'NONE',  ( 6.632571939248276927, 47.92442758682717141, 11.75836653333053938 ) ) ;
#6323=CARTESIAN_POINT ( 'NONE',  ( 11.55679130585532377, 57.69021217686731973, -6.977864065983907516 ) ) ;
#6324=CARTESIAN_POINT ( 'NONE',  ( 9.155849417392163403, 78.82336870447842614, -9.921330499117095414 ) ) ;
#6325=CARTESIAN_POINT ( 'NONE',  ( 11.76794919243112680, 79.57999999999999829, -3.823638476888993942 ) ) ;
#6326=CARTESIAN_POINT ( 'NONE',  ( 7.272992578804311492, 82.87999999999999545, -10.01041549318726709 ) ) ;
#6330=CARTESIAN_POINT ( 'NONE',  ( -7.500000000000000000, 98.93000000000002103, 1.224646799147353059E-15 ) ) ;
#6331=CARTESIAN_POINT ( 'NONE',  ( 5.783632216765496104, 33.96956555804999311, -12.19835297658227979 ) ) ;
#6332=CARTESIAN_POINT ( 'NONE',  ( -13.47745682340583606, 73.95692245389201958, 0.7799622905020241470 ) ) ;
#6333=ADVANCED_FACE ( 'NONE', ( #8123 ), #7947, .T. ) ;
#6335=DIRECTION ( 'NONE',  ( 0.000000000000000000, -1.000000000000000000, 0.000000000000000000 ) ) ;
#6337=ORIENTED_EDGE ( 'NONE', *, *, #16969, .F. ) ;
#6341=CARTESIAN_POINT ( 'NONE',  ( -7.201777607271541370, 59.41183315282604838, 11.41860466315153388 ) ) ;
#6342=CARTESIAN_POINT ( 'NONE',  ( 7.500000000000000000, 108.9300000000000068, -12.00000000000000178 ) ) ;
#6344=CARTESIAN_POINT ( 'NONE',  ( -10.92172942406179104, 53.22999999999999687, 7.935100905948387684 ) ) ;
#6345=CARTESIAN_POINT ( 'NONE',  ( 13.49999999999999822, 50.27999999999999403, 4.386415899144237684 ) ) ;
#6346=CARTESIAN_POINT ( 'NONE',  ( -3.158365208622146092, 71.56643682723847633, 13.12534696263546685 ) ) ;
#6347=( BOUNDED_CURVE ( )  B_SPLINE_CURVE ( 2, ( #6423, #7923, #8012, #3757, #9256, #15757, #17440, #15849, #6513, #3575, #14345, #11894, #2234 ),
 .UNSPECIFIED., .F., .F. ) 
 B_SPLINE_CURVE_WITH_KNOTS ( ( 3, 2, 2, 2, 2, 2, 3 ),
 ( 0.7361111111111110494, 0.7388888888888889284, 0.7444444444444444642, 0.7500000000000000000, 0.7555555555555555358, 0.7611111111111110716, 0.7638888888888888395 ),
 .UNSPECIFIED. ) 
 CURVE ( )  GEOMETRIC_REPRESENTATION_ITEM ( )  RATIONAL_B_SPLINE_CURVE ( ( 0.9755282581475768211, 0.9755282581475762660, 1.000000000000000000, 0.9510565162951535312, 1.000000000000000000, 0.9510565162951535312, 1.000000000000000000, 0.9510565162951535312, 1.000000000000000000, 0.9510565162951535312, 1.000000000000000000, 0.9755282581475772652, 0.9755282581475768211 ) ) 
 REPRESENTATION_ITEM ( '' )  );
#6350=CARTESIAN_POINT ( 'NONE',  ( 1.608760344010755849, 68.73785721169490159, 13.40460866987880451 ) ) ;
#6354=CARTESIAN_POINT ( 'NONE',  ( -7.494032182223336669, 65.39933563442717457, 11.22954942317015181 ) ) ;
#6356=DIRECTION ( 'NONE',  ( 0.000000000000000000, -1.000000000000000000, 0.000000000000000000 ) ) ;
#6358=CARTESIAN_POINT ( 'NONE',  ( -1.627500644183926592, 35.62147431220920168, 13.40154254870227035 ) ) ;
#6363=CARTESIAN_POINT ( 'NONE',  ( 8.343458848123580296, 79.98000000000000398, 11.48378591275253768 ) ) ;
#6364=CARTESIAN_POINT ( 'NONE',  ( -12.95925257371713890, 32.06574706565864830, 3.792278602194695036 ) ) ;
#6366=CARTESIAN_POINT ( 'NONE',  ( 10.77435480767992004, 60.12150780088424540, 8.134627539065268920 ) ) ;
#6368=CARTESIAN_POINT ( 'NONE',  ( -11.94568210041848211, 53.16233194022309050, 6.289003155707704629 ) ) ;
#6369=CARTESIAN_POINT ( 'NONE',  ( -3.636496289402153081, 56.32999999999999829, -11.19198476289190936 ) ) ;
#6371=CARTESIAN_POINT ( 'NONE',  ( 11.59569013348710165, 51.68756802306698006, -6.913263822545960835 ) ) ;
#6372=CARTESIAN_POINT ( 'NONE',  ( -10.49833770927574328, 38.25438360216252676, 8.492147799501781336 ) ) ;
#6373=CARTESIAN_POINT ( 'NONE',  ( 10.14797380081446931, 36.77298809516717881, -8.903775999886867965 ) ) ;
#6375=CARTESIAN_POINT ( 'NONE',  ( -3.427855787583714786, 74.55674710714738751, 13.05757467429366336 ) ) ;
#6377=CARTESIAN_POINT ( 'NONE',  ( -9.860018955205955393, 77.28819560419356094, 9.231716877605229854 ) ) ;
#6379=CARTESIAN_POINT ( 'NONE',  ( -4.171729424061791036, 61.53000000000000114, 12.83926296998457239 ) ) ;
#6381=VERTEX_POINT ( 'NONE', #12351 ) ;
#6384=CARTESIAN_POINT ( 'NONE',  ( 11.76794919243112680, 55.58000000000000540, -3.823638476888993942 ) ) ;
#6387=CARTESIAN_POINT ( 'NONE',  ( 10.64789061155650884, 75.74566424434127043, -8.299534072142243701 ) ) ;
#6388=CARTESIAN_POINT ( 'NONE',  ( 7.272992578804308828, 33.97999999999999687, 10.01041549318726709 ) ) ;
#6390=CARTESIAN_POINT ( 'NONE',  ( -10.92172942406179104, 68.23000000000000398, 7.935100905948387684 ) ) ;
#6391=CIRCLE ( 'NONE', #14274, 12.00000000000000178 ) ;
#6392=CARTESIAN_POINT ( 'NONE',  ( -9.520470885617715595, 53.62999999999999545, -6.917026985038136289 ) ) ;
#6393=DIRECTION ( 'NONE',  ( -0.5000056658327881598, 0.000000000000000000, -0.8660221325896412248 ) ) ;
#6394=CARTESIAN_POINT ( 'NONE',  ( -9.891505788093740037, 59.28644356468626597, 9.187487902970126186 ) ) ;
#6395=CARTESIAN_POINT ( 'NONE',  ( 12.08007619667642629, 45.20759642052237837, 6.045378948472979630 ) ) ;
#6396=CARTESIAN_POINT ( 'NONE',  ( 11.92386745150823835, 69.66398541232135244, -6.330266153154159525 ) ) ;
#6398=CARTESIAN_POINT ( 'NONE',  ( 12.98311147291790668, 30.29531732055727034, 3.773380263830190096 ) ) ;
#6399=CARTESIAN_POINT ( 'NONE',  ( -4.385685656986241909, 55.33775113349322083, -12.76810838760984979 ) ) ;
#6400=CARTESIAN_POINT ( 'NONE',  ( -13.45332018961691567, 49.96890492016202501, 1.122494546679217997 ) ) ;
#6402=CARTESIAN_POINT ( 'NONE',  ( 5.641315611847744549, 42.97511016371111481, -12.26481840930462930 ) ) ;
#6403=CARTESIAN_POINT ( 'NONE',  ( 13.32130220385322517, 39.35314012507830483, 2.189450966719809433 ) ) ;
#6405=CARTESIAN_POINT ( 'NONE',  ( -6.536041484435296312, 70.42036142381789432, -11.81975216884413626 ) ) ;
#6406=CARTESIAN_POINT ( 'NONE',  ( -9.590357845055994090, 61.55798154981976467, -9.505963504770354788 ) ) ;
#6407=VECTOR ( 'NONE', #3267, 1000.000000000000000 ) ;
#6410=CARTESIAN_POINT ( 'NONE',  ( -8.149994195541450992, 40.48961995060131613, -10.76232869325634667 ) ) ;
#6411=ORIENTED_EDGE ( 'NONE', *, *, #9029, .T. ) ;
#6414=CARTESIAN_POINT ( 'NONE',  ( 13.39116189056811734, 57.37028256231064205, 1.710872541480398468 ) ) ;
#6415=CARTESIAN_POINT ( 'NONE',  ( 12.23576758771793749, 78.63913862522007037, -5.705453660566566221 ) ) ;
#6416=CARTESIAN_POINT ( 'NONE',  ( 3.636496289402157078, 80.03000000000000114, -11.19198476289190936 ) ) ;
#6417=CARTESIAN_POINT ( 'NONE',  ( -9.520470885617717371, 75.23000000000000398, 6.917026985038133624 ) ) ;
#6418=DIRECTION ( 'NONE',  ( 0.000000000000000000, 0.000000000000000000, -1.000000000000000000 ) ) ;
#6420=( NAMED_UNIT ( * ) SI_UNIT ( $, .STERADIAN. ) SOLID_ANGLE_UNIT ( ) );
#6423=CARTESIAN_POINT ( 'NONE',  ( -8.291044507619272909E-14, 45.17999999999999972, -13.50000000000000000 ) ) ;
#6424=CARTESIAN_POINT ( 'NONE',  ( 10.21170435963994549, 33.76958486911632207, -8.830561736147624075 ) ) ;
#6425=CARTESIAN_POINT ( 'NONE',  ( -13.47976463482231857, 73.95550874856458279, 0.7393779786335853421 ) ) ;
#6435=CARTESIAN_POINT ( 'NONE',  ( 9.880245923157088939, 66.78702064977453290, -9.199584342333487541 ) ) ;
#6436=CARTESIAN_POINT ( 'NONE',  ( -8.343458848123582072, 50.37999999999999545, 11.48378591275254124 ) ) ;
#6437=CARTESIAN_POINT ( 'NONE',  ( -11.74928976714265261, 71.17669313983024892, 6.649811694681813989 ) ) ;
#6438=EDGE_CURVE ( 'NONE', #16836, #14499, #10971, .T. ) ;
#6440=CARTESIAN_POINT ( 'NONE',  ( -13.49893008054767307, 67.93627681339535229, 0.1832009443085887701 ) ) ;
#6442=CARTESIAN_POINT ( 'NONE',  ( 4.773287838552558782, 55.00798678553170618, -12.62802569744146552 ) ) ;
#6444=CARTESIAN_POINT ( 'NONE',  ( -6.760456215069256203, 65.43070360383805451, 11.70411596025642886 ) ) ;
#6446=CARTESIAN_POINT ( 'NONE',  ( -9.396703253528214006, 35.31151048980861162, 9.692882425390839884 ) ) ;
#6450=CARTESIAN_POINT ( 'NONE',  ( -3.690040334857666249, 40.31264515183992359, -12.98793614100416782 ) ) ;
#6451=CARTESIAN_POINT ( 'NONE',  ( -12.61099646397594576, 32.10463546966393977, 4.817970500361715480 ) ) ;
#6452=CARTESIAN_POINT ( 'NONE',  ( 0.2743714829360081597, 73.17013493549970349, -13.49759525946641858 ) ) ;
#6455=CARTESIAN_POINT ( 'NONE',  ( -0.7596481966012033071, 53.65269506995328896, 13.47926920936900608 ) ) ;
#6456=CARTESIAN_POINT ( 'NONE',  ( -11.76794919243112325, 54.07999999999999119, 3.823638476888994386 ) ) ;
#6457=CARTESIAN_POINT ( 'NONE',  ( -8.343458848123582072, 73.38000000000000966, 11.48378591275254124 ) ) ;
#6459=CARTESIAN_POINT ( 'NONE',  ( 3.474791655989063699, 50.80483670142854891, 13.04534542254549301 ) ) ;
#6460=CONICAL_SURFACE ( 'NONE', #5909, 9.500000000000021316, 0.7853981633974504994 ) ;
#6461=CARTESIAN_POINT ( 'NONE',  ( -12.59156949641007728, 38.10658175097438516, 4.868567088784999441 ) ) ;
#6462=CARTESIAN_POINT ( 'NONE',  ( 13.49495430563132992, 36.44321454405320537, -0.3851982713760790933 ) ) ;
#6464=CARTESIAN_POINT ( 'NONE',  ( -3.081887839508138605, 74.56919532197451872, 13.14385889904788307 ) ) ;
#6465=CARTESIAN_POINT ( 'NONE',  ( -12.13432200433486052, 77.14750715261939717, 5.916777068713412469 ) ) ;
#6466=CARTESIAN_POINT ( 'NONE',  ( -8.343458848123578520, 60.47999999999999687, -11.48378591275254124 ) ) ;
#6467=CARTESIAN_POINT ( 'NONE',  ( 7.499999999999999112, 108.1112172271399743, 5.064597142177447608 ) ) ;
#6470=ORIENTED_EDGE ( 'NONE', *, *, #8177, .F. ) ;
#6471=CARTESIAN_POINT ( 'NONE',  ( 3.636496289402157078, 56.02999999999999403, -11.19198476289190936 ) ) ;
#6475=CARTESIAN_POINT ( 'NONE',  ( 8.583537299616791572, 75.85053009153234882, -10.41983335155395451 ) ) ;
#6477=DIRECTION ( 'NONE',  ( 0.000000000000000000, -1.000000000000000000, 0.000000000000000000 ) ) ;
#6478=CARTESIAN_POINT ( 'NONE',  ( -13.49999999999999822, 73.77999999999998693, -4.386415899144240349 ) ) ;
#6479=CARTESIAN_POINT ( 'NONE',  ( -3.636496289402153081, 38.32999999999999829, -11.19198476289190936 ) ) ;
#6480=LINE ( 'NONE', #14400, #13984 ) ;
#6482=CARTESIAN_POINT ( 'NONE',  ( -11.13989584533736732, 59.21702220567828334, 7.626482110035076367 ) ) ;
#6483=CARTESIAN_POINT ( 'NONE',  ( 9.945261256422160301, 45.07602360461397240, 9.147325197284214227 ) ) ;
#6484=CARTESIAN_POINT ( 'NONE',  ( 13.26845858006661949, 69.34132304966905735, 2.518521654702833956 ) ) ;
#6486=CARTESIAN_POINT ( 'NONE',  ( 12.02149203852282788, 30.65648930801207328, -6.142778965568425065 ) ) ;
#6488=CARTESIAN_POINT ( 'NONE',  ( -4.298585430698084409, 55.33458420718728377, -12.79766616383132671 ) ) ;
#6489=CARTESIAN_POINT ( 'NONE',  ( -5.433699768483149839, 50.48312169129376059, 12.35834494753474289 ) ) ;
#6490=CARTESIAN_POINT ( 'NONE',  ( 5.356475045761456499, 63.98608451589991830, -12.39185946976114927 ) ) ;
#6491=CARTESIAN_POINT ( 'NONE',  ( 13.00839847755452894, 42.55890957469971880, -3.609942547316297823 ) ) ;
#6492=CARTESIAN_POINT ( 'NONE',  ( 10.48980811747609998, 39.10526784545407963, 8.500966251292467746 ) ) ;
#6493=VERTEX_POINT ( 'NONE', #5911 ) ;
#6494=CARTESIAN_POINT ( 'NONE',  ( -7.815479942303253047, 70.47470329232851327, -11.00769136349473065 ) ) ;
#6495=CARTESIAN_POINT ( 'NONE',  ( -7.305932770837913814, 61.45259908546214689, -11.35225092655161383 ) ) ;
#6502=CARTESIAN_POINT ( 'NONE',  ( 2.930883425776768636, 61.07461791577657806, -13.17823006371532735 ) ) ;
#6503=PRODUCT_DEFINITION_SHAPE ( 'NONE', 'NONE',  #8924 ) ;
#6504=CARTESIAN_POINT ( 'NONE',  ( 12.43727753264746028, 57.23865299909770243, 5.250246734765029899 ) ) ;
#6506=CARTESIAN_POINT ( 'NONE',  ( 11.76794919243112680, 70.58000000000001251, -3.823638476888993942 ) ) ;
#6507=CARTESIAN_POINT ( 'NONE',  ( -7.576616670048093940E-16, 75.67999999999999261, 12.37355403259654985 ) ) ;
#6508=CARTESIAN_POINT ( 'NONE',  ( -0.08604155877350383452, 47.67690458564754863, 13.49999999999964295 ) ) ;
#6509=B_SPLINE_CURVE_WITH_KNOTS ( 'NONE', 3,
 ( #11295, #682, #14192, #6094, #2076, #7586, #770, #6178, #12965, #11212, #16586, #4491, #13924, #17108, #7674, #14531, #11731, #11990, #17023, #5286, #6346, #3770, #10585, #4927, #11821, #2246, #15771, #9182, #17371, #15681, #3588, #17283, #15946, #14358, #5108, #6527, #10500, #936, #13139, #2417, #10669, #16033, #17200, #11645, #6258, #1027, #5197, #2334, #13053, #8023, #3941, #5014, #3680, #2593, #9096, #2506, #15863, #13391, #3855, #9269, #7936, #14448, #11906, #10326, #9000, #14621, #6437, #7850, #10414, #7768, #13224, #13309, #1112, #1199, #6611, #9355, #14704, #51, #16205, #10839, #2860, #9531, #5638, #14790, #12248, #6693, #14874, #5454, #13478, #4116, #6960, #2769, #12074, #17453, #8291, #9442, #16299, #8200, #5367, #5548, #8113, #13648, #13564, #142, #4027, #2680, #10752, #9618, #6873, #1455, #14969, #11020, #10932, #232, #1543, #12340, #16116, #4206, #1365, #6782, #1280, #12160, #2563, #3825, #2649, #6580, #6747, #17422, #2473, #16002, #14500, #1250, #5165, #16087, #13106, #10470, #17340, #9153, #2387, #3995, #7823, #10384, #1169, #12044, #9061, #5076, #15738, #14759, #8080, #13444, #11961, #3908, #1081, #9325, #17077, #14593, #14675, #3647, #10557, #993, #13195, #1331, #4981, #15831, #6494, #3736, #7993, #9411, #14414, #2302, #7730, #11877, #6405, #5337, #5251, #10722, #15916, #11789, #17166, #17252, #13361, #9239, #7906, #13281, #10637, #6662, #9849, #5603, #11073, #107, #1774, #198, #1511, #16535, #284, #10895, #16264, #8432, #13786, #4261, #10986, #16446, #9584, #1684, #16355, #11160, #8167 ),
 .UNSPECIFIED., .F., .F.,
 ( 4, 1, 2, 2, 1, 1, 1, 2, 2, 2, 2, 2, 2, 1, 1, 2, 2, 2, 1, 2, 2, 1, 1, 2, 1, 1, 1, 2, 2, 1, 1, 2, 2, 2, 2, 2, 1, 1, 1, 2, 2, 1, 1, 1, 2, 2, 1, 1, 1, 2, 2, 2, 2, 1, 1, 2, 2, 1, 1, 2, 2, 2, 2, 1, 2, 2, 2, 2, 2, 2, 1, 1, 2, 2, 1, 1, 1, 2, 2, 1, 2, 2, 2, 2, 1, 2, 2, 1, 2, 2, 2, 1, 1, 1, 2, 2, 1, 2, 2, 2, 2, 1, 1, 1, 1, 2, 2, 2, 2, 2, 2, 2, 2, 2, 2, 2, 1, 2, 2, 1, 1, 2, 2, 1, 1, 2, 2, 4 ),
 ( 0.1814966425150734142, 0.1816111196666974903, 0.1816397389546035024, 0.1816468937765800262, 0.1816540485985565223, 0.1816683582425095422, 0.1817255968183215664, 0.1819545511215697464, 0.1824124597280660509, 0.1833282769410587154, 0.1835572312443068677, 0.1835858505322129075, 0.1836001601761658997, 0.1836144698201189196, 0.1836717083959309438, 0.1837861855475550199, 0.1842440941540512966, 0.1844730484572994489, 0.1845302870331114731, 0.1845589063210174852, 0.1845732159649705051, 0.1845875256089234973, 0.1847020027605476011, 0.1851599113670439056, 0.1853888656702920579, 0.1855033428219161340, 0.1855319621098221461, 0.1855462717537751660, 0.1855534265757516621, 0.1855605813977281582, 0.1856178199735402101, 0.1860757285800365979, 0.1869915457930293456, 0.1874494543995257334, 0.1874780736874317455, 0.1875066929753377576, 0.1875639315511498095, 0.1876784087027739134, 0.1879073630060221212, 0.1888231802190149522, 0.1906548146450005865, 0.1911127232514970020, 0.1913416775547452098, 0.1913989161305572617, 0.1914060709525337578, 0.1914096483635220058, 0.1914132257745102539, 0.1914275354184632738, 0.1914561547063693137, 0.1915706318579935008, 0.1924864490709868314, 0.1929443576774834967, 0.1931733119807318433, 0.1932877891323560027, 0.1933450277081680824, 0.1933593373521211300, 0.1933664921740976261, 0.1933736469960741500, 0.1934022662839801898, 0.1943180834969736315, 0.1952339007099670731, 0.1952911392857791528, 0.1953197585736852204, 0.1953483778615912603, 0.1954628550132154197, 0.1956918093164637940, 0.1961497179229604870, 0.1962641950745846742, 0.1962785047185376941, 0.1962928143624907140, 0.1963214336503967539, 0.1963786722262088336, 0.1966076265294572079, 0.1970655351359539009, 0.1971800122875780881, 0.1972372508633901678, 0.1972515605073431877, 0.1972587153293197115, 0.1972658701512962076, 0.1972944894392022475, 0.1975234437424505385, 0.1979813523489470928, 0.1988971695619402569, 0.1991261238651885479, 0.1991833624410006276, 0.1992119817289066397, 0.1992406010168126795, 0.1993550781684368389, 0.1998129867749333932, 0.2016446212009196937, 0.2025604384139128300, 0.2030183470204093843, 0.2030755855962214640, 0.2031042048841275038, 0.2031185145280805238, 0.2031256693500570476, 0.2031328241720335437, 0.2032473013236579806, 0.2034762556269068545, 0.2043920728399024056, 0.2048499814464001811, 0.2049644585980246181, 0.2050216971738368366, 0.2050503164617429597, 0.2050646261056960074, 0.2050717809276725312, 0.2050789357496490550, 0.2053078900528980677, 0.2062237072658940629, 0.2066816158723920327, 0.2069105701756410454, 0.2070250473272655378, 0.2070822859030777841, 0.2071395244788900303, 0.2075974330853880279, 0.2078263873886370128, 0.2079408645402615052, 0.2079981031160737515, 0.2080124127600268269, 0.2080267224039798746, 0.2080553416918859977, 0.2089711589048821316, 0.2090283974806943779, 0.2090856360565066518, 0.2092001132081311443, 0.2094290675113801847, 0.2098869761178782378, 0.2108027933308743440 ),
 .UNSPECIFIED. ) ;
#6510=CARTESIAN_POINT ( 'NONE',  ( -8.891200544363830713E-16, 40.67999999999999261, 13.50000000000000000 ) ) ;
#6513=CARTESIAN_POINT ( 'NONE',  ( 10.92172942406178926, 44.13000000000000256, 7.935100905948387684 ) ) ;
#6514=CARTESIAN_POINT ( 'NONE',  ( 5.336470388020742028, 33.98688528483218363, -12.40243878204504213 ) ) ;
#6515=CARTESIAN_POINT ( 'NONE',  ( -2.994701108386524258, 73.28771383196766465, -13.16632730457292766 ) ) ;
#6517=ORIENTED_EDGE ( 'NONE', *, *, #14361, .F. ) ;
#6518=CARTESIAN_POINT ( 'NONE',  ( 3.636496289402157078, 80.03000000000000114, -11.19198476289190936 ) ) ;
#6523=CARTESIAN_POINT ( 'NONE',  ( -5.526118766865936394, 44.47964708879426610, 12.32381976411106450 ) ) ;
#6525=CARTESIAN_POINT ( 'NONE',  ( 11.59702038864718432, 66.68748371943325992, -6.910806977644125659 ) ) ;
#6526=CARTESIAN_POINT ( 'NONE',  ( -13.49999999999999822, 40.78000000000000114, -4.386415899144240349 ) ) ;
#6527=CARTESIAN_POINT ( 'NONE',  ( -4.555328311572941935, 71.51607439978332081, 12.70834120064674622 ) ) ;
#6530=CARTESIAN_POINT ( 'NONE',  ( -12.69503808151269553, 68.09607240394507244, 4.594974419746471028 ) ) ;
#6532=CARTESIAN_POINT ( 'NONE',  ( 2.474201151127992215, 55.09108309819342963, -13.27610207924121255 ) ) ;
#6534=CARTESIAN_POINT ( 'NONE',  ( -12.86040510649366553, 65.07770000608704208, 4.111097590322251527 ) ) ;
#6535=CARTESIAN_POINT ( 'NONE',  ( -6.936718818989325186, 35.42298707049641848, 11.58157915692249773 ) ) ;
#6536=ORIENTED_EDGE ( 'NONE', *, *, #6196, .F. ) ;
#6539=CARTESIAN_POINT ( 'NONE',  ( -7.993062784379826979, 31.48258056696385410, -10.87940591478879604 ) ) ;
#6541=CARTESIAN_POINT ( 'NONE',  ( 11.48106618170696080, 60.16469814098914526, 7.105216182321891338 ) ) ;
#6543=CARTESIAN_POINT ( 'NONE',  ( -7.133837838234538431, 53.41470899139449102, 11.46116927770655813 ) ) ;
#6544=CARTESIAN_POINT ( 'NONE',  ( 3.636496289402157078, 53.03000000000000114, -11.19198476289190936 ) ) ;
#6545=CARTESIAN_POINT ( 'NONE',  ( 10.92172942406178926, 77.13000000000000966, 7.935100905948387684 ) ) ;
#6546=CARTESIAN_POINT ( 'NONE',  ( 4.773616553820369646, 50.85195731075037884, 12.62846895061231578 ) ) ;
#6547=CARTESIAN_POINT ( 'NONE',  ( -9.258348693882576086, 37.54127912305889936, -9.843850005556705085 ) ) ;
#6548=CARTESIAN_POINT ( 'NONE',  ( 13.28445700308491162, 36.34535166002273598, 2.405321636251910977 ) ) ;
#6551=CARTESIAN_POINT ( 'NONE',  ( -6.401350755636498135, 77.44499155070386109, 11.88582777253868450 ) ) ;
#6552=CARTESIAN_POINT ( 'NONE',  ( -12.79004503783874469, 79.77371121109450769, -4.343132741677108832 ) ) ;
#6554=CARTESIAN_POINT ( 'NONE',  ( 7.500000000000000000, 104.2024577724304208, 9.199283337799339932 ) ) ;
#6558=CARTESIAN_POINT ( 'NONE',  ( -7.272992578804307939, 53.47999999999998977, -10.01041549318727064 ) ) ;
#6562=EDGE_CURVE ( 'NONE', #16381, #14613, #1644, .T. ) ;
#6563=CARTESIAN_POINT ( 'NONE',  ( 6.109412881612292345, 75.95670156276325713, -12.03862480236976396 ) ) ;
#6565=CARTESIAN_POINT ( 'NONE',  ( -13.50000000000000000, 76.92999999999999261, -3.306546357697853733E-15 ) ) ;
#6566=CARTESIAN_POINT ( 'NONE',  ( -11.76794919243112325, 44.92999999999999972, -2.882316262207890869E-15 ) ) ;
#6568=CARTESIAN_POINT ( 'NONE',  ( -11.18263218352950972, 58.64562392974652028, -7.562986225119091799 ) ) ;
#6569=CARTESIAN_POINT ( 'NONE',  ( 13.49528878454824543, 45.41772704297711272, 0.3573627978170749731 ) ) ;
#6570=CARTESIAN_POINT ( 'NONE',  ( 13.10377846605443963, 69.54542809245315027, -3.246696344792387556 ) ) ;
#6571=CIRCLE ( 'NONE', #7984, 12.00000000000000178 ) ;
#6572=CARTESIAN_POINT ( 'NONE',  ( 1.653273178848926472E-15, 80.93000000000000682, 13.50000000000000000 ) ) ;
#6574=CARTESIAN_POINT ( 'NONE',  ( -10.18807947666135583, 55.58911967552339917, -8.857645364605666316 ) ) ;
#6575=CARTESIAN_POINT ( 'NONE',  ( -10.93185410481415154, 50.22943847104855308, 7.921438598450179391 ) ) ;
#6576=CARTESIAN_POINT ( 'NONE',  ( 11.49298963318043398, 63.69447171356610937, -7.082473735879659671 ) ) ;
#6577=CARTESIAN_POINT ( 'NONE',  ( 8.081592316167094836, 42.87346269304677548, -10.81406279893415068 ) ) ;
#6578=CARTESIAN_POINT ( 'NONE',  ( 11.13323897052192635, 39.14259498289401762, 7.635513019236351617 ) ) ;
#6579=ORIENTED_EDGE ( 'NONE', *, *, #13611, .T. ) ;
#6580=CARTESIAN_POINT ( 'NONE',  ( -13.38634760227498255, 70.86891057379173731, -1.749485324747906301 ) ) ;
#6581=CARTESIAN_POINT ( 'NONE',  ( -2.555879417051283298, 61.27177513301734990, -13.26191791090011307 ) ) ;
#6584=VERTEX_POINT ( 'NONE', #8652 ) ;
#6587=CARTESIAN_POINT ( 'NONE',  ( 3.060653757609212544, 47.79012880483755055, 13.14927094501084426 ) ) ;
#6588=TOROIDAL_SURFACE ( 'NONE', #6022, 6.000000000000001776, 6.000000000000000000 ) ;
#6589=CARTESIAN_POINT ( 'NONE',  ( 2.337253843264979203, 71.76409061300877568, 13.29619868658769199 ) ) ;
#6590=CARTESIAN_POINT ( 'NONE',  ( 13.35987737257807950, 57.49792048163389779, -1.940069495529155308 ) ) ;
#6591=CARTESIAN_POINT ( 'NONE',  ( 7.272992578804308828, 72.98000000000000398, 10.01041549318726709 ) ) ;
#6592=CARTESIAN_POINT ( 'NONE',  ( 11.76794919243112325, 76.28000000000000114, 3.823638476888996607 ) ) ;
#6593=CARTESIAN_POINT ( 'NONE',  ( -9.858871623890049563, 47.28812877695573746, 9.222456157666663046 ) ) ;
#6597=AXIS2_PLACEMENT_3D ( 'NONE', #9393, #16248, #2633 ) ;
#6599=CARTESIAN_POINT ( 'NONE',  ( 5.806605737915351284, 33.96866633168072269, -12.18742560399044983 ) ) ;
#6600=CARTESIAN_POINT ( 'NONE',  ( -3.655908334455305386, 73.31145551481743894, -12.99555118694178724 ) ) ;
#6601=ORIENTED_EDGE ( 'NONE', *, *, #15801, .T. ) ;
#6603=CARTESIAN_POINT ( 'NONE',  ( 11.76794919243112325, 73.42999999999999261, 1.441158131103945434E-15 ) ) ;
#6604=ORIENTED_EDGE ( 'NONE', *, *, #5085, .F. ) ;
#6605=EDGE_CURVE ( 'NONE', #13128, #15397, #2389, .T. ) ;
#6606=CARTESIAN_POINT ( 'NONE',  ( -12.70590379749083532, 41.09495175222023278, 4.565257769830444623 ) ) ;
#6608=CARTESIAN_POINT ( 'NONE',  ( -1.180642086793956880, 44.63755760315241616, 13.45088169940935785 ) ) ;
#6610=CARTESIAN_POINT ( 'NONE',  ( 8.343458848123583849, 39.88000000000000256, -11.48378591275253768 ) ) ;
#6611=CARTESIAN_POINT ( 'NONE',  ( -11.84785472851091725, 71.16967805033135619, 6.471368726115286130 ) ) ;
#6613=CARTESIAN_POINT ( 'NONE',  ( -13.49960910270157477, 67.93362544972310957, 0.1058906348414896115 ) ) ;
#6615=CARTESIAN_POINT ( 'NONE',  ( 4.837186686068091213, 55.00564863163254614, -12.60363724258546725 ) ) ;
#6617=CARTESIAN_POINT ( 'NONE',  ( -13.47566967663552262, 64.96175637022594174, 0.9213295838320114672 ) ) ;
#6618=CARTESIAN_POINT ( 'NONE',  ( -7.866623628157809911, 35.38328011712205523, 10.98017150749901738 ) ) ;
#6620=ORIENTED_EDGE ( 'NONE', *, *, #14405, .F. ) ;
#6621=CARTESIAN_POINT ( 'NONE',  ( 8.343458848123580296, 49.97999999999999687, 11.48378591275253768 ) ) ;
#6623=CARTESIAN_POINT ( 'NONE',  ( -10.15547274497371077, 31.58743970881114294, -8.894744516544626833 ) ) ;
#6626=CARTESIAN_POINT ( 'NONE',  ( 4.946212110863060119, 59.85840281924108552, 12.56136872037263075 ) ) ;
#6628=CARTESIAN_POINT ( 'NONE',  ( -9.936413839488240640, 53.28410195231833058, 9.138806663926128948 ) ) ;
#6629=CARTESIAN_POINT ( 'NONE',  ( -7.272992578804310604, 51.37999999999998835, 10.01041549318726709 ) ) ;
#6631=CARTESIAN_POINT ( 'NONE',  ( 4.171729424061789260, 70.82999999999999829, 12.83926296998457417 ) ) ;
#6632=CARTESIAN_POINT ( 'NONE',  ( 3.336094116535059495, 50.79992621253678919, 13.08131499243033602 ) ) ;
#6633=CARTESIAN_POINT ( 'NONE',  ( -12.98164777139678527, 37.79751183502862233, -3.705885770400368706 ) ) ;
#6635=CARTESIAN_POINT ( 'NONE',  ( 9.257065025830906180, 36.04160388237846746, 9.826378808067678605 ) ) ;
#6638=CARTESIAN_POINT ( 'NONE',  ( -13.04317161032976813, 77.05446084332930923, 3.489292788701963577 ) ) ;
#6639=CARTESIAN_POINT ( 'NONE',  ( -7.311605416996860285, 79.45288813049690191, -11.35076817521309067 ) ) ;
#6640=CARTESIAN_POINT ( 'NONE',  ( 7.500000000000000000, 103.1885367479068663, 9.367496997597603681 ) ) ;
#6642=CARTESIAN_POINT ( 'NONE',  ( 3.636496289402154414, 42.82999999999999829, 11.19198476289190936 ) ) ;
#6647=CARTESIAN_POINT ( 'NONE',  ( 10.86178057370645611, 75.73342452336723341, -8.018662730335858413 ) ) ;
#6648=CARTESIAN_POINT ( 'NONE',  ( 3.780205736804012180E-08, 55.17999999864077409, -13.50000000000000000 ) ) ;
#6649=CARTESIAN_POINT ( 'NONE',  ( -3.636496289402155746, 39.52999999999999403, 11.19198476289190936 ) ) ;
#6650=CARTESIAN_POINT ( 'NONE',  ( -7.060065731298120539, 41.41782043715235062, 11.50681685508514462 ) ) ;
#6651=CARTESIAN_POINT ( 'NONE',  ( -8.735628014122772456, 58.51658140302173905, -10.29271241388457092 ) ) ;
#6653=DIRECTION ( 'NONE',  ( -0.000000000000000000, -1.000000000000000000, -0.000000000000000000 ) ) ;
#6655=CARTESIAN_POINT ( 'NONE',  ( 7.500000000000001776, 88.93000000000000682, -12.00000000000000178 ) ) ;
#6656=CARTESIAN_POINT ( 'NONE',  ( -11.13669601958308597, 55.64279577809516297, -7.630683010739963912 ) ) ;
#6657=CARTESIAN_POINT ( 'NONE',  ( -13.46035977005674766, 49.89415119664435849, -1.037902563494175867 ) ) ;
#6658=CARTESIAN_POINT ( 'NONE',  ( 12.58047463934393662, 63.60811412330714631, -4.909781203544855366 ) ) ;
#6659=CARTESIAN_POINT ( 'NONE',  ( 11.34081891867551306, 42.70472919525936817, -7.328857843363596025 ) ) ;
#6660=CARTESIAN_POINT ( 'NONE',  ( 13.48360322846664161, 39.45292921673981112, -0.6651861330368826764 ) ) ;
#6662=CARTESIAN_POINT ( 'NONE',  ( -4.529881605775227804, 70.34304711494489482, -12.71783548896780403 ) ) ;
#6663=ORIENTED_EDGE ( 'NONE', *, *, #2092, .F. ) ;
#6667=CARTESIAN_POINT ( 'NONE',  ( 4.755586391641281274, 61.00868452792411034, -12.63465254569289975 ) ) ;
#6670=CARTESIAN_POINT ( 'NONE',  ( 2.286894564728605861, 71.76228337285282066, 13.30503304841837497 ) ) ;
#6671=CARTESIAN_POINT ( 'NONE',  ( 12.40506120401485646, 57.23570088601564265, 5.326196437455172017 ) ) ;
#6672=CARTESIAN_POINT ( 'NONE',  ( 2.272985001014427788E-15, 65.18000000000000682, -12.37355403259654985 ) ) ;
#6673=CARTESIAN_POINT ( 'NONE',  ( -7.272992578804310604, 72.38000000000000966, 10.01041549318726709 ) ) ;
#6674=CARTESIAN_POINT ( 'NONE',  ( -3.822134760076489890, 47.54257014335207998, 12.94763724393711968 ) ) ;
#6675=CARTESIAN_POINT ( 'NONE',  ( -8.291044507619272909E-14, 45.17999999999999972, -13.50000000000000000 ) ) ;
#6680=AXIS2_PLACEMENT_3D ( 'NONE', #8423, #3357, #361 ) ;
#6682=CARTESIAN_POINT ( 'NONE',  ( 12.88504001644114538, 33.57466858618573013, -4.031382377887867463 ) ) ;
#6683=CARTESIAN_POINT ( 'NONE',  ( -2.291594122932853139, 73.26239727050499084, -13.30408214462689820 ) ) ;
#6686=CARTESIAN_POINT ( 'NONE',  ( 3.636496289402157078, 74.03000000000000114, -11.19198476289190936 ) ) ;
#6687=ORIENTED_EDGE ( 'NONE', *, *, #6778, .T. ) ;
#6689=CARTESIAN_POINT ( 'NONE',  ( -7.582614570348264138, 44.39550065529663669, 11.16986078532532645 ) ) ;
#6691=CIRCLE ( 'NONE', #1584, 8.999999999999994671 ) ;
#6692=CARTESIAN_POINT ( 'NONE',  ( 4.171729424061791924, 46.02999999999999403, -12.83926296998457239 ) ) ;
#6693=CARTESIAN_POINT ( 'NONE',  ( -12.92401890517933261, 71.06980940734364083, 3.901267114863464336 ) ) ;
#6696=CARTESIAN_POINT ( 'NONE',  ( -13.41621384453693189, 67.98230079670533144, 1.502188851297376671 ) ) ;
#6698=CARTESIAN_POINT ( 'NONE',  ( 13.49861495593725635, 54.43666664097244023, -0.1944882449894331511 ) ) ;
#6701=CARTESIAN_POINT ( 'NONE',  ( -12.68351458231185447, 65.09718742194731078, 4.623735391779430159 ) ) ;
#6702=CARTESIAN_POINT ( 'NONE',  ( -12.58659164438495104, 35.10707630348271380, 4.881418642039425215 ) ) ;
#6705=LINE ( 'NONE', #1468, #5041 ) ;
#6706=( BOUNDED_CURVE ( )  B_SPLINE_CURVE ( 2, ( #11543, #16920, #5438, #16187, #12061, #15932, #14430, #10571, #14607, #9254, #9427, #17438, #7747 ),
 .UNSPECIFIED., .F., .F. ) 
 B_SPLINE_CURVE_WITH_KNOTS ( ( 3, 2, 2, 2, 2, 2, 3 ),
 ( 0.9305555555555555802, 0.9333333333333333481, 0.9388888888888888840, 0.9444444444444444198, 0.9499999999999999556, 0.9555555555555556024, 0.9583333333333333703 ),
 .UNSPECIFIED. ) 
 CURVE ( )  GEOMETRIC_REPRESENTATION_ITEM ( )  RATIONAL_B_SPLINE_CURVE ( ( 0.9755282581475768211, 0.9755282581475768211, 1.000000000000000000, 0.9510565162951535312, 1.000000000000000000, 0.9510565162951535312, 1.000000000000000000, 0.9510565162951535312, 1.000000000000000000, 0.9510565162951535312, 1.000000000000000000, 0.9755282581475768211, 0.9755282581475768211 ) ) 
 REPRESENTATION_ITEM ( '' )  );
#6707=CARTESIAN_POINT ( 'NONE',  ( -2.700228618987395190, 31.27709026527809044, -13.22723019811440714 ) ) ;
#6708=CARTESIAN_POINT ( 'NONE',  ( 4.609769263287132546, 73.01405650375669154, -12.68860813546349142 ) ) ;
#6712=CARTESIAN_POINT ( 'NONE',  ( -10.28587142665795362, 53.26568820729779219, 8.746296120241217054 ) ) ;
#6713=CARTESIAN_POINT ( 'NONE',  ( 2.272985001014427788E-15, 47.17999999999999972, -12.37355403259654985 ) ) ;
#6715=CARTESIAN_POINT ( 'NONE',  ( 10.92172942406178926, 65.12999999999999545, 7.935100905948387684 ) ) ;
#6716=CARTESIAN_POINT ( 'NONE',  ( 12.94092419851276610, 51.29169664346532898, 3.859288104999398783 ) ) ;
#6717=CARTESIAN_POINT ( 'NONE',  ( -6.877963339358277750, 37.43436270134902344, -11.62861394030559481 ) ) ;
#6718=CARTESIAN_POINT ( 'NONE',  ( 8.740290627326368522, 36.01677850278021964, 10.29110420094504086 ) ) ;
#6720=CARTESIAN_POINT ( 'NONE',  ( -6.897567406690312986, 74.42478730465043668, 11.61684038191101642 ) ) ;
#6721=CARTESIAN_POINT ( 'NONE',  ( -13.32725792319063274, 77.00693031600384586, 2.197311418460218491 ) ) ;
#6722=CARTESIAN_POINT ( 'NONE',  ( -10.87722630759161824, 80.23258579900503662, 7.996187592776850650 ) ) ;
#6724=CARTESIAN_POINT ( 'NONE',  ( 7.500000000000000000, 107.5003227710673315, 6.479247348114224536 ) ) ;
#6725=CYLINDRICAL_SURFACE ( 'NONE', #9504, 12.00000000000000178 ) ;
#6727=CARTESIAN_POINT ( 'NONE',  ( 2.272985001014427393E-15, 50.17999999999999261, -12.37355403259654807 ) ) ;
#6732=CARTESIAN_POINT ( 'NONE',  ( 9.387778834394914895, 75.81219621400516928, -9.711846743374673352 ) ) ;
#6733=ADVANCED_FACE ( 'NONE', ( #7761 ), #4747, .T. ) ;
#6734=CARTESIAN_POINT ( 'NONE',  ( 6.750022565184456980, 31.92926174983938026, 11.69132992304556495 ) ) ;
#6735=CARTESIAN_POINT ( 'NONE',  ( 2.272985001014427788E-15, 44.17999999999998550, -12.37355403259654985 ) ) ;
#6736=CARTESIAN_POINT ( 'NONE',  ( -6.920156336968187105, 41.42368190141654338, 11.59162295123014097 ) ) ;
#6737=CARTESIAN_POINT ( 'NONE',  ( -5.810482910230065023, 58.39149269753883686, -12.18558815465718936 ) ) ;
#6740=CARTESIAN_POINT ( 'NONE',  ( 0.000000000000000000, 80.93000000000000682, 0.000000000000000000 ) ) ;
#6742=CARTESIAN_POINT ( 'NONE',  ( -10.13962047673653899, 49.58657935891523749, -8.912807818290596984 ) ) ;
#6743=CARTESIAN_POINT ( 'NONE',  ( 13.36848944045340026, 63.49574276624128544, -1.879770406124993354 ) ) ;
#6744=CARTESIAN_POINT ( 'NONE',  ( 8.526517230384889956, 42.85320048867875187, -10.46736331332614611 ) ) ;
#6745=CARTESIAN_POINT ( 'NONE',  ( 5.574008873715639467, 38.88201036329166982, 12.30346572087647772 ) ) ;
#6747=CARTESIAN_POINT ( 'NONE',  ( -13.37563197002901028, 70.86603882634364027, -1.829879408878430036 ) ) ;
#6750=ORIENTED_EDGE ( 'NONE', *, *, #9376, .T. ) ;
#6754=CARTESIAN_POINT ( 'NONE',  ( 9.300701112953893457, 60.81627165076186259, -9.785047430583880157 ) ) ;
#6756=CARTESIAN_POINT ( 'NONE',  ( 2.493575575080797968, 71.76962337619772825, 13.26771539037355119 ) ) ;
#6757=CARTESIAN_POINT ( 'NONE',  ( 13.49926719046979784, 57.43485129297997815, -0.1416316033574115951 ) ) ;
#6758=CARTESIAN_POINT ( 'NONE',  ( 11.76794919243112325, 67.43000000000000682, 1.441158131103945434E-15 ) ) ;
#6759=CARTESIAN_POINT ( 'NONE',  ( 3.636496289402157078, 74.03000000000000114, -11.19198476289190936 ) ) ;
#6760=CARTESIAN_POINT ( 'NONE',  ( -9.831588973340092963, 47.28954498157629871, 9.251600547029006805 ) ) ;
#6765=CARTESIAN_POINT ( 'NONE',  ( -4.171729424061791036, 76.53000000000000114, 12.83926296998457239 ) ) ;
#6768=CARTESIAN_POINT ( 'NONE',  ( 13.48854948779883856, 33.44913808748793826, -0.5559301001735216241 ) ) ;
#6769=CARTESIAN_POINT ( 'NONE',  ( -4.986796838729953940, 73.35992462257202362, -12.54519991607214457 ) ) ;
#6770=EDGE_LOOP ( 'NONE', ( #15669, #8559, #14163, #12129, #9128, #14435, #8079, #5277, #3911, #485, #8018, #6107, #12810, #5975, #7841, #14389, #6604, #15855, #12000, #2133, #741, #410, #3930, #7665, #8717, #4916, #11764, #6663, #496, #7361, #16908, #5279, #12303, #14758, #2025, #2692, #14222, #14715, #6601 ) ) ;
#6772=CARTESIAN_POINT ( 'NONE',  ( -8.291044507619272909E-14, 45.17999999999999972, -13.50000000000000000 ) ) ;
#6773=EDGE_LOOP ( 'NONE', ( #15808, #11284, #15648, #14847 ) ) ;
#6776=CARTESIAN_POINT ( 'NONE',  ( -0.7753613165686097375, 44.65212122024217933, 13.47790793914508001 ) ) ;
#6778=EDGE_CURVE ( 'NONE', #15607, #5186, #5433, .T. ) ;
#6780=CARTESIAN_POINT ( 'NONE',  ( -8.343458848123576743, 43.47999999999998977, -11.48378591275254301 ) ) ;
#6781=CARTESIAN_POINT ( 'NONE',  ( 13.50000000000000000, 47.42999999999999972, 1.653273178848926867E-15 ) ) ;
#6782=CARTESIAN_POINT ( 'NONE',  ( -13.40458808007928049, 70.87413862071015558, -1.602539714754670719 ) ) ;
#6784=CARTESIAN_POINT ( 'NONE',  ( -11.80864895165088591, 67.68745830797494989, -6.543130247569663105 ) ) ;
#6786=CARTESIAN_POINT ( 'NONE',  ( 11.48581846909945270, 54.69492073424584788, -7.094357488526240374 ) ) ;
#6788=CARTESIAN_POINT ( 'NONE',  ( -11.89680182002208042, 64.69398173927839935, -6.380922029939451789 ) ) ;
#6790=CARTESIAN_POINT ( 'NONE',  ( -13.47775970262104295, 34.90311458208528705, -0.7771305193947938283 ) ) ;
#6792=VERTEX_POINT ( 'NONE', #2901 ) ;
#6794=EDGE_CURVE ( 'NONE', #5870, #10663, #10010, .T. ) ;
#6796=CARTESIAN_POINT ( 'NONE',  ( 2.107853069822502790E-14, 31.18000000000000682, -13.50000000000000000 ) ) ;
#6797=CARTESIAN_POINT ( 'NONE',  ( 4.584035459419017577, 73.01499104528438977, -12.69792770427072348 ) ) ;
#6801=CARTESIAN_POINT ( 'NONE',  ( -13.39856879038537585, 52.87025179575815770, -1.714939770267754460 ) ) ;
#6802=CARTESIAN_POINT ( 'NONE',  ( -11.76794919243112325, 50.77999999999998693, -3.823638476888998827 ) ) ;
#6803=CARTESIAN_POINT ( 'NONE',  ( -10.92172942406179104, 64.23000000000000398, 7.935100905948387684 ) ) ;
#6804=CARTESIAN_POINT ( 'NONE',  ( 3.659205458685654833, 50.81139327735426292, 12.99542509430799875 ) ) ;
#6805=CARTESIAN_POINT ( 'NONE',  ( -5.561034285559797397, 37.38178090531955178, -12.30142152455749915 ) ) ;
#6806=CARTESIAN_POINT ( 'NONE',  ( 4.138376238514326566, 35.82879951124870388, 12.85007333697660492 ) ) ;
#6808=CARTESIAN_POINT ( 'NONE',  ( -9.503523212203964121, 74.30641799480795839, 9.597461011868634984 ) ) ;
#6809=( BOUNDED_CURVE ( )  B_SPLINE_CURVE ( 2, ( #4081, #9496, #14843, #2737, #12141, #9512, #5528, #11001, #7115, #5436, #10823, #7032, #5707 ),
 .UNSPECIFIED., .F., .F. ) 
 B_SPLINE_CURVE_WITH_KNOTS ( ( 3, 2, 2, 2, 2, 2, 3 ),
 ( 0.1805555555555555525, 0.1833333333333333204, 0.1888888888888888840, 0.1944444444444444475, 0.2000000000000000111, 0.2055555555555555469, 0.2083333333333333148 ),
 .UNSPECIFIED. ) 
 CURVE ( )  GEOMETRIC_REPRESENTATION_ITEM ( )  RATIONAL_B_SPLINE_CURVE ( ( 0.9755282581475768211, 0.9755282581475768211, 1.000000000000000000, 0.9510565162951535312, 1.000000000000000000, 0.9510565162951535312, 1.000000000000000000, 0.9510565162951535312, 1.000000000000000000, 0.9510565162951535312, 1.000000000000000000, 0.9755282581475768211, 0.9755282581475765991 ) ) 
 REPRESENTATION_ITEM ( '' )  );
#6810=CARTESIAN_POINT ( 'NONE',  ( -10.79961255144821841, 76.62273742997086856, -8.101642849603434726 ) ) ;
#6811=CARTESIAN_POINT ( 'NONE',  ( -6.743467333083651205, 79.42893378531856285, -11.69562671412998611 ) ) ;
#6813=CARTESIAN_POINT ( 'NONE',  ( -9.639429313059489246, 80.92999999999997840, 7.743379967843619482 ) ) ;
#6816=CARTESIAN_POINT ( 'NONE',  ( 9.520470885617715595, 52.12999999999999545, 6.917026985038134512 ) ) ;
#6820=CARTESIAN_POINT ( 'NONE',  ( -12.51283734680061421, 40.74519236365699015, -5.085795480612188335 ) ) ;
#6822=CARTESIAN_POINT ( 'NONE',  ( 12.07265237676784153, 75.20733480710443075, 6.044380633809719683 ) ) ;
#6824=CARTESIAN_POINT ( 'NONE',  ( -7.000496543013151829, 41.42031948789649221, 11.54310368834964251 ) ) ;
#6825=CARTESIAN_POINT ( 'NONE',  ( -7.758731431966043424, 58.47177289251840904, -11.07319905588548536 ) ) ;
#6826=CARTESIAN_POINT ( 'NONE',  ( 0.6222550924804421957, 44.70229475783964546, 13.50000000005490719 ) ) ;
#6829=EDGE_CURVE ( 'NONE', #225, #10490, #14880, .T. ) ;
#6831=CARTESIAN_POINT ( 'NONE',  ( -13.43717355439436645, 49.88445258502782309, -1.313953709901692468 ) ) ;
#6833=CARTESIAN_POINT ( 'NONE',  ( 13.37133377648401833, 63.49501688011058320, -1.859467621360270995 ) ) ;
#6834=CARTESIAN_POINT ( 'NONE',  ( 12.29909249565109874, 42.22626233038081978, 5.566308865609547851 ) ) ;
#6840=EDGE_LOOP ( 'NONE', ( #1015, #3183, #2106, #10298 ) ) ;
#6841=CARTESIAN_POINT ( 'NONE',  ( -8.711585423346765111, 43.51545218957856775, -10.31301875482525432 ) ) ;
#6842=CARTESIAN_POINT ( 'NONE',  ( -7.499999999999997335, 107.2276959944579886, 6.931232109908918027 ) ) ;
#6843=CARTESIAN_POINT ( 'NONE',  ( 10.55993636637368915, 60.75057338229004245, -8.410584490247227762 ) ) ;
#6845=CARTESIAN_POINT ( 'NONE',  ( 9.788623329136655116, 72.06825703125207383, 9.296935394730732938 ) ) ;
#6846=CARTESIAN_POINT ( 'NONE',  ( 12.07674395289608427, 66.65302372406806342, -6.058184999537175486 ) ) ;
#6847=CARTESIAN_POINT ( 'NONE',  ( 5.007094059867902125, 56.86068527283545393, 12.53717015245978139 ) ) ;
#6848=CARTESIAN_POINT ( 'NONE',  ( 11.76794919243112680, 73.58000000000001251, -3.823638476888993942 ) ) ;
#6849=CARTESIAN_POINT ( 'NONE',  ( 11.76794919243112680, 70.58000000000001251, -3.823638476888993942 ) ) ;
#6851=CARTESIAN_POINT ( 'NONE',  ( -11.31822579835496434, 47.20583829161283518, 7.358718820380858006 ) ) ;
#6852=CARTESIAN_POINT ( 'NONE',  ( 5.395622418065101122, 45.98446605595357539, -12.37542908175213796 ) ) ;
#6855=CARTESIAN_POINT ( 'NONE',  ( -2.328902225919929236, 56.59619329505072471, 13.29813340977210778 ) ) ;
#6858=CARTESIAN_POINT ( 'NONE',  ( 11.94107144633697892, 33.66270217958954447, -6.298310357517227231 ) ) ;
#6859=CARTESIAN_POINT ( 'NONE',  ( -9.645889337515697548, 73.56097694870044279, -9.444937062324340715 ) ) ;
#6860=LINE ( 'NONE', #5801, #14230 ) ;
#6863=CARTESIAN_POINT ( 'NONE',  ( -8.343458848123578520, 42.47999999999999687, -11.48378591275254124 ) ) ;
#6866=CARTESIAN_POINT ( 'NONE',  ( -13.48209528736951768, 40.90592558830504544, -0.6972090822305906377 ) ) ;
#6869=CARTESIAN_POINT ( 'NONE',  ( -11.51090208011366478, 44.19368821836776817, 7.064733831953415866 ) ) ;
#6871=CARTESIAN_POINT ( 'NONE',  ( 10.92172942406178926, 42.13000000000000256, 7.935100905948387684 ) ) ;
#6872=CARTESIAN_POINT ( 'NONE',  ( -13.49999999999999822, 48.77999999999998693, -4.386415899144240349 ) ) ;
#6873=CARTESIAN_POINT ( 'NONE',  ( -13.49787322744430362, 70.92177515562346457, -0.2398385319287087425 ) ) ;
#6877=CARTESIAN_POINT ( 'NONE',  ( -2.941772209709978103, 67.28577460440457969, -13.17558263144108466 ) ) ;
#6879=B_SPLINE_CURVE_WITH_KNOTS ( 'NONE', 3,
 ( #10983, #10893, #13616, #16353, #9669, #16443, #8428, #15019, #2911, #7013, #13781, #1680, #7096, #366, #5771, #11155, #16531, #4438, #14048, #538, #16620, #5863, #4698, #15280, #8603, #4524, #15540, #7265, #1770, #626, #9931, #15366, #12649, #12738, #4870, #12567, #3363, #3181, #453, #7359, #1936, #8689, #11242, #11591, #10273, #795, #14219, #16792, #12827, #11328, #13955, #1852, #6037, #5948, #15624, #16706, #4611, #10018, #12911, #3272, #11420, #15454, #8867, #10103, #8779, #7179, #14135, #2023, #7448, #2104, #714, #6125, #11504, #16880, #4785, #10186, #16967, #3452, #7531, #6205, #3532, #13868, #4903, #14335, #574, #12858, #7478, #4816, #6235, #8895, #5981, #658, #12684, #3481, #4731, #15655, #2136, #1967, #2224, #10302, #6067, #11363, #15313, #10050, #10217, #12598, #15400, #11450, #3308, #13988, #488, #16824, #14250, #11274, #8809, #4558, #9963, #5894, #7562, #10132, #16650, #15486, #3396, #8637, #1884, #12940, #14166, #7299, #16738, #8721, #3565, #748, #8979, #6322, #10646, #9417, #4001, #1256, #13029, #4990, #2480, #11797, #10564, #912, #11708, #13367, #14422, #9247, #2310, #17085, #7830, #17174, #10392, #16009, #14765, #7653, #5084, #6587, #15746, #3657, #9069, #11885, #7739 ),
 .UNSPECIFIED., .F., .F.,
 ( 4, 2, 2, 2, 2, 1, 1, 1, 2, 2, 2, 2, 1, 1, 2, 2, 1, 2, 2, 2, 2, 1, 1, 2, 2, 2, 2, 1, 2, 2, 1, 1, 2, 2, 1, 1, 1, 2, 2, 2, 2, 2, 1, 1, 1, 2, 2, 1, 2, 2, 2, 2, 1, 2, 2, 1, 1, 2, 2, 2, 2, 2, 2, 2, 2, 2, 1, 1, 2, 2, 1, 2, 2, 1, 2, 2, 2, 2, 1, 2, 2, 1, 2, 2, 2, 2, 1, 1, 1, 1, 1, 1, 2, 2, 2, 2, 2, 4 ),
 ( 0.6225616101408076863, 0.6262466207516538264, 0.6267072470780096216, 0.6268224036595985149, 0.6268367982322970988, 0.6268511928049957938, 0.6268799819503929616, 0.6269375602411875192, 0.6271678734043656389, 0.6280891260570777845, 0.6285497523834339129, 0.6287800655466120325, 0.6288952221282010369, 0.6289528004189955945, 0.6289671949916941784, 0.6289815895643928734, 0.6290103787097900412, 0.6299316313625022978, 0.6308528840152144435, 0.6310831971783924521, 0.6311119863237897309, 0.6311407754691870098, 0.6311983537599814564, 0.6313135103415704608, 0.6317741366679265891, 0.6326953893206387347, 0.6331560156469947520, 0.6332135939377891987, 0.6332279885104878936, 0.6332423830831864775, 0.6332711722285837563, 0.6333863288101727607, 0.6336166419733507693, 0.6345378946260628039, 0.6349985209524187102, 0.6352288341155967188, 0.6353439906971857232, 0.6353727798425830020, 0.6354015689879802808, 0.6354591472787747275, 0.6363803999314867621, 0.6373016525841987967, 0.6374168091657878010, 0.6374743874565823587, 0.6375031766019796375, 0.6375103738883288740, 0.6375175711746782214, 0.6375319657473768054, 0.6377622789105548140, 0.6382229052369109423, 0.6391441578896229769, 0.6396047842159791053, 0.6396335733613763841, 0.6396479679340749680, 0.6396551652204243155, 0.6396623625067735519, 0.6397199407975681096, 0.6398350973791571139, 0.6400654105423351226, 0.6409866631950471572, 0.6419079158477593028, 0.6421382290109373114, 0.6422533855925263158, 0.6423685421741153201, 0.6428291685004713374, 0.6432897948268273547, 0.6433473731176219124, 0.6433761622630190802, 0.6433905568357177751, 0.6434049514084163590, 0.6435201079900053633, 0.6437504211531833720, 0.6442110474795395003, 0.6444413606427175090, 0.6445565172243065133, 0.6446716738058955176, 0.6465141791113196978, 0.6469748054376757151, 0.6470899620192647195, 0.6471475403100592771, 0.6471763294554564450, 0.6472051186008537238, 0.6474354317640317324, 0.6483566844167438781, 0.6483854735621411569, 0.6484142627075384357, 0.6484718409983329934, 0.6485869975799219977, 0.6488173107431000064, 0.6492779370694561347, 0.6495082502326341434, 0.6496234068142231477, 0.6496521959596204265, 0.6496809851050177054, 0.6497385633958121520, 0.6501991897221682803, 0.6511204423748804260, 0.6520416950275925716 ),
 .UNSPECIFIED. ) ;
#6880=CARTESIAN_POINT ( 'NONE',  ( 12.86363371229788477, 54.28279489801139590, 4.098915096101688249 ) ) ;
#6881=CARTESIAN_POINT ( 'NONE',  ( -13.09608275284783296, 64.81328617085095800, -3.281779600780347916 ) ) ;
#6884=CARTESIAN_POINT ( 'NONE',  ( -13.21814477936476706, 34.83246129253718948, -2.760861401621048206 ) ) ;
#6886=CARTESIAN_POINT ( 'NONE',  ( 12.83398559654505533, 78.27937745505627731, 4.188225396753645136 ) ) ;
#6888=CARTESIAN_POINT ( 'NONE',  ( -5.362442804292004261, 31.37413780983099798, -12.38972965817070993 ) ) ;
#6889=CARTESIAN_POINT ( 'NONE',  ( 8.302743629395873626, 72.86345579277633533, -10.64494644169182003 ) ) ;
#6890=CARTESIAN_POINT ( 'NONE',  ( 2.612430725649731666, 59.77398820739121987, 13.24767911791428432 ) ) ;
#6892=CARTESIAN_POINT ( 'NONE',  ( 8.343458848123583849, 72.88000000000000966, -11.48378591275253768 ) ) ;
#6893=CARTESIAN_POINT ( 'NONE',  ( -11.56380442966215050, 52.67022467909172434, -6.968482334245324594 ) ) ;
#6894=CARTESIAN_POINT ( 'NONE',  ( 9.520470885617717371, 52.72999999999999687, -6.917026985038131848 ) ) ;
#6895=CARTESIAN_POINT ( 'NONE',  ( 13.49999999999999822, 71.28000000000000114, 4.386415899144237684 ) ) ;
#6897=CARTESIAN_POINT ( 'NONE',  ( 11.67283399857811155, 69.68278107398599275, -6.798365021777054373 ) ) ;
#6898=CARTESIAN_POINT ( 'NONE',  ( -12.91217337725079517, 37.78870154777813894, -3.941070675155305292 ) ) ;
#6900=CARTESIAN_POINT ( 'NONE',  ( 5.972235571882229976, 35.89753408868532603, 12.11506502541500296 ) ) ;
#6902=CARTESIAN_POINT ( 'NONE',  ( -12.28445251099280355, 74.13502960058168867, 5.602360786159263917 ) ) ;
#6903=CARTESIAN_POINT ( 'NONE',  ( -13.49315368495419065, 76.90577415051416210, -0.6964660162547660072 ) ) ;
#6904=CARTESIAN_POINT ( 'NONE',  ( -4.960630769662208728, 79.35887515246722046, -12.55750558105645354 ) ) ;
#6905=CARTESIAN_POINT ( 'NONE',  ( -3.565931047812489929, 80.93000000000003524, 12.36697741789239480 ) ) ;
#6908=CARTESIAN_POINT ( 'NONE',  ( -11.76794919243112325, 45.08000000000000540, 3.823638476888994830 ) ) ;
#6910=CARTESIAN_POINT ( 'NONE',  ( -9.982813566452611198, 40.57839600760536314, -9.089889854899778854 ) ) ;
#6912=CARTESIAN_POINT ( 'NONE',  ( 13.06332958711276859, 75.55131820085146899, -3.405797684387579238 ) ) ;
#6914=CARTESIAN_POINT ( 'NONE',  ( -9.593668878646951725, 41.30170092094060408, 9.501538401032471270 ) ) ;
#6915=CARTESIAN_POINT ( 'NONE',  ( -4.434027931263471167, 58.33950993581493094, -12.75153076942259034 ) ) ;
#6917=CARTESIAN_POINT ( 'NONE',  ( 2.904295422893758527, 44.78442768824688613, 13.18389593751376410 ) ) ;
#6922=CARTESIAN_POINT ( 'NONE',  ( -13.47928820673223527, 49.90421348230867693, -0.7476691059968105790 ) ) ;
#6923=CARTESIAN_POINT ( 'NONE',  ( 12.10713279764149775, 63.65069317145754724, -6.000162191947801205 ) ) ;
#6924=CARTESIAN_POINT ( 'NONE',  ( 12.35813771356544422, 42.23148437247772335, 5.433829964281000180 ) ) ;
#6925=CARTESIAN_POINT ( 'NONE',  ( 6.741586065090841018, 38.92882405296342085, 11.69831271653080584 ) ) ;
#6926=VERTEX_POINT ( 'NONE', #337 ) ;
#6929=ORIENTED_EDGE ( 'NONE', *, *, #7092, .F. ) ;
#6930=CARTESIAN_POINT ( 'NONE',  ( -9.339320245421074418, 43.54553106418224928, -9.750580036500519299 ) ) ;
#6931=CARTESIAN_POINT ( 'NONE',  ( -7.499999999999999112, 103.4461236652718696, 9.346045933502388436 ) ) ;
#6932=CARTESIAN_POINT ( 'NONE',  ( 12.04411969963108220, 60.65532207379116159, -6.117687879866321232 ) ) ;
#6935=CARTESIAN_POINT ( 'NONE',  ( 0.000000000000000000, 102.9300000000000068, 0.000000000000000000 ) ) ;
#6936=CARTESIAN_POINT ( 'NONE',  ( 11.58799853746032227, 66.68808562819272368, -6.925914820338668676 ) ) ;
#6937=CARTESIAN_POINT ( 'NONE',  ( 2.660236471785744961, 56.77572940497019260, 13.23661507586563779 ) ) ;
#6938=CARTESIAN_POINT ( 'NONE',  ( 9.520470885617717371, 55.73000000000000398, -6.917026985038131848 ) ) ;
#6939=CARTESIAN_POINT ( 'NONE',  ( 3.636496289402154414, 66.82999999999999829, 11.19198476289190936 ) ) ;
#6940=CARTESIAN_POINT ( 'NONE',  ( -12.01013503625162215, 47.15762422974843560, 6.171082197149440951 ) ) ;
#6942=CARTESIAN_POINT ( 'NONE',  ( -2.838270712586780596E-14, 67.18000000000000682, -13.50000000000000178 ) ) ;
#6944=CARTESIAN_POINT ( 'NONE',  ( -8.547853120570341190, 56.35218660269319457, 10.44914891313210070 ) ) ;
#6947=CARTESIAN_POINT ( 'NONE',  ( 12.03035526396323363, 33.65579982725444097, -6.125565056414373544 ) ) ;
#6948=B_SPLINE_CURVE_WITH_KNOTS ( 'NONE', 3,
 ( #687, #14362, #14279, #4674, #3592, #10165, #10079, #11481, #14451, #1029, #3425, #10331, #15430, #15685, #11734, #2338, #7590, #6180, #17112, #11394, #11566, #3339, #6262, #7422, #8754, #16940, #15774, #17026, #8840, #14197, #10416, #9098, #3507, #10246, #1995, #4842, #4930, #16766, #15599, #16856, #4759, #2250, #2079, #7504, #8920, #2165, #12969, #16208, #1202, #9271, #2684, #17287, #5199, #7852, #14707, #11908, #12163, #17203, #5458, #6530, #14623, #10671, #14877, #5111, #2419, #15951, #3943, #54, #15866, #3773, #17455, #16119, #14534, #5289, #6696, #16035, #1116, #13311, #9358, #10841, #13393, #11993, #11823, #6440, #6613, #5369, #2509, #13227, #8204, #4119, #10589, #9533, #13566, #3857, #10756, #10504, #4030, #8115, #2773, #2596, #17375, #9186, #7939, #8025, #1282, #12076, #9444, #14792, #13481, #1369, #6784, #234, #5640, #15234, #3130, #11108, #317, #145, #13736, #7134, #9969, #493, #14972, #12342, #1721, #11022, #4296, #5900, #16394, #9709, #11279, #1634, #15053, #8555, #2953, #8381, #2862, #9796, #6964, #7217, #12250, #11197, #8642, #8470, #5726, #15317, #5551, #8294, #7051, #16481, #12604, #10934, #16301, #12522, #16573, #9621, #4385, #406, #15142, #13651, #12431, #1803, #3039, #16656, #13820, #6877, #1457, #5813, #4478, #9884, #1545, #3220, #4563, #13908, #4208, #10398, #11456, #10310, #7484, #3665, #6243, #1890, #6076, #16832, #2147, #15755, #13995, #17004 ),
 .UNSPECIFIED., .F., .F.,
 ( 4, 2, 1, 1, 2, 2, 1, 2, 2, 2, 1, 1, 2, 2, 2, 2, 2, 2, 2, 2, 1, 1, 1, 1, 1, 2, 2, 2, 1, 2, 2, 1, 1, 1, 2, 2, 2, 2, 2, 1, 1, 2, 2, 2, 2, 2, 2, 1, 1, 2, 1, 1, 2, 2, 2, 2, 1, 1, 1, 2, 2, 2, 2, 2, 2, 2, 2, 2, 2, 1, 1, 1, 2, 1, 2, 2, 1, 1, 2, 1, 2, 2, 1, 1, 2, 2, 2, 2, 1, 2, 2, 2, 2, 2, 1, 1, 2, 2, 1, 1, 2, 2, 1, 1, 1, 2, 2, 2, 2, 1, 2, 2, 1, 2, 4 ),
 ( 0.2402135124365048502, 0.2406730745069247945, 0.2409028555421347806, 0.2410177460597397736, 0.2410464686891410080, 0.2410751913185422701, 0.2411326365773447389, 0.2420517607181846276, 0.2429708848590244885, 0.2432006658942344468, 0.2432581111530369433, 0.2432868337824382055, 0.2433011950971388226, 0.2433155564118394398, 0.2434304469294444606, 0.2438900089998645160, 0.2448091331407046545, 0.2457282572815447930, 0.2466473814223849315, 0.2466617427370855764, 0.2466761040517861936, 0.2467048266811874557, 0.2467622719399899522, 0.2468771624575949730, 0.2471069434928050146, 0.2475665055632250700, 0.2494047538449053469, 0.2498643159153254301, 0.2499792064329304508, 0.2499935677476310680, 0.2500007484049813766, 0.2500079290623317130, 0.2500366516917329474, 0.2500940969505354716, 0.2503238779857455132, 0.2512430021265857349, 0.2517025641970058181, 0.2519323452322158596, 0.2519610678616171495, 0.2519897904910183839, 0.2520472357498209082, 0.2521621262674259567, 0.2530812504082661785, 0.2535408124786862616, 0.2537705935138963587, 0.2538854840315013517, 0.2539142066609026416, 0.2539429292903038760, 0.2540003745491064002, 0.2544599366195265389, 0.2546897176547365804, 0.2548046081723416290, 0.2548620534311440977, 0.2549194986899466220, 0.2558386228307868437, 0.2558673454601880781, 0.2558960680895893680, 0.2559535133483918923, 0.2560684038659968853, 0.2562981849012069269, 0.2567577469716270100, 0.2576768711124672318, 0.2577917616300722248, 0.2579066521476772733, 0.2581364331828873149, 0.2585959952533073980, 0.2595151193941475642, 0.2597449004293576058, 0.2597736230587588957, 0.2598023456881601301, 0.2598597909469626543, 0.2599746814645676474, 0.2604342435349877305, 0.2606640245701977721, 0.2607214698290002963, 0.2607501924584015307, 0.2607789150878028206, 0.2608938056054078136, 0.2613533676758278412, 0.2615831487110378828, 0.2616980392286428758, 0.2617267618580441657, 0.2617554844874454001, 0.2618129297462479244, 0.2622724918166679520, 0.2631916159575080072, 0.2636511780279280348, 0.2637660685455330833, 0.2638809590631380764, 0.2641107400983480624, 0.2650298642391881176, 0.2654894263096081453, 0.2656043168272131938, 0.2656330394566144282, 0.2656617620860157181, 0.2657192073448181868, 0.2659489883800282284, 0.2668681125208683391, 0.2673276745912884222, 0.2675574556264984638, 0.2675718169411990810, 0.2675789975985494173, 0.2675861782558996982, 0.2676149008853009881, 0.2676723461441035123, 0.2677872366617085609, 0.2687063608025491157, 0.2691659228729693654, 0.2693957039081795179, 0.2695105944257845665, 0.2695249557404851837, 0.2695321363978355200, 0.2695393170551858009, 0.2695680396845870908, 0.2696254849433896150 ),
 .UNSPECIFIED. ) ;
#6957=CARTESIAN_POINT ( 'NONE',  ( -13.46697175398167978, 43.89732407946095805, -0.9441447902741053610 ) ) ;
#6959=CARTESIAN_POINT ( 'NONE',  ( 8.343458848123583849, 30.87999999999999901, -11.48378591275253768 ) ) ;
#6960=CARTESIAN_POINT ( 'NONE',  ( -13.10414842226016496, 71.04706212969732348, 3.294509102343420093 ) ) ;
#6962=B_SPLINE_CURVE_WITH_KNOTS ( 'NONE', 3,
 ( #14921, #16076, #12202, #14748, #4158, #13686, #2814, #12032, #17411, #5326, #7004, #4, #3983, #10796, #10973, #16434, #95, #187, #6736, #8419, #6824, #5593, #6650, #5409, #14831, #10710, #1500, #9398, #16341, #16160, #13605, #5500, #9571, #2637, #8068, #10883, #15090, #1320, #6914, #13432, #16253, #12291, #1586, #4249, #12115, #4070, #9485, #12380, #2725, #9659, #8153, #13518, #1409, #2900, #8331, #271, #2989, #1238, #5680, #11060, #4336, #9745, #17192, #6606, #5102, #5191, #17366, #5280, #13472, #3934, #9436, #14785, #8107, #1358, #11013, #43, #16564, #15225, #2943, #310, #5540, #1797, #7209, #14962, #5449, #16384, #16197, #6866, #4110, #10924, #12242, #2852, #4200, #8286, #9611, #226, #7296, #12681, #571, #5978, #11360, #16735, #8240, #10789, #4986, #5405, #2306, #6820, #2720, #12109, #12197, #6318, #857, #5588, #16336, #17081, #15742, #10388, #3653, #9391, #9065, #14418, #907, #4153, #13110, #2632, #7734, #16247, #16155, #9653, #14915, #14742, #15003, #6910, #4064, #10876, #7649, #13025, #17170, #90, #11704, #997, #6410, #9480, #11793, #8063, #5080, #14826, #10475, #15835, #13512, #3740, #1404, #5495, #9565, #12286, #13065, #9014, #12979, #15696, #3435, #6272, #14372, #12896, #5029, #3517, #2349, #11491, #6450, #2089, #10175, #783, #1039, #6190, #7516, #11834, #10256, #11577, #11746, #16952, #15788, #2007, #10429 ),
 .UNSPECIFIED., .F., .F.,
 ( 4, 2, 2, 1, 2, 2, 1, 2, 2, 2, 2, 2, 1, 1, 2, 2, 1, 1, 1, 2, 2, 1, 1, 2, 2, 2, 2, 2, 1, 1, 1, 2, 2, 2, 1, 1, 2, 2, 1, 2, 2, 2, 2, 1, 2, 2, 1, 2, 2, 2, 1, 1, 2, 2, 2, 1, 1, 2, 2, 2, 2, 2, 2, 2, 2, 2, 2, 2, 1, 1, 1, 1, 2, 2, 1, 1, 1, 2, 2, 1, 2, 2, 2, 2, 1, 1, 2, 2, 2, 2, 2, 2, 2, 2, 1, 2, 2, 1, 2, 2, 2, 2, 1, 2, 2, 1, 2, 2, 4 ),
 ( 0.7695219113824839363, 0.7713661461956111687, 0.7722882636021747293, 0.7725187929538156473, 0.7726340576296361062, 0.7726916899675463357, 0.7727493223054565652, 0.7732103810087384010, 0.7741324984153019617, 0.7745935571185837976, 0.7747088217944042565, 0.7747376379633593713, 0.7747664541323144860, 0.7748240864702247155, 0.7750546158218656334, 0.7759767332284291941, 0.7764377919317110299, 0.7766683212833518368, 0.7767259536212620663, 0.7767403617057396792, 0.7767475657479784301, 0.7767547697902171810, 0.7767835859591722958, 0.7768988506349927547, 0.7778209680415559824, 0.7787430854481192100, 0.7787574935325967118, 0.7787719016170743247, 0.7788007177860294394, 0.7788583501239395579, 0.7789736147997600169, 0.7792041441514008238, 0.7796652028546823265, 0.7805873202612454431, 0.7807025849370659021, 0.7807602172749760205, 0.7807890334439311353, 0.7808034415284087482, 0.7808178496128862500, 0.7810483789645270569, 0.7815094376678085597, 0.7824315550743716763, 0.7826620844260124832, 0.7827773491018328311, 0.7828061652707879459, 0.7828349814397430606, 0.7828926137776531791, 0.7833536724809347929, 0.7838147311842162956, 0.7839299958600367546, 0.7840452605358571025, 0.7842757898874979094, 0.7847368485907794122, 0.7848521132665998712, 0.7848809294355548749, 0.7849097456045099896, 0.7849673779424202191, 0.7851979072940610260, 0.7861200247006241426, 0.7865810834039056454, 0.7868116127555464523, 0.7868692450934566818, 0.7869268774313668002, 0.7870421421071872592, 0.7879642595137503758, 0.7888863769203133813, 0.7889151930892684961, 0.7889296011737461090, 0.7889440092582236108, 0.7890016415961338403, 0.7891169062719541882, 0.7893474356235949951, 0.7898084943268767200, 0.7907306117334399476, 0.7908458764092602955, 0.7909035087471705250, 0.7909323249161256397, 0.7909467330006031416, 0.7909539370428418925, 0.7909611410850807545, 0.7911916704367216724, 0.7916527291400033972, 0.7925748465465670689, 0.7928053758982079868, 0.7929206405740284458, 0.7929494567429835605, 0.7929638648274611734, 0.7929782729119386753, 0.7930359052498489048, 0.7934969639531307406, 0.7944190813596944123, 0.7948801400629762481, 0.7949954047387967071, 0.7950530370767069366, 0.7951106694146171661, 0.7953411987662580840, 0.7958022574695399198, 0.7959175221453603788, 0.7959751544832706083, 0.7960327868211808378, 0.7962633161728217557, 0.7967243748761035915, 0.7969549042277445094, 0.7970125365656547389, 0.7970413527346098537, 0.7970701689035649684, 0.7971854335793854274, 0.7981075509859490991, 0.7990296683925127708 ),
 .UNSPECIFIED. ) ;
#6964=CARTESIAN_POINT ( 'NONE',  ( -9.084995278830836796, 67.53291598612975122, -9.998823687146330741 ) ) ;
#6966=CARTESIAN_POINT ( 'NONE',  ( 12.91186397080207549, 54.28858565486373067, 3.944841525484266587 ) ) ;
#6967=CARTESIAN_POINT ( 'NONE',  ( -10.31666293591003480, 64.59608009038818466, -8.707265613171941254 ) ) ;
#6970=CARTESIAN_POINT ( 'NONE',  ( -13.46595428245841042, 34.89684888571769505, -0.9600937702945907537 ) ) ;
#6972=CARTESIAN_POINT ( 'NONE',  ( 13.47848861578399138, 78.45635379196389181, -0.7637651279454616970 ) ) ;
#6973=FACE_OUTER_BOUND ( 'NONE', #2307, .T. ) ;
#6974=AXIS2_PLACEMENT_3D ( 'NONE', #737, #8711, #16813 ) ;
#6977=CARTESIAN_POINT ( 'NONE',  ( 4.754929249172622718, 73.00875652715450315, -12.63496230640105189 ) ) ;
#6979=EDGE_CURVE ( 'NONE', #7754, #14613, #3048, .T. ) ;
#6981=CARTESIAN_POINT ( 'NONE',  ( 4.171729424061789260, 74.83000000000001251, 12.83926296998457417 ) ) ;
#6982=CARTESIAN_POINT ( 'NONE',  ( -11.24005743194561546, 52.64918859648530969, -7.477416982239327936 ) ) ;
#6983=CARTESIAN_POINT ( 'NONE',  ( 9.520470885617717371, 43.72999999999999687, -6.917026985038131848 ) ) ;
#6984=CARTESIAN_POINT ( 'NONE',  ( -8.343458848123582072, 67.37999999999998124, 11.48378591275254124 ) ) ;
#6986=CARTESIAN_POINT ( 'NONE',  ( 11.61110246750533292, 69.17349466423988247, 6.887194277108547702 ) ) ;
#6990=CARTESIAN_POINT ( 'NONE',  ( -13.08483029837249845, 74.04834311179649831, 3.325739040386578971 ) ) ;
#6991=CARTESIAN_POINT ( 'NONE',  ( -11.07543414285489902, 76.63905281824719395, -7.719769595326448020 ) ) ;
#6997=CARTESIAN_POINT ( 'NONE',  ( -7.272992578804310604, 51.37999999999998835, 10.01041549318726886 ) ) ;
#7000=CARTESIAN_POINT ( 'NONE',  ( 10.94004585081460768, 75.13044969108922544, 7.925841433480270481 ) ) ;
#7003=CARTESIAN_POINT ( 'NONE',  ( -7.576616670048093940E-16, 33.67999999999999972, 12.37355403259654985 ) ) ;
#7004=CARTESIAN_POINT ( 'NONE',  ( -4.368811843459432964, 41.52287850255721935, 12.77356621052920893 ) ) ;
#7005=CARTESIAN_POINT ( 'NONE',  ( 5.349201313263153068, 51.98641939972569759, -12.39963371175743490 ) ) ;
#7006=CARTESIAN_POINT ( 'NONE',  ( -7.122634015147881748, 38.41518589931285987, 11.46826829916993873 ) ) ;
#7007=CARTESIAN_POINT ( 'NONE',  ( -8.343458848123578520, 54.48000000000001108, -11.48378591275254124 ) ) ;
#7010=CARTESIAN_POINT ( 'NONE',  ( -6.622037744496604539, 49.42396662578299527, -11.76708925107785753 ) ) ;
#7011=CARTESIAN_POINT ( 'NONE',  ( 11.53816879259289685, 63.16854332020811569, 7.008656503616835565 ) ) ;
#7012=CARTESIAN_POINT ( 'NONE',  ( 10.32716819451351498, 42.09648712927666736, 8.701702194760818188 ) ) ;
#7013=CARTESIAN_POINT ( 'NONE',  ( 5.937526285386327984, 48.96352261484946666, -12.12418171604482353 ) ) ;
#7014=EDGE_LOOP ( 'NONE', ( #11832, #651, #906, #2870 ) ) ;
#7015=CARTESIAN_POINT ( 'NONE',  ( -9.520470885617715595, 74.62999999999999545, -6.917026985038136289 ) ) ;
#7020=CARTESIAN_POINT ( 'NONE',  ( -11.53224498248871122, 43.66710377932096776, -7.048982063341345139 ) ) ;
#7021=CARTESIAN_POINT ( 'NONE',  ( -7.500000000000000000, 107.4971863040494213, 6.484415072061723961 ) ) ;
#7022=CARTESIAN_POINT ( 'NONE',  ( 6.365913562993081420, 60.94642428639450316, -11.90484108844855804 ) ) ;
#7026=CARTESIAN_POINT ( 'NONE',  ( 13.50062667129575722, 66.42363412073690654, 0.1755086108962339297 ) ) ;
#7027=CARTESIAN_POINT ( 'NONE',  ( 1.467847692288238193, 56.73277838508402482, 13.41996759063894373 ) ) ;
#7028=CARTESIAN_POINT ( 'NONE',  ( 9.520470885617715595, 64.12999999999999545, 6.917026985038134512 ) ) ;
#7029=CARTESIAN_POINT ( 'NONE',  ( -3.636496289402153081, 68.32999999999999829, -11.19198476289190936 ) ) ;
#7030=CARTESIAN_POINT ( 'NONE',  ( -13.49150454620358275, 46.94646972587323575, 0.4788601354586907166 ) ) ;
#7032=CARTESIAN_POINT ( 'NONE',  ( 2.138189944381248875, 73.75688142232027644, 13.49999999999999645 ) ) ;
#7033=CARTESIAN_POINT ( 'NONE',  ( 9.477935110687690567, 30.80768188101512806, -9.621815863905913702 ) ) ;
#7035=CARTESIAN_POINT ( 'NONE',  ( -3.315231683446368205, 56.56075311393848182, 13.08712957443356117 ) ) ;
#7038=CARTESIAN_POINT ( 'NONE',  ( 11.44289832574866139, 33.69789852399187424, -7.163812845423511710 ) ) ;
#7042=EDGE_LOOP ( 'NONE', ( #8194, #4742, #9280, #5977 ) ) ;
#7043=CARTESIAN_POINT ( 'NONE',  ( -4.489940415681219044, 62.51839048220814021, 12.73204617180344300 ) ) ;
#7044=ORIENTED_EDGE ( 'NONE', *, *, #4192, .F. ) ;
#7047=CARTESIAN_POINT ( 'NONE',  ( -13.47256314982935166, 43.95974442004008154, 0.8609111014920134419 ) ) ;
#7049=CARTESIAN_POINT ( 'NONE',  ( 8.343458848123578520, 32.97999999999999687, 11.48378591275254124 ) ) ;
#7050=CARTESIAN_POINT ( 'NONE',  ( 1.708800344670653191E-06, 35.68004753840243382, 13.49999999999978328 ) ) ;
#7051=CARTESIAN_POINT ( 'NONE',  ( -5.995605309098753999, 67.39875943548146608, -12.09707223761978412 ) ) ;
#7053=CARTESIAN_POINT ( 'NONE',  ( 11.53575417012443616, 54.69162266907183323, -7.012590288925422577 ) ) ;
#7054=ADVANCED_FACE ( 'NONE', ( #7069 ), #4584, .F. ) ;
#7055=CARTESIAN_POINT ( 'NONE',  ( -9.572234266482416487, 64.55715410289911915, -9.527515327432464431 ) ) ;
#7057=CARTESIAN_POINT ( 'NONE',  ( -13.38605536481362890, 34.99161834286027783, 1.764857785377393684 ) ) ;
#7059=CARTESIAN_POINT ( 'NONE',  ( 11.85483473061306015, 78.19086039256470144, 6.458558312265882506 ) ) ;
#7060=CARTESIAN_POINT ( 'NONE',  ( 13.50000000000000355, 47.57999999999999119, -4.386415899144233244 ) ) ;
#7062=CARTESIAN_POINT ( 'NONE',  ( 5.236401750311364900, 72.99073825183825193, -12.44474146415180904 ) ) ;
#7063=CARTESIAN_POINT ( 'NONE',  ( 1.086230788847387219, 79.14096883825459372, -13.45868988004304612 ) ) ;
#7065=CARTESIAN_POINT ( 'NONE',  ( 13.50000000000000355, 60.57999999999998408, -4.386415899144233244 ) ) ;
#7066=CARTESIAN_POINT ( 'NONE',  ( -13.00272673885899266, 53.06012234098268721, 3.637067801120180022 ) ) ;
#7067=CARTESIAN_POINT ( 'NONE',  ( 11.76794919243112325, 40.27999999999998693, 3.823638476888996607 ) ) ;
#7068=CARTESIAN_POINT ( 'NONE',  ( -8.343458848123582072, 58.38000000000000256, 11.48378591275254124 ) ) ;
#7069=FACE_OUTER_BOUND ( 'NONE', #8525, .T. ) ;
#7070=CARTESIAN_POINT ( 'NONE',  ( 12.70536037991022305, 69.26510775276948095, 4.563833866671145323 ) ) ;
#7071=CARTESIAN_POINT ( 'NONE',  ( -2.012210829378426435, 37.25231257445182109, -13.35686934311003959 ) ) ;
#7074=CARTESIAN_POINT ( 'NONE',  ( -10.25778635652197224, 74.26711310232562369, 8.777052303075189243 ) ) ;
#7075=CARTESIAN_POINT ( 'NONE',  ( -4.990650801110085411, 76.36006663702048058, -12.54403061954694110 ) ) ;
#7077=CARTESIAN_POINT ( 'NONE',  ( 0.000000000000000000, 80.93000000000000682, 0.000000000000000000 ) ) ;
#7078=CARTESIAN_POINT ( 'NONE',  ( -11.42802927808057767, 80.93000000000002103, 3.799729825752809820 ) ) ;
#7081=CARTESIAN_POINT ( 'NONE',  ( -7.272992578804310604, 33.38000000000000256, 10.01041549318726886 ) ) ;
#7083=CARTESIAN_POINT ( 'NONE',  ( -8.740054970619736352, 32.34338933063859400, 10.29130291274103470 ) ) ;
#7084=CARTESIAN_POINT ( 'NONE',  ( 12.75897847405612318, 75.26823319679101587, 4.501030925202505806 ) ) ;
#7086=CARTESIAN_POINT ( 'NONE',  ( -11.76794919243112325, 32.77999999999999403, -3.823638476888998827 ) ) ;
#7088=CARTESIAN_POINT ( 'NONE',  ( 0.5526492435590804053, 52.16013233706370045, -13.49040056943439581 ) ) ;
#7090=CARTESIAN_POINT ( 'NONE',  ( 0.09524022798341912066, 37.17657551321138953, -13.49966522572602301 ) ) ;
#7092=EDGE_CURVE ( 'NONE', #13300, #5695, #12220, .T. ) ;
#7094=CARTESIAN_POINT ( 'NONE',  ( 12.18353207652669923, 63.21590633337540055, 5.835071146089095606 ) ) ;
#7095=CARTESIAN_POINT ( 'NONE',  ( 13.21374623997747122, 42.52811597142575550, -2.775631991069858806 ) ) ;
#7096=CARTESIAN_POINT ( 'NONE',  ( 5.970456528392105611, 48.96224137250303698, -12.10801974513590906 ) ) ;
#7098=ORIENTED_EDGE ( 'NONE', *, *, #5375, .T. ) ;
#7099=CARTESIAN_POINT ( 'NONE',  ( -9.520470885617715595, 71.62999999999999545, -6.917026985038136289 ) ) ;
#7103=EDGE_LOOP ( 'NONE', ( #1682, #10561, #16383, #16909 ) ) ;
#7104=CARTESIAN_POINT ( 'NONE',  ( -6.177155207478421062, 43.40604133974412093, -12.00656696816257885 ) ) ;
#7105=CARTESIAN_POINT ( 'NONE',  ( -7.499999999999997335, 105.3828822090421085, 8.693347190813732084 ) ) ;
#7106=CARTESIAN_POINT ( 'NONE',  ( 13.10225137871006673, 60.54575384758864232, -3.255519868551609353 ) ) ;
#7109=CARTESIAN_POINT ( 'NONE',  ( 11.78404408794452074, 66.18568652898561311, 6.586852905507519118 ) ) ;
#7110=CARTESIAN_POINT ( 'NONE',  ( 3.262996936836821682, 56.79731715246284551, 13.09972757844540858 ) ) ;
#7111=CARTESIAN_POINT ( 'NONE',  ( -11.76794919243112325, 62.92999999999999972, -2.882316262207890869E-15 ) ) ;
#7112=CARTESIAN_POINT ( 'NONE',  ( -11.76794919243112325, 66.07999999999999829, 3.823638476888994386 ) ) ;
#7113=CARTESIAN_POINT ( 'NONE',  ( -12.65132248824962602, 46.75933051274522256, -4.715090284878137972 ) ) ;
#7114=CARTESIAN_POINT ( 'NONE',  ( 12.41168389898173707, 45.62405102665109524, -5.326589421794383661 ) ) ;
#7115=CARTESIAN_POINT ( 'NONE',  ( 10.92172942406178926, 74.12999999999999545, 7.935100905948387684 ) ) ;
#7116=CARTESIAN_POINT ( 'NONE',  ( 1.468262939039568948, 31.12731509695948873, -13.42493789908898094 ) ) ;
#7117=CARTESIAN_POINT ( 'NONE',  ( -2.973838119809171232, 56.57298728218007966, 13.17046594805706050 ) ) ;
#7120=CARTESIAN_POINT ( 'NONE',  ( 8.740325781130335869, 33.01677564961078559, 10.29107445509964336 ) ) ;
#7122=CARTESIAN_POINT ( 'NONE',  ( 4.295754402788634962, 40.02552785855749562, -12.79831863505647860 ) ) ;
#7125=CARTESIAN_POINT ( 'NONE',  ( -9.353866460873140554, 62.31375578855443109, 9.736707939222794650 ) ) ;
#7128=CARTESIAN_POINT ( 'NONE',  ( -13.24414797687638057, 44.02231978228942921, 2.615972014630898457 ) ) ;
#7130=CARTESIAN_POINT ( 'NONE',  ( 10.92172942406179104, 65.72999999999998977, -7.935100905948385908 ) ) ;
#7131=CARTESIAN_POINT ( 'NONE',  ( -9.520470885617715595, 83.62999999999999545, -6.917026985038136289 ) ) ;
#7132=CARTESIAN_POINT ( 'NONE',  ( -4.171729424061787483, 48.32999999999999829, -12.83926296998457417 ) ) ;
#7133=CARTESIAN_POINT ( 'NONE',  ( -6.200018879092032975, 46.40684524066041661, -11.99220497138590602 ) ) ;
#7134=CARTESIAN_POINT ( 'NONE',  ( -11.15157066607664049, 67.64369004200317192, -7.609460659245025127 ) ) ;
#7138=CARTESIAN_POINT ( 'NONE',  ( 11.05849770819798117, 54.13800262379849215, 7.750384364272157711 ) ) ;
#7139=CARTESIAN_POINT ( 'NONE',  ( -10.33389146060662078, 64.59699217978335639, -8.686821934247454635 ) ) ;
#7140=ORIENTED_EDGE ( 'NONE', *, *, #4192, .T. ) ;
#7141=CARTESIAN_POINT ( 'NONE',  ( -8.388358401731302649, 34.50044823484911660, -10.57791826008529767 ) ) ;
#7143=CARTESIAN_POINT ( 'NONE',  ( 11.87658369898086086, 78.19247217947236095, 6.418497554539179362 ) ) ;
#7144=DIRECTION ( 'NONE',  ( -1.000000000000000000, -1.734723475976807094E-16, -0.000000000000000000 ) ) ;
#7146=CARTESIAN_POINT ( 'NONE',  ( 12.77798252166430792, 72.27295531305313148, 4.357763951314068684 ) ) ;
#7147=CARTESIAN_POINT ( 'NONE',  ( 4.953551091470167478, 79.00132416387516798, -12.55835749735045859 ) ) ;
#7149=CARTESIAN_POINT ( 'NONE',  ( -10.92172942406178926, 58.63000000000000256, -7.935100905948389460 ) ) ;
#7150=CARTESIAN_POINT ( 'NONE',  ( -13.49426538080809834, 52.94671897916216352, 0.4876541610707976759 ) ) ;
#7152=CARTESIAN_POINT ( 'NONE',  ( 9.520470885617715595, 37.12999999999999545, 6.917026985038134512 ) ) ;
#7153=CARTESIAN_POINT ( 'NONE',  ( 13.49999999999999822, 56.27999999999999403, 4.386415899144237684 ) ) ;
#7154=CARTESIAN_POINT ( 'NONE',  ( 2.138189944381236884, 78.10311857767972299, -13.50000000000000000 ) ) ;
#7156=CARTESIAN_POINT ( 'NONE',  ( 3.700846756827888218, 68.81299210504440111, 12.98334767858451677 ) ) ;
#7157=CARTESIAN_POINT ( 'NONE',  ( -0.2970657467180017886, 37.19068138831143955, -13.50000000000001066 ) ) ;
#7160=CARTESIAN_POINT ( 'NONE',  ( -12.51477381949817413, 73.74582926830240126, -5.065646498870927772 ) ) ;
#7161=CARTESIAN_POINT ( 'NONE',  ( -2.278090379941454025, 76.26191102292980872, -13.30664668557865760 ) ) ;
#7162=FACE_OUTER_BOUND ( 'NONE', #15, .T. ) ;
#7166=CARTESIAN_POINT ( 'NONE',  ( 3.636496289402157078, 35.03000000000000114, -11.19198476289190936 ) ) ;
#7168=CARTESIAN_POINT ( 'NONE',  ( -9.429961120686421339, 32.30986108813164037, 9.660530610400291707 ) ) ;
#7169=CARTESIAN_POINT ( 'NONE',  ( 13.32338872245472849, 75.35360622757792726, 2.176581829586916594 ) ) ;
#7171=CARTESIAN_POINT ( 'NONE',  ( -3.636496289402153081, 32.32999999999999829, -11.19198476289190936 ) ) ;
#7172=CARTESIAN_POINT ( 'NONE',  ( 10.04873594665206937, 51.77822116537775088, -9.015151377439948988 ) ) ;
#7173=CARTESIAN_POINT ( 'NONE',  ( -4.644322785898420847, 38.51283592794423072, 12.67769253242001959 ) ) ;
#7174=CARTESIAN_POINT ( 'NONE',  ( 6.594030187424503531, 36.93740925139908171, -11.79378183334034880 ) ) ;
#7175=CARTESIAN_POINT ( 'NONE',  ( 0.000000000000000000, 3.999999999999961808, 0.000000000000000000 ) ) ;
#7177=CARTESIAN_POINT ( 'NONE',  ( 7.072526022525592815, 62.94270560853125573, 11.49911144502164895 ) ) ;
#7178=CARTESIAN_POINT ( 'NONE',  ( 12.46071941648464332, 42.24086282136816095, 5.195455325495793808 ) ) ;
#7179=CARTESIAN_POINT ( 'NONE',  ( 13.30280394725709314, 48.51140726369936829, -2.319129228756254157 ) ) ;
#7182=CARTESIAN_POINT ( 'NONE',  ( 3.636496289402154414, 69.82999999999999829, 11.19198476289190936 ) ) ;
#7186=CARTESIAN_POINT ( 'NONE',  ( -10.09708985121333136, 43.58387330091565559, -8.971927331284039298 ) ) ;
#7190=CARTESIAN_POINT ( 'NONE',  ( 11.79401460576306526, 66.18640916527446905, 6.568962329648897480 ) ) ;
#7191=CARTESIAN_POINT ( 'NONE',  ( 10.77767612607841485, 57.12170114078097782, 8.130105570404699833 ) ) ;
#7193=CARTESIAN_POINT ( 'NONE',  ( 3.636496289402154414, 63.82999999999999829, 11.19198476289190936 ) ) ;
#7194=CARTESIAN_POINT ( 'NONE',  ( 13.49999999999999822, 32.27999999999999403, 4.386415899144237684 ) ) ;
#7195=CARTESIAN_POINT ( 'NONE',  ( -3.636496289402155746, 66.53000000000000114, 11.19198476289190936 ) ) ;
#7196=CARTESIAN_POINT ( 'NONE',  ( -11.34494330406672624, 46.65582902796952425, -7.317300534094159481 ) ) ;
#7197=CARTESIAN_POINT ( 'NONE',  ( 5.569239368393173351, 45.97791013593247555, -12.29771055457881879 ) ) ;
#7198=CARTESIAN_POINT ( 'NONE',  ( -4.023268246324633536E-14, 60.18000000000000682, -13.50000000000000000 ) ) ;
#7200=CARTESIAN_POINT ( 'NONE',  ( 0.06185192672290352328, 31.17777603289167843, -13.49999999999999467 ) ) ;
#7203=CARTESIAN_POINT ( 'NONE',  ( 10.54218125873905443, 33.10822676551072163, 8.435822891053812000 ) ) ;
#7205=CARTESIAN_POINT ( 'NONE',  ( 5.219660855938430544, 39.99127885146727834, -12.45468320406492069 ) ) ;
#7207=CARTESIAN_POINT ( 'NONE',  ( -13.46448297031965247, 61.96386121747416098, 0.9786549340198757996 ) ) ;
#7209=CARTESIAN_POINT ( 'NONE',  ( -13.49062013346076938, 40.94740657223831448, 0.5061247442112529749 ) ) ;
#7211=CARTESIAN_POINT ( 'NONE',  ( -12.43644091682779163, 44.12163909514725191, 5.256796654357501986 ) ) ;
#7212=CARTESIAN_POINT ( 'NONE',  ( 4.171729424061791924, 66.03000000000000114, -12.83926296998457239 ) ) ;
#7213=CARTESIAN_POINT ( 'NONE',  ( 13.49999999999999822, 33.27999999999999403, 4.386415899144237684 ) ) ;
#7214=CARTESIAN_POINT ( 'NONE',  ( 2.607531440858944223E-15, 42.17999999999999261, -14.19474002721660355 ) ) ;
#7215=EDGE_CURVE ( 'NONE', #568, #668, #14109, .T. ) ;
#7217=CARTESIAN_POINT ( 'NONE',  ( -8.495721255044264453, 67.50532034020808680, -10.49469503808201765 ) ) ;
#7219=CARTESIAN_POINT ( 'NONE',  ( 8.925127373670504127, 54.02551875695034056, 10.13307151360432634 ) ) ;
#7221=CARTESIAN_POINT ( 'NONE',  ( -7.708711337361060956, 64.46994343615379819, -11.08696526454483333 ) ) ;
#7224=CARTESIAN_POINT ( 'NONE',  ( -10.19850433080654639, 34.58972380950302750, -8.845366638170691687 ) ) ;
#7226=CARTESIAN_POINT ( 'NONE',  ( 10.50252084001531117, 78.10619439663850017, 8.482238275819085516 ) ) ;
#7229=CARTESIAN_POINT ( 'NONE',  ( 13.37722696026129832, 72.36650144554805308, 1.816547976767812322 ) ) ;
#7232=CARTESIAN_POINT ( 'NONE',  ( 4.171729424061789260, 59.82999999999999119, 12.83926296998457417 ) ) ;
#7233=CARTESIAN_POINT ( 'NONE',  ( -8.842990959453766564, 52.52165125223628195, -10.20056964289610058 ) ) ;
#7235=CARTESIAN_POINT ( 'NONE',  ( 11.76794919243112325, 37.42999999999999972, 1.441158131103945434E-15 ) ) ;
#7236=CARTESIAN_POINT ( 'NONE',  ( 8.343458848123583849, 59.87999999999998835, -11.48378591275253768 ) ) ;
#7239=CARTESIAN_POINT ( 'NONE',  ( 11.75284362809797223, 69.18342969977395285, 6.642835211192756439 ) ) ;
#7241=CARTESIAN_POINT ( 'NONE',  ( 1.395181907640911101, 35.73016548663857606, 13.42772203881113846 ) ) ;
#7243=CARTESIAN_POINT ( 'NONE',  ( -13.48320498675965595, 73.90678838288567931, -0.6742141303992607027 ) ) ;
#7245=CARTESIAN_POINT ( 'NONE',  ( -4.659656022607111758, 76.34776334268970288, -12.67034846265207726 ) ) ;
#7246=CYLINDRICAL_SURFACE ( 'NONE', #7899, 13.50000000000000000 ) ;
#7251=CARTESIAN_POINT ( 'NONE',  ( -11.76794919243112325, 42.07999999999999829, 3.823638476888994830 ) ) ;
#7253=CARTESIAN_POINT ( 'NONE',  ( -4.222908164277692222, 32.52819618069426610, 12.82270994545682186 ) ) ;
#7254=CARTESIAN_POINT ( 'NONE',  ( -8.891200544363830713E-16, 37.67999999999999261, 13.50000000000000000 ) ) ;
#7255=CARTESIAN_POINT ( 'NONE',  ( 13.49999999999999822, 62.28000000000000824, 4.386415899144236796 ) ) ;
#7257=CARTESIAN_POINT ( 'NONE',  ( 13.50000000000000000, 83.43000000000000682, 1.653273178848926867E-15 ) ) ;
#7258=CARTESIAN_POINT ( 'NONE',  ( 9.335235950531815854E-15, 58.17999999999999972, -13.50000000000000178 ) ) ;
#7259=CARTESIAN_POINT ( 'NONE',  ( -4.357703367820035645, 38.52328190763838478, 12.77734288095807713 ) ) ;
#7260=CARTESIAN_POINT ( 'NONE',  ( 5.801264985213661518, 36.96892180672517014, -12.19006904687155313 ) ) ;
#7261=CARTESIAN_POINT ( 'NONE',  ( -13.50000000000000000, 69.93000000000000682, -3.306546357697853733E-15 ) ) ;
#7262=LINE ( 'NONE', #12646, #2705 ) ;
#7263=CARTESIAN_POINT ( 'NONE',  ( 11.56743521769684158, 63.17051234748981159, 6.960209698953964796 ) ) ;
#7264=CARTESIAN_POINT ( 'NONE',  ( 8.112166317082673217, 41.98791513809585751, 10.79114295580683702 ) ) ;
#7265=CARTESIAN_POINT ( 'NONE',  ( 8.998313441448996031, 48.83125608138507801, -10.07864022935939374 ) ) ;
#7269=CARTESIAN_POINT ( 'NONE',  ( 7.272992578804311492, 67.87999999999998124, -10.01041549318726886 ) ) ;
#7273=CARTESIAN_POINT ( 'NONE',  ( -0.01386867818632892685, 43.18049866634735423, -13.49999465302926716 ) ) ;
#7274=CARTESIAN_POINT ( 'NONE',  ( 8.446640517145640834E-14, 43.67999999999999972, 13.50000000000000000 ) ) ;
#7278=CARTESIAN_POINT ( 'NONE',  ( 8.606806894175420553, 66.01052269069948863, 10.40195802859246577 ) ) ;
#7280=CARTESIAN_POINT ( 'NONE',  ( -3.636496289402155746, 63.53000000000000114, 11.19198476289190936 ) ) ;
#7281=CARTESIAN_POINT ( 'NONE',  ( -10.92172942406178926, 33.63000000000000256, -7.935100905948389460 ) ) ;
#7282=CARTESIAN_POINT ( 'NONE',  ( 11.76794919243112325, 61.27999999999999403, 3.823638476888996607 ) ) ;
#7283=CARTESIAN_POINT ( 'NONE',  ( -13.35791772474320815, 46.86141354909250367, -1.958702153931820567 ) ) ;
#7284=CARTESIAN_POINT ( 'NONE',  ( 11.35334624979329909, 45.70351276252048933, -7.307357026597509631 ) ) ;
#7287=CARTESIAN_POINT ( 'NONE',  ( 11.25043742152392312, 30.71012671521651427, -7.461806818123373652 ) ) ;
#7288=CARTESIAN_POINT ( 'NONE',  ( -13.43724082756498639, 55.88450770272648782, -1.312471336124251930 ) ) ;
#7289=CARTESIAN_POINT ( 'NONE',  ( 0.000000000000000000, 80.93000000000000682, 0.000000000000000000 ) ) ;
#7290=CARTESIAN_POINT ( 'NONE',  ( 9.155616606007495051, 33.03665467976623660, 9.920960544697097205 ) ) ;
#7292=CARTESIAN_POINT ( 'NONE',  ( 10.31333816299139805, 39.76410056892473222, -8.711213421668183798 ) ) ;
#7293=VERTEX_POINT ( 'NONE', #598 ) ;
#7294=CARTESIAN_POINT ( 'NONE',  ( -10.96121799096760974, 62.22774600049994831, 7.881493374224405102 ) ) ;
#7296=CARTESIAN_POINT ( 'NONE',  ( -13.27118709707405131, 40.84240854419702771, -2.487365594126258017 ) ) ;
#7299=CARTESIAN_POINT ( 'NONE',  ( 8.173436778830255989, 47.99018683713303091, 10.78145662369851898 ) ) ;
#7300=CARTESIAN_POINT ( 'NONE',  ( 13.49999999999999822, 65.28000000000000114, 4.386415899144236796 ) ) ;
#7301=CARTESIAN_POINT ( 'NONE',  ( -10.92172942406179104, 32.22999999999999687, 7.935100905948387684 ) ) ;
#7302=CARTESIAN_POINT ( 'NONE',  ( -4.171729424061787483, 39.32999999999999829, -12.83926296998457417 ) ) ;
#7304=CARTESIAN_POINT ( 'NONE',  ( -9.620510893913072792, 46.55969245225834641, -9.470785098964443094 ) ) ;
#7305=PLANE ( 'NONE',  #16703 ) ;
#7307=CARTESIAN_POINT ( 'NONE',  ( 10.81364905848734104, 54.12376407303845127, 8.082190041977272088 ) ) ;
#7309=CARTESIAN_POINT ( 'NONE',  ( -6.109331651355537574, 64.40329291578021298, -12.03877916920419366 ) ) ;
#7311=ORIENTED_EDGE ( 'NONE', *, *, #13864, .F. ) ;
#7312=CARTESIAN_POINT ( 'NONE',  ( 0.5902846111940708296, 67.15877554305052399, -13.50000000000000178 ) ) ;
#7313=CARTESIAN_POINT ( 'NONE',  ( -5.644265419545289042, 34.38500592501070230, -12.26351404149298752 ) ) ;
#7316=CARTESIAN_POINT ( 'NONE',  ( 8.676621035646554958, 78.01381292210301410, 10.34245816167857690 ) ) ;
#7318=CARTESIAN_POINT ( 'NONE',  ( 12.50000000000000000, 98.93000000000002103, 1.224646799147353059E-15 ) ) ;
#7319=FACE_OUTER_BOUND ( 'NONE', #4264, .T. ) ;
#7320=CARTESIAN_POINT ( 'NONE',  ( 11.41197208916220518, 72.16015570436597670, 7.212546593606687040 ) ) ;
#7322=CARTESIAN_POINT ( 'NONE',  ( 10.92172942406178926, 60.13000000000000256, 7.935100905948387684 ) ) ;
#7323=CARTESIAN_POINT ( 'NONE',  ( -5.816118839772840055, 52.39170762701569828, -12.18289214338606818 ) ) ;
#7324=CARTESIAN_POINT ( 'NONE',  ( -7.272992578804310604, 36.37999999999998835, 10.01041549318726709 ) ) ;
#7326=CARTESIAN_POINT ( 'NONE',  ( 10.92172942406178926, 53.12999999999999545, 7.935100905948387684 ) ) ;
#7330=CARTESIAN_POINT ( 'NONE',  ( 11.69227698284627337, 69.17914002359731285, 6.748504071555379902 ) ) ;
#7334=CARTESIAN_POINT ( 'NONE',  ( -13.35524205937507602, 73.86096575848492307, -1.971718875867300103 ) ) ;
#7335=CARTESIAN_POINT ( 'NONE',  ( -2.392111896138028104, 76.26601152105787662, -13.28637674647000821 ) ) ;
#7337=CARTESIAN_POINT ( 'NONE',  ( -4.441163314466836098, 79.33975151259672032, -12.74869167447762308 ) ) ;
#7341=CARTESIAN_POINT ( 'NONE',  ( 9.520470885617715595, 37.12999999999999545, 6.917026985038134512 ) ) ;
#7346=CARTESIAN_POINT ( 'NONE',  ( 5.918455295475054889, 74.89572671431407969, 12.13351137210443653 ) ) ;
#7348=CARTESIAN_POINT ( 'NONE',  ( 13.49791439481672839, 60.43900620806144275, -0.2626274307333924529 ) ) ;
#7350=CARTESIAN_POINT ( 'NONE',  ( 4.171729424061789260, 82.82999999999999829, 12.83926296998457417 ) ) ;
#7351=CARTESIAN_POINT ( 'NONE',  ( -2.420164038214338120, 58.26702013926823298, -13.28133895319109747 ) ) ;
#7353=CARTESIAN_POINT ( 'NONE',  ( -4.373507997709555895, 38.52270764513675516, 12.77194180747198615 ) ) ;
#7356=DIRECTION ( 'NONE',  ( -1.000000000000000000, -0.000000000000000000, -0.000000000000000000 ) ) ;
#7357=CARTESIAN_POINT ( 'NONE',  ( 9.628276390875990742, 63.06008494831254296, 9.462902099174160142 ) ) ;
#7358=CARTESIAN_POINT ( 'NONE',  ( 5.447755521502024578, 41.87741670420104612, 12.35200281313600001 ) ) ;
#7359=CARTESIAN_POINT ( 'NONE',  ( 11.05250497172135304, 48.72225972937487626, -7.756270235652836575 ) ) ;
#7361=ORIENTED_EDGE ( 'NONE', *, *, #13479, .F. ) ;
#7362=CARTESIAN_POINT ( 'NONE',  ( 3.636496289402154414, 63.82999999999999829, 11.19198476289190936 ) ) ;
#7366=CARTESIAN_POINT ( 'NONE',  ( 0.7057993694291405662, 80.92999999999997840, -13.10211957505608638 ) ) ;
#7368=CARTESIAN_POINT ( 'NONE',  ( 10.20702290661970579, 66.09018350808118214, 8.835545813414038108 ) ) ;
#7371=CARTESIAN_POINT ( 'NONE',  ( 11.76794919243112680, 46.57999999999999829, -3.823638476888993942 ) ) ;
#7372=CARTESIAN_POINT ( 'NONE',  ( 13.50000000000000000, 32.42999999999999972, 1.653273178848926867E-15 ) ) ;
#7373=CARTESIAN_POINT ( 'NONE',  ( 9.520470885617717371, 58.73000000000000398, -6.917026985038131848 ) ) ;
#7374=CARTESIAN_POINT ( 'NONE',  ( -13.42542795491608310, 46.98152504557900500, 1.474995282428532395 ) ) ;
#7376=CARTESIAN_POINT ( 'NONE',  ( 11.92132692379593628, 45.66421514304773410, -6.337276081506336922 ) ) ;
#7377=CARTESIAN_POINT ( 'NONE',  ( 6.262084934075358156, 69.95073729743167235, -11.96369458021704446 ) ) ;
#7379=CARTESIAN_POINT ( 'NONE',  ( 5.816537829104611923, 30.96824124766034103, -12.18269343281530048 ) ) ;
#7380=CARTESIAN_POINT ( 'NONE',  ( -12.17509508611693292, 55.71589168976755957, -5.832679525784597807 ) ) ;
#7381=CARTESIAN_POINT ( 'NONE',  ( -2.463123716452229051, 50.59134218680501505, 13.27377621386196260 ) ) ;
#7382=DIRECTION ( 'NONE',  ( 0.000000000000000000, 0.000000000000000000, -1.000000000000000000 ) ) ;
#7383=CARTESIAN_POINT ( 'NONE',  ( 4.662704016964861253, 43.01217040675273040, -12.67144116224080719 ) ) ;
#7384=CARTESIAN_POINT ( 'NONE',  ( 9.961534293312238830, 39.78284768016499839, -9.113236095871735998 ) ) ;
#7386=CARTESIAN_POINT ( 'NONE',  ( -13.45835841592290016, 61.96676735775977107, 1.061614036730301525 ) ) ;
#7392=CARTESIAN_POINT ( 'NONE',  ( 4.964042911967482929, 58.00092663269024484, -12.55448936394250303 ) ) ;
#7393=CARTESIAN_POINT ( 'NONE',  ( -7.272992578804307939, 77.48000000000000398, -10.01041549318726886 ) ) ;
#7394=CARTESIAN_POINT ( 'NONE',  ( -4.171729424061787483, 42.32999999999999829, -12.83926296998457417 ) ) ;
#7396=CARTESIAN_POINT ( 'NONE',  ( -6.293574425437782338, 46.41065374424994161, -11.94324194161466934 ) ) ;
#7399=CARTESIAN_POINT ( 'NONE',  ( 4.934664456648047981, 53.85797222871626388, 12.56582013419890664 ) ) ;
#7402=EDGE_LOOP ( 'NONE', ( #12126, #6687, #3492, #6620 ) ) ;
#7405=CARTESIAN_POINT ( 'NONE',  ( -6.892083252854373399, 34.43494372278320981, -11.62035706217954889 ) ) ;
#7407=CARTESIAN_POINT ( 'NONE',  ( 7.127680621519133730, 77.94494083559413866, 11.47363209226457492 ) ) ;
#7411=CARTESIAN_POINT ( 'NONE',  ( 12.99914974011805668, 72.56016066728088276, -3.643509121896943093 ) ) ;
#7413=CARTESIAN_POINT ( 'NONE',  ( 4.171729424061791924, 64.03000000000000114, -12.83926296998457239 ) ) ;
#7414=CARTESIAN_POINT ( 'NONE',  ( -2.186818166953001796, 52.25862599162246624, -13.32198785724745527 ) ) ;
#7416=CARTESIAN_POINT ( 'NONE',  ( 11.76794919243112325, 34.42999999999999261, 1.441158131103945434E-15 ) ) ;
#7418=CARTESIAN_POINT ( 'NONE',  ( 4.171729424061791924, 54.03000000000000114, -12.83926296998457239 ) ) ;
#7422=CARTESIAN_POINT ( 'NONE',  ( -4.433484632589104635, 68.52052440024017699, 12.75127848232592775 ) ) ;
#7426=CARTESIAN_POINT ( 'NONE',  ( -13.47341305627475272, 73.90037531866931886, -0.8597925056511297459 ) ) ;
#7427=CARTESIAN_POINT ( 'NONE',  ( -7.413775151259285323, 76.45717531281798074, -11.28405773006812574 ) ) ;
#7431=CARTESIAN_POINT ( 'NONE',  ( 7.272992578804308828, 33.97999999999999687, 10.01041549318726886 ) ) ;
#7433=AXIS2_PLACEMENT_3D ( 'NONE', #7175, #1766, #8685 ) ;
#7434=CARTESIAN_POINT ( 'NONE',  ( -5.829253055094191005, 32.46794701112467862, 12.18592114757813327 ) ) ;
#7435=CARTESIAN_POINT ( 'NONE',  ( 1.327664892297638843, 74.72773790534441218, 13.43455645011153621 ) ) ;
#7437=CARTESIAN_POINT ( 'NONE',  ( -13.50000000000000000, 78.93000000000000682, -3.306546357697853733E-15 ) ) ;
#7439=CARTESIAN_POINT ( 'NONE',  ( 11.63962625337223145, 51.68454806329603457, -6.839222346739858516 ) ) ;
#7440=CARTESIAN_POINT ( 'NONE',  ( -12.73620748938531833, 38.09169207387569855, 4.479728807359646403 ) ) ;
#7442=CARTESIAN_POINT ( 'NONE',  ( 11.22854147624287435, 36.71152521474294872, -7.494658285005058040 ) ) ;
#7446=CARTESIAN_POINT ( 'NONE',  ( 0.1518789328228659086, 62.68546100971695978, 13.49937261551957590 ) ) ;
#7447=FACE_OUTER_BOUND ( 'NONE', #3302, .T. ) ;
#7448=CARTESIAN_POINT ( 'NONE',  ( 13.49806724646292899, 48.45090782768691895, -0.6033653513361341147 ) ) ;
#7451=CARTESIAN_POINT ( 'NONE',  ( -7.272992578804307939, 68.48000000000000398, -10.01041549318727064 ) ) ;
#7455=CARTESIAN_POINT ( 'NONE',  ( -0.02772103388578331384, 43.18099674618451189, -13.49997331539339562 ) ) ;
#7456=CARTESIAN_POINT ( 'NONE',  ( 0.7664276751979015589, 76.15244233678546948, -13.47830342854411079 ) ) ;
#7458=CARTESIAN_POINT ( 'NONE',  ( 6.534285954687437226, 65.92034066636635714, 11.81874242131197050 ) ) ;
#7459=CARTESIAN_POINT ( 'NONE',  ( -10.92172942406178926, 82.62999999999999545, -7.935100905948389460 ) ) ;
#7460=CARTESIAN_POINT ( 'NONE',  ( 7.272992578804308828, 45.98000000000000398, 10.01041549318726709 ) ) ;
#7462=CARTESIAN_POINT ( 'NONE',  ( -12.41832812777009920, 59.12332451315333515, 5.299458117618179642 ) ) ;
#7463=CARTESIAN_POINT ( 'NONE',  ( 13.04194034339959885, 45.55439597745233726, -3.489029769191362096 ) ) ;
#7464=CARTESIAN_POINT ( 'NONE',  ( 10.10108856181172143, 69.77545969696819839, -8.956536834962969706 ) ) ;
#7466=CARTESIAN_POINT ( 'NONE',  ( 12.67585016484028948, 30.59854293864694696, -4.663455345598352508 ) ) ;
#7467=CARTESIAN_POINT ( 'NONE',  ( -13.50529826739625783, 55.92983664685408485, 2.178437852371490542E-05 ) ) ;
#7468=CARTESIAN_POINT ( 'NONE',  ( 4.171729424061791924, 54.03000000000000114, -12.83926296998457239 ) ) ;
#7469=CARTESIAN_POINT ( 'NONE',  ( 9.829015088374500664, 63.78966567892446449, -9.254229041624375540 ) ) ;
#7470=CARTESIAN_POINT ( 'NONE',  ( 1.486569204522005805, 43.12668836574830067, -13.41992218948748317 ) ) ;
#7471=CARTESIAN_POINT ( 'NONE',  ( 9.048820653867387875, 39.82882913570732342, -10.03219236511709056 ) ) ;
#7472=EDGE_LOOP ( 'NONE', ( #14520, #6270, #6536, #6470 ) ) ;
#7473=CARTESIAN_POINT ( 'NONE',  ( -11.09391357339225337, 62.21979212502633771, 7.692540733092653404 ) ) ;
#7478=CARTESIAN_POINT ( 'NONE',  ( 13.07592573315582385, 48.31048427460937944, 3.357180248748443674 ) ) ;
#7479=CARTESIAN_POINT ( 'NONE',  ( 10.48295876490647593, 57.75483760623548335, -8.506347226123828875 ) ) ;
#7480=CARTESIAN_POINT ( 'NONE',  ( 10.57584348060936286, 78.74972999058537937, -8.393457333304862544 ) ) ;
#7481=CARTESIAN_POINT ( 'NONE',  ( 11.76794919243112325, 79.28000000000001535, 3.823638476888996607 ) ) ;
#7484=CARTESIAN_POINT ( 'NONE',  ( -0.2663380794371886795, 67.18957635750793145, -13.49772504475413193 ) ) ;
#7487=CARTESIAN_POINT ( 'NONE',  ( 11.62722211559520424, 54.17461734033530973, 6.859929859063566226 ) ) ;
#7488=VERTEX_POINT ( 'NONE', #12320 ) ;
#7490=ORIENTED_EDGE ( 'NONE', *, *, #9438, .T. ) ;
#7491=CARTESIAN_POINT ( 'NONE',  ( 6.758386942186555224, 66.93077324841343057, -11.70470293470154921 ) ) ;
#7493=EDGE_CURVE ( 'NONE', #8734, #6926, #9425, .T. ) ;
#7494=FACE_OUTER_BOUND ( 'NONE', #15199, .T. ) ;
#7498=CARTESIAN_POINT ( 'NONE',  ( 11.59770818944004134, 72.17250917721062820, 6.911720118166459592 ) ) ;
#7500=CARTESIAN_POINT ( 'NONE',  ( -4.171729424061787483, 52.32999999999999829, -12.83926296998457417 ) ) ;
#7501=CARTESIAN_POINT ( 'NONE',  ( -5.864567678274497986, 52.39362192653054962, -12.15966658976413584 ) ) ;
#7502=CARTESIAN_POINT ( 'NONE',  ( 2.607531440858944223E-15, 51.18000000000000682, -14.19474002721660355 ) ) ;
#7504=CARTESIAN_POINT ( 'NONE',  ( -11.34163888740973825, 68.20410188839301213, 7.325683172086050909 ) ) ;
#7508=CARTESIAN_POINT ( 'NONE',  ( -8.342243388378552282, 65.36176465702267535, 10.61802124403202541 ) ) ;
#7512=EDGE_CURVE ( 'NONE', #15397, #10663, #5001, .T. ) ;
#7514=CARTESIAN_POINT ( 'NONE',  ( -11.76794919243112325, 33.07999999999999119, 3.823638476888994830 ) ) ;
#7516=CARTESIAN_POINT ( 'NONE',  ( -2.869462971216817593, 40.28317531134132423, -13.19152261891324684 ) ) ;
#7517=CARTESIAN_POINT ( 'NONE',  ( -12.91569140150223483, 31.78915324831410771, -3.928925989131344387 ) ) ;
#7518=CARTESIAN_POINT ( 'NONE',  ( 3.660164850489102228, 74.81160598410180285, 12.99436167334853387 ) ) ;
#7521=CARTESIAN_POINT ( 'NONE',  ( 13.50000000000000355, 77.58000000000001251, -4.386415899144233244 ) ) ;
#7522=CARTESIAN_POINT ( 'NONE',  ( 13.09516998140269806, 51.54708633261468265, -3.291187128613837665 ) ) ;
#7523=VECTOR ( 'NONE', #17165, 1000.000000000000000 ) ;
#7524=CARTESIAN_POINT ( 'NONE',  ( -13.34762704780204601, 38.00086476210552888, 2.022771026582171672 ) ) ;
#7525=CARTESIAN_POINT ( 'NONE',  ( 11.32356926193947722, 36.70559104637850822, -7.350409248560260345 ) ) ;
#7528=CARTESIAN_POINT ( 'NONE',  ( -3.390861109279693419, 77.55806408242118266, 13.06768226514972397 ) ) ;
#7530=CARTESIAN_POINT ( 'NONE',  ( 8.270203509715585710, 41.99506318914406222, 10.67024559312394949 ) ) ;
#7531=CARTESIAN_POINT ( 'NONE',  ( 13.48921303027230323, 48.41115837036991110, 0.5474105875851942304 ) ) ;
#7534=CARTESIAN_POINT ( 'NONE',  ( 2.272985001014427393E-15, 62.17999999999999972, -12.37355403259654807 ) ) ;
#7536=DIRECTION ( 'NONE',  ( 0.000000000000000000, 0.000000000000000000, -1.000000000000000000 ) ) ;
#7537=ADVANCED_FACE ( 'NONE', ( #8008 ), #9007, .T. ) ;
#7539=CARTESIAN_POINT ( 'NONE',  ( -4.886222543804722207, 80.92999999999999261, -11.77926528190734423 ) ) ;
#7540=CARTESIAN_POINT ( 'NONE',  ( -7.576616670048093940E-16, 33.67999999999999972, 12.37355403259654985 ) ) ;
#7543=CARTESIAN_POINT ( 'NONE',  ( 10.92172942406178926, 78.13000000000000966, 7.935100905948387684 ) ) ;
#7544=CARTESIAN_POINT ( 'NONE',  ( -9.520470885617717371, 45.22999999999999687, 6.917026985038133624 ) ) ;
#7545=CARTESIAN_POINT ( 'NONE',  ( -9.957257356812577953, 59.28301542262214952, 9.116086396973207329 ) ) ;
#7546=CARTESIAN_POINT ( 'NONE',  ( 12.67739711398077596, 45.26084057892622070, 4.680113183824990308 ) ) ;
#7548=CARTESIAN_POINT ( 'NONE',  ( 3.904524039968586990, 80.82037356980362119, 12.92421824227555760 ) ) ;
#7549=CARTESIAN_POINT ( 'NONE',  ( 13.49560925073025430, 30.44260291568510013, -0.3671350940585685896 ) ) ;
#7550=CARTESIAN_POINT ( 'NONE',  ( -13.45459026473954545, 55.96837007948868603, 1.107234817202036092 ) ) ;
#7552=CARTESIAN_POINT ( 'NONE',  ( 9.123705676088246008, 63.82520120319571078, -9.962466972052720138 ) ) ;
#7554=CARTESIAN_POINT ( 'NONE',  ( 11.95191421947951227, 39.66185529926528375, -6.277088439489496352 ) ) ;
#7556=CARTESIAN_POINT ( 'NONE',  ( -7.444042646070399449, 61.45851055580283173, -11.26259205123165863 ) ) ;
#7558=EDGE_CURVE ( 'NONE', #149, #2392, #16369, .T. ) ;
#7562=CARTESIAN_POINT ( 'NONE',  ( 10.48475946639971923, 48.10524804026067613, 8.504759123327721326 ) ) ;
#7564=CARTESIAN_POINT ( 'NONE',  ( 2.430993506533023485, 58.09259044382305603, -13.27931747540271701 ) ) ;
#7565=CARTESIAN_POINT ( 'NONE',  ( 11.05296802401333700, 78.72228217906655345, -7.752379973867670415 ) ) ;
#7566=CARTESIAN_POINT ( 'NONE',  ( 11.76794919243112680, 76.57999999999998408, -3.823638476888993942 ) ) ;
#7567=CARTESIAN_POINT ( 'NONE',  ( -8.691771469529815392E-16, 40.67999999999999972, 14.19474002721660355 ) ) ;
#7573=CARTESIAN_POINT ( 'NONE',  ( -13.49999999999999822, 78.78000000000000114, -4.386415899144240349 ) ) ;
#7574=CARTESIAN_POINT ( 'NONE',  ( 3.084857733306134442, 34.06908001793591723, -13.14282405559487721 ) ) ;
#7582=FACE_OUTER_BOUND ( 'NONE', #8805, .T. ) ;
#7583=CARTESIAN_POINT ( 'NONE',  ( 2.445080149700053643E-15, 39.17999999999999972, -13.50000000000000000 ) ) ;
#7584=CARTESIAN_POINT ( 'NONE',  ( 2.479997878773285702, 71.76914845574894741, 13.27026003324255932 ) ) ;
#7585=CARTESIAN_POINT ( 'NONE',  ( 8.343458848123578520, 50.97999999999999687, 11.48378591275254124 ) ) ;
#7586=CARTESIAN_POINT ( 'NONE',  ( -0.3693890974730637544, 71.66671813216132136, 13.49494611521610388 ) ) ;
#7590=CARTESIAN_POINT ( 'NONE',  ( -4.236652733600446474, 68.52767330046546590, 12.81802689691797248 ) ) ;
#7592=CARTESIAN_POINT ( 'NONE',  ( 5.205044219673900407, 54.99195532384126750, -12.45725450968071435 ) ) ;
#7595=CARTESIAN_POINT ( 'NONE',  ( -4.275606992132293449, 65.52616433460548251, 12.83507194185807343 ) ) ;
#7596=CYLINDRICAL_SURFACE ( 'NONE', #3660, 13.50000000000000000 ) ;
#7597=CARTESIAN_POINT ( 'NONE',  ( -10.81341862071700888, 35.23731261369557899, 8.112425484178327650 ) ) ;
#7602=CARTESIAN_POINT ( 'NONE',  ( -13.34330937586820198, 32.00188493264690948, 2.051126618964131065 ) ) ;
#7603=CARTESIAN_POINT ( 'NONE',  ( 7.833167725097554879, 74.97547919491985624, 10.99603809193803805 ) ) ;
#7604=CARTESIAN_POINT ( 'NONE',  ( 13.49758425966062170, 60.40291432109311387, 0.7880808366232104900 ) ) ;
#7606=CARTESIAN_POINT ( 'NONE',  ( 13.50000000000000000, 62.42999999999999972, 1.653273178848926867E-15 ) ) ;
#7608=AXIS2_PLACEMENT_3D ( 'NONE', #1240, #6653, #16162 ) ;
#7610=CARTESIAN_POINT ( 'NONE',  ( 10.92172942406178926, 74.12999999999999545, 7.935100905948387684 ) ) ;
#7611=CARTESIAN_POINT ( 'NONE',  ( 13.47580859582107671, 51.45868852590849940, -0.8310248978193689462 ) ) ;
#7612=CARTESIAN_POINT ( 'NONE',  ( -12.66827453022257721, 38.09892961922952281, 4.669650815327920590 ) ) ;
#7613=CARTESIAN_POINT ( 'NONE',  ( 11.60544498200051322, 36.68704456685242121, -6.899790396877484078 ) ) ;
#7616=CARTESIAN_POINT ( 'NONE',  ( -3.875797842856171904, 77.54063790311734294, 12.93175633931209134 ) ) ;
#7617=CARTESIAN_POINT ( 'NONE',  ( -2.094509993892973210, 80.60457276769930957, 13.33968883972704944 ) ) ;
#7618=CARTESIAN_POINT ( 'NONE',  ( 5.374832067266447133, 41.87461798944549685, 12.38404490627867105 ) ) ;
#7619=ORIENTED_EDGE ( 'NONE', *, *, #6216, .T. ) ;
#7620=CIRCLE ( 'NONE', #1106, 12.00000000000000178 ) ;
#7623=CARTESIAN_POINT ( 'NONE',  ( 11.76794919243112325, 58.42999999999999261, 1.441158131103945434E-15 ) ) ;
#7625=CARTESIAN_POINT ( 'NONE',  ( 2.138189944381238661, 55.75688142232026934, 13.50000000000000000 ) ) ;
#7626=CARTESIAN_POINT ( 'NONE',  ( 1.921271214528800453, 76.11093797914737991, -13.37211609379623667 ) ) ;
#7628=CARTESIAN_POINT ( 'NONE',  ( 1.293886105031521572, 65.72652579852442045, 13.44153297767990018 ) ) ;
#7630=CARTESIAN_POINT ( 'NONE',  ( 11.76794919243112325, 52.28000000000000114, 3.823638476888996607 ) ) ;
#7632=CARTESIAN_POINT ( 'NONE',  ( -11.07257681465629773, 59.22107823441397301, 7.723217015962382526 ) ) ;
#7634=CARTESIAN_POINT ( 'NONE',  ( 10.59059375150318516, 45.11097004264419752, 8.373194485267964282 ) ) ;
#7635=CARTESIAN_POINT ( 'NONE',  ( 11.15661179884298981, 69.71598163396143377, -7.601483556432171440 ) ) ;
#7636=EDGE_CURVE ( 'NONE', #13489, #13982, #539, .T. ) ;
#7637=CARTESIAN_POINT ( 'NONE',  ( 3.040576530018048729, 80.78928174342134128, 13.16481631334213098 ) ) ;
#7638=CARTESIAN_POINT ( 'NONE',  ( 13.28204714884621396, 30.34495749442142198, 2.416062439415011642 ) ) ;
#7639=CARTESIAN_POINT ( 'NONE',  ( -13.24809406675781176, 55.83842994404133719, -2.595915310630025452 ) ) ;
#7640=CARTESIAN_POINT ( 'NONE',  ( -12.82172618473797776, 50.08243652013945280, 4.237200570767894803 ) ) ;
#7641=CARTESIAN_POINT ( 'NONE',  ( 2.757549515546722230, 64.08084869351907287, -13.21536860246509271 ) ) ;
#7643=CARTESIAN_POINT ( 'NONE',  ( 10.33236877401481735, 39.76306948997951451, -8.688624863794741415 ) ) ;
#7644=ORIENTED_EDGE ( 'NONE', *, *, #15559, .F. ) ;
#7645=CARTESIAN_POINT ( 'NONE',  ( -10.07187023573678353, 61.58299827724115261, -8.989296097550834475 ) ) ;
#7647=VERTEX_POINT ( 'NONE', #1346 ) ;
#7649=CARTESIAN_POINT ( 'NONE',  ( -8.694191427202177636, 40.51460945123136526, -10.32880532873150869 ) ) ;
#7650=ORIENTED_EDGE ( 'NONE', *, *, #5216, .T. ) ;
#7653=CARTESIAN_POINT ( 'NONE',  ( 3.279879460145345593, 47.79795238127255885, 13.09551564182569017 ) ) ;
#7654=CARTESIAN_POINT ( 'NONE',  ( 10.91216525745976895, 57.73057897943527905, -7.953499367341933635 ) ) ;
#7655=CARTESIAN_POINT ( 'NONE',  ( 6.542932766149395896, 78.93933411452208304, -11.81244280098690780 ) ) ;
#7656=CARTESIAN_POINT ( 'NONE',  ( -7.272992578804310604, 78.38000000000000966, 10.01041549318726709 ) ) ;
#7657=FACE_OUTER_BOUND ( 'NONE', #16863, .T. ) ;
#7658=DIRECTION ( 'NONE',  ( 0.000000000000000000, -1.000000000000000000, 0.000000000000000000 ) ) ;
#7663=DIRECTION ( 'NONE',  ( 0.000000000000000000, -1.000000000000000000, 0.000000000000000000 ) ) ;
#7664=CARTESIAN_POINT ( 'NONE',  ( 3.151976139588944736, 34.06667296235463027, -13.12692461614821582 ) ) ;
#7665=ORIENTED_EDGE ( 'NONE', *, *, #237, .F. ) ;
#7667=EDGE_LOOP ( 'NONE', ( #8347, #1962, #820, #1019 ) ) ;
#7669=CARTESIAN_POINT ( 'NONE',  ( 4.961522565702499499, 77.85890369619608009, 12.55714296570731392 ) ) ;
#7670=CARTESIAN_POINT ( 'NONE',  ( -7.187129287260045629, 59.41245409490487361, 11.42782594799617968 ) ) ;
#7673=CARTESIAN_POINT ( 'NONE',  ( 10.92172942406178926, 57.13000000000000256, 7.935100905948387684 ) ) ;
#7674=CARTESIAN_POINT ( 'NONE',  ( -2.520299001384201265, 71.58939712408532330, 13.26745337539860259 ) ) ;
#7675=EDGE_CURVE ( 'NONE', #5870, #9540, #2022, .T. ) ;
#7678=CARTESIAN_POINT ( 'NONE',  ( 1.939380092513621090, 68.74973318765675856, 13.35997747337515307 ) ) ;
#7682=CARTESIAN_POINT ( 'NONE',  ( -3.417358507291479164, 65.55712218665007640, 13.09022083234078870 ) ) ;
#7683=CARTESIAN_POINT ( 'NONE',  ( -11.52888015854885317, 80.93000000000003524, -3.329402692648984363 ) ) ;
#7684=CARTESIAN_POINT ( 'NONE',  ( -6.469357084119882195, 35.44227298974823270, 11.85135619912656502 ) ) ;
#7687=CARTESIAN_POINT ( 'NONE',  ( 9.520470885617717371, 31.72999999999999332, -6.917026985038131848 ) ) ;
#7688=CARTESIAN_POINT ( 'NONE',  ( -13.17209843300189576, 32.03655692023156831, 3.006699176096832460 ) ) ;
#7690=CARTESIAN_POINT ( 'NONE',  ( 13.07535219888350753, 60.31039798475667624, 3.359492778058866591 ) ) ;
#7692=CARTESIAN_POINT ( 'NONE',  ( -11.70956602232489630, 53.18020972713351568, 6.735112246977101869 ) ) ;
#7694=CARTESIAN_POINT ( 'NONE',  ( 3.636496289402157078, 59.03000000000000114, -11.19198476289190936 ) ) ;
#7696=CARTESIAN_POINT ( 'NONE',  ( 13.49481123919801639, 51.44323841525638130, -0.3855105674034914887 ) ) ;
#7697=CARTESIAN_POINT ( 'NONE',  ( -13.47601568130759198, 37.90221951456256733, -0.8043930999376557311 ) ) ;
#7698=CARTESIAN_POINT ( 'NONE',  ( 13.22368575055132212, 36.52637389139642465, -2.727991382493684114 ) ) ;
#7700=CARTESIAN_POINT ( 'NONE',  ( -2.197460307225001408, 74.60102142208326370, 13.32837458805170527 ) ) ;
#7701=CARTESIAN_POINT ( 'NONE',  ( -10.58220227879168540, 77.24934925134837727, 8.383323893021028539 ) ) ;
#7703=CARTESIAN_POINT ( 'NONE',  ( -5.506042237581730170, 80.48045121655667344, 12.33370346659203953 ) ) ;
#7704=CARTESIAN_POINT ( 'NONE',  ( 7.500000000000001776, 108.6199039925687089, -2.572187159835566117 ) ) ;
#7708=CARTESIAN_POINT ( 'NONE',  ( -3.636496289402153081, 56.32999999999999829, -11.19198476289190936 ) ) ;
#7712=CARTESIAN_POINT ( 'NONE',  ( 8.593253602144370618, 75.85007813313070812, -10.41182175112990294 ) ) ;
#7714=CARTESIAN_POINT ( 'NONE',  ( 0.8232864874221478280, 65.70960053299302217, 13.47579076975969059 ) ) ;
#7715=CARTESIAN_POINT ( 'NONE',  ( 8.343458848123578520, 68.98000000000000398, 11.48378591275254124 ) ) ;
#7716=CARTESIAN_POINT ( 'NONE',  ( -3.636496289402153081, 50.32999999999999829, -11.19198476289190936 ) ) ;
#7719=CARTESIAN_POINT ( 'NONE',  ( -11.48516908419409432, 59.19542272029885766, 7.107131117762169659 ) ) ;
#7720=CARTESIAN_POINT ( 'NONE',  ( 10.21623194528608458, 45.09073215856821548, 8.828689258619535352 ) ) ;
#7721=CARTESIAN_POINT ( 'NONE',  ( 12.89448783432755796, 69.57384785835293428, -4.011012806986094859 ) ) ;
#7723=CARTESIAN_POINT ( 'NONE',  ( 12.36279736334451052, 30.62854102080525465, -5.439322983125138400 ) ) ;
#7724=CARTESIAN_POINT ( 'NONE',  ( -12.03366613076771330, 55.70437945554667891, -6.119706988989864982 ) ) ;
#7725=CARTESIAN_POINT ( 'NONE',  ( -13.38202365434617924, 49.99395983722415338, 1.829691088066569771 ) ) ;
#7726=CARTESIAN_POINT ( 'NONE',  ( 5.480047553734324062, 63.98142194296197260, -12.33786472815376456 ) ) ;
#7727=CARTESIAN_POINT ( 'NONE',  ( 13.01599110912158608, 42.55788555145221608, -3.582463918765408373 ) ) ;
#7728=CARTESIAN_POINT ( 'NONE',  ( 12.79213715724993072, 39.27444083374449946, 4.317700622619438988 ) ) ;
#7730=CARTESIAN_POINT ( 'NONE',  ( -7.516515514640333073, 70.46163409174739911, -11.21472715495389139 ) ) ;
#7731=CARTESIAN_POINT ( 'NONE',  ( -12.79841870162076134, 61.77472664241843603, -4.318434748836910586 ) ) ;
#7733=VERTEX_POINT ( 'NONE', #2553 ) ;
#7734=CARTESIAN_POINT ( 'NONE',  ( -10.27255720726481591, 40.59369077641002832, -8.759258848260193631 ) ) ;
#7735=ORIENTED_EDGE ( 'NONE', *, *, #11716, .F. ) ;
#7738=EDGE_CURVE ( 'NONE', #10449, #5905, #6195, .T. ) ;
#7739=CARTESIAN_POINT ( 'NONE',  ( -7.291143994141260196E-08, 47.67999796853253258, 13.49999999999999822 ) ) ;
#7740=CARTESIAN_POINT ( 'NONE',  ( 1.744899927265306738, 58.11728114404964174, -13.38849203301896651 ) ) ;
#7741=CARTESIAN_POINT ( 'NONE',  ( 12.17625345903434386, 78.64407479153155123, -5.830030459730453529 ) ) ;
#7742=CARTESIAN_POINT ( 'NONE',  ( -11.76794919243112325, 74.92999999999999261, -2.882316262207890869E-15 ) ) ;
#7744=DIRECTION ( 'NONE',  ( 0.000000000000000000, -1.000000000000000000, 0.000000000000000000 ) ) ;
#7747=CARTESIAN_POINT ( 'NONE',  ( 2.445080149700053643E-15, 33.17999999999999261, -13.50000000000000000 ) ) ;
#7750=CIRCLE ( 'NONE', #11414, 8.999999999999998224 ) ;
#7751=CARTESIAN_POINT ( 'NONE',  ( 3.850668321557367602, 34.04163834952560563, -12.93976093828572616 ) ) ;
#7752=CARTESIAN_POINT ( 'NONE',  ( -13.49747450356258227, 73.94233775771490969, 0.3603895268416468789 ) ) ;
#7753=ORIENTED_EDGE ( 'NONE', *, *, #7763, .T. ) ;
#7754=VERTEX_POINT ( 'NONE', #5503 ) ;
#7760=CARTESIAN_POINT ( 'NONE',  ( -4.525246487782226268, 44.51717099873670946, 12.71929788871430844 ) ) ;
#7761=FACE_OUTER_BOUND ( 'NONE', #838, .T. ) ;
#7763=EDGE_CURVE ( 'NONE', #13217, #12592, #9879, .T. ) ;
#7764=CARTESIAN_POINT ( 'NONE',  ( 7.500000000000000888, 98.93000000000002103, 1.224646799147353059E-15 ) ) ;
#7766=CARTESIAN_POINT ( 'NONE',  ( 12.85627864483936023, 66.57813439057589733, -4.122644307487381532 ) ) ;
#7767=CARTESIAN_POINT ( 'NONE',  ( 4.171729424061791924, 52.03000000000000114, -12.83926296998457239 ) ) ;
#7768=CARTESIAN_POINT ( 'NONE',  ( -11.83475973592285513, 71.17061926079419720, 6.495264808528300904 ) ) ;
#7771=CARTESIAN_POINT ( 'NONE',  ( 1.898107115681752832, 68.74824965014141753, 13.36594710483466741 ) ) ;
#7773=CARTESIAN_POINT ( 'NONE',  ( 4.982188148456265786, 55.00030919837298882, -12.54727938898756534 ) ) ;
#7775=CARTESIAN_POINT ( 'NONE',  ( -7.868944743446579793, 65.38296008073473331, 10.97062159917515345 ) ) ;
#7776=CARTESIAN_POINT ( 'NONE',  ( -7.373414840961570960, 62.40459273648136929, 11.31939194178672814 ) ) ;
#7777=CARTESIAN_POINT ( 'NONE',  ( -9.387694602222815377, 35.31196052404588670, 9.701610092094997029 ) ) ;
#7782=CARTESIAN_POINT ( 'NONE',  ( -13.35193275233298138, 31.99983217731938012, 1.993971145068321293 ) ) ;
#7783=CARTESIAN_POINT ( 'NONE',  ( 0.5206494563258732278, 73.16127936737596826, -13.48995723633962207 ) ) ;
#7784=CARTESIAN_POINT ( 'NONE',  ( 8.660314696132404677, 60.01309689425234239, 10.35850926495430002 ) ) ;
#7786=CARTESIAN_POINT ( 'NONE',  ( -3.829800477185295815, 53.54229456450769220, 12.94543166439263082 ) ) ;
#7787=CARTESIAN_POINT ( 'NONE',  ( 9.520470885617717371, 61.72999999999999687, -6.917026985038131848 ) ) ;
#7789=CARTESIAN_POINT ( 'NONE',  ( 2.607531440858944223E-15, 78.18000000000000682, -14.19474002721660355 ) ) ;
#7790=CARTESIAN_POINT ( 'NONE',  ( 13.40849521964058333, 51.37530757315951746, 1.569414197331337135 ) ) ;
#7791=CARTESIAN_POINT ( 'NONE',  ( -13.43247398786117230, 37.88223963647511283, -1.378765868932373406 ) ) ;
#7792=CARTESIAN_POINT ( 'NONE',  ( 13.48777555382222815, 36.44979078757540236, -0.5747704346103513773 ) ) ;
#7794=CARTESIAN_POINT ( 'NONE',  ( -1.245489582415950203, 74.63522726745355840, 13.44493988206992441 ) ) ;
#7795=VECTOR ( 'NONE', #1068, 1000.000000000000000 ) ;
#7796=CARTESIAN_POINT ( 'NONE',  ( -7.500000000000000000, 108.9300000000000068, -12.00000000000000178 ) ) ;
#7797=CARTESIAN_POINT ( 'NONE',  ( -1.443680002102475823, 80.62806861202990660, 13.42304612100068262 ) ) ;
#7798=CARTESIAN_POINT ( 'NONE',  ( 7.500000000000001776, 108.6662573213694856, -2.063574628993714466 ) ) ;
#7799=VERTEX_POINT ( 'NONE', #17330 ) ;
#7802=CARTESIAN_POINT ( 'NONE',  ( 7.272992578804308828, 60.97999999999999687, 10.01041549318726886 ) ) ;
#7806=CARTESIAN_POINT ( 'NONE',  ( 4.683166727831639342, 76.01126718398232640, -12.67683038080413205 ) ) ;
#7808=CARTESIAN_POINT ( 'NONE',  ( -13.49999999999999822, 70.78000000000000114, -4.386415899144240349 ) ) ;
#7809=CARTESIAN_POINT ( 'NONE',  ( 3.636496289402157078, 44.03000000000000114, -11.19198476289190936 ) ) ;
#7810=CARTESIAN_POINT ( 'NONE',  ( 6.750022862106053623, 30.42926176209967792, 11.69132975161703669 ) ) ;
#7811=CARTESIAN_POINT ( 'NONE',  ( -9.960320236238985103, 59.28285562016890964, 9.112740665185853572 ) ) ;
#7812=CARTESIAN_POINT ( 'NONE',  ( 13.06318910310979398, 45.30856193264118303, 3.408955850317910485 ) ) ;
#7813=CARTESIAN_POINT ( 'NONE',  ( 13.41584005935412982, 69.37759815817189235, 1.505070243511359207 ) ) ;
#7814=CARTESIAN_POINT ( 'NONE',  ( 5.606696772960964026, 80.88329787685947281, 12.29363097722763953 ) ) ;
#7815=CARTESIAN_POINT ( 'NONE',  ( 13.29343906038742240, 30.34724986304589223, 2.352712674252016356 ) ) ;
#7817=CARTESIAN_POINT ( 'NONE',  ( -6.971261592005899566, 55.43845261729841667, -11.56146040202950864 ) ) ;
#7818=CARTESIAN_POINT ( 'NONE',  ( -13.48137232301679767, 49.90553325806488516, -0.7090744274153022442 ) ) ;
#7819=CARTESIAN_POINT ( 'NONE',  ( 7.823624482728693152, 63.88493689099392014, -11.00187558684504729 ) ) ;
#7820=CARTESIAN_POINT ( 'NONE',  ( 9.806806863896056825, 42.79088325685976457, -9.280060988516410703 ) ) ;
#7821=CARTESIAN_POINT ( 'NONE',  ( 11.17315624111993344, 39.14503853878225215, 7.577034674267142833 ) ) ;
#7823=CARTESIAN_POINT ( 'NONE',  ( -12.53540363503289967, 70.74778265195330107, -5.016157258731891666 ) ) ;
#7824=CARTESIAN_POINT ( 'NONE',  ( -6.468465248468677764, 61.41772682254438109, -11.85174451472239987 ) ) ;
#7825=AXIS2_PLACEMENT_3D ( 'NONE', #7796, #17049, #3529 ) ;
#7827=ORIENTED_EDGE ( 'NONE', *, *, #183, .T. ) ;
#7830=CARTESIAN_POINT ( 'NONE',  ( 3.401931530595172948, 47.80226563792746219, 13.06448585452245048 ) ) ;
#7831=CARTESIAN_POINT ( 'NONE',  ( 13.49968223111125987, 57.43320969734387660, -0.09375648845182017743 ) ) ;
#7832=CARTESIAN_POINT ( 'NONE',  ( -7.272992578804307939, 68.48000000000000398, -10.01041549318726886 ) ) ;
#7833=CARTESIAN_POINT ( 'NONE',  ( 11.76794919243112325, 79.28000000000001535, 3.823638476888996607 ) ) ;
#7835=AXIS2_PLACEMENT_3D ( 'NONE', #10404, #15761, #2327 ) ;
#7839=CARTESIAN_POINT ( 'NONE',  ( 4.929499733297499908, 34.00225962392094914, -12.56974289013172275 ) ) ;
#7840=CARTESIAN_POINT ( 'NONE',  ( -2.303000823595952262, 73.26280741842690247, -13.30211301100326970 ) ) ;
#7841=ORIENTED_EDGE ( 'NONE', *, *, #8720, .F. ) ;
#7843=CARTESIAN_POINT ( 'NONE',  ( 2.272985001014427393E-15, 80.18000000000002103, -12.37355403259654807 ) ) ;
#7844=ORIENTED_EDGE ( 'NONE', *, *, #16200, .T. ) ;
#7846=CARTESIAN_POINT ( 'NONE',  ( -9.386590952217790829, 44.31237695230070983, 9.713897901698546278 ) ) ;
#7848=CARTESIAN_POINT ( 'NONE',  ( 12.75591148537818142, 66.58942501576625261, -4.420261642715005657 ) ) ;
#7849=CARTESIAN_POINT ( 'NONE',  ( -10.92172942406178926, 49.62999999999999545, -7.935100905948389460 ) ) ;
#7850=CARTESIAN_POINT ( 'NONE',  ( -11.81742131952455210, 71.17185724881636588, 6.526822490041712221 ) ) ;
#7852=CARTESIAN_POINT ( 'NONE',  ( -11.71143577085923049, 68.17956492373299682, 6.715245685198016012 ) ) ;
#7855=CARTESIAN_POINT ( 'NONE',  ( 10.10871875307872791, 54.77537364579058021, -8.963922330543132588 ) ) ;
#7858=CARTESIAN_POINT ( 'NONE',  ( -9.838551016974426133, 65.28917364825832692, 9.244084696182136796 ) ) ;
#7859=CARTESIAN_POINT ( 'NONE',  ( -0.8900008408070171351, 35.64814624292192491, 13.47797923260558406 ) ) ;
#7865=CARTESIAN_POINT ( 'NONE',  ( -13.38778841787257967, 31.99111624269271914, 1.750747606360489872 ) ) ;
#7866=CARTESIAN_POINT ( 'NONE',  ( 0.6169822239420026389, 73.15781583020579149, -13.48596981513675885 ) ) ;
#7867=CARTESIAN_POINT ( 'NONE',  ( 13.43413273411696984, 60.37283339418769401, 1.647395493114142351 ) ) ;
#7868=CARTESIAN_POINT ( 'NONE',  ( -8.796156758802018416, 53.34094639218631073, 10.25032176464773670 ) ) ;
#7869=CARTESIAN_POINT ( 'NONE',  ( 11.76794919243112325, 58.42999999999999261, 1.441158131103945434E-15 ) ) ;
#7870=CARTESIAN_POINT ( 'NONE',  ( 10.29002516399447664, 51.09446916187894061, 8.745445847329625266 ) ) ;
#7872=CARTESIAN_POINT ( 'NONE',  ( -12.50081041153300809, 37.74404765314170618, -5.115235228920670174 ) ) ;
#7873=CARTESIAN_POINT ( 'NONE',  ( 11.09743137222288567, 36.14041904309804210, 7.687522710969313167 ) ) ;
#7875=CARTESIAN_POINT ( 'NONE',  ( -0.5868455399888620194, 74.65889916526552383, 13.48724515689395709 ) ) ;
#7876=CARTESIAN_POINT ( 'NONE',  ( -7.867229263053499011, 77.38331958151701429, 10.97973947346444312 ) ) ;
#7877=CARTESIAN_POINT ( 'NONE',  ( -12.21983403303726412, 80.14045539099613791, 5.738378725442176531 ) ) ;
#7878=CARTESIAN_POINT ( 'NONE',  ( 7.500000000000000000, 108.7258046340738247, -1.043242051446488183 ) ) ;
#7880=CARTESIAN_POINT ( 'NONE',  ( 0.000000000000000000, 0.000000000000000000, 0.000000000000000000 ) ) ;
#7882=ORIENTED_EDGE ( 'NONE', *, *, #15463, .T. ) ;
#7883=CARTESIAN_POINT ( 'NONE',  ( -11.76794919243112325, 53.92999999999999972, -2.882316262207890869E-15 ) ) ;
#7885=CARTESIAN_POINT ( 'NONE',  ( 3.785595641572113985E-06, 49.17999986388394973, -13.49999999999946887 ) ) ;
#7887=CARTESIAN_POINT ( 'NONE',  ( 10.53320440394615787, 75.75205876548513118, -8.444065835725185210 ) ) ;
#7889=CARTESIAN_POINT ( 'NONE',  ( 8.343458848123583849, 32.88000000000000256, -11.48378591275253768 ) ) ;
#7890=CARTESIAN_POINT ( 'NONE',  ( 2.607531440858944223E-15, 76.18000000000000682, -14.19474002721660355 ) ) ;
#7891=CARTESIAN_POINT ( 'NONE',  ( -7.272992578804307939, 38.47999999999999687, -10.01041549318726886 ) ) ;
#7893=CARTESIAN_POINT ( 'NONE',  ( -8.783995296284150101, 58.51886061770396452, -10.25141294735016473 ) ) ;
#7894=CARTESIAN_POINT ( 'NONE',  ( 8.830119991140810143, 45.02099320959101902, 10.21491743141267250 ) ) ;
#7895=CARTESIAN_POINT ( 'NONE',  ( 10.17242564541387573, 69.77167130980720344, -8.875356370481091162 ) ) ;
#7896=EDGE_CURVE ( 'NONE', #5186, #4213, #5941, .T. ) ;
#7897=CARTESIAN_POINT ( 'NONE',  ( -2.138189944381236884, 66.25688142232024802, -13.50000000000000000 ) ) ;
#7898=CARTESIAN_POINT ( 'NONE',  ( 1.469576158976823947E-15, 80.93000000000000682, 12.00000000000000178 ) ) ;
#7899=AXIS2_PLACEMENT_3D ( 'NONE', #11137, #174, #9912 ) ;
#7900=CARTESIAN_POINT ( 'NONE',  ( -3.266778053494848510, 55.29741596993616781, -13.10567149089917294 ) ) ;
#7901=CARTESIAN_POINT ( 'NONE',  ( -12.61725017451394137, 50.10401918287165302, 4.802055765613469696 ) ) ;
#7902=CARTESIAN_POINT ( 'NONE',  ( 12.92176334759158607, 63.28989646019751802, 3.909127044249662841 ) ) ;
#7903=CARTESIAN_POINT ( 'NONE',  ( 11.58099081591013402, 42.68941737403753223, -6.962115988610442230 ) ) ;
#7904=CARTESIAN_POINT ( 'NONE',  ( 13.27807327384993918, 39.34399554834261892, 2.441573368172686553 ) ) ;
#7906=CARTESIAN_POINT ( 'NONE',  ( -5.200545543539695892, 70.36798564403922285, -12.45811891570486907 ) ) ;
#7907=CARTESIAN_POINT ( 'NONE',  ( -4.019890708354314945, 61.32453985535606478, -12.88763352006148466 ) ) ;
#7909=ORIENTED_EDGE ( 'NONE', *, *, #4495, .T. ) ;
#7913=CARTESIAN_POINT ( 'NONE',  ( 3.073068557420711056, 61.06950378709134952, -13.14558087420024712 ) ) ;
#7914=CARTESIAN_POINT ( 'NONE',  ( 9.703214173663569753, 72.06388277513445928, 9.386303311651374770 ) ) ;
#7915=CARTESIAN_POINT ( 'NONE',  ( 13.39493254271660128, 57.37134799861901513, 1.681008321832105468 ) ) ;
#7917=CARTESIAN_POINT ( 'NONE',  ( 7.272992578804311492, 70.87999999999998124, -10.01041549318726709 ) ) ;
#7918=CARTESIAN_POINT ( 'NONE',  ( -11.76794919243112325, 74.92999999999999261, -2.882316262207890869E-15 ) ) ;
#7919=CARTESIAN_POINT ( 'NONE',  ( -1.404360861943162231, 47.62954975977737604, 13.42896419968065658 ) ) ;
#7921=CARTESIAN_POINT ( 'NONE',  ( -4.171729424061787483, 75.33000000000001251, -12.83926296998457417 ) ) ;
#7923=CARTESIAN_POINT ( 'NONE',  ( 2.138189944381200469, 45.10311857767973720, -13.50000000000001421 ) ) ;
#7924=CARTESIAN_POINT ( 'NONE',  ( 10.15193879533094545, 33.77277897302748499, -8.899270537352469645 ) ) ;
#7925=CARTESIAN_POINT ( 'NONE',  ( -7.690819183321357499, 73.46921467895631963, -11.09564406485981003 ) ) ;
#7928=CARTESIAN_POINT ( 'NONE',  ( 11.76794919243112680, 76.57999999999998408, -3.823638476888993942 ) ) ;
#7929=ORIENTED_EDGE ( 'NONE', *, *, #3866, .F. ) ;
#7931=CARTESIAN_POINT ( 'NONE',  ( -10.11920711176065701, 44.27449785737638166, 8.935975526465597341 ) ) ;
#7933=CARTESIAN_POINT ( 'NONE',  ( 10.70226043262125870, 66.74271198536885663, -8.240297481720242345 ) ) ;
#7935=CARTESIAN_POINT ( 'NONE',  ( 13.50000000000000355, 45.57999999999998408, -4.386415899144233244 ) ) ;
#7936=CARTESIAN_POINT ( 'NONE',  ( -8.912460682575348514, 71.33536275098259694, 10.15239226002055517 ) ) ;
#7939=CARTESIAN_POINT ( 'NONE',  ( -12.85088929819618109, 67.78133704544254101, -4.136414102390641112 ) ) ;
#7941=CARTESIAN_POINT ( 'NONE',  ( 10.52332088831184720, 54.75260603147985705, -8.456359092437114811 ) ) ;
#7943=CARTESIAN_POINT ( 'NONE',  ( -12.70587675808030070, 65.09482543421927403, 4.561926965439528914 ) ) ;
#7944=CARTESIAN_POINT ( 'NONE',  ( -9.395184304882585380, 35.31158635481718022, 9.694355262636014103 ) ) ;
#7947=CYLINDRICAL_SURFACE ( 'NONE', #17163, 13.50000000000000000 ) ;
#7949=CARTESIAN_POINT ( 'NONE',  ( -7.466064059507305117, 31.45946987589979926, -11.24836648485607071 ) ) ;
#7950=DIRECTION ( 'NONE',  ( 0.000000000000000000, 1.000000000000000000, 0.000000000000000000 ) ) ;
#7952=CARTESIAN_POINT ( 'NONE',  ( 3.131229719746321916, 59.79264428906494544, 13.13212888701132997 ) ) ;
#7955=CARTESIAN_POINT ( 'NONE',  ( -6.655638788749627111, 53.43463457656628890, 11.74728228429494159 ) ) ;
#7956=CARTESIAN_POINT ( 'NONE',  ( 11.76794919243112325, 52.43000000000000682, 1.441158131103945434E-15 ) ) ;
#7958=CARTESIAN_POINT ( 'NONE',  ( -8.343458848123582072, 70.37999999999999545, 11.48378591275254124 ) ) ;
#7959=CARTESIAN_POINT ( 'NONE',  ( 12.72881000398506579, 51.26746853374235258, 4.501197650617609014 ) ) ;
#7960=CARTESIAN_POINT ( 'NONE',  ( -10.71889181782863254, 37.61765628241656856, -8.218708770179583567 ) ) ;
#7961=CARTESIAN_POINT ( 'NONE',  ( 13.30455254956636324, 36.34955702229247265, 2.288870851817195184 ) ) ;
#7963=CARTESIAN_POINT ( 'NONE',  ( -0.6217783953300516364, 74.65764314461276285, 13.48567423263519771 ) ) ;
#7964=CARTESIAN_POINT ( 'NONE',  ( -13.50003724147074458, 76.93564051261272141, 0.1657311543569034151 ) ) ;
#7965=CARTESIAN_POINT ( 'NONE',  ( -12.24434757080924641, 80.13838886078774237, 5.685888707796101116 ) ) ;
#7967=CARTESIAN_POINT ( 'NONE',  ( 7.500000000000000000, 107.9345255869306044, -5.560661329642322848 ) ) ;
#7970=CARTESIAN_POINT ( 'NONE',  ( 2.272985001014427393E-15, 53.17999999999999972, -12.37355403259654807 ) ) ;
#7974=AXIS2_PLACEMENT_3D ( 'NONE', #11662, #3869, #2606 ) ;
#7975=CARTESIAN_POINT ( 'NONE',  ( -8.891200544363830713E-16, 34.67999999999999261, 13.50000000000000000 ) ) ;
#7976=CARTESIAN_POINT ( 'NONE',  ( 10.27537742884199368, 75.76631104229213065, -8.763344131083259825 ) ) ;
#7978=CARTESIAN_POINT ( 'NONE',  ( 4.171729424061789260, 67.82999999999999829, 12.83926296998457417 ) ) ;
#7979=CARTESIAN_POINT ( 'NONE',  ( -9.520470885617717371, 36.22999999999999687, 6.917026985038133624 ) ) ;
#7981=CARTESIAN_POINT ( 'NONE',  ( -9.718168175322020375, 58.56428136966050602, -9.379168268827697830 ) ) ;
#7982=CARTESIAN_POINT ( 'NONE',  ( 4.611897008443751389, 44.84600509516975109, 12.68780702028759144 ) ) ;
#7983=CARTESIAN_POINT ( 'NONE',  ( 13.18589603968220203, 69.53262849552022828, -2.898846619569253047 ) ) ;
#7984=AXIS2_PLACEMENT_3D ( 'NONE', #5093, #11892, #4013 ) ;
#7987=CARTESIAN_POINT ( 'NONE',  ( -0.5738463663737329856, 55.20063339759468590, -13.48779904819468101 ) ) ;
#7988=CARTESIAN_POINT ( 'NONE',  ( -10.51139941513729958, 49.60641348581317089, -8.476086535629807628 ) ) ;
#7989=CARTESIAN_POINT ( 'NONE',  ( 13.31815325490439861, 63.50779534182326813, -2.215341855570049479 ) ) ;
#7990=CARTESIAN_POINT ( 'NONE',  ( 9.372370473719398021, 42.81294516566138952, -9.725257989828588023 ) ) ;
#7991=CARTESIAN_POINT ( 'NONE',  ( 8.950822057147354016, 39.02672537493957350, 10.10929111056123553 ) ) ;
#7993=CARTESIAN_POINT ( 'NONE',  ( -7.766575051535378194, 70.47255142998834287, -11.04220757594332447 ) ) ;
#7995=ORIENTED_EDGE ( 'NONE', *, *, #6196, .T. ) ;
#7999=CARTESIAN_POINT ( 'NONE',  ( 4.736358946727592389, 61.00938531345052240, -12.64187847761339434 ) ) ;
#8002=EDGE_CURVE ( 'NONE', #12569, #3120, #10097, .T. ) ;
#8003=CARTESIAN_POINT ( 'NONE',  ( 10.32313480350834389, 72.09643373092249874, 8.701801321890403784 ) ) ;
#8004=CARTESIAN_POINT ( 'NONE',  ( 12.42105065504388506, 57.62284780083921021, -5.288814127532169174 ) ) ;
#8005=CARTESIAN_POINT ( 'NONE',  ( -11.76794919243112325, 68.93000000000000682, -2.882316262207890869E-15 ) ) ;
#8006=CARTESIAN_POINT ( 'NONE',  ( 3.636496289402154414, 72.83000000000001251, 11.19198476289190936 ) ) ;
#8007=CARTESIAN_POINT ( 'NONE',  ( -9.925988568760681474, 47.28464472409913810, 9.150140798969051303 ) ) ;
#8008=FACE_OUTER_BOUND ( 'NONE', #15106, .T. ) ;
#8010=CARTESIAN_POINT ( 'NONE',  ( -13.49999999999999822, 75.78000000000000114, -4.386415899144240349 ) ) ;
#8012=CARTESIAN_POINT ( 'NONE',  ( 4.171729424061791924, 45.03000000000000114, -12.83926296998457239 ) ) ;
#8013=CARTESIAN_POINT ( 'NONE',  ( 13.47686814967910074, 33.45793751627489598, -0.8093861106240824999 ) ) ;
#8014=CARTESIAN_POINT ( 'NONE',  ( -9.748234396007397606, 73.56618743211103606, -9.339340668855360406 ) ) ;
#8015=ORIENTED_EDGE ( 'NONE', *, *, #4516, .T. ) ;
#8017=CARTESIAN_POINT ( 'NONE',  ( 7.272992578804308828, 78.97999999999998977, 10.01041549318726886 ) ) ;
#8018=ORIENTED_EDGE ( 'NONE', *, *, #2551, .F. ) ;
#8020=CARTESIAN_POINT ( 'NONE',  ( -8.891200544363830713E-16, 58.67999999999999261, 13.50000000000000000 ) ) ;
#8022=CARTESIAN_POINT ( 'NONE',  ( 13.49999999999999822, 39.27999999999999403, 4.386415899144237684 ) ) ;
#8023=CARTESIAN_POINT ( 'NONE',  ( -6.568958932228524894, 71.43823863022225851, 11.79934775472050212 ) ) ;
#8025=CARTESIAN_POINT ( 'NONE',  ( -12.82751988175667357, 67.77861818588846177, -4.208333171070940182 ) ) ;
#8027=CARTESIAN_POINT ( 'NONE',  ( 11.54301513894250064, 54.69114107474510433, -7.000628745448283397 ) ) ;
#8030=EDGE_CURVE ( 'NONE', #15045, #4640, #5660, .T. ) ;
#8031=CARTESIAN_POINT ( 'NONE',  ( -13.03270642126316048, 64.80436272303023770, -3.522134089092859632 ) ) ;
#8033=CARTESIAN_POINT ( 'NONE',  ( -11.83548569472881162, 34.68943475006721400, -6.493960592972081614 ) ) ;
#8034=ORIENTED_EDGE ( 'NONE', *, *, #2906, .T. ) ;
#8036=CARTESIAN_POINT ( 'NONE',  ( -8.357336213632441613, 31.49890460822483362, -10.60832285590191049 ) ) ;
#8037=CARTESIAN_POINT ( 'NONE',  ( 11.40946131305635802, 72.70018184489865121, -7.219862210453702467 ) ) ;
#8041=CARTESIAN_POINT ( 'NONE',  ( -9.666059139767755326, 53.29810990967069273, 9.426597848540740898 ) ) ;
#8042=CARTESIAN_POINT ( 'NONE',  ( -3.636496289402155746, 48.52999999999999403, 11.19198476289190936 ) ) ;
#8043=CARTESIAN_POINT ( 'NONE',  ( 4.171729424061791924, 66.03000000000000114, -12.83926296998457239 ) ) ;
#8044=CARTESIAN_POINT ( 'NONE',  ( 4.957982560739019995, 50.85884492221607189, 12.55662115431407955 ) ) ;
#8045=CARTESIAN_POINT ( 'NONE',  ( -13.07003727117247038, 37.80950068799819519, -3.384012662600688337 ) ) ;
#8047=CARTESIAN_POINT ( 'NONE',  ( 12.63456399010862619, 36.25766377199223456, 4.761015956925509940 ) ) ;
#8050=CARTESIAN_POINT ( 'NONE',  ( -7.560656945971843790, 74.39645029488065120, 11.18730623038837280 ) ) ;
#8053=CARTESIAN_POINT ( 'NONE',  ( -13.27243981434447484, 76.84295076259492419, -2.470663295667402171 ) ) ;
#8054=CARTESIAN_POINT ( 'NONE',  ( -13.15097131915865702, 79.82156063716328731, -3.058016821922826090 ) ) ;
#8056=CARTESIAN_POINT ( 'NONE',  ( 7.500000000000000000, 104.6873333394687080, -9.035253535952437076 ) ) ;
#8059=CARTESIAN_POINT ( 'NONE',  ( -9.520470885617717371, 51.22999999999999687, 6.917026985038133624 ) ) ;
#8063=CARTESIAN_POINT ( 'NONE',  ( -8.070270851187604677, 40.48603366841279438, -10.82230097288300641 ) ) ;
#8065=CARTESIAN_POINT ( 'NONE',  ( 5.856966054657046783, 75.96662800222769363, -12.16416065871167262 ) ) ;
#8066=CARTESIAN_POINT ( 'NONE',  ( 0.000000000000000000, 108.9300000000000068, 6.000000000000001776 ) ) ;
#8067=CARTESIAN_POINT ( 'NONE',  ( 11.76794919243112325, 37.28000000000000114, 3.823638476888996607 ) ) ;
#8068=CARTESIAN_POINT ( 'NONE',  ( -9.321700413722924239, 41.31521659627871657, 9.765034796684853191 ) ) ;
#8069=CARTESIAN_POINT ( 'NONE',  ( -8.798798133082613049, 58.51955967947071713, -10.23870886399114255 ) ) ;
#8072=FACE_OUTER_BOUND ( 'NONE', #2365, .T. ) ;
#8073=CARTESIAN_POINT ( 'NONE',  ( -10.08120899900550427, 55.58349057628856826, -8.978837819965084677 ) ) ;
#8075=CARTESIAN_POINT ( 'NONE',  ( -12.29411837055197054, 49.72588110055323085, -5.581586529286209242 ) ) ;
#8076=CARTESIAN_POINT ( 'NONE',  ( 12.94123504964344384, 63.56776154898143005, -3.846256073626998173 ) ) ;
#8077=CARTESIAN_POINT ( 'NONE',  ( 11.96321250603508624, 42.66099223898741144, -6.255588818712046084 ) ) ;
#8078=CARTESIAN_POINT ( 'NONE',  ( 11.14178970317686712, 39.14311694041391831, 7.623027801797891634 ) ) ;
#8079=ORIENTED_EDGE ( 'NONE', *, *, #16100, .F. ) ;
#8080=CARTESIAN_POINT ( 'NONE',  ( -9.905601374715363505, 70.57426321601532493, -9.172207517655735387 ) ) ;
#8082=ORIENTED_EDGE ( 'NONE', *, *, #8935, .F. ) ;
#8086=CARTESIAN_POINT ( 'NONE',  ( 5.801648381285460232, 60.96920856786400122, -12.20604370177328946 ) ) ;
#8090=CARTESIAN_POINT ( 'NONE',  ( 13.49670674025940187, 57.44045678757618845, -0.3048764090252299996 ) ) ;
#8091=CARTESIAN_POINT ( 'NONE',  ( -7.272992578804310604, 69.38000000000000966, 10.01041549318726709 ) ) ;
#8092=CARTESIAN_POINT ( 'NONE',  ( -4.171729424061791036, 34.53000000000000114, 12.83926296998457239 ) ) ;
#8093=CARTESIAN_POINT ( 'NONE',  ( 9.520470885617717371, 79.72999999999998977, -6.917026985038131848 ) ) ;
#8094=CARTESIAN_POINT ( 'NONE',  ( -9.891620756194170028, 47.28642918340351287, 9.187267813302650410 ) ) ;
#8096=CARTESIAN_POINT ( 'NONE',  ( 13.49999999999999822, 38.27999999999999403, 4.386415899144236796 ) ) ;
#8100=CARTESIAN_POINT ( 'NONE',  ( -2.138189944381236884, 51.25688142232026934, -13.50000000000000000 ) ) ;
#8101=CARTESIAN_POINT ( 'NONE',  ( 12.93524070685253058, 33.56853690860952355, -3.868045386693336418 ) ) ;
#8102=CARTESIAN_POINT ( 'NONE',  ( -7.480073533223071891, 73.46007376390073773, -11.23826375466742178 ) ) ;
#8104=EDGE_LOOP ( 'NONE', ( #12855, #2825, #1102, #8976 ) ) ;
#8105=CARTESIAN_POINT ( 'NONE',  ( -3.984372987094109586, 62.53673597769582670, 12.89868305420871408 ) ) ;
#8107=CARTESIAN_POINT ( 'NONE',  ( -13.32866946258720908, 41.00521990185777810, 2.143963826540092654 ) ) ;
#8109=CARTESIAN_POINT ( 'NONE',  ( -0.6445126736188436789, 44.65682569745120389, 13.48462267080572374 ) ) ;
#8112=CARTESIAN_POINT ( 'NONE',  ( -4.171729424061791036, 44.53000000000000114, 12.83926296998457239 ) ) ;
#8113=CARTESIAN_POINT ( 'NONE',  ( -13.46053110311059342, 70.96573976700906883, 1.032151187161497674 ) ) ;
#8115=CARTESIAN_POINT ( 'NONE',  ( -13.32209690758261367, 67.85292585843949098, -2.195106065840739973 ) ) ;
#8117=CARTESIAN_POINT ( 'NONE',  ( 13.37361882778371580, 54.49663737476366521, -1.905621438755049413 ) ) ;
#8120=CARTESIAN_POINT ( 'NONE',  ( -13.40504862348259607, 64.98588083424387207, 1.603266894393355679 ) ) ;
#8121=CARTESIAN_POINT ( 'NONE',  ( -12.97126758716428796, 35.06420632578307561, 3.750847537641872620 ) ) ;
#8123=FACE_OUTER_BOUND ( 'NONE', #17053, .T. ) ;
#8124=CARTESIAN_POINT ( 'NONE',  ( -7.638144213919573211, 31.46690397426329966, -11.13304072010164170 ) ) ;
#8125=CARTESIAN_POINT ( 'NONE',  ( 3.487563165784445474, 73.05459837061692951, -13.04193799940900966 ) ) ;
#8127=CARTESIAN_POINT ( 'NONE',  ( 3.272115130898746838, 59.79762580205674283, 13.09749008070057918 ) ) ;
#8129=CARTESIAN_POINT ( 'NONE',  ( -13.47893375659474025, 52.90398739453420518, -0.7538941320434108251 ) ) ;
#8132=CARTESIAN_POINT ( 'NONE',  ( -11.76794919243112325, 48.07999999999998408, 3.823638476888994386 ) ) ;
#8133=CARTESIAN_POINT ( 'NONE',  ( 10.92172942406179104, 65.72999999999998977, -7.935100905948385908 ) ) ;
#8134=CARTESIAN_POINT ( 'NONE',  ( 4.913540562192366679, 50.85718164286154064, 12.57411717337579482 ) ) ;
#8135=CARTESIAN_POINT ( 'NONE',  ( -5.826744371414541490, 37.39211206380475971, -12.17872776587915951 ) ) ;
#8136=CARTESIAN_POINT ( 'NONE',  ( 13.31893752994962199, 36.35261631618632094, 2.203904136930395108 ) ) ;
#8138=CARTESIAN_POINT ( 'NONE',  ( -8.133420942632833217, 74.37112280558582711, 10.77516524646321194 ) ) ;
#8139=CARTESIAN_POINT ( 'NONE',  ( -13.29830443190622802, 76.84825558968388748, -2.324888195045509587 ) ) ;
#8140=CARTESIAN_POINT ( 'NONE',  ( -12.10733961092197397, 79.71006380404250535, -5.975826969573788894 ) ) ;
#8142=DIRECTION ( 'NONE',  ( 0.000000000000000000, -1.000000000000000000, 0.000000000000000000 ) ) ;
#8145=CARTESIAN_POINT ( 'NONE',  ( -7.576616670048093940E-16, 48.67999999999999261, 12.37355403259654807 ) ) ;
#8149=CARTESIAN_POINT ( 'NONE',  ( 8.343458848123580296, 34.97999999999998977, 11.48378591275253768 ) ) ;
#8150=CARTESIAN_POINT ( 'NONE',  ( 11.76865692967993482, 75.18437996510870391, 6.618042598872824200 ) ) ;
#8152=CARTESIAN_POINT ( 'NONE',  ( -3.636496289402153081, 41.32999999999999829, -11.19198476289190936 ) ) ;
#8153=CARTESIAN_POINT ( 'NONE',  ( -11.42231603963109521, 41.19917354752983130, 7.196541539523007458 ) ) ;
#8154=CARTESIAN_POINT ( 'NONE',  ( -4.745348413369673501, 58.35092235193497601, -12.64042052586673570 ) ) ;
#8155=( BOUNDED_CURVE ( )  B_SPLINE_CURVE ( 2, ( #1620, #10827, #126, #5440, #12325, #15126, #14955, #10741, #12235, #16105, #3023, #2845, #8364 ),
 .UNSPECIFIED., .F., .F. ) 
 B_SPLINE_CURVE_WITH_KNOTS ( ( 3, 2, 2, 2, 2, 2, 3 ),
 ( 0.8194444444444444198, 0.8222222222222221877, 0.8277777777777777235, 0.8333333333333333703, 0.8388888888888889062, 0.8444444444444444420, 0.8472222222222222099 ),
 .UNSPECIFIED. ) 
 CURVE ( )  GEOMETRIC_REPRESENTATION_ITEM ( )  RATIONAL_B_SPLINE_CURVE ( ( 0.9755282581475768211, 0.9755282581475768211, 1.000000000000000000, 0.9510565162951535312, 1.000000000000000000, 0.9510565162951535312, 1.000000000000000000, 0.9510565162951535312, 1.000000000000000000, 0.9510565162951535312, 1.000000000000000000, 0.9755282581475768211, 0.9755282581475768211 ) ) 
 REPRESENTATION_ITEM ( '' )  );
#8157=CARTESIAN_POINT ( 'NONE',  ( 10.92172942406178926, 59.13000000000000256, 7.935100905948387684 ) ) ;
#8158=CARTESIAN_POINT ( 'NONE',  ( 9.901291193213106467, 30.07383486385095495, 9.184156744704926822 ) ) ;
#8160=CARTESIAN_POINT ( 'NONE',  ( -5.372626086858939942, 49.37446523726847403, -12.39129945928973520 ) ) ;
#8161=CARTESIAN_POINT ( 'NONE',  ( 11.50550600207001040, 63.69365567215912449, -7.062106151818590583 ) ) ;
#8162=B_SPLINE_CURVE_WITH_KNOTS ( 'NONE', 3,
 ( #4610, #2021, #12826, #11327 ),
 .UNSPECIFIED., .F., .F.,
 ( 4, 4 ),
 ( 0.000000000000000000, 0.003336555488825435588 ),
 .UNSPECIFIED. ) ;
#8163=CARTESIAN_POINT ( 'NONE',  ( 13.40526361136180356, 42.48724074931151051, -1.642292961744375335 ) ) ;
#8167=CARTESIAN_POINT ( 'NONE',  ( -3.320475467054404886E-07, 70.18000001193918536, -13.49999999999999467 ) ) ;
#8168=CARTESIAN_POINT ( 'NONE',  ( 6.767892274421971166, 80.93000000000000682, 11.68099457074693603 ) ) ;
#8170=ORIENTED_EDGE ( 'NONE', *, *, #6979, .T. ) ;
#8171=CARTESIAN_POINT ( 'NONE',  ( -5.673269603926692994, 43.38613141203421719, -12.25006288933690968 ) ) ;
#8172=CARTESIAN_POINT ( 'NONE',  ( -7.500000000000000000, 103.1860286984271795, 9.367496997597605457 ) ) ;
#8173=CARTESIAN_POINT ( 'NONE',  ( 7.050225702995494892, 60.91835954970743927, -11.51657226464040029 ) ) ;
#8175=CARTESIAN_POINT ( 'NONE',  ( 2.104705901570253168, 71.75572894129780366, 13.33549315723480966 ) ) ;
#8176=CARTESIAN_POINT ( 'NONE',  ( 12.44807024653844785, 57.62036106608136521, -5.224809667552474224 ) ) ;
#8177=EDGE_CURVE ( 'NONE', #225, #7733, #13671, .T. ) ;
#8178=CARTESIAN_POINT ( 'NONE',  ( -11.76794919243112325, 66.07999999999999829, 3.823638476888994386 ) ) ;
#8179=CARTESIAN_POINT ( 'NONE',  ( -9.520470885617715595, 80.63000000000000966, -6.917026985038136289 ) ) ;
#8180=ADVANCED_FACE ( 'NONE', ( #4587 ), #12626, .F. ) ;
#8181=CARTESIAN_POINT ( 'NONE',  ( -11.01735871152694379, 47.22449060650489372, 7.813986986152833047 ) ) ;
#8183=CARTESIAN_POINT ( 'NONE',  ( 1.771727720396010897, 46.11629509651881875, -13.49999888936976156 ) ) ;
#8189=CARTESIAN_POINT ( 'NONE',  ( 12.43340273364695747, 33.62204941335177466, -5.272404384565503754 ) ) ;
#8190=CARTESIAN_POINT ( 'NONE',  ( -5.043811212648944498, 73.36206509383546859, -12.52241046721988127 ) ) ;
#8191=CARTESIAN_POINT ( 'NONE',  ( 7.500000000000000888, 102.9300000000000068, -9.367496997597600128 ) ) ;
#8193=CARTESIAN_POINT ( 'NONE',  ( -3.489578404781044974, 62.55452843961951714, 13.04738054726565721 ) ) ;
#8194=ORIENTED_EDGE ( 'NONE', *, *, #5923, .F. ) ;
#8197=CARTESIAN_POINT ( 'NONE',  ( -12.16175685827595210, 44.14530326537092009, 5.861221165930757593 ) ) ;
#8199=CARTESIAN_POINT ( 'NONE',  ( -13.49999999999999822, 47.07999999999999829, 4.386415899144235908 ) ) ;
#8200=CARTESIAN_POINT ( 'NONE',  ( -13.45347138943250798, 70.96881323304897649, 1.119889726645023176 ) ) ;
#8201=EDGE_CURVE ( 'NONE', #10469, #10491, #5578, .T. ) ;
#8204=CARTESIAN_POINT ( 'NONE',  ( -13.47769472573310523, 67.89946296695690364, -0.8856965346868491684 ) ) ;
#8206=CARTESIAN_POINT ( 'NONE',  ( 13.05062916916600280, 54.30688700786019751, 3.454156714176291665 ) ) ;
#8207=CARTESIAN_POINT ( 'NONE',  ( 0.000000000000000000, 80.93000000000000682, 0.000000000000000000 ) ) ;
#8208=CARTESIAN_POINT ( 'NONE',  ( -11.82157965976159808, 64.68840243461779949, -6.519625715133806843 ) ) ;
#8210=CARTESIAN_POINT ( 'NONE',  ( -8.343458848123578520, 63.48000000000001108, -11.48378591275254124 ) ) ;
#8211=CARTESIAN_POINT ( 'NONE',  ( -13.33969213930383013, 35.00272133652679685, 2.074452581059428091 ) ) ;
#8213=CARTESIAN_POINT ( 'NONE',  ( 13.43072676519339659, 78.38231396256115602, 1.366956873940078587 ) ) ;
#8217=CARTESIAN_POINT ( 'NONE',  ( 8.548604269041621961, 72.85217239673389145, -10.44934178869447905 ) ) ;
#8221=CARTESIAN_POINT ( 'NONE',  ( -13.50000000000000000, 70.92999999999999261, -3.306546357697853733E-15 ) ) ;
#8222=CARTESIAN_POINT ( 'NONE',  ( -13.47987952135760636, 52.90456830356593798, -0.7369079465333779888 ) ) ;
#8224=CARTESIAN_POINT ( 'NONE',  ( 9.520470885617717371, 49.72999999999999687, -6.917026985038131848 ) ) ;
#8225=CARTESIAN_POINT ( 'NONE',  ( -4.171729424061787483, 63.32999999999999829, -12.83926296998457417 ) ) ;
#8226=CARTESIAN_POINT ( 'NONE',  ( 12.49292108473675356, 51.24384918054708038, 5.116345218930953287 ) ) ;
#8227=CARTESIAN_POINT ( 'NONE',  ( -5.505992092405349148, 37.37965637996170898, -12.32618761653607820 ) ) ;
#8228=CARTESIAN_POINT ( 'NONE',  ( 11.19183201792044535, 36.14618292256778886, 7.549567337428954694 ) ) ;
#8230=CARTESIAN_POINT ( 'NONE',  ( -10.88893267353162209, 74.23195708089093614, 7.985199624914343985 ) ) ;
#8231=CARTESIAN_POINT ( 'NONE',  ( -13.15105693501601003, 77.03838810807653203, 3.057644733085780331 ) ) ;
#8232=CARTESIAN_POINT ( 'NONE',  ( -10.15331777804710356, 79.58698102410616571, -8.908116406432318612 ) ) ;
#8234=CARTESIAN_POINT ( 'NONE',  ( 3.114363690246614080, 80.93000000000004945, 12.90281209101391369 ) ) ;
#8237=CARTESIAN_POINT ( 'NONE',  ( -11.76794919243112325, 47.92999999999999972, -2.882316262207890869E-15 ) ) ;
#8240=CARTESIAN_POINT ( 'NONE',  ( -12.99798557104473495, 40.79969145139732234, -3.647469504750259883 ) ) ;
#8241=CARTESIAN_POINT ( 'NONE',  ( 4.171729424061791924, 36.03000000000000114, -12.83926296998457239 ) ) ;
#8242=CARTESIAN_POINT ( 'NONE',  ( 13.11911623483412725, 75.54314320642072289, -3.184815548587396794 ) ) ;
#8244=CARTESIAN_POINT ( 'NONE',  ( 11.76794919243112325, 34.28000000000000114, 3.823638476888996607 ) ) ;
#8245=CARTESIAN_POINT ( 'NONE',  ( -5.892354067706281562, 58.39472778308726220, -12.14630281014331281 ) ) ;
#8247=CARTESIAN_POINT ( 'NONE',  ( -4.023268246324633536E-14, 60.18000000000000682, -13.50000000000000000 ) ) ;
#8248=CARTESIAN_POINT ( 'NONE',  ( 9.135248883881359916, 30.03565898711111259, 9.940076883576240974 ) ) ;
#8249=CARTESIAN_POINT ( 'NONE',  ( -13.50000000000000000, 57.92999999999999972, -3.306546357697853733E-15 ) ) ;
#8250=CARTESIAN_POINT ( 'NONE',  ( -10.03685761320076075, 49.58118651522960363, -9.028742826659037490 ) ) ;
#8252=CARTESIAN_POINT ( 'NONE',  ( 12.88414385799500117, 63.28531013651519999, 4.031028846843240920 ) ) ;
#8253=CARTESIAN_POINT ( 'NONE',  ( 12.36777513855581390, 42.23235083080415109, 5.411869368907026967 ) ) ;
#8260=ORIENTED_EDGE ( 'NONE', *, *, #2675, .T. ) ;
#8261=CARTESIAN_POINT ( 'NONE',  ( -3.110033635544421582, 43.29182205780823267, -13.14495504916145485 ) ) ;
#8262=CARTESIAN_POINT ( 'NONE',  ( -7.500000000000000000, 108.3824470675415341, -4.067225351102824682 ) ) ;
#8263=CARTESIAN_POINT ( 'NONE',  ( 11.56001456171610720, 60.68998491048684940, -6.972525382906384905 ) ) ;
#8266=CARTESIAN_POINT ( 'NONE',  ( 13.31917153282089039, 66.50765729681475591, -2.211295458653834256 ) ) ;
#8267=CARTESIAN_POINT ( 'NONE',  ( 3.121749870751446387, 56.79230302867953384, 13.13415442199402960 ) ) ;
#8268=CARTESIAN_POINT ( 'NONE',  ( 7.272992578804311492, 55.87999999999998835, -10.01041549318726709 ) ) ;
#8269=CARTESIAN_POINT ( 'NONE',  ( -11.76794919243112325, 71.92999999999999261, -2.882316262207890869E-15 ) ) ;
#8270=AXIS2_PLACEMENT_3D ( 'NONE', #867, #4946, #16781 ) ;
#8271=CARTESIAN_POINT ( 'NONE',  ( -11.68579365184739061, 47.18153587550196448, 6.763020047883973263 ) ) ;
#8274=CARTESIAN_POINT ( 'NONE',  ( -6.594413527910950812, 56.43719554618320444, 11.79074946145723146 ) ) ;
#8276=CARTESIAN_POINT ( 'NONE',  ( -10.92172942406179104, 52.22999999999999687, 7.935100905948387684 ) ) ;
#8277=CARTESIAN_POINT ( 'NONE',  ( 13.04518082719695649, 33.55387728658139679, -3.474737096573298878 ) ) ;
#8283=CARTESIAN_POINT ( 'NONE',  ( -13.49999999999999822, 43.07999999999999829, 4.386415899144235020 ) ) ;
#8286=CARTESIAN_POINT ( 'NONE',  ( -13.46460078802627258, 40.89617066210697516, -0.9799208027847087221 ) ) ;
#8288=CARTESIAN_POINT ( 'NONE',  ( -13.47942042829293641, 43.95571666567489189, 0.7453506697733148778 ) ) ;
#8290=CARTESIAN_POINT ( 'NONE',  ( 4.171729424061791924, 43.03000000000000114, -12.83926296998457239 ) ) ;
#8291=CARTESIAN_POINT ( 'NONE',  ( -13.44824536596492237, 70.97096667731948116, 1.181153100867837313 ) ) ;
#8292=VECTOR ( 'NONE', #10412, 1000.000000000000000 ) ;
#8294=CARTESIAN_POINT ( 'NONE',  ( -6.505070197219007255, 67.41913341053678721, -11.83553212610193128 ) ) ;
#8296=CARTESIAN_POINT ( 'NONE',  ( 12.92435448664457631, 54.56979870081450912, -3.901149989671772289 ) ) ;
#8297=CARTESIAN_POINT ( 'NONE',  ( -1.103415079611737237, 64.21967456855061585, -13.45889604906427195 ) ) ;
#8298=ADVANCED_FACE ( 'NONE', ( #2777 ), #14796, .T. ) ;
#8301=CARTESIAN_POINT ( 'NONE',  ( -13.27056125883154714, 34.84229683454460513, -2.490662099278118546 ) ) ;
#8302=VERTEX_POINT ( 'NONE', #2688 ) ;
#8303=CARTESIAN_POINT ( 'NONE',  ( 12.47629078338616537, 78.24213358348909253, 5.161934717677671536 ) ) ;
#8307=CARTESIAN_POINT ( 'NONE',  ( 10.33443572568632085, 72.76295794329135447, -8.686189713967003456 ) ) ;
#8310=CARTESIAN_POINT ( 'NONE',  ( -13.49999999999999822, 76.77999999999998693, -4.386415899144240349 ) ) ;
#8311=CARTESIAN_POINT ( 'NONE',  ( -11.31104933256506762, 52.65366644603506074, -7.369657635140959506 ) ) ;
#8312=CARTESIAN_POINT ( 'NONE',  ( 7.272992578804311492, 43.87999999999999545, -10.01041549318726709 ) ) ;
#8313=CARTESIAN_POINT ( 'NONE',  ( 8.343458848123583849, 62.88000000000000256, -11.48378591275253768 ) ) ;
#8314=DIRECTION ( 'NONE',  ( 0.000000000000000000, 0.000000000000000000, 1.000000000000000000 ) ) ;
#8315=CARTESIAN_POINT ( 'NONE',  ( 11.67243386019293716, 69.17774755439334911, 6.782755736582077866 ) ) ;
#8317=CARTESIAN_POINT ( 'NONE',  ( 1.708800344670653191E-06, 35.68004753840243382, 13.49999999999978328 ) ) ;
#8319=CARTESIAN_POINT ( 'NONE',  ( -10.48937736199612480, 74.25448204741239522, 8.498420214693403807 ) ) ;
#8320=CARTESIAN_POINT ( 'NONE',  ( -13.49504752740739555, 76.94266908463271193, 0.3689546535713391640 ) ) ;
#8322=CARTESIAN_POINT ( 'NONE',  ( -4.310646433793312582, 79.33501006869653338, -12.79332600423342470 ) ) ;
#8326=CARTESIAN_POINT ( 'NONE',  ( 3.636496289402154414, 45.82999999999999829, 11.19198476289190936 ) ) ;
#8329=CARTESIAN_POINT ( 'NONE',  ( 13.49033203594054697, 75.44763660926943771, -0.5127258900949339671 ) ) ;
#8331=CARTESIAN_POINT ( 'NONE',  ( -12.21084993027352716, 41.14197536515471398, 5.780306110364526795 ) ) ;
#8333=CARTESIAN_POINT ( 'NONE',  ( 0.000000000000000000, 80.93000000000000682, -13.50000000000000000 ) ) ;
#8334=CARTESIAN_POINT ( 'NONE',  ( 6.229800185101045606, 44.90808656577910085, 11.97664669193207132 ) ) ;
#8335=CARTESIAN_POINT ( 'NONE',  ( -13.49999999999999822, 54.77999999999998693, -4.386415899144240349 ) ) ;
#8338=CARTESIAN_POINT ( 'NONE',  ( -7.304906251596263722, 49.45255025094410684, -11.35316560862786339 ) ) ;
#8339=CARTESIAN_POINT ( 'NONE',  ( 10.90660565521129044, 63.12913462907602025, 7.957536297550788618 ) ) ;
#8340=CARTESIAN_POINT ( 'NONE',  ( 13.48614902602365362, 42.45108007468103040, -0.6119829615113150378 ) ) ;
#8341=CARTESIAN_POINT ( 'NONE',  ( 3.563393355819833186, 38.80806997300490480, 13.02747425359752675 ) ) ;
#8343=CARTESIAN_POINT ( 'NONE',  ( -7.576616670048093940E-16, 75.67999999999997840, 12.37355403259654807 ) ) ;
#8347=ORIENTED_EDGE ( 'NONE', *, *, #17236, .F. ) ;
#8348=CARTESIAN_POINT ( 'NONE',  ( -4.129969626718125397, 43.32850618201838699, -12.85291258290743954 ) ) ;
#8349=CARTESIAN_POINT ( 'NONE',  ( 0.000000000000000000, 80.93000000000000682, 0.000000000000000000 ) ) ;
#8350=CARTESIAN_POINT ( 'NONE',  ( 12.91929742426344419, 60.57042407115622495, -3.917859330391978645 ) ) ;
#8353=CARTESIAN_POINT ( 'NONE',  ( 13.44750236278916589, 66.38875313069046058, 1.189447314180342330 ) ) ;
#8354=CARTESIAN_POINT ( 'NONE',  ( 8.142818167418832687, 56.98927294900627771, 10.76880729706688200 ) ) ;
#8355=CARTESIAN_POINT ( 'NONE',  ( 11.76794919243112325, 55.42999999999999972, 1.441158131103945434E-15 ) ) ;
#8356=CARTESIAN_POINT ( 'NONE',  ( 9.520470885617715595, 70.12999999999999545, 6.917026985038134512 ) ) ;
#8357=CARTESIAN_POINT ( 'NONE',  ( -11.59131112589550838, 47.18803745467646138, 6.922104400456148277 ) ) ;
#8359=CARTESIAN_POINT ( 'NONE',  ( 5.515696437122907803, 45.97993358946585118, -12.32182730336969634 ) ) ;
#8360=CARTESIAN_POINT ( 'NONE',  ( 1.102182119232618108E-15, 108.9300000000000068, -6.000000000000001776 ) ) ;
#8361=CARTESIAN_POINT ( 'NONE',  ( 8.632143809700615122, 30.84828256068346164, -10.38016917814384144 ) ) ;
#8364=CARTESIAN_POINT ( 'NONE',  ( 2.445080149700053643E-15, 39.17999999999999972, -13.50000000000000000 ) ) ;
#8365=CARTESIAN_POINT ( 'NONE',  ( 11.33052969111197150, 33.70514019894347513, -7.339663749698858375 ) ) ;
#8367=CARTESIAN_POINT ( 'NONE',  ( 0.6587682488342593290, 40.15634701798867212, -13.48451925025889864 ) ) ;
#8369=ORIENTED_EDGE ( 'NONE', *, *, #3366, .T. ) ;
#8370=CARTESIAN_POINT ( 'NONE',  ( -3.942068916870681949, 62.53825775923972685, 12.91162929084544331 ) ) ;
#8375=CARTESIAN_POINT ( 'NONE',  ( -13.45911978172200030, 43.89364414836797579, -1.050976612551407952 ) ) ;
#8377=CARTESIAN_POINT ( 'NONE',  ( 13.50000000000000355, 30.57999999999999829, -4.386415899144233244 ) ) ;
#8378=CARTESIAN_POINT ( 'NONE',  ( -8.343458848123582072, 49.37999999999998835, 11.48378591275254124 ) ) ;
#8381=CARTESIAN_POINT ( 'NONE',  ( -9.946115144241847617, 67.57636767219140950, -9.129800658857289974 ) ) ;
#8383=CARTESIAN_POINT ( 'NONE',  ( 10.93217480255018792, 54.72939847821437098, -7.926001620418541727 ) ) ;
#8384=CARTESIAN_POINT ( 'NONE',  ( -3.235480449190796914, 64.29635529473749500, -13.10656066990217994 ) ) ;
#8386=CARTESIAN_POINT ( 'NONE',  ( -2.138189944381240881, 64.60311857767972299, 13.49999999999999822 ) ) ;
#8387=CARTESIAN_POINT ( 'NONE',  ( -11.84697983171742308, 34.69028098126747750, -6.472949912695511898 ) ) ;
#8390=CARTESIAN_POINT ( 'NONE',  ( 12.02766759040286537, 78.20374727343299526, 6.138006497614846069 ) ) ;
#8391=DIRECTION ( 'NONE',  ( 0.000000000000000000, -1.000000000000000000, 0.000000000000000000 ) ) ;
#8393=CARTESIAN_POINT ( 'NONE',  ( 11.30732042667622217, 72.70668772296686200, -7.376702573910818295 ) ) ;
#8394=CARTESIAN_POINT ( 'NONE',  ( 12.10710496143796000, 78.64972431541795572, -5.972800933619774710 ) ) ;
#8396=CARTESIAN_POINT ( 'NONE',  ( -8.343458848123576743, 64.47999999999998977, -11.48378591275254301 ) ) ;
#8397=CARTESIAN_POINT ( 'NONE',  ( -13.46262499177027649, 52.89525612230203677, -1.006202793444178178 ) ) ;
#8398=CARTESIAN_POINT ( 'NONE',  ( 9.520470885617715595, 43.13000000000000256, 6.917026985038134512 ) ) ;
#8400=CARTESIAN_POINT ( 'NONE',  ( 10.92172942406178926, 59.13000000000000256, 7.935100905948387684 ) ) ;
#8401=EDGE_CURVE ( 'NONE', #760, #10228, #16918, .T. ) ;
#8403=CARTESIAN_POINT ( 'NONE',  ( 9.962334412389218130, 69.07724864637550866, 9.110570040184843066 ) ) ;
#8404=CARTESIAN_POINT ( 'NONE',  ( -1.094976389599479960, 37.21933971898220506, -13.45805156410629166 ) ) ;
#8405=CARTESIAN_POINT ( 'NONE',  ( -13.50000000000000000, 72.92999999999999261, -3.306546357697853733E-15 ) ) ;
#8407=CARTESIAN_POINT ( 'NONE',  ( -8.233788210363634619, 74.36659837790818983, 10.69896094284675847 ) ) ;
#8408=CARTESIAN_POINT ( 'NONE',  ( -7.578294665328167312, 76.46427856810599621, -11.17381362175432358 ) ) ;
#8414=CARTESIAN_POINT ( 'NONE',  ( 9.520470885617715595, 43.13000000000000256, 6.917026985038134512 ) ) ;
#8416=CARTESIAN_POINT ( 'NONE',  ( -2.816865131317705995, 32.57878533943133448, 13.20872976553534173 ) ) ;
#8417=CARTESIAN_POINT ( 'NONE',  ( 13.24501161275586902, 75.52252332348925279, -2.622349305493431704 ) ) ;
#8419=CARTESIAN_POINT ( 'NONE',  ( -6.990220506518823207, 41.42075001818317048, 11.54933267199740499 ) ) ;
#8421=CARTESIAN_POINT ( 'NONE',  ( 1.146149308888379847, 52.13878882479240673, -13.45154095393029792 ) ) ;
#8422=CARTESIAN_POINT ( 'NONE',  ( -0.8900169510020742303, 38.64814324494936670, 13.47797843473638046 ) ) ;
#8423=CARTESIAN_POINT ( 'NONE',  ( 0.000000000000000000, 108.9300000000000068, 0.000000000000000000 ) ) ;
#8424=CARTESIAN_POINT ( 'NONE',  ( -0.4935672077447687545, 55.19774674342932030, -13.49105727626698403 ) ) ;
#8425=CARTESIAN_POINT ( 'NONE',  ( -3.349185717234338444, 49.30034724615263997, -13.08421705775778321 ) ) ;
#8426=CARTESIAN_POINT ( 'NONE',  ( 8.447120960974235260, 63.00251278634441832, 10.55471404757047260 ) ) ;
#8427=CARTESIAN_POINT ( 'NONE',  ( 13.48201631440997161, 42.45403165440193050, -0.6969096715845409795 ) ) ;
#8428=CARTESIAN_POINT ( 'NONE',  ( 5.872522573940052837, 48.96601633533685316, -12.15592568072844948 ) ) ;
#8431=CARTESIAN_POINT ( 'NONE',  ( -7.272992578804307939, 80.47999999999998977, -10.01041549318727064 ) ) ;
#8432=CARTESIAN_POINT ( 'NONE',  ( -2.595053155729497796, 70.27330850474520219, -13.24824729708691251 ) ) ;
#8435=ORIENTED_EDGE ( 'NONE', *, *, #3081, .F. ) ;
#8436=CARTESIAN_POINT ( 'NONE',  ( -8.739346652766617041, 43.51675563888475295, -10.28954507209749814 ) ) ;
#8437=CARTESIAN_POINT ( 'NONE',  ( -7.500000000000000000, 107.9394166107543214, -5.548846425319426068 ) ) ;
#8438=CARTESIAN_POINT ( 'NONE',  ( 13.06095779972256388, 60.55178070539100332, -3.418504200385884761 ) ) ;
#8441=CARTESIAN_POINT ( 'NONE',  ( 3.575946890483998608, 65.80826063327815234, 13.01961353005121325 ) ) ;
#8442=CARTESIAN_POINT ( 'NONE',  ( 5.688864601221035322, 56.88665272175017407, 12.25002412551037345 ) ) ;
#8443=CARTESIAN_POINT ( 'NONE',  ( -7.576616670048093940E-16, 63.67999999999997840, 12.37355403259654985 ) ) ;
#8444=CARTESIAN_POINT ( 'NONE',  ( 13.50000000000000355, 35.58000000000000540, -4.386415899144233244 ) ) ;
#8445=CARTESIAN_POINT ( 'NONE',  ( -11.76794919243112325, 62.78000000000000114, -3.823638476888998827 ) ) ;
#8447=CARTESIAN_POINT ( 'NONE',  ( -13.50089624978355651, 46.93407419958843008, 0.1205557709537223021 ) ) ;
#8448=CARTESIAN_POINT ( 'NONE',  ( 11.21015142536170472, 45.71264101303631122, -7.528624130298565476 ) ) ;
#8449=CARTESIAN_POINT ( 'NONE',  ( 0.000000000000000000, 80.93000000000000682, 0.000000000000000000 ) ) ;
#8451=CARTESIAN_POINT ( 'NONE',  ( 5.712863636558116909, 30.97219126872883166, -12.23179765126074159 ) ) ;
#8452=CARTESIAN_POINT ( 'NONE',  ( -0.4447041180500230784, 56.66422576703538283, 13.50000000034898129 ) ) ;
#8454=CARTESIAN_POINT ( 'NONE',  ( 12.63326194426385740, 33.25766702093661564, 4.760573950502951845 ) ) ;
#8456=CARTESIAN_POINT ( 'NONE',  ( 4.747830034773906860, 40.00896622368698274, -12.63869487930051250 ) ) ;
#8459=CARTESIAN_POINT ( 'NONE',  ( -11.54364396704453455, 62.19215880004057340, 7.031275361532858703 ) ) ;
#8464=CARTESIAN_POINT ( 'NONE',  ( -12.30465744001379491, 44.13348343788968009, 5.561576354214327722 ) ) ;
#8467=CARTESIAN_POINT ( 'NONE',  ( 10.92172942406179104, 33.72999999999999687, -7.935100905948385908 ) ) ;
#8468=CARTESIAN_POINT ( 'NONE',  ( 4.171729424061789260, 49.82999999999999829, 12.83926296998457417 ) ) ;
#8469=CARTESIAN_POINT ( 'NONE',  ( -4.051944394872408317, 46.32562282393774922, -12.87823981119249162 ) ) ;
#8470=CARTESIAN_POINT ( 'NONE',  ( -7.810976174431880636, 67.47450371884892206, -11.01108770444237805 ) ) ;
#8472=CARTESIAN_POINT ( 'NONE',  ( 10.67668064206492673, 54.11596557450559430, 8.261870253898289107 ) ) ;
#8474=CARTESIAN_POINT ( 'NONE',  ( -4.764317252036915917, 64.35142252853242439, -12.63898182757053590 ) ) ;
#8476=CARTESIAN_POINT ( 'NONE',  ( -10.29247617992475305, 34.59463260972069776, -8.736624418168057460 ) ) ;
#8478=ORIENTED_EDGE ( 'NONE', *, *, #12907, .T. ) ;
#8479=CARTESIAN_POINT ( 'NONE',  ( 13.15909340670060956, 78.53732640481597116, -3.027695048772149455 ) ) ;
#8482=CARTESIAN_POINT ( 'NONE',  ( 13.26538156545109715, 72.34104678837115898, 2.525128613255597898 ) ) ;
#8483=CARTESIAN_POINT ( 'NONE',  ( 2.425613699440361870, 79.09278513441491043, -13.28036210628224545 ) ) ;
#8485=CARTESIAN_POINT ( 'NONE',  ( 13.49999999999999822, 63.28000000000000114, 4.386415899144237684 ) ) ;
#8486=CARTESIAN_POINT ( 'NONE',  ( -13.47760860327369770, 52.90318445468975739, -0.7773389074900003415 ) ) ;
#8487=CARTESIAN_POINT ( 'NONE',  ( 11.76794919243112325, 37.28000000000000114, 3.823638476888996607 ) ) ;
#8488=CARTESIAN_POINT ( 'NONE',  ( -4.171729424061787483, 57.32999999999999829, -12.83926296998457417 ) ) ;
#8489=DIRECTION ( 'NONE',  ( 1.000000000000000000, -6.302562568933760152E-16, 0.000000000000000000 ) ) ;
#8491=CARTESIAN_POINT ( 'NONE',  ( 10.59389018096545598, 69.11125758787252948, 8.370637211927217436 ) ) ;
#8492=CARTESIAN_POINT ( 'NONE',  ( -4.025229608893389432, 37.32472329120690802, -12.88605937129256240 ) ) ;
#8493=CARTESIAN_POINT ( 'NONE',  ( 1.551971865843149168, 35.73580183865620086, 13.41075256337061994 ) ) ;
#8495=CARTESIAN_POINT ( 'NONE',  ( -13.47478197652914744, 73.95848700326827441, 0.8248428433375331048 ) ) ;
#8496=CARTESIAN_POINT ( 'NONE',  ( -2.473062413272049120, 76.26891320680448416, -13.27157550910005490 ) ) ;
#8503=CARTESIAN_POINT ( 'NONE',  ( -3.636496289402155746, 42.53000000000000114, 11.19198476289190936 ) ) ;
#8505=CARTESIAN_POINT ( 'NONE',  ( -4.877653597743472957, 32.50418107437187842, 12.58959954281929683 ) ) ;
#8506=CARTESIAN_POINT ( 'NONE',  ( 13.42353994245471149, 75.48170283343853271, -1.486489711945228942 ) ) ;
#8509=CARTESIAN_POINT ( 'NONE',  ( 10.92172942406178926, 80.13000000000000966, 7.935100905948387684 ) ) ;
#8510=PRODUCT_DEFINITION_FORMATION_WITH_SPECIFIED_SOURCE ( 'ANY', '', #16206, .NOT_KNOWN. ) ;
#8511=CARTESIAN_POINT ( 'NONE',  ( 4.226080210030811912, 52.02818700926958684, -12.82458535216174234 ) ) ;
#8512=CARTESIAN_POINT ( 'NONE',  ( -4.231956850230545797, 38.52784562378656830, 12.81957946664639003 ) ) ;
#8513=CARTESIAN_POINT ( 'NONE',  ( 5.747437457432605257, 36.97097174469260494, -12.21544146112736406 ) ) ;
#8515=CARTESIAN_POINT ( 'NONE',  ( -4.638092529099512085, 49.34696448392821111, -12.67954046638503307 ) ) ;
#8516=CARTESIAN_POINT ( 'NONE',  ( 11.58098153987704038, 63.17143452739731657, 6.937646968679790582 ) ) ;
#8517=CARTESIAN_POINT ( 'NONE',  ( 13.47601834983935731, 42.40223155771326446, 0.8051276974000854958 ) ) ;
#8521=CARTESIAN_POINT ( 'NONE',  ( -7.272992578804310604, 66.37999999999999545, 10.01041549318726886 ) ) ;
#8525=EDGE_LOOP ( 'NONE', ( #14331, #17421 ) ) ;
#8527=CARTESIAN_POINT ( 'NONE',  ( -12.47476134584739604, 43.74194706654176201, -5.166698879916627796 ) ) ;
#8528=CARTESIAN_POINT ( 'NONE',  ( -7.500000000000000000, 106.5829119071944575, -7.723695278929459285 ) ) ;
#8529=( BOUNDED_CURVE ( )  B_SPLINE_CURVE ( 2, ( #14776, #10825, #6765, #17357, #5270, #12143, #2489, #8010, #14515, #9077, #7921, #10655, #2319 ),
 .UNSPECIFIED., .F., .F. ) 
 B_SPLINE_CURVE_WITH_KNOTS ( ( 3, 2, 2, 2, 2, 2, 3 ),
 ( 0.1527777777777777624, 0.1555555555555555580, 0.1611111111111111216, 0.1666666666666666574, 0.1722222222222222210, 0.1777777777777777846, 0.1805555555555555525 ),
 .UNSPECIFIED. ) 
 CURVE ( )  GEOMETRIC_REPRESENTATION_ITEM ( )  RATIONAL_B_SPLINE_CURVE ( ( 0.9755282581475765991, 0.9755282581475765991, 1.000000000000000000, 0.9510565162951535312, 1.000000000000000000, 0.9510565162951535312, 1.000000000000000000, 0.9510565162951535312, 1.000000000000000000, 0.9510565162951535312, 1.000000000000000000, 0.9755282581475768211, 0.9755282581475768211 ) ) 
 REPRESENTATION_ITEM ( '' )  );
#8532=CARTESIAN_POINT ( 'NONE',  ( 12.78284368098255541, 66.27342296526084908, 4.345939930100551685 ) ) ;
#8533=CARTESIAN_POINT ( 'NONE',  ( 7.543221400131883136, 56.96276011477866774, 11.19924875908237460 ) ) ;
#8534=CARTESIAN_POINT ( 'NONE',  ( 9.520470885617715595, 58.13000000000000256, 6.917026985038134512 ) ) ;
#8535=CARTESIAN_POINT ( 'NONE',  ( -7.272992578804307939, 71.48000000000000398, -10.01041549318726886 ) ) ;
#8536=CARTESIAN_POINT ( 'NONE',  ( -11.46833886424943572, 46.66385032393301913, -7.122929392610004129 ) ) ;
#8537=CARTESIAN_POINT ( 'NONE',  ( 9.002869684684736029, 45.83076699320872649, -10.06118444092847675 ) ) ;
#8538=CARTESIAN_POINT ( 'NONE',  ( -3.320475467054404886E-07, 70.18000001193918536, -13.49999999999999467 ) ) ;
#8540=CARTESIAN_POINT ( 'NONE',  ( 10.17545303761933084, 30.77154226042120300, -8.873128808189237660 ) ) ;
#8541=CARTESIAN_POINT ( 'NONE',  ( -5.357411621921722045, 56.48603353374912217, 12.39176923702621735 ) ) ;
#8542=CARTESIAN_POINT ( 'NONE',  ( -3.437742735893688728, 50.55636824846342137, 13.05557927389223494 ) ) ;
#8543=CARTESIAN_POINT ( 'NONE',  ( 10.11142744917618508, 33.08470593442759622, 8.956104572044239376 ) ) ;
#8546=ORIENTED_EDGE ( 'NONE', *, *, #6216, .F. ) ;
#8547=CARTESIAN_POINT ( 'NONE',  ( -13.47511189851588931, 61.90170573638860674, -0.8193731989312416086 ) ) ;
#8551=CARTESIAN_POINT ( 'NONE',  ( -13.45089070962791489, 43.97009932163807377, 1.157149274454969401 ) ) ;
#8553=CARTESIAN_POINT ( 'NONE',  ( 13.49999999999999822, 36.27999999999999403, 4.386415899144237684 ) ) ;
#8554=CARTESIAN_POINT ( 'NONE',  ( -0.2540371354857682284, 46.18913186441219665, -13.49794113769755555 ) ) ;
#8555=CARTESIAN_POINT ( 'NONE',  ( -10.09036394839171003, 67.58397492445097043, -8.968536542104889264 ) ) ;
#8558=CARTESIAN_POINT ( 'NONE',  ( 10.14209061328275752, 54.08650388490638505, 8.919889534789382068 ) ) ;
#8559=ORIENTED_EDGE ( 'NONE', *, *, #5983, .T. ) ;
#8560=CARTESIAN_POINT ( 'NONE',  ( -0.2710101708259924358, 64.18974430090325711, -13.49761915939118317 ) ) ;
#8562=CARTESIAN_POINT ( 'NONE',  ( 5.339658159925267711, 66.98672795088741339, -12.39911587653581293 ) ) ;
#8563=CARTESIAN_POINT ( 'NONE',  ( -3.202417373558799074, 34.29514631974450367, -13.11514094275671383 ) ) ;
#8565=CARTESIAN_POINT ( 'NONE',  ( 12.71205548718733702, 78.26577299247003339, 4.546657709176281870 ) ) ;
#8568=CARTESIAN_POINT ( 'NONE',  ( 11.46276161444878383, 72.16349900300471631, 7.131289053549557444 ) ) ;
#8570=CARTESIAN_POINT ( 'NONE',  ( -13.49999999999999822, 64.78000000000000114, -4.386415899144240349 ) ) ;
#8571=CARTESIAN_POINT ( 'NONE',  ( -2.527007466902615462, 52.27086174099205351, -13.26155452052046080 ) ) ;
#8573=CARTESIAN_POINT ( 'NONE',  ( -9.520470885617717371, 39.23000000000000398, 6.917026985038133624 ) ) ;
#8574=CARTESIAN_POINT ( 'NONE',  ( 13.50000000000000000, 53.43000000000000682, 1.653273178848926867E-15 ) ) ;
#8578=CARTESIAN_POINT ( 'NONE',  ( 11.63057281378106289, 69.17483938076107108, 6.854191306154013397 ) ) ;
#8580=CARTESIAN_POINT ( 'NONE',  ( -10.92172942406179104, 79.23000000000000398, 7.935100905948387684 ) ) ;
#8582=CARTESIAN_POINT ( 'NONE',  ( -13.46249943993917775, 73.96494795259233967, 1.009710742264189332 ) ) ;
#8585=FACE_OUTER_BOUND ( 'NONE', #10146, .T. ) ;
#8586=CYLINDRICAL_SURFACE ( 'NONE', #12513, 13.50000000000000000 ) ;
#8589=CARTESIAN_POINT ( 'NONE',  ( -7.272992578804307939, 35.47999999999999687, -10.01041549318727064 ) ) ;
#8591=CARTESIAN_POINT ( 'NONE',  ( -11.23704444756839216, 32.21100520952357016, 7.482062774987143783 ) ) ;
#8592=CARTESIAN_POINT ( 'NONE',  ( 6.301401044479416846, 74.91092896658807376, 11.94220124380246162 ) ) ;
#8594=CARTESIAN_POINT ( 'NONE',  ( -13.50000000000000000, 81.93000000000000682, -3.306546357697853733E-15 ) ) ;
#8595=CARTESIAN_POINT ( 'NONE',  ( 0.8749885751862738203, 52.14854123505212158, -13.47204428328692849 ) ) ;
#8598=CARTESIAN_POINT ( 'NONE',  ( 0.3867960985429125254, 37.16609886577710853, -13.49524483310550060 ) ) ;
#8599=CARTESIAN_POINT ( 'NONE',  ( -7.500000000000000000, 98.93000000000002103, -8.999999999999996447 ) ) ;
#8600=CARTESIAN_POINT ( 'NONE',  ( -3.695260882689679338, 49.31284492995563795, -12.98818747258629536 ) ) ;
#8601=CARTESIAN_POINT ( 'NONE',  ( 2.626233336093215076, 62.77444219063707465, 13.24209077638737675 ) ) ;
#8602=LINE ( 'NONE', #6204, #13608 ) ;
#8603=CARTESIAN_POINT ( 'NONE',  ( 8.545810036750047800, 48.85228211165327394, -10.45080393046335132 ) ) ;
#8606=CARTESIAN_POINT ( 'NONE',  ( -11.76794919243112325, 65.93000000000000682, -2.882316262207890869E-15 ) ) ;
#8611=CARTESIAN_POINT ( 'NONE',  ( -0.4867513977796573132, 43.19750178289612563, -13.49122469273548575 ) ) ;
#8612=DIRECTION ( 'NONE',  ( 0.000000000000000000, -1.000000000000000000, 0.000000000000000000 ) ) ;
#8615=CARTESIAN_POINT ( 'NONE',  ( 5.757975047644410260, 65.88943174946119541, 12.21048708421974816 ) ) ;
#8616=CARTESIAN_POINT ( 'NONE',  ( -13.50000000000000000, 79.93000000000000682, -3.306546357697853733E-15 ) ) ;
#8617=CARTESIAN_POINT ( 'NONE',  ( -3.636496289402155746, 60.53000000000000114, 11.19198476289190936 ) ) ;
#8618=CARTESIAN_POINT ( 'NONE',  ( 11.76794919243112325, 58.28000000000000114, 3.823638476888996607 ) ) ;
#8619=CARTESIAN_POINT ( 'NONE',  ( -11.32173173042431991, 46.65434610059125475, -7.353121830783978297 ) ) ;
#8620=CARTESIAN_POINT ( 'NONE',  ( 10.63213266513623978, 45.74654076961098070, -8.319152667901684950 ) ) ;
#8621=CARTESIAN_POINT ( 'NONE',  ( 7.721945602315970270, 69.88954231929918137, -11.07992460466698681 ) ) ;
#8624=CARTESIAN_POINT ( 'NONE',  ( 6.449393272122638798, 30.94317789798385121, -11.86697286938268725 ) ) ;
#8625=CARTESIAN_POINT ( 'NONE',  ( -13.38148664391157361, 55.99414316929159696, 1.834830169894675844 ) ) ;
#8626=DIRECTION ( 'NONE',  ( 0.000000000000000000, 0.000000000000000000, -1.000000000000000000 ) ) ;
#8628=CARTESIAN_POINT ( 'NONE',  ( 1.628308837847167748E-06, 32.68004529479373588, 13.49999999999980460 ) ) ;
#8629=CARTESIAN_POINT ( 'NONE',  ( -0.5902394228252099140, 73.20122283213095216, -13.49999999999999289 ) ) ;
#8630=CARTESIAN_POINT ( 'NONE',  ( 9.828641339704693891, 39.78975999636411132, -9.256972243478518436 ) ) ;
#8631=ORIENTED_EDGE ( 'NONE', *, *, #4346, .F. ) ;
#8632=CARTESIAN_POINT ( 'NONE',  ( -12.74970089692343045, 62.09010389230079596, 4.438088001292920026 ) ) ;
#8633=( BOUNDED_CURVE ( )  B_SPLINE_CURVE ( 2, ( #9481, #2896, #8241, #5496, #14827, #1581, #14658, #12027, #1316, #8149, #268, #2546, #7975 ),
 .UNSPECIFIED., .F., .T. ) 
 B_SPLINE_CURVE_WITH_KNOTS ( ( 3, 2, 2, 2, 2, 2, 3 ),
 ( 0.9027777777777777901, 0.9055555555555555580, 0.9111111111111110938, 0.9166666666666666297, 0.9222222222222222765, 0.9277777777777778123, 0.9305555555555555802 ),
 .UNSPECIFIED. ) 
 CURVE ( )  GEOMETRIC_REPRESENTATION_ITEM ( )  RATIONAL_B_SPLINE_CURVE ( ( 0.9755282581475768211, 0.9755282581475768211, 1.000000000000000000, 0.9510565162951535312, 1.000000000000000000, 0.9510565162951535312, 1.000000000000000000, 0.9510565162951535312, 1.000000000000000000, 0.9510565162951535312, 1.000000000000000000, 0.9755282581475768211, 0.9755282581475768211 ) ) 
 REPRESENTATION_ITEM ( '' )  );
#8637=CARTESIAN_POINT ( 'NONE',  ( 9.670042864717805386, 48.06219784168897036, 9.420394723061004782 ) ) ;
#8639=CARTESIAN_POINT ( 'NONE',  ( -10.92172942406178926, 37.62999999999999545, -7.935100905948389460 ) ) ;
#8640=CARTESIAN_POINT ( 'NONE',  ( -8.343458848123576743, 42.47999999999999687, -11.48378591275254301 ) ) ;
#8641=CARTESIAN_POINT ( 'NONE',  ( -7.112170435543458069, 46.44454114888061724, -11.48319410635906479 ) ) ;
#8642=CARTESIAN_POINT ( 'NONE',  ( -7.930396875273861390, 67.47978613725511821, -10.92539274502803259 ) ) ;
#8644=CARTESIAN_POINT ( 'NONE',  ( 5.585949171536172209, 53.88247118449140061, 12.30201563545229781 ) ) ;
#8646=CARTESIAN_POINT ( 'NONE',  ( -8.208207767219146689, 64.49222101755708536, -10.71938957358478461 ) ) ;
#8647=ORIENTED_EDGE ( 'NONE', *, *, #9376, .F. ) ;
#8649=CARTESIAN_POINT ( 'NONE',  ( -7.797167812233946727, 34.47380972907037489, -11.02479444021394350 ) ) ;
#8651=CARTESIAN_POINT ( 'NONE',  ( 9.010525653276635794, 78.02962374744581098, 10.05410809128824745 ) ) ;
#8652=CARTESIAN_POINT ( 'NONE',  ( 1.753268986668952691E-06, 80.68004880551006863, 13.49999999999977263 ) ) ;
#8653=DIRECTION ( 'NONE',  ( 0.000000000000000000, 0.000000000000000000, 1.000000000000000000 ) ) ;
#8655=CARTESIAN_POINT ( 'NONE',  ( 12.94854022286095763, 72.56673908956170749, -3.819461041215378660 ) ) ;
#8658=CARTESIAN_POINT ( 'NONE',  ( 4.171729424061791924, 67.03000000000000114, -12.83926296998457239 ) ) ;
#8659=CARTESIAN_POINT ( 'NONE',  ( -7.714235717713363805, 52.46982633924920947, -11.10504961456102357 ) ) ;
#8660=CARTESIAN_POINT ( 'NONE',  ( 2.272985001014427788E-15, 41.17999999999999972, -12.37355403259654985 ) ) ;
#8662=CARTESIAN_POINT ( 'NONE',  ( 13.50000000000000355, 53.57999999999999829, -4.386415899144233244 ) ) ;
#8663=CARTESIAN_POINT ( 'NONE',  ( 0.9450715873491259966, 50.71399393198645811, 13.47525569251407518 ) ) ;
#8665=CARTESIAN_POINT ( 'NONE',  ( 5.110268676760429507, 68.86456870269141461, 12.49542038485116535 ) ) ;
#8667=CARTESIAN_POINT ( 'NONE',  ( -8.891200544363830713E-16, 70.68000000000000682, 13.50000000000000000 ) ) ;
#8669=CARTESIAN_POINT ( 'NONE',  ( -13.42711900164165861, 73.88114203177188699, -1.405880853923186180 ) ) ;
#8670=AXIS2_PLACEMENT_3D ( 'NONE', #14156, #15475, #4549 ) ;
#8671=CARTESIAN_POINT ( 'NONE',  ( -9.171191987446322358, 76.53731527584839966, -9.908219757055420018 ) ) ;
#8672=CARTESIAN_POINT ( 'NONE',  ( -1.545162525932825686E-06, 79.18000005555833809, -13.49999999999990941 ) ) ;
#8673=CARTESIAN_POINT ( 'NONE',  ( 0.000000000000000000, 80.93000000000000682, 0.000000000000000000 ) ) ;
#8676=CARTESIAN_POINT ( 'NONE',  ( -9.520470885617717371, 42.22999999999999687, 6.917026985038133624 ) ) ;
#8677=CARTESIAN_POINT ( 'NONE',  ( -8.992656840795357098, 32.33142381460860548, 10.07316879344405791 ) ) ;
#8678=CARTESIAN_POINT ( 'NONE',  ( 1.328803061132558749, 74.72777884802709991, 13.43444388716402038 ) ) ;
#8679=EDGE_CURVE ( 'NONE', #3801, #8975, #16621, .T. ) ;
#8680=CARTESIAN_POINT ( 'NONE',  ( -0.2851956912289982382, 53.66974537925386102, 13.49700562860493314 ) ) ;
#8681=CARTESIAN_POINT ( 'NONE',  ( -7.272992578804307939, 32.47999999999999687, -10.01041549318726886 ) ) ;
#8682=CARTESIAN_POINT ( 'NONE',  ( 3.968858122459704152, 52.03755112169107377, -12.90597491634626870 ) ) ;
#8683=CARTESIAN_POINT ( 'NONE',  ( -4.870330804223598875, 38.50445280852472507, 12.59249463255201462 ) ) ;
#8684=CARTESIAN_POINT ( 'NONE',  ( 5.672580605102411688, 36.97381777227605681, -12.25043497061033015 ) ) ;
#8685=DIRECTION ( 'NONE',  ( 0.000000000000000000, 0.000000000000000000, 1.000000000000000000 ) ) ;
#8687=CARTESIAN_POINT ( 'NONE',  ( 10.21212867364205046, 63.09039058033595637, 8.832471590444903597 ) ) ;
#8688=CARTESIAN_POINT ( 'NONE',  ( 6.884270893848766448, 41.93466036346448789, 11.62526077269765601 ) ) ;
#8689=CARTESIAN_POINT ( 'NONE',  ( 11.58339546198362591, 48.68871274354637535, -6.950020419437135111 ) ) ;
#8692=CARTESIAN_POINT ( 'NONE',  ( -7.272992578804307939, 71.48000000000000398, -10.01041549318727064 ) ) ;
#8700=CARTESIAN_POINT ( 'NONE',  ( 8.134860252326546970, 65.98893604550748648, 10.77385971222135552 ) ) ;
#8702=CARTESIAN_POINT ( 'NONE',  ( -11.76794919243112325, 53.77999999999999403, -3.823638476888998827 ) ) ;
#8703=CARTESIAN_POINT ( 'NONE',  ( -13.49999999999999822, 34.07999999999999829, 4.386415899144235908 ) ) ;
#8704=CARTESIAN_POINT ( 'NONE',  ( -11.76794919243112325, 59.77999999999998693, -3.823638476888998827 ) ) ;
#8705=CARTESIAN_POINT ( 'NONE',  ( -9.913970262008090728, 46.57449140322882641, -9.165228541796420103 ) ) ;
#8707=CARTESIAN_POINT ( 'NONE',  ( 10.67523966630402121, 45.74411538286880585, -8.263863657552700914 ) ) ;
#8708=CARTESIAN_POINT ( 'NONE',  ( 5.565866721395538619, 69.97797074884671531, -12.29937346137027632 ) ) ;
#8709=CARTESIAN_POINT ( 'NONE',  ( 1.832901445459844014, 31.11425710500970254, -13.38003086484803106 ) ) ;
#8710=CARTESIAN_POINT ( 'NONE',  ( -10.58832603877217871, 56.24920692690567137, 8.377620954876409343 ) ) ;
#8711=DIRECTION ( 'NONE',  ( 0.000000000000000000, -1.000000000000000000, 0.000000000000000000 ) ) ;
#8712=CARTESIAN_POINT ( 'NONE',  ( 9.818219314833713796, 33.06951371705229548, 9.274956680371715834 ) ) ;
#8713=CARTESIAN_POINT ( 'NONE',  ( 4.083253397203186807, 43.03321070571565343, -12.86830022185737477 ) ) ;
#8714=CARTESIAN_POINT ( 'NONE',  ( 8.099268731515945063, 39.87266764020058218, -10.80082015226388314 ) ) ;
#8716=CARTESIAN_POINT ( 'NONE',  ( -11.14572871157717593, 62.21664499426510275, 7.617379339931979132 ) ) ;
#8717=ORIENTED_EDGE ( 'NONE', *, *, #10666, .F. ) ;
#8720=EDGE_CURVE ( 'NONE', #14307, #5870, #2866, .T. ) ;
#8721=CARTESIAN_POINT ( 'NONE',  ( 7.053763874080417828, 47.94203897529205705, 11.51277963570407792 ) ) ;
#8722=CARTESIAN_POINT ( 'NONE',  ( 4.049944587781194372, 58.03463076063811599, -12.88329806241152298 ) ) ;
#8723=CARTESIAN_POINT ( 'NONE',  ( -13.50000000000000000, 31.92999999999999972, -3.306546357697853733E-15 ) ) ;
#8724=CARTESIAN_POINT ( 'NONE',  ( 4.171729424061791924, 42.03000000000000114, -12.83926296998457239 ) ) ;
#8726=AXIS2_PLACEMENT_3D ( 'NONE', #5746, #4407, #8314 ) ;
#8730=CARTESIAN_POINT ( 'NONE',  ( 10.70119226595359585, 54.11735038901769457, 8.230103751483696328 ) ) ;
#8734=VERTEX_POINT ( 'NONE', #7050 ) ;
#8736=CARTESIAN_POINT ( 'NONE',  ( -3.526270707235371837, 34.30679044915609666, -13.03322718403512326 ) ) ;
#8738=AXIS2_PLACEMENT_3D ( 'NONE', #8207, #1286, #12079 ) ;
#8739=CARTESIAN_POINT ( 'NONE',  ( 9.433938897025715420, 78.05027556318721338, 9.660859765897237494 ) ) ;
#8740=CARTESIAN_POINT ( 'NONE',  ( 2.138189944381242213, 48.10311857767972299, -13.49999999999999822 ) ) ;
#8744=CARTESIAN_POINT ( 'NONE',  ( 12.97739931409362235, 72.56301366025002153, -3.719884340965235126 ) ) ;
#8746=CARTESIAN_POINT ( 'NONE',  ( -13.49999999999999822, 62.07999999999999119, 4.386415899144235908 ) ) ;
#8747=CARTESIAN_POINT ( 'NONE',  ( -5.127610894157791144, 52.36511171218869265, -12.49413350819052582 ) ) ;
#8748=CARTESIAN_POINT ( 'NONE',  ( 9.520470885617717371, 40.72999999999999687, -6.917026985038131848 ) ) ;
#8750=CARTESIAN_POINT ( 'NONE',  ( 13.50000000000000000, 56.42999999999999972, 1.653273178848926867E-15 ) ) ;
#8751=CARTESIAN_POINT ( 'NONE',  ( 10.92172942406179104, 77.73000000000000398, -7.935100905948385908 ) ) ;
#8752=AXIS2_PLACEMENT_3D ( 'NONE', #6740, #5413, #5596 ) ;
#8754=CARTESIAN_POINT ( 'NONE',  ( -4.574181969382655311, 68.51537738898377938, 12.70201094514906970 ) ) ;
#8756=CARTESIAN_POINT ( 'NONE',  ( -1.844924112955495524E-14, 72.18000000000000682, -13.50000000000000000 ) ) ;
#8758=CARTESIAN_POINT ( 'NONE',  ( -13.46880766683457686, 73.96184857042898386, 0.9211851228833413119 ) ) ;
#8763=CARTESIAN_POINT ( 'NONE',  ( -7.576616670048093940E-16, 36.67999999999999972, 12.37355403259654807 ) ) ;
#8765=CARTESIAN_POINT ( 'NONE',  ( -1.567828446471241755, 32.62365072876585970, 13.40870118950181400 ) ) ;
#8768=CARTESIAN_POINT ( 'NONE',  ( -0.3449943859400333435, 53.66759530121692734, 13.49560261416635498 ) ) ;
#8770=CARTESIAN_POINT ( 'NONE',  ( 2.607531440858944223E-15, 81.18000000000000682, -14.19474002721660355 ) ) ;
#8771=CARTESIAN_POINT ( 'NONE',  ( 13.14200413229988129, 51.53974922401104664, -3.092116881306331333 ) ) ;
#8772=CARTESIAN_POINT ( 'NONE',  ( -7.051585598576367353, 38.41817575276711949, 11.51199000259391703 ) ) ;
#8775=CARTESIAN_POINT ( 'NONE',  ( 1.653273178848926472E-15, 80.93000000000000682, 13.50000000000000000 ) ) ;
#8776=FACE_BOUND ( 'NONE', #9238, .T. ) ;
#8777=CARTESIAN_POINT ( 'NONE',  ( 0.2771608746823925329, 62.68996565959619716, 13.49715969379329472 ) ) ;
#8778=DIRECTION ( 'NONE',  ( 0.000000000000000000, -1.000000000000000000, 0.000000000000000000 ) ) ;
#8779=CARTESIAN_POINT ( 'NONE',  ( 13.23997872644318896, 48.52304506666694550, -2.636916081698648107 ) ) ;
#8782=CARTESIAN_POINT ( 'NONE',  ( -7.272992578804310604, 69.37999999999999545, 10.01041549318726886 ) ) ;
#8785=CARTESIAN_POINT ( 'NONE',  ( -0.9595081608899134196, 43.21449727781597971, -13.46834895437819135 ) ) ;
#8786=CARTESIAN_POINT ( 'NONE',  ( -2.648919002459650063, 80.92999999999994998, -12.65678160791745022 ) ) ;
#8789=CARTESIAN_POINT ( 'NONE',  ( -11.76794919243112325, 50.92999999999999972, -2.882316262207890869E-15 ) ) ;
#8791=CARTESIAN_POINT ( 'NONE',  ( -12.04654261135511639, 59.15468403854464441, 6.098114165576594914 ) ) ;
#8792=CARTESIAN_POINT ( 'NONE',  ( 12.88012409951591586, 45.57522996959129102, -4.047174811376564207 ) ) ;
#8793=B_SPLINE_CURVE_WITH_KNOTS ( 'NONE', 3,
 ( #13134, #1277, #2677, #5364, #3849, #8109, #13474, #14442, #1360, #6776, #9265, #6608, #10409, #5104, #5193, #3675, #17196, #11987, #10749, #9089, #7760, #1022, #16113, #6523, #11817, #4024, #10581, #13388, #10496, #15942, #2502, #14526, #15859, #2413, #6689, #3766, #1107, #9178, #7846, #13219, #11902, #17279, #7931, #13305, #9439, #1196, #17368, #5282, #10665, #3937, #9352, #2590, #16201, #3033, #1799, #13903, #11191, #5451, #14870, #12426, #10836, #2946, #4112, #9526, #5807, #6869, #1629, #12244, #2764, #228, #4203, #8197, #8464, #7211, #46, #9614, #16475, #13560, #1450, #137, #7128, #5544, #1539, #10927, #16387, #8551, #16295, #7047, #14964, #2854, #11016, #5633, #8288, #9789, #11102, #15049, #312, #13645, #4291, #6957, #12335, #9702, #8375, #13731, #5720, #4381, #15136, #13816, #1717, #16567, #12516, #400, #4473, #9877, #15228, #3125, #14848, #13876, #8527, #9675, #7020, #287, #9762, #16539, #1689, #10899, #202, #5517, #13790, #15025, #7186, #12488, #6930, #12575, #11164, #10989, #8436, #6841, #16358, #2918, #14938, #4265, #4353, #16270, #12217, #10812, #5608, #7104, #4085, #1604, #2741, #8171, #5423, #5779, #12308, #16175, #13534, #9501, #15107, #1424, #4446, #111, #4176, #9588, #8348, #16450, #3006, #13621, #2830, #8261, #13704, #1514, #12399, #9853, #5696, #11077, #15200, #3100, #632, #4619, #3189, #9939, #8785, #1859, #12656, #8611, #2111, #11336, #5871, #4705, #13963, #1943, #16713, #16798, #8954, #16629, #7455, #7273, #4532, #11427 ),
 .UNSPECIFIED., .F., .F.,
 ( 4, 2, 1, 2, 2, 1, 2, 2, 2, 2, 2, 2, 2, 2, 2, 2, 2, 2, 1, 2, 2, 2, 2, 2, 1, 1, 1, 2, 2, 2, 2, 1, 1, 1, 2, 2, 1, 2, 2, 2, 2, 1, 2, 2, 1, 1, 1, 2, 2, 2, 2, 2, 2, 1, 1, 1, 1, 2, 2, 2, 1, 2, 2, 2, 2, 1, 2, 2, 1, 1, 2, 2, 1, 2, 2, 1, 1, 2, 2, 2, 1, 1, 1, 2, 2, 1, 2, 2, 2, 2, 1, 2, 2, 1, 1, 2, 2, 2, 2, 2, 1, 2, 1, 2, 2, 1, 1, 2, 2, 2, 1, 2, 2, 1, 1, 2, 1, 2, 2, 4 ),
 ( 0.7109395711855112099, 0.7111682227467994721, 0.7112253856371215655, 0.7112539670822826121, 0.7112682578048631354, 0.7112825485274436588, 0.7113968743080877344, 0.7118541774306642589, 0.7127687836758173079, 0.7136833899209703569, 0.7139120414822586191, 0.7141406930435468814, 0.7145979961661234059, 0.7155126024112765659, 0.7159699055338530904, 0.7161985570951413527, 0.7162271385403022883, 0.7162557199854633350, 0.7163128828757854283, 0.7164272086564296149, 0.7173418149015825529, 0.7182564211467356019, 0.7187137242693121264, 0.7187280149918926497, 0.7187423057144731731, 0.7187708871596342197, 0.7188280500499563130, 0.7189423758306004997, 0.7191710273918888729, 0.7196283305144656195, 0.7198569820757539928, 0.7199141449660760861, 0.7199427264112371327, 0.7199570171338176561, 0.7199641624951078622, 0.7199677351757530763, 0.7199713078563981794, 0.7200856336370424771, 0.7210002398821965253, 0.7211145656628408229, 0.7212288914434851206, 0.7214575430047736049, 0.7219148461273506845, 0.7228294523725047327, 0.7232867554950818123, 0.7235154070563702966, 0.7236297328370145943, 0.7236868957273367986, 0.7237440586176588919, 0.7246586648628129401, 0.7248873164241015354, 0.7249444793144236288, 0.7249587700370041521, 0.7249730607595846754, 0.7250016422047458331, 0.7251159679853900197, 0.7255732711079670993, 0.7260305742305441790, 0.7261449000111884766, 0.7262020629015105699, 0.7262592257918326633, 0.7264878773531212586, 0.7274024835982753068, 0.7283170898434294660, 0.7285457414047180613, 0.7286600671853622480, 0.7286743579079427713, 0.7286886486305232946, 0.7287172300756844523, 0.7287743929660065456, 0.7292316960885836252, 0.7310609085788918327, 0.7311180714692140370, 0.7311466529143750837, 0.7311752343595361303, 0.7312895601401804280, 0.7315182117014689123, 0.7319755148240459919, 0.7328901210692001511, 0.7333474241917772307, 0.7335760757530658260, 0.7336332386433879194, 0.7336475293659684427, 0.7336546747272587599, 0.7336618200885489660, 0.7336904015337100127, 0.7338047273143543103, 0.7347193335595083585, 0.7356339398046622957, 0.7360912429272392643, 0.7361198243724004220, 0.7361341150949809453, 0.7361484058175614686, 0.7362055687078835620, 0.7363198944885278596, 0.7365485460498163439, 0.7370058491723933125, 0.7372345007336817968, 0.7373488265143259834, 0.7374059894046481878, 0.7374631522949702811, 0.7383777585401242183, 0.7386064101014127026, 0.7386349915465737492, 0.7386492822691542726, 0.7386635729917347959, 0.7387207358820570002, 0.7388350616627011869, 0.7392923647852781555, 0.7397496679078551240, 0.7398639936884994217, 0.7398782844110799450, 0.7398925751336604684, 0.7399211565788215150, 0.7399783194691436083, 0.7400926452497877950, 0.7401498081401099993, 0.7401783895852710460, 0.7401926803078515693, 0.7402069710304320926 ),
 .UNSPECIFIED. ) ;
#8794=CARTESIAN_POINT ( 'NONE',  ( 8.071977012489314873, 69.87388874300927455, -10.82096426686017665 ) ) ;
#8796=CARTESIAN_POINT ( 'NONE',  ( 12.00366664929724969, 30.65787929842621651, -6.177632669743041482 ) ) ;
#8797=ADVANCED_FACE ( 'NONE', ( #15577 ), #10223, .T. ) ;
#8798=CARTESIAN_POINT ( 'NONE',  ( -12.73519230341753961, 56.09167882185248288, 4.479426581004548602 ) ) ;
#8799=CARTESIAN_POINT ( 'NONE',  ( -2.973539139891043348, 50.57300316080052482, 13.17058001520311805 ) ) ;
#8800=CARTESIAN_POINT ( 'NONE',  ( 4.129670684472704245, 32.82848721344360854, 12.85288430302258256 ) ) ;
#8801=CARTESIAN_POINT ( 'NONE',  ( 5.614818628722479055, 42.97613777251347500, -12.27697129638437268 ) ) ;
#8802=CARTESIAN_POINT ( 'NONE',  ( 12.90854670894318268, 39.57182124627381370, -3.955391283021399751 ) ) ;
#8804=CARTESIAN_POINT ( 'NONE',  ( -13.24278598375631510, 61.83745329285113002, -2.622749156585664210 ) ) ;
#8805=EDGE_LOOP ( 'NONE', ( #15394, #7753 ) ) ;
#8809=CARTESIAN_POINT ( 'NONE',  ( 10.71586849478361536, 48.11818100869080439, 8.210984778465897804 ) ) ;
#8810=CARTESIAN_POINT ( 'NONE',  ( 2.469740553831996976, 58.09120330256963172, -13.27217913048357723 ) ) ;
#8811=CARTESIAN_POINT ( 'NONE',  ( 7.866550464026706102, 78.88325915401534871, -10.98022871454362281 ) ) ;
#8812=CARTESIAN_POINT ( 'NONE',  ( -7.576616670048093940E-16, 75.67999999999999261, 12.37355403259654985 ) ) ;
#8814=MANIFOLD_SOLID_BREP ( 'Chamfer1', #11991 ) ;
#8815=CARTESIAN_POINT ( 'NONE',  ( -9.672208996725832009, 46.56228947212231617, -9.418029512036609319 ) ) ;
#8816=EDGE_CURVE ( 'NONE', #668, #13318, #15140, .T. ) ;
#8817=CARTESIAN_POINT ( 'NONE',  ( 6.750022565184456980, 31.92926174983938026, 11.69132992304556495 ) ) ;
#8819=CARTESIAN_POINT ( 'NONE',  ( 8.150611293951293135, 53.98965040082899947, 10.77109208829301323 ) ) ;
#8824=CARTESIAN_POINT ( 'NONE',  ( 5.407998797888095233, 66.98416787033841047, -12.36956158942780704 ) ) ;
#8826=CARTESIAN_POINT ( 'NONE',  ( 1.982521523170245906E-06, 77.68005525700222336, 13.49999999999970690 ) ) ;
#8827=CARTESIAN_POINT ( 'NONE',  ( -3.733449871309725498, 59.54576182871864631, 12.97394819335584337 ) ) ;
#8829=DIRECTION ( 'NONE',  ( 1.000000000000000000, 8.673617379884035472E-17, 0.000000000000000000 ) ) ;
#8831=CARTESIAN_POINT ( 'NONE',  ( 13.34200449954298939, 72.35767147386656006, 2.065204973313191861 ) ) ;
#8832=CARTESIAN_POINT ( 'NONE',  ( 8.336922857196812586, 66.86199470162991076, -10.62209661523931814 ) ) ;
#8834=CARTESIAN_POINT ( 'NONE',  ( -13.49999999999999822, 56.07999999999999119, 4.386415899144235908 ) ) ;
#8835=CARTESIAN_POINT ( 'NONE',  ( -2.425051341520653825, 52.26719589608618577, -13.28041211626022644 ) ) ;
#8837=CARTESIAN_POINT ( 'NONE',  ( -13.49999999999999822, 51.78000000000000114, -4.386415899144240349 ) ) ;
#8840=CARTESIAN_POINT ( 'NONE',  ( -6.210469887590529758, 68.45252731434959514, 11.99403323395378607 ) ) ;
#8843=CARTESIAN_POINT ( 'NONE',  ( 10.92172942406178926, 71.12999999999999545, 7.935100905948387684 ) ) ;
#8845=CARTESIAN_POINT ( 'NONE',  ( -5.251609085175493519, 65.49012858565386352, 12.43669339650761607 ) ) ;
#8850=CARTESIAN_POINT ( 'NONE',  ( 13.50000000000000000, 50.42999999999999972, 1.653273178848926867E-15 ) ) ;
#8852=CARTESIAN_POINT ( 'NONE',  ( -12.95000749831451969, 31.79345314003229817, -3.814302809370596847 ) ) ;
#8853=CARTESIAN_POINT ( 'NONE',  ( 9.825225734620730123, 75.07017187311475936, 9.260671064715687351 ) ) ;
#8856=CARTESIAN_POINT ( 'NONE',  ( 2.607531440858944223E-15, 75.17999999999997840, -14.19474002721660355 ) ) ;
#8857=CARTESIAN_POINT ( 'NONE',  ( 13.40294794219552621, 51.48823289360313282, -1.671099717773980586 ) ) ;
#8858=CARTESIAN_POINT ( 'NONE',  ( -13.50005243685980183, 37.92238217705867953, -0.2158979556258536492 ) ) ;
#8861=CARTESIAN_POINT ( 'NONE',  ( 11.98477050297872104, 36.65933795633807790, -6.214151509854474398 ) ) ;
#8864=CARTESIAN_POINT ( 'NONE',  ( -12.38439141012284139, 77.12633956890614684, 5.378321227196528831 ) ) ;
#8865=CARTESIAN_POINT ( 'NONE',  ( 4.178864255851000829E-14, 61.67999999999999261, 13.50000000000000000 ) ) ;
#8866=CARTESIAN_POINT ( 'NONE',  ( 3.201461801489201786, 41.79502229956779047, 13.11535449225857519 ) ) ;
#8867=CARTESIAN_POINT ( 'NONE',  ( 13.23077815530012025, 48.52472391739948421, -2.682647111088163339 ) ) ;
#8870=CARTESIAN_POINT ( 'NONE',  ( -7.272992578804307939, 62.47999999999999687, -10.01041549318727064 ) ) ;
#8872=CARTESIAN_POINT ( 'NONE',  ( -8.291044507619272909E-14, 57.17999999999999972, -13.50000000000000000 ) ) ;
#8874=CYLINDRICAL_SURFACE ( 'NONE', #15843, 13.50000000000000000 ) ;
#8876=CARTESIAN_POINT ( 'NONE',  ( 3.231997696289118593, 65.79610242286665311, 13.10760892499458308 ) ) ;
#8877=CARTESIAN_POINT ( 'NONE',  ( -8.343458848123582072, 80.37999999999999545, 11.48378591275254124 ) ) ;
#8878=CARTESIAN_POINT ( 'NONE',  ( -3.636496289402155746, 45.53000000000000114, 11.19198476289190936 ) ) ;
#8879=CARTESIAN_POINT ( 'NONE',  ( -13.49458077393223832, 58.94641242465065289, 0.4787677073000579098 ) ) ;
#8880=CARTESIAN_POINT ( 'NONE',  ( 13.35249357306756046, 45.35820753028740882, 2.049345934875174802 ) ) ;
#8882=CARTESIAN_POINT ( 'NONE',  ( 1.486929454577674337, 80.73346438489225818, 13.41791445272210126 ) ) ;
#8883=CARTESIAN_POINT ( 'NONE',  ( 13.07011386205427428, 30.55034935990153500, -3.379670409494439198 ) ) ;
#8884=CARTESIAN_POINT ( 'NONE',  ( -13.46192632266902400, 55.96507060572447756, 1.013190883000425924 ) ) ;
#8885=CARTESIAN_POINT ( 'NONE',  ( 10.92172942406178926, 53.12999999999999545, 7.935100905948387684 ) ) ;
#8886=CARTESIAN_POINT ( 'NONE',  ( 2.742138326991311548, 64.08140283275047011, -13.21857401153399003 ) ) ;
#8888=CARTESIAN_POINT ( 'NONE',  ( 13.03162247184152989, 39.55575396952983880, -3.525209484468003307 ) ) ;
#8890=CARTESIAN_POINT ( 'NONE',  ( -8.595979405193384437, 61.50968794902038894, -10.42067916570242581 ) ) ;
#8895=CARTESIAN_POINT ( 'NONE',  ( 13.06477345830753833, 48.30888743458975654, 3.400253739448160228 ) ) ;
#8896=CARTESIAN_POINT ( 'NONE',  ( 11.47375603530613830, 57.69570350741216203, -7.113939845970555176 ) ) ;
#8897=CARTESIAN_POINT ( 'NONE',  ( 7.201239011038929050, 78.91185591551062828, -11.41894328749275545 ) ) ;
#8899=CARTESIAN_POINT ( 'NONE',  ( -11.76794919243112325, 78.07999999999999829, 3.823638476888994386 ) ) ;
#8901=CIRCLE ( 'NONE', #10029, 8.999999999999994671 ) ;
#8902=DIRECTION ( 'NONE',  ( 0.000000000000000000, -1.000000000000000000, 0.000000000000000000 ) ) ;
#8905=CARTESIAN_POINT ( 'NONE',  ( -4.171729424061791036, 73.53000000000000114, 12.83926296998457239 ) ) ;
#8906=CARTESIAN_POINT ( 'NONE',  ( 4.197136615133925552, 34.02912076247848461, -12.83120157241570602 ) ) ;
#8912=CARTESIAN_POINT ( 'NONE',  ( 10.45936966163889892, 78.10386111577918200, 8.535314755708947487 ) ) ;
#8913=CARTESIAN_POINT ( 'NONE',  ( -0.3722949396608798422, 59.66661364915144361, 13.49486841530188208 ) ) ;
#8915=CARTESIAN_POINT ( 'NONE',  ( 12.50000000000000000, 98.93000000000002103, 1.224646799147353059E-15 ) ) ;
#8916=CARTESIAN_POINT ( 'NONE',  ( 7.607773347999265745, 71.96560712441068119, 11.15221199550204645 ) ) ;
#8917=CARTESIAN_POINT ( 'NONE',  ( 8.343458848123583849, 57.87999999999998835, -11.48378591275253768 ) ) ;
#8918=CARTESIAN_POINT ( 'NONE',  ( -1.737554137020194345, 52.24245571627063356, -13.38942718112060959 ) ) ;
#8920=CARTESIAN_POINT ( 'NONE',  ( -11.45953766701369858, 68.19652247961239766, 7.139846150206698994 ) ) ;
#8924=PRODUCT_DEFINITION ( 'UNKNOWN', '', #8510, #1183 ) ;
#8925=CARTESIAN_POINT ( 'NONE',  ( -2.195697726732460442, 65.60106443141478394, 13.32051239355739725 ) ) ;
#8932=CARTESIAN_POINT ( 'NONE',  ( -11.99429206528581737, 31.70121606863765606, -6.201385207760043095 ) ) ;
#8933=CARTESIAN_POINT ( 'NONE',  ( 9.381058047339037032, 75.04754594223111042, 9.717309665381625550 ) ) ;
#8934=CARTESIAN_POINT ( 'NONE',  ( 13.50001914872373909, 60.43013035372702291, -0.003958280579135459859 ) ) ;
#8935=EDGE_CURVE ( 'NONE', #16628, #11619, #706, .T. ) ;
#8936=CARTESIAN_POINT ( 'NONE',  ( 2.138189944381242213, 63.10311857767972299, -13.49999999999999822 ) ) ;
#8937=CARTESIAN_POINT ( 'NONE',  ( -10.92172942406179104, 76.23000000000000398, 7.935100905948387684 ) ) ;
#8938=CARTESIAN_POINT ( 'NONE',  ( 13.50106199340143043, 51.43115321150168739, -0.03627323424068121249 ) ) ;
#8940=CARTESIAN_POINT ( 'NONE',  ( -12.98462285426537299, 38.06247337552851917, 3.704199847612075214 ) ) ;
#8941=CARTESIAN_POINT ( 'NONE',  ( 12.65007964138050411, 36.60209030862610291, -4.758271190386921035 ) ) ;
#8944=CARTESIAN_POINT ( 'NONE',  ( -6.376503178677815242, 77.44599626364721701, 11.89916936316262763 ) ) ;
#8945=CARTESIAN_POINT ( 'NONE',  ( -13.49999999999999822, 61.07999999999999829, 4.386415899144235020 ) ) ;
#8946=CARTESIAN_POINT ( 'NONE',  ( 6.484162807585885702, 41.91833735075831413, 11.84678101249536475 ) ) ;
#8950=CARTESIAN_POINT ( 'NONE',  ( -11.76794919243112325, 59.92999999999999972, -2.882316262207890869E-15 ) ) ;
#8952=FACE_OUTER_BOUND ( 'NONE', #461, .T. ) ;
#8954=CARTESIAN_POINT ( 'NONE',  ( -0.06471714588535149026, 43.18232697961442312, -13.49985647836149028 ) ) ;
#8955=CARTESIAN_POINT ( 'NONE',  ( 0.8629412905205349205, 76.14897181464817777, -13.47239168749351990 ) ) ;
#8956=VECTOR ( 'NONE', #10312, 1000.000000000000000 ) ;
#8957=EDGE_CURVE ( 'NONE', #10808, #10491, #11315, .T. ) ;
#8959=CARTESIAN_POINT ( 'NONE',  ( -4.171729424061791036, 77.53000000000000114, 12.83926296998457239 ) ) ;
#8960=CARTESIAN_POINT ( 'NONE',  ( -11.76794919243112325, 53.92999999999999972, -2.882316262207890869E-15 ) ) ;
#8961=FACE_OUTER_BOUND ( 'NONE', #130, .T. ) ;
#8962=CARTESIAN_POINT ( 'NONE',  ( -13.47367793928326840, 58.90090033977541140, -0.8432173026106429825 ) ) ;
#8963=CARTESIAN_POINT ( 'NONE',  ( 13.49685988162643469, 45.41999658439461030, 0.2915229779186118697 ) ) ;
#8964=CARTESIAN_POINT ( 'NONE',  ( 13.43090557185185752, 69.38241981859624730, 1.365210260054945390 ) ) ;
#8966=CARTESIAN_POINT ( 'NONE',  ( 13.29842525421480914, 30.34827244870920637, 2.324384417915165812 ) ) ;
#8967=CARTESIAN_POINT ( 'NONE',  ( -12.94454544090478976, 56.06735303853458419, 3.835177592674254843 ) ) ;
#8968=CARTESIAN_POINT ( 'NONE',  ( -8.647676296952441888, 50.34754238603772336, 10.36673610620846375 ) ) ;
#8969=CARTESIAN_POINT ( 'NONE',  ( 0.5905603839040489689, 64.15876562730046828, -13.50000000000000000 ) ) ;
#8971=CARTESIAN_POINT ( 'NONE',  ( 13.45524155940220368, 39.46821381739253809, -1.102643116948291313 ) ) ;
#8972=ORIENTED_EDGE ( 'NONE', *, *, #10059, .F. ) ;
#8973=CARTESIAN_POINT ( 'NONE',  ( -4.862930340901737480, 61.35534921865077251, -12.59544805092636999 ) ) ;
#8975=VERTEX_POINT ( 'NONE', #7898 ) ;
#8976=ORIENTED_EDGE ( 'NONE', *, *, #15443, .F. ) ;
#8979=CARTESIAN_POINT ( 'NONE',  ( 6.668950942393352399, 47.92593842342445498, 11.73779662346200503 ) ) ;
#8981=CARTESIAN_POINT ( 'NONE',  ( 4.566661204442511668, 58.01567420843213796, -12.70452432719981672 ) ) ;
#8982=CARTESIAN_POINT ( 'NONE',  ( 2.592248576106782831, 79.08679227953400925, -13.24881110508173698 ) ) ;
#8983=CARTESIAN_POINT ( 'NONE',  ( -7.272992578804307939, 83.47999999999998977, -10.01041549318726886 ) ) ;
#8985=CARTESIAN_POINT ( 'NONE',  ( 4.171729424061789260, 40.82999999999999829, 12.83926296998457417 ) ) ;
#8988=CARTESIAN_POINT ( 'NONE',  ( 12.50000000000000000, 98.93000000000002103, -8.999999999999996447 ) ) ;
#8989=CARTESIAN_POINT ( 'NONE',  ( 2.927080096553553279, 34.07475512125041206, -13.17907647301958285 ) ) ;
#8991=CARTESIAN_POINT ( 'NONE',  ( 0.000000000000000000, 80.93000000000000682, -13.50000000000000000 ) ) ;
#8992=ORIENTED_EDGE ( 'NONE', *, *, #139, .T. ) ;
#8995=CARTESIAN_POINT ( 'NONE',  ( 6.742658785962751367, 77.92880199888011816, 11.70377657027630747 ) ) ;
#8996=CARTESIAN_POINT ( 'NONE',  ( -0.4161179423075612727, 59.66503801145354657, 13.49364511791329058 ) ) ;
#8999=CARTESIAN_POINT ( 'NONE',  ( 13.50000000000000355, 48.57999999999999829, -4.386415899144233244 ) ) ;
#9000=CARTESIAN_POINT ( 'NONE',  ( -11.39744115779548395, 71.20036747441211844, 7.238542865686949490 ) ) ;
#9004=CARTESIAN_POINT ( 'NONE',  ( 1.442968444427624064, 68.73190990305209880, 13.42312217546540687 ) ) ;
#9006=CARTESIAN_POINT ( 'NONE',  ( 6.247472632322534913, 54.95119552819922859, -11.96753039951391884 ) ) ;
#9007=TOROIDAL_SURFACE ( 'NONE', #1362, 6.000000000000001776, 6.000000000000000000 ) ;
#9009=CARTESIAN_POINT ( 'NONE',  ( -9.792966264564828549, 65.29152017548152287, 9.292365692678918876 ) ) ;
#9011=CARTESIAN_POINT ( 'NONE',  ( -1.471159980561823621, 35.62713808519091430, 13.41980265001063088 ) ) ;
#9014=CARTESIAN_POINT ( 'NONE',  ( -5.388417691150885425, 40.37512624867186872, -12.37871880772484801 ) ) ;
#9015=CARTESIAN_POINT ( 'NONE',  ( -11.82702148097626882, 31.68881418104456316, -6.509358658607543369 ) ) ;
#9018=CARTESIAN_POINT ( 'NONE',  ( 10.62943871048521416, 60.11330761422155433, 8.322610308588142658 ) ) ;
#9019=B_SPLINE_CURVE_WITH_KNOTS ( 'NONE', 3,
 ( #712, #16965, #2276, #7797, #3530, #14387, #7617, #6123, #12994, #4956, #11502, #16878, #10359, #4783, #10185, #876, #965, #3617, #7703, #17137, #11851, #15804, #3708, #9126, #14475, #2363, #16146, #15890, #9383, #12019, #14649, #10697, #14907, #3971, #3881, #4144, #5485, #6722, #16236, #16064, #10528, #4055, #5226, #2537, #10867, #9299, #7877, #7965, #14818, #2801, #14733, #9469, #10611, #12278, #2621, #1308, #3799, #9211, #12100, #14562, #2447, #13254, #2711, #13336, #17482, #8054, #13419, #1141, #6552, #5397, #1489, #15978, #8140, #11932, #10781, #17398, #1227, #13505, #8232, #1395, #17312, #9557, #6639, #5137, #5314, #6811, #12189, #81, #13593, #6904, #3248, #7337, #9733, #16598, #4237, #8322, #16685, #11049, #15259, #16421, #1574, #16510, #8672 ),
 .UNSPECIFIED., .F., .F.,
 ( 4, 2, 2, 1, 2, 2, 2, 2, 2, 2, 2, 2, 2, 1, 2, 2, 2, 2, 2, 2, 2, 1, 2, 2, 2, 2, 2, 2, 2, 2, 2, 2, 2, 2, 2, 2, 2, 2, 2, 2, 2, 2, 2, 2, 2, 1, 2, 1, 2, 2, 1, 1, 2, 2, 4 ),
 ( 0.004923257755196806459, 0.005842365896827374054, 0.006072142932235015736, 0.006301919967642657418, 0.006761474038457940781, 0.007680582180088505774, 0.007795470697792326181, 0.007910359215496145721, 0.008140136250903783066, 0.008599690321719061226, 0.009518798463349617545, 0.009748575498757256624, 0.009863464016461077899, 0.009978352534164899174, 0.01043790660498018601, 0.01135701474661075794, 0.01181656881742604304, 0.01227612288824132813, 0.01319523102987190180, 0.01365478510068719037, 0.01376967361839101164, 0.01388456213609483118, 0.01411433917150247894, 0.01503344731313306475, 0.01549300138394835852, 0.01560788990165218500, 0.01572277841935600801, 0.01595255545476365749, 0.01687166359639424851, 0.01779077173802484646, 0.01870987987965544094, 0.01916943395047073992, 0.01962898802128603543, 0.02146720430454722439, 0.02192675837536253031, 0.02238631244617782234, 0.02330542058780842030, 0.02376497465862371927, 0.02422452872943901131, 0.02514363687106960232, 0.02606274501270019334, 0.02698185315433078435, 0.02882006943759196638, 0.02927962350840725841, 0.02950940054381490790, 0.02973917757922255739, 0.03065828572085315534, 0.03111783979166844738, 0.03123272830937227212, 0.03126145043879823004, 0.03129017256822418797, 0.03134761682707610381, 0.03157739386248376023, 0.03249650200411437900, 0.03433471828737562348 ),
 .UNSPECIFIED. ) ;
#9021=CARTESIAN_POINT ( 'NONE',  ( -9.922634972987312452, 53.28481884420132531, 9.153759857451145621 ) ) ;
#9022=CARTESIAN_POINT ( 'NONE',  ( 9.520470885617717371, 55.73000000000000398, -6.917026985038131848 ) ) ;
#9024=CARTESIAN_POINT ( 'NONE',  ( 13.50000000000000355, 71.58000000000001251, -4.386415899144233244 ) ) ;
#9025=CARTESIAN_POINT ( 'NONE',  ( 11.71290578796123150, 51.67940127277162077, -6.712522446964136691 ) ) ;
#9026=CARTESIAN_POINT ( 'NONE',  ( -13.49476779773840640, 37.91485606517741758, -0.4350515032986518316 ) ) ;
#9027=CARTESIAN_POINT ( 'NONE',  ( 13.48567759012120959, 36.45142198522849952, -0.6217841871730820369 ) ) ;
#9029=EDGE_CURVE ( 'NONE', #14499, #10678, #1242, .T. ) ;
#9030=CARTESIAN_POINT ( 'NONE',  ( -6.083868223356676097, 74.45772641535832292, 12.05141389497554449 ) ) ;
#9031=B_SPLINE_CURVE_WITH_KNOTS ( 'NONE', 3,
 ( #12554, #16429, #9741, #14036, #3350, #8765, #4424, #440, #9833, #3257, #15441, #2985, #15086, #8416, #15178, #4687, #6023, #7253, #16778, #11231, #11056, #16692, #5758, #8505, #11407, #7434, #14120, #13942, #1838, #2008, #16606, #4599, #11142, #12639, #10090, #13767, #13854, #1669, #7083, #8677, #12467, #351, #10006, #1758, #7168, #5849, #16518, #1924, #12813, #5676, #9918, #3165, #8591, #12726, #612, #525, #5934, #11314, #10514, #17037, #11492, #9109, #9197, #784, #2261, #952, #2176, #4771, #14291, #6451, #4942, #17124, #15789, #3696, #11578, #11835, #6364, #7688, #2350, #2433, #10430, #14548, #7602, #14461, #7782, #4855, #17212, #7865, #3518, #13154, #1040, #10343, #3783, #13067, #701, #5123, #3605, #5030, #15610, #15877, #6273, #6111, #16866, #14206, #10258, #11747, #10176, #15526, #3436, #8852, #2090, #7517, #12897, #6191, #16953, #8932, #12980, #863, #11661, #15697, #9015, #14373, #2874, #13577, #16128, #12174, #10681, #14891, #1292, #12260, #9283, #6623, #13491, #5299, #16047, #156, #3954, #12002, #5562, #8036, #9367, #1212, #6539, #10945, #16311, #4218, #8124, #7949, #12084, #9632, #5470, #2695, #17467, #14981, #11919, #14635, #14717, #10766, #6888, #5210, #10600, #17384, #10851, #13239, #15963, #17297, #3868, #2605, #1127, #1469, #14802, #2521, #6707, #13320, #13404, #5380, #65, #4039, #9454, #1379, #6796 ),
 .UNSPECIFIED., .F., .F.,
 ( 4, 2, 1, 1, 2, 2, 2, 2, 2, 2, 1, 2, 2, 2, 2, 2, 1, 2, 2, 1, 2, 2, 1, 1, 1, 2, 2, 2, 2, 2, 1, 2, 2, 1, 1, 1, 2, 2, 2, 2, 2, 2, 1, 1, 2, 2, 2, 2, 1, 1, 2, 2, 2, 2, 2, 1, 2, 2, 2, 2, 2, 2, 2, 2, 2, 2, 2, 1, 2, 2, 1, 1, 2, 2, 1, 2, 2, 2, 2, 2, 2, 2, 2, 1, 1, 2, 2, 2, 1, 1, 2, 2, 1, 2, 2, 2, 1, 2, 1, 1, 2, 2, 2, 2, 4 ),
 ( 0.9460866550216218140, 0.9470057531069978607, 0.9471206403676698526, 0.9471780839980058486, 0.9472068058131738466, 0.9472355276283418446, 0.9474653021496858285, 0.9479248511923739073, 0.9488439492777499540, 0.9490737237990939379, 0.9491886110597659298, 0.9492460546901019258, 0.9493034983204379218, 0.9497630473631260006, 0.9506821454485020473, 0.9511416944911900151, 0.9512565817518620070, 0.9512853035670300050, 0.9513140253821980030, 0.9513714690125339990, 0.9516012435338779829, 0.9525203416192540296, 0.9529798906619421084, 0.9532096651832860923, 0.9532671088136220883, 0.9532958306287900863, 0.9533245524439580842, 0.9534394397046300762, 0.9543585377900056788, 0.9552776358753812813, 0.9553350795057172773, 0.9553422599595092768, 0.9553494404133011653, 0.9553638013208851643, 0.9553925231360531622, 0.9555074103967251542, 0.9557371849180691381, 0.9561967339607569949, 0.9571158320461327085, 0.9573456065674765814, 0.9573743283826445793, 0.9573886892902285783, 0.9574030501978125773, 0.9574604938281485733, 0.9575753810888205653, 0.9580349301315084221, 0.9589540282168842467, 0.9591838027382282306, 0.9592986899989002225, 0.9593561336292362185, 0.9593848554444042165, 0.9594135772595722145, 0.9598731263022600713, 0.9607922243876357848, 0.9612517734303236416, 0.9613666606909956336, 0.9614241043213316296, 0.9614815479516676255, 0.9617113224730114984, 0.9626304205583873230, 0.9630899696010751798, 0.9633197441224191637, 0.9634346313830910447, 0.9634920750134270406, 0.9635495186437630366, 0.9644686167291388612, 0.9653877148145145748, 0.9654451584448505708, 0.9654738802600185688, 0.9655026020751865667, 0.9656174893358585587, 0.9658472638572024316, 0.9663068128998903994, 0.9672259109852661130, 0.9674556855066100969, 0.9675131291369460929, 0.9675705727672820888, 0.9676854600279539698, 0.9681450090706418266, 0.9690641071560175401, 0.9695236561987053969, 0.9695523780138733949, 0.9695810998290413929, 0.9696385434593773889, 0.9697534307200493808, 0.9699832052413933647, 0.9709023033267691893, 0.9713618523694570461, 0.9714767396301290381, 0.9715341832604650341, 0.9715629050756330320, 0.9715916268908010300, 0.9718214014121450139, 0.9722809504548328707, 0.9725107249761768546, 0.9726256122368487356, 0.9727404994975207275, 0.9732000485402085843, 0.9734298230615525682, 0.9735447103222245602, 0.9736021539525605561, 0.9736595975828965521, 0.9745786956682722657, 0.9750382447109602335, 0.9754977937536480903 ),
 .UNSPECIFIED. ) ;
#9032=CARTESIAN_POINT ( 'NONE',  ( -10.68563015858318010, 77.24352929578411420, 8.250311360857775611 ) ) ;
#9033=CARTESIAN_POINT ( 'NONE',  ( 1.321426517745528884, 62.72752481348654641, 13.43884102842175565 ) ) ;
#9034=CARTESIAN_POINT ( 'NONE',  ( 7.500000000000000888, 105.5999945338998316, -8.557281619885975132 ) ) ;
#9035=ORIENTED_EDGE ( 'NONE', *, *, #12229, .T. ) ;
#9038=ORIENTED_EDGE ( 'NONE', *, *, #16246, .T. ) ;
#9039=CARTESIAN_POINT ( 'NONE',  ( -9.520470885617715595, 56.63000000000000256, -6.917026985038136289 ) ) ;
#9043=CARTESIAN_POINT ( 'NONE',  ( 13.04935142376444190, 75.55330351446269788, -3.459312735805662786 ) ) ;
#9045=CARTESIAN_POINT ( 'NONE',  ( 2.983352907350662608, 65.78734330260596153, 13.16637178637216188 ) ) ;
#9046=CARTESIAN_POINT ( 'NONE',  ( -8.343458848123576743, 73.47999999999998977, -11.48378591275254301 ) ) ;
#9047=CARTESIAN_POINT ( 'NONE',  ( -9.520470885617715595, 47.62999999999999545, -6.917026985038136289 ) ) ;
#9049=CARTESIAN_POINT ( 'NONE',  ( -13.47567420470207367, 58.95825367557104357, 0.8183608827415700393 ) ) ;
#9050=CARTESIAN_POINT ( 'NONE',  ( 11.46240780194647613, 45.16347604483497946, 7.131845818427484218 ) ) ;
#9051=CARTESIAN_POINT ( 'NONE',  ( 12.81028693375460925, 69.27666315554829168, 4.259893263560612375 ) ) ;
#9052=CARTESIAN_POINT ( 'NONE',  ( 1.732537601945078443, 80.74229332225066003, 13.38860820060650347 ) ) ;
#9053=CARTESIAN_POINT ( 'NONE',  ( 13.27581331548750398, 30.34371935371627771, 2.450248975568062093 ) ) ;
#9054=CARTESIAN_POINT ( 'NONE',  ( -7.369715979180460508, 55.45532736720758038, -11.31094860067307550 ) ) ;
#9056=CARTESIAN_POINT ( 'NONE',  ( -12.54398616578646930, 50.11135895507305094, 4.993044113767551195 ) ) ;
#9057=CARTESIAN_POINT ( 'NONE',  ( 6.774078098304966211, 63.93013539151233715, -11.69604546737801876 ) ) ;
#9059=CARTESIAN_POINT ( 'NONE',  ( 13.30714225929327377, 39.35008739665155986, 2.274010068040550614 ) ) ;
#9061=CARTESIAN_POINT ( 'NONE',  ( -10.69487954465043877, 70.61620775606867539, -8.249985653213133929 ) ) ;
#9062=CARTESIAN_POINT ( 'NONE',  ( -10.08509511462296615, 61.58369563808273028, -8.974460719705570355 ) ) ;
#9065=CARTESIAN_POINT ( 'NONE',  ( -11.00449575567194849, 40.63425626336776020, -7.832253106132067266 ) ) ;
#9069=CARTESIAN_POINT ( 'NONE',  ( 1.281689085039503961, 47.72602004897316874, 13.44796667457771377 ) ) ;
#9070=CARTESIAN_POINT ( 'NONE',  ( 2.374394324664103717, 58.09462585364141063, -13.28956834044282331 ) ) ;
#9071=CARTESIAN_POINT ( 'NONE',  ( 12.19260015540604769, 78.64272030694958460, -5.795731624687062045 ) ) ;
#9072=CARTESIAN_POINT ( 'NONE',  ( 3.636496289402157078, 74.03000000000000114, -11.19198476289190936 ) ) ;
#9073=CARTESIAN_POINT ( 'NONE',  ( -13.49999999999999822, 37.07999999999999119, 4.386415899144235908 ) ) ;
#9077=CARTESIAN_POINT ( 'NONE',  ( -8.343458848123578520, 75.48000000000000398, -11.48378591275254124 ) ) ;
#9080=CARTESIAN_POINT ( 'NONE',  ( 7.499999999999998224, 108.9300000000000068, -9.367496997597600128 ) ) ;
#9081=CARTESIAN_POINT ( 'NONE',  ( 4.272114809023935145, 34.02640058480978524, -12.80647630758542022 ) ) ;
#9082=CARTESIAN_POINT ( 'NONE',  ( -13.34776453198840152, 73.85917255742896259, -2.021718343860550604 ) ) ;
#9089=CARTESIAN_POINT ( 'NONE',  ( -4.441115907745108338, 44.52024772551524023, 12.74888276553507538 ) ) ;
#9090=CARTESIAN_POINT ( 'NONE',  ( -7.684034168813939303, 59.39112170478899344, 11.10103013205298872 ) ) ;
#9093=CARTESIAN_POINT ( 'NONE',  ( 7.771422898618976838, 66.88723588304965517, -11.03881805963236573 ) ) ;
#9095=CARTESIAN_POINT ( 'NONE',  ( 8.343458848123578520, 53.97999999999998977, 11.48378591275254124 ) ) ;
#9096=CARTESIAN_POINT ( 'NONE',  ( -8.147096294993618315, 71.37051073404745694, 10.76453482734664391 ) ) ;
#9098=CARTESIAN_POINT ( 'NONE',  ( -8.053875534609741038, 68.37512698675379852, 10.85470679754551071 ) ) ;
#9101=CARTESIAN_POINT ( 'NONE',  ( 5.720610333239705803, 54.97207370978246388, -12.22862423939397658 ) ) ;
#9103=CARTESIAN_POINT ( 'NONE',  ( -11.34091630496454073, 65.20426177971908999, 7.324935009242633299 ) ) ;
#9104=CARTESIAN_POINT ( 'NONE',  ( 6.750022862106053623, 29.92926176209967437, 11.69132975161703669 ) ) ;
#9105=CARTESIAN_POINT ( 'NONE',  ( -6.978456841825852131, 35.42124363644111895, 11.55651345503810923 ) ) ;
#9106=ORIENTED_EDGE ( 'NONE', *, *, #482, .T. ) ;
#9107=CARTESIAN_POINT ( 'NONE',  ( 11.76794919243112680, 31.57999999999999119, -3.823638476888993942 ) ) ;
#9108=CARTESIAN_POINT ( 'NONE',  ( 0.000000000000000000, 80.93000000000000682, 0.000000000000000000 ) ) ;
#9109=CARTESIAN_POINT ( 'NONE',  ( -11.62183027776853628, 32.18583764462453445, 6.871631281967373717 ) ) ;
#9110=CARTESIAN_POINT ( 'NONE',  ( 0.4719270757883078371, 73.16303128037343129, -13.49180536696172616 ) ) ;
#9111=CARTESIAN_POINT ( 'NONE',  ( 8.915328836987622907, 60.02504728364877451, 10.14169724999834621 ) ) ;
#9113=CARTESIAN_POINT ( 'NONE',  ( -3.920142863837685177, 53.53904487068937357, 12.91830804447569214 ) ) ;
#9115=ADVANCED_FACE ( 'NONE', ( #1504 ), #2819, .F. ) ;
#9116=CARTESIAN_POINT ( 'NONE',  ( -3.636496289402155746, 54.52999999999999403, 11.19198476289190936 ) ) ;
#9118=CARTESIAN_POINT ( 'NONE',  ( 4.171729424061791924, 78.03000000000000114, -12.83926296998457239 ) ) ;
#9119=CARTESIAN_POINT ( 'NONE',  ( 13.22096164572512222, 51.52648539050532861, -2.730718222746924884 ) ) ;
#9120=CARTESIAN_POINT ( 'NONE',  ( -13.46620905683853486, 37.89699380932566442, -0.9563560816646710094 ) ) ;
#9121=CARTESIAN_POINT ( 'NONE',  ( 12.94672365821387139, 36.56709068650133787, -3.829332532818771284 ) ) ;
#9123=CARTESIAN_POINT ( 'NONE',  ( -6.083576914348308051, 74.45773797485220769, 12.05155980095794277 ) ) ;
#9124=CARTESIAN_POINT ( 'NONE',  ( -9.236354345383572806, 77.31949598331318896, 9.855674949580887301 ) ) ;
#9126=CARTESIAN_POINT ( 'NONE',  ( -6.741112569723631154, 80.43110928230144907, 11.69660190220037421 ) ) ;
#9127=CARTESIAN_POINT ( 'NONE',  ( 7.500000000000000888, 106.7516370761002520, -7.534909587719530677 ) ) ;
#9128=ORIENTED_EDGE ( 'NONE', *, *, #16431, .F. ) ;
#9131=CARTESIAN_POINT ( 'NONE',  ( -11.76794919243112325, 59.77999999999999403, -3.823638476888998827 ) ) ;
#9135=CARTESIAN_POINT ( 'NONE',  ( 8.559272513022497364, 75.85165812557318077, -10.43981238950174451 ) ) ;
#9136=CYLINDRICAL_SURFACE ( 'NONE', #14152, 8.999999999999998224 ) ;
#9137=CARTESIAN_POINT ( 'NONE',  ( 3.097840831347480339, 65.79138985724777910, 13.13976367567505754 ) ) ;
#9138=CARTESIAN_POINT ( 'NONE',  ( -4.171729424061787483, 76.32999999999999829, -12.83926296998457417 ) ) ;
#9139=CARTESIAN_POINT ( 'NONE',  ( -11.76794919243112325, 41.92999999999999261, -2.882316262207890869E-15 ) ) ;
#9141=CIRCLE ( 'NONE', #1487, 4.000000000000004441 ) ;
#9142=CARTESIAN_POINT ( 'NONE',  ( -9.988570099143858627, 59.28138111796381793, 9.081841899843952959 ) ) ;
#9143=CARTESIAN_POINT ( 'NONE',  ( 9.161746794075217082, 45.03695357300266977, 9.915270584471830517 ) ) ;
#9144=CARTESIAN_POINT ( 'NONE',  ( 13.50023044427028651, 69.41460068291787877, 0.4327633727389757490 ) ) ;
#9145=DIRECTION ( 'NONE',  ( 0.000000000000000000, 1.000000000000000000, 0.000000000000000000 ) ) ;
#9146=CARTESIAN_POINT ( 'NONE',  ( 13.08917948282296706, 30.54760429764663954, -3.305587359976819073 ) ) ;
#9147=CARTESIAN_POINT ( 'NONE',  ( -11.19388950051994058, 55.64631903439251914, -7.546317585596763244 ) ) ;
#9148=CARTESIAN_POINT ( 'NONE',  ( -13.49204055340601904, 49.94875050132303329, 0.5461732183256954309 ) ) ;
#9150=CARTESIAN_POINT ( 'NONE',  ( 11.87714970433990658, 42.66748928331573154, -6.417526362764760961 ) ) ;
#9151=CARTESIAN_POINT ( 'NONE',  ( 12.05894746113889937, 39.20340553057236832, 6.158319521186863099 ) ) ;
#9152=ORIENTED_EDGE ( 'NONE', *, *, #2316, .T. ) ;
#9153=CARTESIAN_POINT ( 'NONE',  ( -12.74992687881205811, 70.76992611378939557, -4.437291153396828669 ) ) ;
#9154=CARTESIAN_POINT ( 'NONE',  ( -4.046715542471715388, 61.32550477582727666, -12.87921504933485650 ) ) ;
#9157=ORIENTED_EDGE ( 'NONE', *, *, #10454, .F. ) ;
#9160=CARTESIAN_POINT ( 'NONE',  ( 2.044565740421548927, 61.10653920895618540, -13.35237565107692426 ) ) ;
#9161=CARTESIAN_POINT ( 'NONE',  ( 13.49957401375394639, 57.43371563003871927, -0.1085156115176826724 ) ) ;
#9162=CARTESIAN_POINT ( 'NONE',  ( -11.76794919243112325, 65.78000000000001535, -3.823638476888998827 ) ) ;
#9163=CARTESIAN_POINT ( 'NONE',  ( 11.76794919243112680, 73.58000000000001251, -3.823638476888993942 ) ) ;
#9166=DIRECTION ( 'NONE',  ( 0.000000000000000000, 0.000000000000000000, -1.000000000000000000 ) ) ;
#9170=CARTESIAN_POINT ( 'NONE',  ( 3.123084801584079084, 34.06770800467356253, -13.13381235157419091 ) ) ;
#9171=CARTESIAN_POINT ( 'NONE',  ( -3.648110378726476810, 73.31117878912979791, -12.99774238346768129 ) ) ;
#9174=CARTESIAN_POINT ( 'NONE',  ( -11.76794919243112325, 74.92999999999999261, -2.882316262207890869E-15 ) ) ;
#9178=CARTESIAN_POINT ( 'NONE',  ( -8.693204481589310362, 44.34575204853277341, 10.33905691976574559 ) ) ;
#9180=CARTESIAN_POINT ( 'NONE',  ( 12.71166604806362166, 66.59423623445172780, -4.546593178848175043 ) ) ;
#9181=CARTESIAN_POINT ( 'NONE',  ( 13.50000000000000000, 57.42999999999999261, 1.653273178848926867E-15 ) ) ;
#9182=CARTESIAN_POINT ( 'NONE',  ( -3.964846123382400833, 71.53753483708018734, 12.90535649358312043 ) ) ;
#9183=ADVANCED_FACE ( 'NONE', ( #9232 ), #1324, .F. ) ;
#9186=CARTESIAN_POINT ( 'NONE',  ( -12.89466115481902975, 67.78656044428841199, -3.997873320072883097 ) ) ;
#9188=CARTESIAN_POINT ( 'NONE',  ( 9.257325759640430363, 54.81840794441243503, -9.826123182423009084 ) ) ;
#9190=CARTESIAN_POINT ( 'NONE',  ( -5.186086855064643508, 65.49256697006511274, 12.46412873091786722 ) ) ;
#9191=CARTESIAN_POINT ( 'NONE',  ( -3.070170608275790247, 62.56961157363158321, 13.15440911902680021 ) ) ;
#9192=CARTESIAN_POINT ( 'NONE',  ( -6.686918715536896762, 35.43339511926818375, 11.73038437417416446 ) ) ;
#9194=ORIENTED_EDGE ( 'NONE', *, *, #9973, .F. ) ;
#9196=( BOUNDED_SURFACE ( )  B_SPLINE_SURFACE ( 1, 2, ( 
 ( #4624, #12662, #7459, #13006, #15551, #6215, #551, #1865, #5961, #10199, #3543, #11341, #14062, #16718, #11686, #4966, #10370, #8877, #6049, #12841, #8616, #11602, #2116, #727, #13968, #10031, #15378, #10113, #6136, #2203, #16892, #4797, #7543, #10283, #12921, #15635, #8959, #14315, #15815, #10540, #6565, #8310, #10856, #4135, #9138, #7890, #14896, #3720, #1066, #9636, #5655, #1561, #11945, #17325, #6981, #14577, #2790, #14486, #5475, #14985, #978, #6478, #2286, #9046, #13582, #13092, #11037, #6892, #15902, #14398, #5150, #9224, #3811, #4222, #1475, #12265, #2373, #16224, #3632, #9547, #8221, #7808, #163, #5567, #13181, #17149, #11864, #10949, #12356, #17239, #16316, #2877, #2459, #7715, #13267, #13665, #1155, #250, #6390, #11773, #5061, #10456, #16673, #5915, #593, #681, #8658, #1988, #10073, #15424, #15067, #11294, #12447, #2967, #5828, #3331, #4579, #15158, #3057, #12706, #6004, #8570, #15247, #8396, #11211, #9986, #7413, #16585, #6093, #11386, #332, #8485, #9722, #14103, #12795, #16409, #15334, #11122, #3145, #8746, #14013, #3237, #13923, #4310, #13750, #5741, #13836, #1817, #1649, #7065, #16497, #1905, #7322, #4402, #7232, #16759, #12619, #9812, #4490, #507, #1736, #4666, #7149, #12534, #420, #9900, #11560, #8917, #17199, #13223, #9181, #2245, #7673, #14530, #4926, #10413, #16935, #13052, #5107, #8834, #14275, #10158, #16850, #3679, #3420, #1111, #14447, #846, #4752, #12964, #17022, #11644, #11820, #9095, #2333, #4838, #935, #11474, #6344, #14357, #15595, #15770, #13138, #3502, #7500, #2161, #7767, #2416, #10241, #11730, #17107, #6257, #15508, #7585, #10499, #15680, #1026, #6436, #15862, #10325, #3769, #5013, #7849, #14191, #2075, #12881, #769, #6177, #3587, #8999, #13476, #2505, #5196, #13390, #10930, #12158, #5285, #10668, #2767, #8199, #16115, #5366, #10584, #1279, #49, #14967, #6692, #13647, #1453, #7935, #16032, #1363, #4114, #15945, #17282, #3854, #8112, #2592, #10837, #9529, #14872, #17370, #12246, #6780, #5453, #13563, #8290, #16203, #9616, #140, #5546, #9268, #6871, #13308, #14620, #12073, #16297, #4205, #3940, #9354, #2858, #6526, #4026, #10751, #1198, #17452, #11905, #6610, #9441, #11989, #14703, #8022, #14789, #2679, #16653, #230, #12338, #5636, #3127, #12518, #5984, #402, #8639, #16740, #4646, #10052, #13905, #13734, #5810, #576, #11276, #8553, #11193, #15402, #11018, #15051, #11104, #16569, #12686, #16389, #4293, #12601, #4560, #9705, #4475, #1801, #9881, #1631, #8467, #15230, #11366, #7213, #490, #7049, #5896, #9966, #12428, #16478, #7301, #3310, #8723, #15315, #3217, #1541, #13990, #1887, #314, #6959, #2949, #8377, #4383, #5723, #9791, #15138, #3036 ),
 ( #13818, #1719, #7131, #8983, #17000, #751, #916, #15750, #6159, #10135, #11536, #4994, #5089, #14170, #15659, #14338, #15573, #661, #10220, #2314, #827, #13032, #16914, #13117, #4819, #12862, #6416, #3747, #3484, #6325, #15489, #7481, #3399, #4906, #2058, #16827, #2227, #7656, #6071, #8899, #11801, #17177, #14253, #7393, #11453, #10395, #10481, #15841, #2141, #7566, #12943, #11711, #14082, #4734, #12773, #8812, #6238, #1005, #14425, #3568, #7742, #11625, #1969, #10305, #17088, #3661, #9072, #5174, #10908, #6848, #17262, #1180, #5524, #6591, #5429, #11971, #4093, #2573, #1342, #16013, #2397, #16181, #9336, #9422, #11888, #13455, #17352, #7917, #5264, #6506, #26, #12226, #14853, #10566, #15926, #13371, #10819, #8091, #14686, #10650, #8005, #1431, #1260, #7832, #13205, #2747, #3836, #12137, #12055, #1091, #6758, #13291, #9250, #14603, #118, #9508, #2483, #2661, #16277, #8178, #13541, #9162, #5346, #3919, #14510, #6672, #17433, #10733, #16097, #4005, #14770, #552, #7028, #13882, #7193, #8443, #7280, #11172, #11342, #4539, #7111, #3107, #1611, #5877, #9769, #3196, #210, #15032, #4453, #13712, #1866, #12663, #5962, #16547, #16365, #3013, #8617, #1783, #9860, #13798, #4183, #2837, #5615, #12406, #1696, #15294, #13629, #1521, #15207, #12581, #12316, #12495, #8534, #382, #4273, #11085, #5787, #13971, #469, #11256, #9682, #16635, #9946, #2925, #294, #9595, #14947, #8268, #6938, #10997, #8355, #15115, #5703, #16458, #4360, #4968, #14063, #14147, #15380, #4625, #8960, #8702, #6392, #2204, #6137, #10032, #729, #4798, #16894, #17064, #14316, #7630, #10115, #12922, #16719, #11603, #2118, #3377, #3545, #889, #8789, #12750, #2035, #13008, #7716, #16804, #806, #16979, #11516, #3288, #12842, #10371, #3463, #15636, #6301, #11687, #15467, #15725, #4881, #6217, #3633, #979, #9047, #2288, #14399, #13093, #1947, #10284, #637, #7371, #10200, #6050, #11433, #7460, #15552, #4711, #8878, #14232, #7544, #10457, #6566, #17410, #2724, #11946, #1408, #6735, #7809, #3812, #1237, #9397, #15817, #5062, #3721, #13348, #5238, #16159, #10624, #1319, #14830, #1156, #9139, #14487, #2636, #9484, #8152, #10541, #17326, #15903, #14747, #4069, #2374, #13182, #1067, #9225, #10795, #12114, #6649, #5408, #15989, #17150, #11774, #3893, #10709, #7891, #6479, #13517, #11865, #17240, #14579, #5151, #2460, #8067, #13268, #3, #9311, #3982, #14661, #2549, #7979, #12031, #5325, #16075, #13431, #4248, #5592, #2899, #4157, #15182, #4514, #12558, #14920, #8244, #11059, #3083, #5762, #7003, #16340, #12379, #16610, #5679, #94, #5499, #443, #13604, #9836, #9744, #10882, #16521, #10972, #16252, #1499, #9922, #11145, #9570, #356 ) ),
 .UNSPECIFIED., .F., .F., .F. ) 
 B_SPLINE_SURFACE_WITH_KNOTS ( ( 2, 2 ),
 ( 3, 2, 2, 2, 2, 2, 2, 2, 2, 2, 2, 2, 2, 2, 2, 2, 2, 2, 2, 2, 2, 2, 2, 2, 2, 2, 2, 2, 2, 2, 2, 2, 2, 2, 2, 2, 2, 2, 2, 2, 2, 2, 2, 2, 2, 2, 2, 2, 2, 2, 2, 2, 2, 2, 2, 2, 2, 2, 2, 2, 2, 2, 2, 2, 2, 2, 2, 2, 2, 2, 2, 2, 2, 2, 2, 2, 2, 2, 2, 2, 2, 2, 2, 2, 2, 2, 2, 2, 2, 2, 2, 2, 2, 2, 2, 2, 2, 2, 2, 2, 2, 2, 2, 2, 2, 2, 2, 2, 2, 2, 2, 2, 2, 2, 2, 2, 2, 2, 2, 2, 2, 2, 2, 2, 2, 2, 2, 2, 2, 2, 2, 2, 2, 2, 2, 2, 2, 2, 2, 2, 2, 2, 2, 2, 2, 2, 2, 2, 2, 2, 2, 2, 2, 2, 2, 2, 2, 2, 2, 2, 2, 2, 2, 2, 2, 2, 2, 2, 2, 2, 2, 2, 2, 2, 2, 2, 2, 3 ),
 ( 0.000000000000000000, 1.000000000000000000 ),
 ( 0.000000000000000000, 0.005555555555555555768, 0.01111111111111111154, 0.01666666666666666644, 0.02222222222222222307, 0.02777777777777777624, 0.03333333333333333287, 0.03888888888888888951, 0.04444444444444444614, 0.05000000000000000278, 0.05555555555555555247, 0.06111111111111110911, 0.06666666666666666574, 0.07222222222222221544, 0.07777777777777777901, 0.08333333333333332871, 0.08888888888888889228, 0.09444444444444444198, 0.1000000000000000056, 0.1055555555555555552, 0.1111111111111111049, 0.1166666666666666685, 0.1222222222222222182, 0.1277777777777777679, 0.1333333333333333315, 0.1388888888888888951, 0.1444444444444444309, 0.1499999999999999944, 0.1555555555555555580, 0.1611111111111111216, 0.1666666666666666574, 0.1722222222222222210, 0.1777777777777777846, 0.1833333333333333204, 0.1888888888888888840, 0.1944444444444444475, 0.2000000000000000111, 0.2055555555555555469, 0.2111111111111111105, 0.2166666666666666741, 0.2222222222222222099, 0.2277777777777777735, 0.2333333333333333370, 0.2388888888888889006, 0.2444444444444444364, 0.2500000000000000000, 0.2555555555555555358, 0.2611111111111111271, 0.2666666666666666630, 0.2722222222222221988, 0.2777777777777777901, 0.2833333333333333259, 0.2888888888888888618, 0.2944444444444444531, 0.2999999999999999889, 0.3055555555555555802, 0.3111111111111111160, 0.3166666666666666519, 0.3222222222222222432, 0.3277777777777777790, 0.3333333333333333148, 0.3388888888888889062, 0.3444444444444444420, 0.3499999999999999778, 0.3555555555555555691, 0.3611111111111111049, 0.3666666666666666408, 0.3722222222222222321, 0.3777777777777777679, 0.3833333333333333592, 0.3888888888888888951, 0.3944444444444444309, 0.4000000000000000222, 0.4055555555555555580, 0.4111111111111110938, 0.4166666666666666852, 0.4222222222222222210, 0.4277777777777777568, 0.4333333333333333481, 0.4388888888888888840, 0.4444444444444444198, 0.4500000000000000111, 0.4555555555555555469, 0.4611111111111111382, 0.4666666666666666741, 0.4722222222222222099, 0.4777777777777778012, 0.4833333333333333370, 0.4888888888888888729, 0.4944444444444444642, 0.5000000000000000000, 0.5055555555555555358, 0.5111111111111110716, 0.5166666666666667185, 0.5222222222222222543, 0.5277777777777777901, 0.5333333333333333259, 0.5388888888888888618, 0.5444444444444443976, 0.5500000000000000444, 0.5555555555555555802, 0.5611111111111111160, 0.5666666666666666519, 0.5722222222222221877, 0.5777777777777777235, 0.5833333333333333703, 0.5888888888888889062, 0.5944444444444444420, 0.5999999999999999778, 0.6055555555555555136, 0.6111111111111111605, 0.6166666666666666963, 0.6222222222222222321, 0.6277777777777777679, 0.6333333333333333037, 0.6388888888888888395, 0.6444444444444444864, 0.6500000000000000222, 0.6555555555555555580, 0.6611111111111110938, 0.6666666666666666297, 0.6722222222222222765, 0.6777777777777778123, 0.6833333333333333481, 0.6888888888888888840, 0.6944444444444444198, 0.6999999999999999556, 0.7055555555555556024, 0.7111111111111111382, 0.7166666666666666741, 0.7222222222222222099, 0.7277777777777777457, 0.7333333333333332815, 0.7388888888888889284, 0.7444444444444444642, 0.7500000000000000000, 0.7555555555555555358, 0.7611111111111110716, 0.7666666666666667185, 0.7722222222222222543, 0.7777777777777777901, 0.7833333333333333259, 0.7888888888888888618, 0.7944444444444443976, 0.8000000000000000444, 0.8055555555555555802, 0.8111111111111111160, 0.8166666666666666519, 0.8222222222222221877, 0.8277777777777777235, 0.8333333333333333703, 0.8388888888888889062, 0.8444444444444444420, 0.8499999999999999778, 0.8555555555555555136, 0.8611111111111111605, 0.8666666666666666963, 0.8722222222222222321, 0.8777777777777777679, 0.8833333333333333037, 0.8888888888888888395, 0.8944444444444444864, 0.9000000000000000222, 0.9055555555555555580, 0.9111111111111110938, 0.9166666666666666297, 0.9222222222222222765, 0.9277777777777778123, 0.9333333333333333481, 0.9388888888888888840, 0.9444444444444444198, 0.9499999999999999556, 0.9555555555555556024, 0.9611111111111111382, 0.9666666666666666741, 0.9722222222222222099, 0.9777777777777777457, 0.9814746806989694816 ),
 .UNSPECIFIED. ) 
 GEOMETRIC_REPRESENTATION_ITEM ( )  RATIONAL_B_SPLINE_SURFACE ( (
 ( 1.000000000000000000, 0.9510565162951535312, 1.000000000000000000, 0.9510565162951535312, 1.000000000000000000, 0.9510565162951535312, 1.000000000000000000, 0.9510565162951535312, 1.000000000000000000, 0.9510565162951535312, 1.000000000000000000, 0.9510565162951535312, 1.000000000000000000, 0.9510565162951535312, 1.000000000000000000, 0.9510565162951535312, 1.000000000000000000, 0.9510565162951535312, 1.000000000000000000, 0.9510565162951535312, 1.000000000000000000, 0.9510565162951535312, 1.000000000000000000, 0.9510565162951535312, 1.000000000000000000, 0.9510565162951535312, 1.000000000000000000, 0.9510565162951535312, 1.000000000000000000, 0.9510565162951535312, 1.000000000000000000, 0.9510565162951535312, 1.000000000000000000, 0.9510565162951535312, 1.000000000000000000, 0.9510565162951535312, 1.000000000000000000, 0.9510565162951535312, 1.000000000000000000, 0.9510565162951535312, 1.000000000000000000, 0.9510565162951535312, 1.000000000000000000, 0.9510565162951535312, 1.000000000000000000, 0.9510565162951535312, 1.000000000000000000, 0.9510565162951535312, 1.000000000000000000, 0.9510565162951535312, 1.000000000000000000, 0.9510565162951535312, 1.000000000000000000, 0.9510565162951535312, 1.000000000000000000, 0.9510565162951535312, 1.000000000000000000, 0.9510565162951535312, 1.000000000000000000, 0.9510565162951535312, 1.000000000000000000, 0.9510565162951535312, 1.000000000000000000, 0.9510565162951535312, 1.000000000000000000, 0.9510565162951535312, 1.000000000000000000, 0.9510565162951535312, 1.000000000000000000, 0.9510565162951535312, 1.000000000000000000, 0.9510565162951535312, 1.000000000000000000, 0.9510565162951535312, 1.000000000000000000, 0.9510565162951535312, 1.000000000000000000, 0.9510565162951535312, 1.000000000000000000, 0.9510565162951535312, 1.000000000000000000, 0.9510565162951535312, 1.000000000000000000, 0.9510565162951535312, 1.000000000000000000, 0.9510565162951535312, 1.000000000000000000, 0.9510565162951535312, 1.000000000000000000, 0.9510565162951535312, 1.000000000000000000, 0.9510565162951535312, 1.000000000000000000, 0.9510565162951535312, 1.000000000000000000, 0.9510565162951535312, 1.000000000000000000, 0.9510565162951535312, 1.000000000000000000, 0.9510565162951535312, 1.000000000000000000, 0.9510565162951535312, 1.000000000000000000, 0.9510565162951535312, 1.000000000000000000, 0.9510565162951535312, 1.000000000000000000, 0.9510565162951535312, 1.000000000000000000, 0.9510565162951535312, 1.000000000000000000, 0.9510565162951535312, 1.000000000000000000, 0.9510565162951535312, 1.000000000000000000, 0.9510565162951535312, 1.000000000000000000, 0.9510565162951535312, 1.000000000000000000, 0.9510565162951535312, 1.000000000000000000, 0.9510565162951535312, 1.000000000000000000, 0.9510565162951535312, 1.000000000000000000, 0.9510565162951535312, 1.000000000000000000, 0.9510565162951535312, 1.000000000000000000, 0.9510565162951535312, 1.000000000000000000, 0.9510565162951535312, 1.000000000000000000, 0.9510565162951535312, 1.000000000000000000, 0.9510565162951535312, 1.000000000000000000, 0.9510565162951535312, 1.000000000000000000, 0.9510565162951535312, 1.000000000000000000, 0.9510565162951535312, 1.000000000000000000, 0.9510565162951535312, 1.000000000000000000, 0.9510565162951535312, 1.000000000000000000, 0.9510565162951535312, 1.000000000000000000, 0.9510565162951535312, 1.000000000000000000, 0.9510565162951535312, 1.000000000000000000, 0.9510565162951535312, 1.000000000000000000, 0.9510565162951535312, 1.000000000000000000, 0.9510565162951535312, 1.000000000000000000, 0.9510565162951535312, 1.000000000000000000, 0.9510565162951535312, 1.000000000000000000, 0.9510565162951535312, 1.000000000000000000, 0.9510565162951535312, 1.000000000000000000, 0.9510565162951535312, 1.000000000000000000, 0.9510565162951535312, 1.000000000000000000, 0.9510565162951535312, 1.000000000000000000, 0.9510565162951535312, 1.000000000000000000, 0.9510565162951535312, 1.000000000000000000, 0.9510565162951535312, 1.000000000000000000, 0.9510565162951535312, 1.000000000000000000, 0.9510565162951535312, 1.000000000000000000, 0.9510565162951535312, 1.000000000000000000, 0.9510565162951535312, 1.000000000000000000, 0.9510565162951535312, 1.000000000000000000, 0.9510565162951535312, 1.000000000000000000, 0.9510565162951535312, 1.000000000000000000, 0.9510565162951535312, 1.000000000000000000, 0.9510565162951535312, 1.000000000000000000, 0.9510565162951535312, 1.000000000000000000, 0.9510565162951535312, 1.000000000000000000, 0.9510565162951535312, 1.000000000000000000, 0.9510565162951535312, 1.000000000000000000, 0.9510565162951535312, 1.000000000000000000, 0.9510565162951535312, 1.000000000000000000, 0.9510565162951535312, 1.000000000000000000, 0.9510565162951535312, 1.000000000000000000, 0.9510565162951535312, 1.000000000000000000, 0.9510565162951535312, 1.000000000000000000, 0.9510565162951535312, 1.000000000000000000, 0.9510565162951535312, 1.000000000000000000, 0.9510565162951535312, 1.000000000000000000, 0.9510565162951535312, 1.000000000000000000, 0.9510565162951535312, 1.000000000000000000, 0.9510565162951535312, 1.000000000000000000, 0.9510565162951535312, 1.000000000000000000, 0.9510565162951535312, 1.000000000000000000, 0.9510565162951535312, 1.000000000000000000, 0.9510565162951535312, 1.000000000000000000, 0.9510565162951535312, 1.000000000000000000, 0.9510565162951535312, 1.000000000000000000, 0.9510565162951535312, 1.000000000000000000, 0.9510565162951535312, 1.000000000000000000, 0.9510565162951535312, 1.000000000000000000, 0.9510565162951535312, 1.000000000000000000, 0.9510565162951535312, 1.000000000000000000, 0.9510565162951535312, 1.000000000000000000, 0.9510565162951535312, 1.000000000000000000, 0.9510565162951535312, 1.000000000000000000, 0.9510565162951535312, 1.000000000000000000, 0.9510565162951535312, 1.000000000000000000, 0.9510565162951535312, 1.000000000000000000, 0.9510565162951535312, 1.000000000000000000, 0.9510565162951535312, 1.000000000000000000, 0.9510565162951535312, 1.000000000000000000, 0.9510565162951535312, 1.000000000000000000, 0.9510565162951535312, 1.000000000000000000, 0.9510565162951535312, 1.000000000000000000, 0.9510565162951535312, 1.000000000000000000, 0.9510565162951535312, 1.000000000000000000, 0.9510565162951535312, 1.000000000000000000, 0.9510565162951535312, 1.000000000000000000, 0.9510565162951535312, 1.000000000000000000, 0.9510565162951535312, 1.000000000000000000, 0.9510565162951535312, 1.000000000000000000, 0.9510565162951535312, 1.000000000000000000, 0.9510565162951535312, 1.000000000000000000, 0.9510565162951535312, 1.000000000000000000, 0.9510565162951535312, 1.000000000000000000, 0.9510565162951535312, 1.000000000000000000, 0.9510565162951535312, 1.000000000000000000, 0.9510565162951535312, 1.000000000000000000, 0.9510565162951535312, 1.000000000000000000, 0.9510565162951535312, 1.000000000000000000, 0.9510565162951535312, 1.000000000000000000, 0.9510565162951535312, 1.000000000000000000, 0.9510565162951535312, 1.000000000000000000, 0.9510565162951535312, 1.000000000000000000, 0.9510565162951535312, 1.000000000000000000, 0.9510565162951535312, 1.000000000000000000, 0.9510565162951535312, 1.000000000000000000, 0.9510565162951535312, 1.000000000000000000, 0.9510565162951535312, 1.000000000000000000, 0.9510565162951535312, 1.000000000000000000, 0.9510565162951535312, 1.000000000000000000, 0.9510565162951535312, 1.000000000000000000, 0.9510565162951535312, 1.000000000000000000, 0.9510565162951535312, 1.000000000000000000, 0.9510565162951535312, 1.000000000000000000, 0.9510565162951535312, 1.000000000000000000, 0.9510565162951535312, 1.000000000000000000, 0.9510565162951535312, 1.000000000000000000, 0.9510565162951535312, 1.000000000000000000, 0.9510565162951535312, 1.000000000000000000, 0.9510565162951535312, 1.000000000000000000, 0.9510565162951535312, 1.000000000000000000, 0.9510565162951535312, 1.000000000000000000, 0.9674309245812854341, 0.9782075447827165426),
 ( 1.000000000000000000, 0.9510565162951535312, 1.000000000000000000, 0.9510565162951535312, 1.000000000000000000, 0.9510565162951535312, 1.000000000000000000, 0.9510565162951535312, 1.000000000000000000, 0.9510565162951535312, 1.000000000000000000, 0.9510565162951535312, 1.000000000000000000, 0.9510565162951535312, 1.000000000000000000, 0.9510565162951535312, 1.000000000000000000, 0.9510565162951535312, 1.000000000000000000, 0.9510565162951535312, 1.000000000000000000, 0.9510565162951535312, 1.000000000000000000, 0.9510565162951535312, 1.000000000000000000, 0.9510565162951535312, 1.000000000000000000, 0.9510565162951535312, 1.000000000000000000, 0.9510565162951535312, 1.000000000000000000, 0.9510565162951535312, 1.000000000000000000, 0.9510565162951535312, 1.000000000000000000, 0.9510565162951535312, 1.000000000000000000, 0.9510565162951535312, 1.000000000000000000, 0.9510565162951535312, 1.000000000000000000, 0.9510565162951535312, 1.000000000000000000, 0.9510565162951535312, 1.000000000000000000, 0.9510565162951535312, 1.000000000000000000, 0.9510565162951535312, 1.000000000000000000, 0.9510565162951535312, 1.000000000000000000, 0.9510565162951535312, 1.000000000000000000, 0.9510565162951535312, 1.000000000000000000, 0.9510565162951535312, 1.000000000000000000, 0.9510565162951535312, 1.000000000000000000, 0.9510565162951535312, 1.000000000000000000, 0.9510565162951535312, 1.000000000000000000, 0.9510565162951535312, 1.000000000000000000, 0.9510565162951535312, 1.000000000000000000, 0.9510565162951535312, 1.000000000000000000, 0.9510565162951535312, 1.000000000000000000, 0.9510565162951535312, 1.000000000000000000, 0.9510565162951535312, 1.000000000000000000, 0.9510565162951535312, 1.000000000000000000, 0.9510565162951535312, 1.000000000000000000, 0.9510565162951535312, 1.000000000000000000, 0.9510565162951535312, 1.000000000000000000, 0.9510565162951535312, 1.000000000000000000, 0.9510565162951535312, 1.000000000000000000, 0.9510565162951535312, 1.000000000000000000, 0.9510565162951535312, 1.000000000000000000, 0.9510565162951535312, 1.000000000000000000, 0.9510565162951535312, 1.000000000000000000, 0.9510565162951535312, 1.000000000000000000, 0.9510565162951535312, 1.000000000000000000, 0.9510565162951535312, 1.000000000000000000, 0.9510565162951535312, 1.000000000000000000, 0.9510565162951535312, 1.000000000000000000, 0.9510565162951535312, 1.000000000000000000, 0.9510565162951535312, 1.000000000000000000, 0.9510565162951535312, 1.000000000000000000, 0.9510565162951535312, 1.000000000000000000, 0.9510565162951535312, 1.000000000000000000, 0.9510565162951535312, 1.000000000000000000, 0.9510565162951535312, 1.000000000000000000, 0.9510565162951535312, 1.000000000000000000, 0.9510565162951535312, 1.000000000000000000, 0.9510565162951535312, 1.000000000000000000, 0.9510565162951535312, 1.000000000000000000, 0.9510565162951535312, 1.000000000000000000, 0.9510565162951535312, 1.000000000000000000, 0.9510565162951535312, 1.000000000000000000, 0.9510565162951535312, 1.000000000000000000, 0.9510565162951535312, 1.000000000000000000, 0.9510565162951535312, 1.000000000000000000, 0.9510565162951535312, 1.000000000000000000, 0.9510565162951535312, 1.000000000000000000, 0.9510565162951535312, 1.000000000000000000, 0.9510565162951535312, 1.000000000000000000, 0.9510565162951535312, 1.000000000000000000, 0.9510565162951535312, 1.000000000000000000, 0.9510565162951535312, 1.000000000000000000, 0.9510565162951535312, 1.000000000000000000, 0.9510565162951535312, 1.000000000000000000, 0.9510565162951535312, 1.000000000000000000, 0.9510565162951535312, 1.000000000000000000, 0.9510565162951535312, 1.000000000000000000, 0.9510565162951535312, 1.000000000000000000, 0.9510565162951535312, 1.000000000000000000, 0.9510565162951535312, 1.000000000000000000, 0.9510565162951535312, 1.000000000000000000, 0.9510565162951535312, 1.000000000000000000, 0.9510565162951535312, 1.000000000000000000, 0.9510565162951535312, 1.000000000000000000, 0.9510565162951535312, 1.000000000000000000, 0.9510565162951535312, 1.000000000000000000, 0.9510565162951535312, 1.000000000000000000, 0.9510565162951535312, 1.000000000000000000, 0.9510565162951535312, 1.000000000000000000, 0.9510565162951535312, 1.000000000000000000, 0.9510565162951535312, 1.000000000000000000, 0.9510565162951535312, 1.000000000000000000, 0.9510565162951535312, 1.000000000000000000, 0.9510565162951535312, 1.000000000000000000, 0.9510565162951535312, 1.000000000000000000, 0.9510565162951535312, 1.000000000000000000, 0.9510565162951535312, 1.000000000000000000, 0.9510565162951535312, 1.000000000000000000, 0.9510565162951535312, 1.000000000000000000, 0.9510565162951535312, 1.000000000000000000, 0.9510565162951535312, 1.000000000000000000, 0.9510565162951535312, 1.000000000000000000, 0.9510565162951535312, 1.000000000000000000, 0.9510565162951535312, 1.000000000000000000, 0.9510565162951535312, 1.000000000000000000, 0.9510565162951535312, 1.000000000000000000, 0.9510565162951535312, 1.000000000000000000, 0.9510565162951535312, 1.000000000000000000, 0.9510565162951535312, 1.000000000000000000, 0.9510565162951535312, 1.000000000000000000, 0.9510565162951535312, 1.000000000000000000, 0.9510565162951535312, 1.000000000000000000, 0.9510565162951535312, 1.000000000000000000, 0.9510565162951535312, 1.000000000000000000, 0.9510565162951535312, 1.000000000000000000, 0.9510565162951535312, 1.000000000000000000, 0.9510565162951535312, 1.000000000000000000, 0.9510565162951535312, 1.000000000000000000, 0.9510565162951535312, 1.000000000000000000, 0.9510565162951535312, 1.000000000000000000, 0.9510565162951535312, 1.000000000000000000, 0.9510565162951535312, 1.000000000000000000, 0.9510565162951535312, 1.000000000000000000, 0.9510565162951535312, 1.000000000000000000, 0.9510565162951535312, 1.000000000000000000, 0.9510565162951535312, 1.000000000000000000, 0.9510565162951535312, 1.000000000000000000, 0.9510565162951535312, 1.000000000000000000, 0.9510565162951535312, 1.000000000000000000, 0.9510565162951535312, 1.000000000000000000, 0.9510565162951535312, 1.000000000000000000, 0.9510565162951535312, 1.000000000000000000, 0.9510565162951535312, 1.000000000000000000, 0.9510565162951535312, 1.000000000000000000, 0.9510565162951535312, 1.000000000000000000, 0.9510565162951535312, 1.000000000000000000, 0.9510565162951535312, 1.000000000000000000, 0.9510565162951535312, 1.000000000000000000, 0.9510565162951535312, 1.000000000000000000, 0.9510565162951535312, 1.000000000000000000, 0.9510565162951535312, 1.000000000000000000, 0.9510565162951535312, 1.000000000000000000, 0.9510565162951535312, 1.000000000000000000, 0.9510565162951535312, 1.000000000000000000, 0.9510565162951535312, 1.000000000000000000, 0.9510565162951535312, 1.000000000000000000, 0.9510565162951535312, 1.000000000000000000, 0.9510565162951535312, 1.000000000000000000, 0.9510565162951535312, 1.000000000000000000, 0.9510565162951535312, 1.000000000000000000, 0.9510565162951535312, 1.000000000000000000, 0.9510565162951535312, 1.000000000000000000, 0.9510565162951535312, 1.000000000000000000, 0.9510565162951535312, 1.000000000000000000, 0.9510565162951535312, 1.000000000000000000, 0.9510565162951535312, 1.000000000000000000, 0.9510565162951535312, 1.000000000000000000, 0.9510565162951535312, 1.000000000000000000, 0.9510565162951535312, 1.000000000000000000, 0.9510565162951535312, 1.000000000000000000, 0.9510565162951535312, 1.000000000000000000, 0.9510565162951535312, 1.000000000000000000, 0.9510565162951535312, 1.000000000000000000, 0.9510565162951535312, 1.000000000000000000, 0.9510565162951535312, 1.000000000000000000, 0.9510565162951535312, 1.000000000000000000, 0.9510565162951535312, 1.000000000000000000, 0.9510565162951535312, 1.000000000000000000, 0.9510565162951535312, 1.000000000000000000, 0.9510565162951535312, 1.000000000000000000, 0.9510565162951535312, 1.000000000000000000, 0.9510565162951535312, 1.000000000000000000, 0.9674309245812854341, 0.9782075447827165426) ) ) 
 REPRESENTATION_ITEM ( '' )  SURFACE ( )  );
#9197=CARTESIAN_POINT ( 'NONE',  ( -11.72349227228382773, 32.17874275710667575, 6.697393093110406426 ) ) ;
#9198=CARTESIAN_POINT ( 'NONE',  ( 0.5398279591931279819, 73.16058978026926241, -13.48920530192332556 ) ) ;
#9199=CARTESIAN_POINT ( 'NONE',  ( 13.49981200716974428, 60.43253933153254565, -0.07419703893695323016 ) ) ;
#9201=CARTESIAN_POINT ( 'NONE',  ( -7.043910900581732193, 53.41849667041662286, 11.51668441602786608 ) ) ;
#9202=CARTESIAN_POINT ( 'NONE',  ( -11.76794919243112325, 53.77999999999999403, -3.823638476888998827 ) ) ;
#9203=CARTESIAN_POINT ( 'NONE',  ( -4.171729424061787483, 72.33000000000001251, -12.83926296998457417 ) ) ;
#9204=CARTESIAN_POINT ( 'NONE',  ( 12.78586417785842322, 51.27373664802115627, 4.335848610435731665 ) ) ;
#9205=CARTESIAN_POINT ( 'NONE',  ( -13.38432117154441414, 37.99212082524375944, 1.778969478457535169 ) ) ;
#9206=CARTESIAN_POINT ( 'NONE',  ( 9.963063945987066461, 36.78277068231086844, -9.111627411219474837 ) ) ;
#9208=CARTESIAN_POINT ( 'NONE',  ( -0.8228155029539212517, 74.65041598456849670, 13.47518950460405840 ) ) ;
#9209=AXIS2_PLACEMENT_3D ( 'NONE', #9108, #15609, #3349 ) ;
#9210=CARTESIAN_POINT ( 'NONE',  ( -3.778147517876603079, 77.54415174377176356, 12.96054201803634776 ) ) ;
#9211=CARTESIAN_POINT ( 'NONE',  ( -13.39192495110588865, 79.99130628515160879, 1.760924835796330301 ) ) ;
#9212=CARTESIAN_POINT ( 'NONE',  ( 7.499999999999998224, 108.6229112031126220, 2.544524385544284950 ) ) ;
#9216=ADVANCED_FACE ( 'NONE', ( #8072 ), #13437, .T. ) ;
#9218=CARTESIAN_POINT ( 'NONE',  ( -7.272992578804310604, 60.37999999999998835, 10.01041549318726886 ) ) ;
#9220=DIRECTION ( 'NONE',  ( 0.000000000000000000, 0.000000000000000000, -1.000000000000000000 ) ) ;
#9222=CARTESIAN_POINT ( 'NONE',  ( 7.500632703326952644, 75.89905631385393292, -11.22916880707215803 ) ) ;
#9223=CARTESIAN_POINT ( 'NONE',  ( 2.138189944381220897, 69.10311857767972299, -13.50000000000000355 ) ) ;
#9224=CARTESIAN_POINT ( 'NONE',  ( 13.49999999999999822, 72.28000000000000114, 4.386415899144237684 ) ) ;
#9225=CARTESIAN_POINT ( 'NONE',  ( 7.272992578804308828, 39.97999999999999687, 10.01041549318726709 ) ) ;
#9227=CARTESIAN_POINT ( 'NONE',  ( -3.112950329740383548, 58.29192748187959694, -13.14439478270550943 ) ) ;
#9228=CARTESIAN_POINT ( 'NONE',  ( 11.46681240161533744, 45.16376727946777692, 7.124761802481938133 ) ) ;
#9229=CARTESIAN_POINT ( 'NONE',  ( 13.47894498165622146, 69.39940522213998975, 0.8726673866746849084 ) ) ;
#9232=FACE_OUTER_BOUND ( 'NONE', #6293, .T. ) ;
#9233=CARTESIAN_POINT ( 'NONE',  ( -0.9607546724729691956, 55.21454159585901778, -13.46853932749331761 ) ) ;
#9234=CARTESIAN_POINT ( 'NONE',  ( -5.721006742059940642, 50.47200087032891958, 12.22828515855315068 ) ) ;
#9235=CARTESIAN_POINT ( 'NONE',  ( 9.756007997868694659, 63.79342300382748476, -9.331417668431956969 ) ) ;
#9236=CARTESIAN_POINT ( 'NONE',  ( 8.258744052426084892, 42.86546257631440682, -10.67932141422061321 ) ) ;
#9237=CARTESIAN_POINT ( 'NONE',  ( 13.48370246411360007, 39.45286182076745973, -0.6632466905270354429 ) ) ;
#9238=EDGE_LOOP ( 'NONE', ( #12149, #12154 ) ) ;
#9239=CARTESIAN_POINT ( 'NONE',  ( -5.218516266495215383, 70.36866619998554029, -12.45060025241497392 ) ) ;
#9240=CARTESIAN_POINT ( 'NONE',  ( -11.01488299834593398, 61.63543230260535211, -7.805738559095912521 ) ) ;
#9247=CARTESIAN_POINT ( 'NONE',  ( 4.358999193701488473, 47.83663064582479763, 12.78017842383276026 ) ) ;
#9249=CARTESIAN_POINT ( 'NONE',  ( 13.44867813269597256, 57.47128097947902603, -1.193486346532614650 ) ) ;
#9250=CARTESIAN_POINT ( 'NONE',  ( 9.520470885617715595, 67.12999999999999545, 6.917026985038134512 ) ) ;
#9251=CARTESIAN_POINT ( 'NONE',  ( 9.520470885617715595, 79.13000000000000966, 6.917026985038134512 ) ) ;
#9252=CARTESIAN_POINT ( 'NONE',  ( -0.7509811273915951713, 47.65300835411569835, 13.47975592905208408 ) ) ;
#9254=CARTESIAN_POINT ( 'NONE',  ( -8.343458848123578520, 33.47999999999999687, -11.48378591275254124 ) ) ;
#9256=CARTESIAN_POINT ( 'NONE',  ( 10.92172942406179104, 44.72999999999999687, -7.935100905948385908 ) ) ;
#9257=CARTESIAN_POINT ( 'NONE',  ( 8.279083854085270033, 33.86453316571641636, -10.66335730974682328 ) ) ;
#9258=CARTESIAN_POINT ( 'NONE',  ( -4.923806175756706871, 73.35756458033155525, -12.57016591232264346 ) ) ;
#9262=CARTESIAN_POINT ( 'NONE',  ( 2.272985001014427393E-15, 74.17999999999997840, -12.37355403259654807 ) ) ;
#9265=CARTESIAN_POINT ( 'NONE',  ( -0.8503698499406177058, 44.64942536108538462, 13.47335349894747836 ) ) ;
#9267=CARTESIAN_POINT ( 'NONE',  ( 11.70509909484535704, 66.68006203444943480, -6.726482417485054377 ) ) ;
#9268=CARTESIAN_POINT ( 'NONE',  ( 13.49999999999999822, 42.27999999999998693, 4.386415899144237684 ) ) ;
#9269=CARTESIAN_POINT ( 'NONE',  ( -8.444600773403701410, 71.35698679582962711, 10.53374541731779779 ) ) ;
#9271=CARTESIAN_POINT ( 'NONE',  ( -11.67156957293478392, 68.18230872327396241, 6.784133325023568695 ) ) ;
#9273=CARTESIAN_POINT ( 'NONE',  ( 9.383209111987648399, 54.81214344578170028, -9.706371691115846190 ) ) ;
#9276=CARTESIAN_POINT ( 'NONE',  ( -12.69097448754075153, 65.09640307793360137, 4.603221522599070248 ) ) ;
#9278=CARTESIAN_POINT ( 'NONE',  ( -0.4450007729775921073, 35.66413109349914379, 13.50000000012882673 ) ) ;
#9280=ORIENTED_EDGE ( 'NONE', *, *, #5806, .T. ) ;
#9281=DIRECTION ( 'NONE',  ( 0.000000000000000000, -1.000000000000000000, 0.000000000000000000 ) ) ;
#9283=CARTESIAN_POINT ( 'NONE',  ( -10.15792449496252559, 31.58756608837766322, -8.891980599737237867 ) ) ;
#9284=PLANE ( 'NONE',  #12477 ) ;
#9285=CARTESIAN_POINT ( 'NONE',  ( 10.66606376283899849, 60.11536726588247603, 8.275573716453372697 ) ) ;
#9287=CARTESIAN_POINT ( 'NONE',  ( -11.05063697790893151, 53.22239444724469593, 7.754578906011509787 ) ) ;
#9288=CARTESIAN_POINT ( 'NONE',  ( 11.76794919243112325, 43.42999999999999972, 1.441158131103945434E-15 ) ) ;
#9289=CARTESIAN_POINT ( 'NONE',  ( 8.343458848123578520, 70.98000000000000398, 11.48378591275254124 ) ) ;
#9290=CARTESIAN_POINT ( 'NONE',  ( 4.989694493860166169, 50.86003338036692156, 12.54404222780582678 ) ) ;
#9292=CARTESIAN_POINT ( 'NONE',  ( -11.87437356564380231, 37.69230843674236553, -6.422561873346305461 ) ) ;
#9293=CARTESIAN_POINT ( 'NONE',  ( 9.155631919984074329, 36.03665308525259547, 9.921063363676065450 ) ) ;
#9295=CARTESIAN_POINT ( 'NONE',  ( -5.934342680240685119, 74.46365109743285871, 12.12580240077073412 ) ) ;
#9296=( BOUNDED_CURVE ( )  B_SPLINE_CURVE ( 2, ( #8247, #12035, #2729, #5412, #10801, #9488, #4253, #15013, #8157, #2904, #13521, #10629, #1411 ),
 .UNSPECIFIED., .F., .F. ) 
 B_SPLINE_CURVE_WITH_KNOTS ( ( 3, 2, 2, 2, 2, 2, 3 ),
 ( 0.4583333333333333148, 0.4611111111111111382, 0.4666666666666666741, 0.4722222222222222099, 0.4777777777777778012, 0.4833333333333333370, 0.4861111111111111049 ),
 .UNSPECIFIED. ) 
 CURVE ( )  GEOMETRIC_REPRESENTATION_ITEM ( )  RATIONAL_B_SPLINE_CURVE ( ( 0.9755282581475768211, 0.9755282581475765991, 1.000000000000000000, 0.9510565162951535312, 1.000000000000000000, 0.9510565162951535312, 1.000000000000000000, 0.9510565162951535312, 1.000000000000000000, 0.9510565162951535312, 1.000000000000000000, 0.9755282581475768211, 0.9755282581475768211 ) ) 
 REPRESENTATION_ITEM ( '' )  );
#9297=CARTESIAN_POINT ( 'NONE',  ( -13.39208215449344941, 76.99130208596071157, 1.760095884909723685 ) ) ;
#9299=CARTESIAN_POINT ( 'NONE',  ( -12.09599699536484074, 80.15074345234548048, 5.999183590577513492 ) ) ;
#9301=DIRECTION ( 'NONE',  ( 0.000000000000000000, 1.000000000000000000, 0.000000000000000000 ) ) ;
#9303=CARTESIAN_POINT ( 'NONE',  ( 11.76794919243112680, 52.57999999999999829, -3.823638476888993942 ) ) ;
#9307=CARTESIAN_POINT ( 'NONE',  ( -2.522983078673279752E-14, 34.17999999999999972, -13.50000000000000000 ) ) ;
#9308=CARTESIAN_POINT ( 'NONE',  ( 6.211406753928388369, 75.95263760063524217, -11.98618433922874971 ) ) ;
#9310=CARTESIAN_POINT ( 'NONE',  ( 0.000000000000000000, 80.93000000000000682, 0.000000000000000000 ) ) ;
#9311=CARTESIAN_POINT ( 'NONE',  ( 3.636496289402154414, 36.82999999999999119, 11.19198476289190936 ) ) ;
#9312=CARTESIAN_POINT ( 'NONE',  ( -8.891200544363830713E-16, 52.67999999999999972, 13.50000000000000000 ) ) ;
#9313=CARTESIAN_POINT ( 'NONE',  ( -11.18802534011951089, 58.64595677209553060, -7.555005769838619045 ) ) ;
#9314=CARTESIAN_POINT ( 'NONE',  ( 2.733029698975450561, 44.77825814313435160, 13.22063484719044446 ) ) ;
#9315=CARTESIAN_POINT ( 'NONE',  ( 11.44248451431741920, 69.69823784285739521, -7.175533620089728615 ) ) ;
#9317=CARTESIAN_POINT ( 'NONE',  ( 8.003658781154468826, 29.98262411852719467, 10.89684441794628178 ) ) ;
#9319=CARTESIAN_POINT ( 'NONE',  ( -7.425056585661820918, 55.45770273588824040, -11.27470554016973558 ) ) ;
#9320=CARTESIAN_POINT ( 'NONE',  ( -10.98422049107948162, 50.22634674789875930, 7.848442420211892312 ) ) ;
#9321=CARTESIAN_POINT ( 'NONE',  ( 13.13202905021172739, 63.54286607046783075, -3.179279687117263720 ) ) ;
#9322=CARTESIAN_POINT ( 'NONE',  ( 9.030750244556848827, 42.82969952195247032, -10.04841296085617408 ) ) ;
#9323=CARTESIAN_POINT ( 'NONE',  ( 13.31381771166605610, 39.35152470227890120, 2.234341475219394191 ) ) ;
#9325=CARTESIAN_POINT ( 'NONE',  ( -9.869436736026338863, 70.57243612470094263, -9.211103986266559573 ) ) ;
#9332=CARTESIAN_POINT ( 'NONE',  ( 0.5926867827603224947, 61.15868919920450963, -13.50000000000000533 ) ) ;
#9334=CARTESIAN_POINT ( 'NONE',  ( 5.868303365318634057, 71.89333723728957182, 12.18994050556831432 ) ) ;
#9335=CARTESIAN_POINT ( 'NONE',  ( 12.27816310394378618, 57.22451155556443325, 5.613071804343426230 ) ) ;
#9336=CARTESIAN_POINT ( 'NONE',  ( -9.520470885617715595, 71.62999999999999545, -6.917026985038136289 ) ) ;
#9337=CARTESIAN_POINT ( 'NONE',  ( 11.76794919243112325, 73.27999999999998693, 3.823638476888996607 ) ) ;
#9338=CARTESIAN_POINT ( 'NONE',  ( -7.135169524617141157, 47.41465332180884928, 11.46036377623952518 ) ) ;
#9340=CARTESIAN_POINT ( 'NONE',  ( 1.653273178848926472E-15, 80.93000000000000682, 13.50000000000000000 ) ) ;
#9345=CARTESIAN_POINT ( 'NONE',  ( 12.00008335267889770, 33.65815378040278461, -6.184496803329829540 ) ) ;
#9346=CARTESIAN_POINT ( 'NONE',  ( -2.171953792510105785, 73.25809419849412052, -13.32423682163636158 ) ) ;
#9347=ORIENTED_EDGE ( 'NONE', *, *, #16652, .T. ) ;
#9349=CARTESIAN_POINT ( 'NONE',  ( 7.272992578804311492, 76.88000000000000966, -10.01041549318726886 ) ) ;
#9352=CARTESIAN_POINT ( 'NONE',  ( -10.23448921847879767, 44.26842627805543628, 8.804069348283245944 ) ) ;
#9354=CARTESIAN_POINT ( 'NONE',  ( -13.49999999999999822, 41.07999999999999119, 4.386415899144235908 ) ) ;
#9355=CARTESIAN_POINT ( 'NONE',  ( -11.85829282994047951, 71.16891807040060769, 6.452231282962286762 ) ) ;
#9358=CARTESIAN_POINT ( 'NONE',  ( -13.42977164799404477, 67.97782640706279267, 1.375757549377632616 ) ) ;
#9363=CARTESIAN_POINT ( 'NONE',  ( -13.23299063688473254, 64.83510572243652348, -2.688547527704578055 ) ) ;
#9364=CARTESIAN_POINT ( 'NONE',  ( -9.394804903059576162, 35.31160530982987211, 9.694722408649251832 ) ) ;
#9367=CARTESIAN_POINT ( 'NONE',  ( -8.048289098797699381, 31.48504910120772493, -10.83861414461898676 ) ) ;
#9370=CARTESIAN_POINT ( 'NONE',  ( 0.6926007647112457644, 59.70487025096267786, 13.50000000000703082 ) ) ;
#9372=CARTESIAN_POINT ( 'NONE',  ( -11.47944231658861369, 53.19580613508185962, 7.116485988125050177 ) ) ;
#9373=CARTESIAN_POINT ( 'NONE',  ( -3.636496289402155746, 51.53000000000000114, 11.19198476289190936 ) ) ;
#9375=CARTESIAN_POINT ( 'NONE',  ( 8.343458848123578520, 67.98000000000000398, 11.48378591275254124 ) ) ;
#9376=EDGE_CURVE ( 'NONE', #14883, #39, #12113, .T. ) ;
#9377=CARTESIAN_POINT ( 'NONE',  ( 12.48943337819306620, 51.24351970055675309, 5.124847635520794142 ) ) ;
#9378=CARTESIAN_POINT ( 'NONE',  ( -8.085997966447257213, 37.48674016390275199, -10.81050427210594300 ) ) ;
#9379=CARTESIAN_POINT ( 'NONE',  ( 9.439026618432063032, 36.05056385420601117, 9.652180085524300068 ) ) ;
#9381=CARTESIAN_POINT ( 'NONE',  ( -8.677731035997348741, 74.34615417660486969, 10.34231826630725237 ) ) ;
#9382=CARTESIAN_POINT ( 'NONE',  ( -13.29658185220932332, 76.84789797714496729, -2.334733406331294781 ) ) ;
#9383=CARTESIAN_POINT ( 'NONE',  ( -8.225013884042102319, 80.36731853247339075, 10.71434597753230911 ) ) ;
#9384=CARTESIAN_POINT ( 'NONE',  ( 7.499999999999998224, 108.7391404411723528, -0.5315352956498786696 ) ) ;
#9387=CARTESIAN_POINT ( 'NONE',  ( -9.520470885617715595, 44.62999999999999545, -6.917026985038136289 ) ) ;
#9391=CARTESIAN_POINT ( 'NONE',  ( -11.36904938338338944, 40.65721801956971859, -7.283062199855843133 ) ) ;
#9393=CARTESIAN_POINT ( 'NONE',  ( 0.000000000000000000, 0.000000000000000000, 0.000000000000000000 ) ) ;
#9394=CARTESIAN_POINT ( 'NONE',  ( 12.66318051525177601, 75.60094073508014390, -4.729132707123133272 ) ) ;
#9395=CARTESIAN_POINT ( 'NONE',  ( 8.343458848123580296, 67.98000000000000398, 11.48378591275253768 ) ) ;
#9396=CARTESIAN_POINT ( 'NONE',  ( 4.171729424061791924, 51.03000000000000114, -12.83926296998457239 ) ) ;
#9397=CARTESIAN_POINT ( 'NONE',  ( 11.76794919243112680, 43.57999999999999119, -3.823638476888993942 ) ) ;
#9398=CARTESIAN_POINT ( 'NONE',  ( -8.657037944518233274, 41.34728218387066789, 10.36125059353578948 ) ) ;
#9400=CARTESIAN_POINT ( 'NONE',  ( -12.77783441696706035, 58.77300612785465006, -4.356290537409963193 ) ) ;
#9401=CARTESIAN_POINT ( 'NONE',  ( 4.678274206804918123, 44.84844931136031221, 12.66349204453718968 ) ) ;
#9403=CARTESIAN_POINT ( 'NONE',  ( -4.171729424061791036, 55.52999999999999403, 12.83926296998457239 ) ) ;
#9404=CARTESIAN_POINT ( 'NONE',  ( 10.38497083786669428, 30.09949477856799760, 8.633462984270375173 ) ) ;
#9405=CARTESIAN_POINT ( 'NONE',  ( -10.71735289789100420, 55.61806186037063071, -8.210225439848542806 ) ) ;
#9406=CARTESIAN_POINT ( 'NONE',  ( -11.21169442594827892, 49.64742185618261772, -7.519853369252744280 ) ) ;
#9407=CARTESIAN_POINT ( 'NONE',  ( 12.87829787502431245, 63.57557519788824152, -4.054628780689018441 ) ) ;
#9408=CARTESIAN_POINT ( 'NONE',  ( 11.92131337477997732, 42.66417587640939502, -6.335005369018095855 ) ) ;
#9409=CARTESIAN_POINT ( 'NONE',  ( 9.285075054945489015, 39.04297856348830464, 9.799891255916394428 ) ) ;
#9411=CARTESIAN_POINT ( 'NONE',  ( -7.756731982646783763, 70.47211894010109745, -11.04912417935179647 ) ) ;
#9412=CARTESIAN_POINT ( 'NONE',  ( -5.281055406448098636E-10, 61.18000001472334759, -13.50000000000000000 ) ) ;
#9417=CARTESIAN_POINT ( 'NONE',  ( 6.605773061280451941, 47.92331672993605451, 11.77343924215295345 ) ) ;
#9419=AXIS2_PLACEMENT_3D ( 'NONE', #14476, #11934, #2539 ) ;
#9420=CARTESIAN_POINT ( 'NONE',  ( 9.811143588542840632, 72.06941418877464400, 9.273190923045845580 ) ) ;
#9421=CARTESIAN_POINT ( 'NONE',  ( 12.38238512554978499, 57.62633858785935814, -5.378349744821834477 ) ) ;
#9422=CARTESIAN_POINT ( 'NONE',  ( -7.272992578804307939, 71.48000000000000398, -10.01041549318726886 ) ) ;
#9423=CARTESIAN_POINT ( 'NONE',  ( -7.576616670048093940E-16, 72.68000000000000682, 12.37355403259654985 ) ) ;
#9424=CARTESIAN_POINT ( 'NONE',  ( -7.098413309481311551, 47.41620383881762990, 11.48314148660388767 ) ) ;
#9425=LINE ( 'NONE', #9340, #16609 ) ;
#9426=CARTESIAN_POINT ( 'NONE',  ( 2.445080149700053643E-15, 39.17999999999999972, -13.50000000000000000 ) ) ;
#9427=CARTESIAN_POINT ( 'NONE',  ( -4.171729424061787483, 33.32999999999999829, -12.83926296998457417 ) ) ;
#9429=CARTESIAN_POINT ( 'NONE',  ( -8.891200544363830713E-16, 52.67999999999999972, 13.50000000000000000 ) ) ;
#9430=CARTESIAN_POINT ( 'NONE',  ( 11.89722853480184028, 33.66600382463642660, -6.380526270711741610 ) ) ;
#9431=CARTESIAN_POINT ( 'NONE',  ( -9.624821359540113974, 73.55990925749743781, -9.466443300615020817 ) ) ;
#9434=CARTESIAN_POINT ( 'NONE',  ( -3.636496289402155746, 72.53000000000000114, 11.19198476289190936 ) ) ;
#9436=CARTESIAN_POINT ( 'NONE',  ( -13.32261196877928455, 41.00656928112289279, 2.181370886427688394 ) ) ;
#9438=EDGE_CURVE ( 'NONE', #16090, #3801, #7620, .T. ) ;
#9439=CARTESIAN_POINT ( 'NONE',  ( -10.12145965770221245, 44.27437845011841233, 8.933423452156974420 ) ) ;
#9441=CARTESIAN_POINT ( 'NONE',  ( 10.92172942406179104, 39.72999999999999687, -7.935100905948385908 ) ) ;
#9442=CARTESIAN_POINT ( 'NONE',  ( -13.45001587941835197, 70.97025115243951632, 1.160810400985216484 ) ) ;
#9444=CARTESIAN_POINT ( 'NONE',  ( -12.56865293787816462, 67.75091737192668973, -4.934974244349399797 ) ) ;
#9446=CARTESIAN_POINT ( 'NONE',  ( 11.65835260217848912, 54.68333460578584493, -6.808186811182635800 ) ) ;
#9449=CARTESIAN_POINT ( 'NONE',  ( -12.43543891747863839, 65.12177667763330646, 5.262208274864947910 ) ) ;
#9450=CARTESIAN_POINT ( 'NONE',  ( -13.47176300034568541, 34.89984414028458559, -0.8728053654163654418 ) ) ;
#9453=CARTESIAN_POINT ( 'NONE',  ( -8.891200544363830713E-16, 79.67999999999999261, 13.50000000000000000 ) ) ;
#9454=CARTESIAN_POINT ( 'NONE',  ( -0.5734647119475105859, 31.20060767735286333, -13.49031509358949243 ) ) ;
#9455=CARTESIAN_POINT ( 'NONE',  ( 5.953140201857509695, 72.96290519792380280, -12.11652618179868668 ) ) ;
#9459=CARTESIAN_POINT ( 'NONE',  ( -13.23519524994845042, 53.02388892134538878, 2.661131415613865236 ) ) ;
#9460=CARTESIAN_POINT ( 'NONE',  ( 9.520470885617717371, 46.73000000000000398, -6.917026985038131848 ) ) ;
#9461=CARTESIAN_POINT ( 'NONE',  ( 10.55906642891832448, 51.10936410628003301, 8.412101771180822141 ) ) ;
#9463=CARTESIAN_POINT ( 'NONE',  ( -10.05898634321896346, 37.58241540748306875, -9.004437385054949061 ) ) ;
#9464=AXIS2_PLACEMENT_3D ( 'NONE', #13202, #1001, #10479 ) ;
#9465=CARTESIAN_POINT ( 'NONE',  ( 9.790434661910198955, 36.06810143375782474, 9.303453747971381915 ) ) ;
#9467=CARTESIAN_POINT ( 'NONE',  ( -12.00341789873817255, 74.15789563195407652, 6.178041647018932991 ) ) ;
#9468=CARTESIAN_POINT ( 'NONE',  ( -11.21206813385310852, 76.64744563254819809, -7.519279139868476847 ) ) ;
#9469=CARTESIAN_POINT ( 'NONE',  ( -12.42682143791030747, 80.12235603135506778, 5.276029534630485962 ) ) ;
#9471=CARTESIAN_POINT ( 'NONE',  ( -4.886222543809949137, 80.93000000000003524, 11.77926528190478095 ) ) ;
#9475=CARTESIAN_POINT ( 'NONE',  ( 7.272992578804308828, 45.97999999999999687, 10.01041549318726886 ) ) ;
#9480=CARTESIAN_POINT ( 'NONE',  ( -8.140112397462228699, 40.48917452635999581, -10.76980339117528196 ) ) ;
#9481=CARTESIAN_POINT ( 'NONE',  ( 2.445080149700053643E-15, 36.17999999999999972, -13.50000000000000000 ) ) ;
#9482=CARTESIAN_POINT ( 'NONE',  ( 11.26111035850912145, 75.15046918880804583, 7.446692750201517441 ) ) ;
#9484=CARTESIAN_POINT ( 'NONE',  ( -7.272992578804307939, 41.47999999999999687, -10.01041549318726886 ) ) ;
#9485=CARTESIAN_POINT ( 'NONE',  ( -11.19689435447929071, 41.21349520832467306, 7.541861633535862808 ) ) ;
#9486=CARTESIAN_POINT ( 'NONE',  ( -9.286707789763200438, 58.54294910056232482, -9.800380398344652022 ) ) ;
#9488=CARTESIAN_POINT ( 'NONE',  ( 13.50000000000000355, 59.57999999999999829, -4.386415899144233244 ) ) ;
#9489=CARTESIAN_POINT ( 'NONE',  ( 11.06245251677889740, 30.13829864597929742, 7.738284462911099837 ) ) ;
#9490=LINE ( 'NONE', #2994, #623 ) ;
#9491=CARTESIAN_POINT ( 'NONE',  ( -12.08639118943488455, 49.70860411622489750, -6.014117973902937564 ) ) ;
#9492=CARTESIAN_POINT ( 'NONE',  ( 13.49574338918140626, 63.41592130795832816, 0.4033985791695099965 ) ) ;
#9493=CARTESIAN_POINT ( 'NONE',  ( 12.94155513399510404, 42.56773774999591353, -3.846463401272276261 ) ) ;
#9495=EDGE_LOOP ( 'NONE', ( #3000, #325, #8647, #9194 ) ) ;
#9496=CARTESIAN_POINT ( 'NONE',  ( 2.138189944381242213, 75.10311857767970878, -13.49999999999999822 ) ) ;
#9497=CARTESIAN_POINT ( 'NONE',  ( -8.891200544363830713E-16, 49.67999999999999261, 13.50000000000000000 ) ) ;
#9501=CARTESIAN_POINT ( 'NONE',  ( -5.427788510536279531, 43.37664531000118728, -12.36142337679662973 ) ) ;
#9503=CARTESIAN_POINT ( 'NONE',  ( 10.10993224895466369, 60.77529409556134965, -8.962226066154812543 ) ) ;
#9504=AXIS2_PLACEMENT_3D ( 'NONE', #10870, #16239, #4148 ) ;
#9507=CARTESIAN_POINT ( 'NONE',  ( 12.39353830234175824, 57.62533442192442834, -5.352606972886608361 ) ) ;
#9508=CARTESIAN_POINT ( 'NONE',  ( -7.576616670048093940E-16, 66.67999999999997840, 12.37355403259654985 ) ) ;
#9509=CARTESIAN_POINT ( 'NONE',  ( 2.272985001014427788E-15, 77.18000000000000682, -12.37355403259654985 ) ) ;
#9510=CARTESIAN_POINT ( 'NONE',  ( -3.807942577807816420, 47.54308049960635429, 12.95182113153237502 ) ) ;
#9512=CARTESIAN_POINT ( 'NONE',  ( 13.50000000000000355, 74.58000000000001251, -4.386415899144233244 ) ) ;
#9518=CARTESIAN_POINT ( 'NONE',  ( 11.23618775536431436, 33.71102971822809025, -7.483199226156876271 ) ) ;
#9519=CARTESIAN_POINT ( 'NONE',  ( -2.604932354848102261, 73.27367133763648610, -13.24695926549161129 ) ) ;
#9522=CARTESIAN_POINT ( 'NONE',  ( -13.49999999999999822, 42.77999999999999403, -4.386415899144240349 ) ) ;
#9523=ORIENTED_EDGE ( 'NONE', *, *, #206, .F. ) ;
#9524=EDGE_CURVE ( 'NONE', #12569, #149, #11323, .T. ) ;
#9526=CARTESIAN_POINT ( 'NONE',  ( -11.23485739642284464, 44.21114091592843209, 7.485350584702932686 ) ) ;
#9529=CARTESIAN_POINT ( 'NONE',  ( -13.49999999999999822, 44.07999999999999829, 4.386415899144235908 ) ) ;
#9530=CARTESIAN_POINT ( 'NONE',  ( -8.691771469529815392E-16, 49.67999999999999972, 14.19474002721660355 ) ) ;
#9531=CARTESIAN_POINT ( 'NONE',  ( -12.73079347874323908, 71.09226311646531826, 4.495458693738632050 ) ) ;
#9533=CARTESIAN_POINT ( 'NONE',  ( -13.43160263846500335, 67.88282665543684402, -1.357254972949814897 ) ) ;
#9535=CARTESIAN_POINT ( 'NONE',  ( 13.19418465749268599, 54.53154371968964398, -2.869303380193378494 ) ) ;
#9537=CARTESIAN_POINT ( 'NONE',  ( -13.45471606681021015, 64.89176115380030296, -1.105190539164891295 ) ) ;
#9539=CARTESIAN_POINT ( 'NONE',  ( -13.47350605204804097, 34.90077836227690966, -0.8454715895919912017 ) ) ;
#9540=VERTEX_POINT ( 'NONE', #2235 ) ;
#9543=CARTESIAN_POINT ( 'NONE',  ( 8.106489558427483644, 72.87234586791355184, -10.79566516057443337 ) ) ;
#9545=CARTESIAN_POINT ( 'NONE',  ( 3.912904983860617136, 59.82044921492690293, 12.92374366791880469 ) ) ;
#9547=CARTESIAN_POINT ( 'NONE',  ( -13.49999999999999822, 71.08000000000001251, 4.386415899144235908 ) ) ;
#9548=CARTESIAN_POINT ( 'NONE',  ( -11.95834195965728242, 52.69827122100793559, -6.277836442959745078 ) ) ;
#9549=CARTESIAN_POINT ( 'NONE',  ( 7.272992578804308828, 45.98000000000000398, 10.01041549318726709 ) ) ;
#9550=CARTESIAN_POINT ( 'NONE',  ( -13.49999999999999822, 63.78000000000000114, -4.386415899144240349 ) ) ;
#9551=CARTESIAN_POINT ( 'NONE',  ( 12.48553484639394462, 51.24315187460019416, 5.134337538193736172 ) ) ;
#9552=CARTESIAN_POINT ( 'NONE',  ( -8.363913707455445490, 37.49932944145390934, -10.59726195709811947 ) ) ;
#9553=CARTESIAN_POINT ( 'NONE',  ( 4.181727136617158003, 35.83035942868416868, 12.83601768139505594 ) ) ;
#9555=CARTESIAN_POINT ( 'NONE',  ( -13.01412793683608804, 74.05813771021030334, 3.589233157574757360 ) ) ;
#9556=CARTESIAN_POINT ( 'NONE',  ( -12.78816704283054762, 76.77399786514027369, -4.329514614045784526 ) ) ;
#9557=CARTESIAN_POINT ( 'NONE',  ( -8.236863458086046919, 79.49291995815075040, -10.73295259625500009 ) ) ;
#9559=CARTESIAN_POINT ( 'NONE',  ( 5.896062637424393849, 80.92999999999999261, 12.11648925032670832 ) ) ;
#9560=FACE_OUTER_BOUND ( 'NONE', #2586, .T. ) ;
#9562=CARTESIAN_POINT ( 'NONE',  ( 9.520470885617717371, 43.72999999999999687, -6.917026985038131848 ) ) ;
#9565=CARTESIAN_POINT ( 'NONE',  ( -5.605660797254122585, 40.38350727605969581, -12.28115835899099118 ) ) ;
#9566=CARTESIAN_POINT ( 'NONE',  ( 6.750022862106050958, 31.26259509543302784, 11.69132975161703492 ) ) ;
#9567=CARTESIAN_POINT ( 'NONE',  ( 13.06941462424293121, 75.55044996165509019, -3.382384493177171603 ) ) ;
#9570=CARTESIAN_POINT ( 'NONE',  ( 8.050216715958701030, 31.03187307936174832, 8.940658242654158983 ) ) ;
#9571=CARTESIAN_POINT ( 'NONE',  ( -9.319066580405237943, 41.31534733134024151, 9.767548834432302485 ) ) ;
#9572=CARTESIAN_POINT ( 'NONE',  ( -12.47057163453939310, 58.74156942395950409, -5.176736132799251600 ) ) ;
#9574=CARTESIAN_POINT ( 'NONE',  ( 2.929103925447447132, 44.78531871342022441, 13.17840735884215064 ) ) ;
#9575=CARTESIAN_POINT ( 'NONE',  ( -13.50000000000000000, 54.92999999999999972, -3.306546357697853733E-15 ) ) ;
#9578=CARTESIAN_POINT ( 'NONE',  ( -12.17504944591498273, 49.71587186443941420, -5.832774803456854507 ) ) ;
#9579=CARTESIAN_POINT ( 'NONE',  ( 12.94006017376627860, 63.29219168140004825, 3.847937226494118956 ) ) ;
#9580=CARTESIAN_POINT ( 'NONE',  ( 10.64860572984884790, 42.11438410854437109, 8.298049206624620311 ) ) ;
#9581=CARTESIAN_POINT ( 'NONE',  ( 4.045770767957217018, 38.82545391565042081, 12.87990362912008990 ) ) ;
#9584=CARTESIAN_POINT ( 'NONE',  ( -1.962467107901933794, 70.25054030898461122, -13.35786085374755849 ) ) ;
#9587=ORIENTED_EDGE ( 'NONE', *, *, #3408, .F. ) ;
#9588=CARTESIAN_POINT ( 'NONE',  ( -4.189387794536774123, 43.33065430922783179, -12.83365974533868936 ) ) ;
#9589=CARTESIAN_POINT ( 'NONE',  ( -7.499999999999999112, 105.3920397463311218, -8.709571264514705646 ) ) ;
#9590=CARTESIAN_POINT ( 'NONE',  ( 13.00154923021119302, 60.55982641677310596, -3.634527857254126193 ) ) ;
#9593=CARTESIAN_POINT ( 'NONE',  ( 9.959380740143405575, 66.78290531437225752, -9.113807157362280975 ) ) ;
#9594=CARTESIAN_POINT ( 'NONE',  ( 6.860306926835040287, 56.93364315233684181, 11.63957199842341517 ) ) ;
#9595=CARTESIAN_POINT ( 'NONE',  ( 2.272985001014427788E-15, 56.17999999999999972, -12.37355403259654985 ) ) ;
#9596=CARTESIAN_POINT ( 'NONE',  ( -7.272992578804310604, 63.37999999999998835, 10.01041549318726709 ) ) ;
#9597=CARTESIAN_POINT ( 'NONE',  ( -11.37861599013445257, 47.20202813202893566, 7.264810526584298600 ) ) ;
#9599=CARTESIAN_POINT ( 'NONE',  ( 3.542742451760277689, 46.05382628669764244, -13.14678535250671843 ) ) ;
#9601=EDGE_CURVE ( 'NONE', #11528, #16381, #17009, .T. ) ;
#9605=CARTESIAN_POINT ( 'NONE',  ( 10.40591568030824732, 33.75906600926769130, -8.600427378247252008 ) ) ;
#9608=ORIENTED_EDGE ( 'NONE', *, *, #12715, .F. ) ;
#9609=CARTESIAN_POINT ( 'NONE',  ( -5.591496387441557303, 62.47704092548192278, 12.28760602409226088 ) ) ;
#9610=ORIENTED_EDGE ( 'NONE', *, *, #1462, .T. ) ;
#9611=CARTESIAN_POINT ( 'NONE',  ( -13.43504215837644011, 40.88299209765439457, -1.356889373904522245 ) ) ;
#9614=CARTESIAN_POINT ( 'NONE',  ( -12.83028172577782655, 44.08205989162794936, 4.222530735082791864 ) ) ;
#9616=CARTESIAN_POINT ( 'NONE',  ( 10.92172942406179104, 42.72999999999999687, -7.935100905948385908 ) ) ;
#9617=CARTESIAN_POINT ( 'NONE',  ( 10.92172942406178926, 50.13000000000000256, 7.935100905948387684 ) ) ;
#9618=CARTESIAN_POINT ( 'NONE',  ( -13.49804976266443113, 70.92212470242434108, -0.2296839510666886242 ) ) ;
#9619=ADVANCED_FACE ( 'NONE', ( #392 ), #1875, .T. ) ;
#9621=CARTESIAN_POINT ( 'NONE',  ( -5.522359042343270019, 67.38028659687103072, -12.31888227721426077 ) ) ;
#9623=CARTESIAN_POINT ( 'NONE',  ( 11.88709381102925100, 54.19314474854091657, 6.403576458692946005 ) ) ;
#9624=CARTESIAN_POINT ( 'NONE',  ( -11.87378271711010846, 65.16811738021863221, 6.431528113332499963 ) ) ;
#9625=ORIENTED_EDGE ( 'NONE', *, *, #8816, .F. ) ;
#9626=CARTESIAN_POINT ( 'NONE',  ( 2.445080149700053643E-15, 63.17999999999998550, -13.50000000000000000 ) ) ;
#9627=CARTESIAN_POINT ( 'NONE',  ( -12.50808303647379027, 35.11473487356274603, 5.079913338622167096 ) ) ;
#9629=CARTESIAN_POINT ( 'NONE',  ( 13.06764686229368877, 78.55070251195772357, -3.389196011057948876 ) ) ;
#9632=CARTESIAN_POINT ( 'NONE',  ( -6.500262833459416356, 31.41893658545258461, -11.83852468435292238 ) ) ;
#9633=CARTESIAN_POINT ( 'NONE',  ( 5.937628886501558512, 72.96351727730900905, -12.12413192913790994 ) ) ;
#9634=CARTESIAN_POINT ( 'NONE',  ( 7.500000000000000888, 98.93000000000002103, 1.224646799147353059E-15 ) ) ;
#9636=CARTESIAN_POINT ( 'NONE',  ( 13.50000000000000355, 75.57999999999999829, -4.386415899144233244 ) ) ;
#9637=CARTESIAN_POINT ( 'NONE',  ( -13.16475778499479077, 53.03611007690431478, 2.991896333637389827 ) ) ;
#9638=CARTESIAN_POINT ( 'NONE',  ( -11.76794919243112325, 50.92999999999999972, -2.882316262207890869E-15 ) ) ;
#9639=CARTESIAN_POINT ( 'NONE',  ( 8.343458848123578520, 64.97999999999998977, 11.48378591275254124 ) ) ;
#9640=CARTESIAN_POINT ( 'NONE',  ( 1.449568327994486205, 50.73212129594191566, 13.42208168688401138 ) ) ;
#9641=CARTESIAN_POINT ( 'NONE',  ( 12.79854278110677335, 69.27532975822802541, 4.295070630454624450 ) ) ;
#9643=CARTESIAN_POINT ( 'NONE',  ( 13.30596133608670684, 36.34985342903621586, 2.280658287200722611 ) ) ;
#9645=CARTESIAN_POINT ( 'NONE',  ( -13.01763028107069786, 74.05766348689789424, 3.576502924852020371 ) ) ;
#9646=CARTESIAN_POINT ( 'NONE',  ( -9.698786012810412416, 76.56353993267508429, -9.394740705748864329 ) ) ;
#9648=CARTESIAN_POINT ( 'NONE',  ( -3.737279461696752201E-15, 73.17999999999999261, -13.50000000000000000 ) ) ;
#9651=CARTESIAN_POINT ( 'NONE',  ( -11.76794919243112325, 44.77999999999999403, -3.823638476888998827 ) ) ;
#9653=CARTESIAN_POINT ( 'NONE',  ( -10.26398047125928059, 40.59323998322559390, -8.769304803125226755 ) ) ;
#9654=CARTESIAN_POINT ( 'NONE',  ( -0.5908154233732432203, 34.20124354298254588, -13.50000000000000000 ) ) ;
#9655=CARTESIAN_POINT ( 'NONE',  ( 13.37172142950504039, 75.49701186157564337, -1.917096768542019269 ) ) ;
#9658=LINE ( 'NONE', #13857, #10753 ) ;
#9659=CARTESIAN_POINT ( 'NONE',  ( -11.34595542185857830, 41.20413535737528576, 7.316697782643927894 ) ) ;
#9660=CARTESIAN_POINT ( 'NONE',  ( 0.2967297785716159764, 52.16933069184229055, -13.50000000000000355 ) ) ;
#9661=CARTESIAN_POINT ( 'NONE',  ( 6.246728678326504358, 44.90877324909803292, 11.96783861637221946 ) ) ;
#9662=DIRECTION ( 'NONE',  ( 0.000000000000000000, 0.000000000000000000, -1.000000000000000000 ) ) ;
#9664=CARTESIAN_POINT ( 'NONE',  ( -8.291044507619272909E-14, 57.17999999999999972, -13.50000000000000000 ) ) ;
#9665=CARTESIAN_POINT ( 'NONE',  ( -8.170351414437741155, 49.48998335967211659, -10.77201803496731181 ) ) ;
#9666=VECTOR ( 'NONE', #9766, 1000.000000000000000 ) ;
#9667=CARTESIAN_POINT ( 'NONE',  ( 12.85582805263922523, 63.28191613100854340, 4.121090797647687154 ) ) ;
#9668=CARTESIAN_POINT ( 'NONE',  ( 9.124530604564489167, 42.03482481052925834, 9.963362446407785455 ) ) ;
#9669=CARTESIAN_POINT ( 'NONE',  ( 5.573104024729542694, 48.97745214738866082, -12.29793966966750318 ) ) ;
#9675=CARTESIAN_POINT ( 'NONE',  ( -11.96708799091716280, 43.69658687964136590, -6.330084694767312392 ) ) ;
#9676=CARTESIAN_POINT ( 'NONE',  ( -7.499999999999998224, 108.6662573213694429, 2.063574628993714022 ) ) ;
#9677=CARTESIAN_POINT ( 'NONE',  ( 13.47423762379474610, 60.45965211740971057, -0.8577208552641553130 ) ) ;
#9679=CARTESIAN_POINT ( 'NONE',  ( 1.653273178848926472E-15, 80.93000000000000682, 13.50000000000000000 ) ) ;
#9680=CARTESIAN_POINT ( 'NONE',  ( 13.45263629682293782, 66.39079416573831338, 1.129939417163000615 ) ) ;
#9681=CARTESIAN_POINT ( 'NONE',  ( 2.041061911512047189, 56.75340703010081000, 13.34548534108487061 ) ) ;
#9682=CARTESIAN_POINT ( 'NONE',  ( -11.76794919243112325, 56.92999999999999972, -2.882316262207890869E-15 ) ) ;
#9683=CARTESIAN_POINT ( 'NONE',  ( 7.272992578804308828, 63.97999999999998977, 10.01041549318726709 ) ) ;
#9684=AXIS2_PLACEMENT_3D ( 'NONE', #8449, #6221, #11607 ) ;
#9685=CARTESIAN_POINT ( 'NONE',  ( -12.37777064474171240, 47.12682678988542051, 5.391107621120311499 ) ) ;
#9687=DIRECTION ( 'NONE',  ( 0.000000000000000000, 0.000000000000000000, -1.000000000000000000 ) ) ;
#9688=CARTESIAN_POINT ( 'NONE',  ( 10.46257632922059777, 30.75595908514958055, -8.531413285560027759 ) ) ;
#9691=CARTESIAN_POINT ( 'NONE',  ( 12.00000000000000533, 98.93000000000002103, 1.224646799147353059E-15 ) ) ;
#9692=CARTESIAN_POINT ( 'NONE',  ( 13.35604756179318464, 33.50086920132254420, -2.024719069001440275 ) ) ;
#9694=CARTESIAN_POINT ( 'NONE',  ( 0.01847178140511852168, 40.17933609548848750, -13.50000000169804792 ) ) ;
#9697=CARTESIAN_POINT ( 'NONE',  ( -4.171729424061791036, 43.53000000000000114, 12.83926296998457239 ) ) ;
#9702=CARTESIAN_POINT ( 'NONE',  ( -13.46309576110611239, 43.89548648200645431, -0.9975764637713919747 ) ) ;
#9703=ADVANCED_FACE ( 'NONE', ( #3555 ), #6311, .T. ) ;
#9705=CARTESIAN_POINT ( 'NONE',  ( -8.343458848123576743, 34.47999999999998977, -11.48378591275254301 ) ) ;
#9706=CARTESIAN_POINT ( 'NONE',  ( -13.49999999999999822, 46.07999999999999119, 4.386415899144235908 ) ) ;
#9707=CIRCLE ( 'NONE', #2051, 8.999999999999994671 ) ;
#9709=CARTESIAN_POINT ( 'NONE',  ( -10.25381866242074658, 67.59266383462906447, -8.782231892207333246 ) ) ;
#9711=CARTESIAN_POINT ( 'NONE',  ( 13.05622502498204973, 54.30767452267900097, 3.432944569055587536 ) ) ;
#9712=CARTESIAN_POINT ( 'NONE',  ( -6.044985788396838977, 64.40073192607152919, -12.07114179645960306 ) ) ;
#9714=CARTESIAN_POINT ( 'NONE',  ( -11.84369742284435212, 34.69003919059396424, -6.478953855484251179 ) ) ;
#9715=ORIENTED_EDGE ( 'NONE', *, *, #12398, .F. ) ;
#9716=CARTESIAN_POINT ( 'NONE',  ( 13.40174896357971690, 78.37331495776443546, 1.625770599117996040 ) ) ;
#9717=CARTESIAN_POINT ( 'NONE',  ( 13.50000000000000000, 47.42999999999999972, 1.653273178848926867E-15 ) ) ;
#9718=CARTESIAN_POINT ( 'NONE',  ( -13.49999999999999822, 36.78000000000000114, -4.386415899144240349 ) ) ;
#9719=CARTESIAN_POINT ( 'NONE',  ( 2.393234054935799549, 73.09397480562172689, -13.29186828747294946 ) ) ;
#9720=CARTESIAN_POINT ( 'NONE',  ( 6.595643076912385716, 59.92293436221358860, 11.77912079893219044 ) ) ;
#9722=CARTESIAN_POINT ( 'NONE',  ( 10.92172942406178926, 63.12999999999998835, 7.935100905948387684 ) ) ;
#9723=CARTESIAN_POINT ( 'NONE',  ( -11.20884234386199907, 52.64724540846238909, -7.524086072081253462 ) ) ;
#9724=CARTESIAN_POINT ( 'NONE',  ( 3.636496289402154414, 42.82999999999999829, 11.19198476289190936 ) ) ;
#9725=CARTESIAN_POINT ( 'NONE',  ( 13.50000000000000000, 59.42999999999999972, 1.653273178848926867E-15 ) ) ;
#9727=CARTESIAN_POINT ( 'NONE',  ( 10.16932816747080714, 69.08810190452132360, 8.881946212672056973 ) ) ;
#9728=CARTESIAN_POINT ( 'NONE',  ( -2.390223969659595493, 37.26593391360592022, -13.29042876175976140 ) ) ;
#9731=CARTESIAN_POINT ( 'NONE',  ( -8.353752051756876185, 74.36112887588994624, 10.60510391640503158 ) ) ;
#9732=CARTESIAN_POINT ( 'NONE',  ( -7.214465774454332347, 76.44870526399246558, -11.41059411142753177 ) ) ;
#9733=CARTESIAN_POINT ( 'NONE',  ( -4.375655242806324452, 79.33737030707416693, -12.77121110675854787 ) ) ;
#9735=CARTESIAN_POINT ( 'NONE',  ( -11.29885598845895878, 80.93000000000000682, 4.264693269851297153 ) ) ;
#9738=CARTESIAN_POINT ( 'NONE',  ( -9.520470885617717371, 48.23000000000000398, 6.917026985038133624 ) ) ;
#9741=CARTESIAN_POINT ( 'NONE',  ( -0.8899778701273365344, 32.64814878773904638, 13.47798037021882500 ) ) ;
#9742=CARTESIAN_POINT ( 'NONE',  ( 12.20100399948782055, 75.21792834827131458, 5.778299298237292270 ) ) ;
#9744=CARTESIAN_POINT ( 'NONE',  ( 2.272985001014427788E-15, 32.17999999999999972, -12.37355403259654985 ) ) ;
#9745=CARTESIAN_POINT ( 'NONE',  ( -12.56035316918483069, 41.10966195528746425, 4.948503074325818929 ) ) ;
#9747=CARTESIAN_POINT ( 'NONE',  ( 4.956108786688578682, 52.00122210954356916, -12.55763373905415392 ) ) ;
#9748=CARTESIAN_POINT ( 'NONE',  ( -7.264190498165104870, 38.40920588462986984, 11.37994681411909781 ) ) ;
#9751=CARTESIAN_POINT ( 'NONE',  ( -7.121125983345519828, 49.44472971541036088, -11.47042538111829657 ) ) ;
#9752=CARTESIAN_POINT ( 'NONE',  ( 9.577391939495372597, 63.05751216351371369, 9.514465974150908778 ) ) ;
#9753=CARTESIAN_POINT ( 'NONE',  ( 13.33619231753804613, 42.35646018360174025, 2.097296710946952025 ) ) ;
#9754=CARTESIAN_POINT ( 'NONE',  ( 4.704464924678342541, 38.84934771415909438, 12.65631601052290911 ) ) ;
#9756=ORIENTED_EDGE ( 'NONE', *, *, #13864, .T. ) ;
#9757=CARTESIAN_POINT ( 'NONE',  ( -7.272992578804307939, 77.48000000000000398, -10.01041549318727064 ) ) ;
#9762=CARTESIAN_POINT ( 'NONE',  ( -11.13438765174952927, 43.64266397379046225, -7.633879821230919127 ) ) ;
#9763=CARTESIAN_POINT ( 'NONE',  ( -7.500000000000000888, 106.0136413093990910, 8.254396200996682254 ) ) ;
#9764=CARTESIAN_POINT ( 'NONE',  ( 9.400436423136840247, 60.81129539022329311, -9.689632365782298251 ) ) ;
#9766=DIRECTION ( 'NONE',  ( -0.000000000000000000, -1.000000000000000000, -0.000000000000000000 ) ) ;
#9767=CARTESIAN_POINT ( 'NONE',  ( 13.40858775979793194, 66.48465639307120512, -1.568604466400953301 ) ) ;
#9769=CARTESIAN_POINT ( 'NONE',  ( -3.636496289402153081, 62.32999999999999829, -11.19198476289190936 ) ) ;
#9770=CARTESIAN_POINT ( 'NONE',  ( 8.343458848123583849, 35.87999999999999545, -11.48378591275253768 ) ) ;
#9771=CARTESIAN_POINT ( 'NONE',  ( -3.636496289402155746, 63.53000000000000114, 11.19198476289190936 ) ) ;
#9772=CARTESIAN_POINT ( 'NONE',  ( -13.17996130359396645, 46.82475302137621753, -2.970985941612378500 ) ) ;
#9773=CARTESIAN_POINT ( 'NONE',  ( 13.10097267581912206, 45.54584849643477895, -3.258082403950691042 ) ) ;
#9774=CARTESIAN_POINT ( 'NONE',  ( 2.445080149700053643E-15, 48.17999999999999972, -13.50000000000000000 ) ) ;
#9776=CARTESIAN_POINT ( 'NONE',  ( 11.40617213196905411, 30.70028543943833910, -7.221826826951074807 ) ) ;
#9777=CARTESIAN_POINT ( 'NONE',  ( -9.410437633937705826, 56.31096153803149917, 9.682104401986398656 ) ) ;
#9780=CARTESIAN_POINT ( 'NONE',  ( 9.114660220015876391, 33.03466814584144373, 9.958601439926033194 ) ) ;
#9782=CARTESIAN_POINT ( 'NONE',  ( 4.392283583417332160, 40.02202581670101011, -12.76555334419149013 ) ) ;
#9784=ORIENTED_EDGE ( 'NONE', *, *, #16834, .T. ) ;
#9785=CARTESIAN_POINT ( 'NONE',  ( -6.523130144822721910, 62.44009285821610433, 11.82982051691417702 ) ) ;
#9789=CARTESIAN_POINT ( 'NONE',  ( -13.48346897527509114, 43.95311960857426214, 0.6707733342585510128 ) ) ;
#9791=CARTESIAN_POINT ( 'NONE',  ( 10.92172942406178926, 30.12999999999999545, 7.935100905948387684 ) ) ;
#9792=CARTESIAN_POINT ( 'NONE',  ( 8.343458848123583849, 47.88000000000000256, -11.48378591275253768 ) ) ;
#9794=CARTESIAN_POINT ( 'NONE',  ( -2.552045539003058749, 46.27175948752068280, -13.25665630414003893 ) ) ;
#9795=EDGE_CURVE ( 'NONE', #4872, #13385, #12385, .T. ) ;
#9796=CARTESIAN_POINT ( 'NONE',  ( -9.409590922929337964, 67.54892891243062536, -9.687992896030786838 ) ) ;
#9798=CARTESIAN_POINT ( 'NONE',  ( 0.6922064125909698218, 53.70486120015097953, 13.50000000000462919 ) ) ;
#9799=CARTESIAN_POINT ( 'NONE',  ( -10.42167427526279688, 64.60167514499391928, -8.581475041684891281 ) ) ;
#9802=CARTESIAN_POINT ( 'NONE',  ( -11.72378450257766147, 35.17872340265273579, 6.696941732122135171 ) ) ;
#9804=ORIENTED_EDGE ( 'NONE', *, *, #10715, .T. ) ;
#9805=CARTESIAN_POINT ( 'NONE',  ( 13.15122240745925808, 78.31917349788055560, 3.127322199626254129 ) ) ;
#9808=DIRECTION ( 'NONE',  ( 0.000000000000000000, -1.000000000000000000, 0.000000000000000000 ) ) ;
#9809=CARTESIAN_POINT ( 'NONE',  ( 9.843127303906451075, 72.78901079599570778, -9.241637740177777616 ) ) ;
#9810=CARTESIAN_POINT ( 'NONE',  ( 4.939422578511702966, 79.00184200604905982, -12.56392261057602688 ) ) ;
#9812=CARTESIAN_POINT ( 'NONE',  ( -8.343458848123582072, 59.37999999999999545, 11.48378591275254124 ) ) ;
#9813=CARTESIAN_POINT ( 'NONE',  ( -13.46416202051893407, 52.96403103733616291, 0.9835209988710441609 ) ) ;
#9814=CARTESIAN_POINT ( 'NONE',  ( -7.272992578804307939, 38.47999999999999687, -10.01041549318726886 ) ) ;
#9815=CARTESIAN_POINT ( 'NONE',  ( 0.000000000000000000, 0.000000000000000000, 0.000000000000000000 ) ) ;
#9816=CARTESIAN_POINT ( 'NONE',  ( 4.171729424061791924, 57.02999999999999403, -12.83926296998457239 ) ) ;
#9819=CARTESIAN_POINT ( 'NONE',  ( 9.423612524159942438, 69.04964748713040024, 9.673382742204811535 ) ) ;
#9824=CARTESIAN_POINT ( 'NONE',  ( -11.98704755772539698, 73.70041729349563298, -6.222936530383990750 ) ) ;
#9825=CARTESIAN_POINT ( 'NONE',  ( -4.140906574081368419, 76.32871695187549221, -12.85379821556370850 ) ) ;
#9826=DIRECTION ( 'NONE',  ( 0.000000000000000000, 0.000000000000000000, -1.000000000000000000 ) ) ;
#9828=CARTESIAN_POINT ( 'NONE',  ( 0.7057993694277138186, 80.93000000000002103, 13.10211957505607927 ) ) ;
#9831=CARTESIAN_POINT ( 'NONE',  ( 11.76794919243112680, 40.57999999999999829, -3.823638476888993942 ) ) ;
#9833=CARTESIAN_POINT ( 'NONE',  ( -1.652382928431953335, 32.62058735545888766, 13.39849679836423846 ) ) ;
#9834=CARTESIAN_POINT ( 'NONE',  ( 13.50411512954748794, 75.43386579576426243, -0.1159153957384908701 ) ) ;
#9836=CARTESIAN_POINT ( 'NONE',  ( -3.636496289402153081, 32.32999999999999829, -11.19198476289190936 ) ) ;
#9837=CARTESIAN_POINT ( 'NONE',  ( 10.92172942406179104, 83.73000000000000398, -7.935100905948385908 ) ) ;
#9838=CARTESIAN_POINT ( 'NONE',  ( -1.921282587139656828, 58.24907104121455603, -13.36368293974023480 ) ) ;
#9839=CARTESIAN_POINT ( 'NONE',  ( -2.287907212011502267, 38.59768353198680302, 13.30634456475851657 ) ) ;
#9840=EDGE_CURVE ( 'NONE', #14181, #13443, #4431, .T. ) ;
#9842=CARTESIAN_POINT ( 'NONE',  ( 12.50000000000000000, 98.93000000000002103, 9.000000000000000000 ) ) ;
#9843=CARTESIAN_POINT ( 'NONE',  ( 7.124828474515464194, 62.94491023264873775, 11.46677771899573806 ) ) ;
#9844=CARTESIAN_POINT ( 'NONE',  ( 13.09035282259576860, 42.30865731531114449, 3.417435527121966299 ) ) ;
#9845=CARTESIAN_POINT ( 'NONE',  ( -1.003760800223034469E-07, 53.67999720368429450, 13.49999999999999822 ) ) ;
#9847=ORIENTED_EDGE ( 'NONE', *, *, #4375, .F. ) ;
#9848=CARTESIAN_POINT ( 'NONE',  ( 7.272992578804311492, 70.87999999999998124, -10.01041549318726886 ) ) ;
#9849=CARTESIAN_POINT ( 'NONE',  ( -4.413477281977257860, 70.33879155025191210, -12.75886604156020177 ) ) ;
#9853=CARTESIAN_POINT ( 'NONE',  ( -2.262111960729766835, 43.26133720115711867, -13.30912863721355244 ) ) ;
#9854=CARTESIAN_POINT ( 'NONE',  ( -7.500000000000000888, 103.9506177843312145, -9.262340467025644841 ) ) ;
#9855=CARTESIAN_POINT ( 'NONE',  ( 8.973903266457636363, 60.83235153706387877, -10.08882510061240190 ) ) ;
#9858=CARTESIAN_POINT ( 'NONE',  ( 8.728437868593859505, 66.01621931896406181, 10.29985775731656616 ) ) ;
#9859=CARTESIAN_POINT ( 'NONE',  ( 12.06178501699019101, 57.20667319345715640, 6.066949433009045656 ) ) ;
#9860=CARTESIAN_POINT ( 'NONE',  ( -9.520470885617717371, 60.22999999999999687, 6.917026985038133624 ) ) ;
#9861=CARTESIAN_POINT ( 'NONE',  ( 11.76794919243112325, 70.43000000000000682, 1.441158131103945434E-15 ) ) ;
#9862=CARTESIAN_POINT ( 'NONE',  ( -12.23227011786221929, 46.71983014421766711, -5.734458843251163174 ) ) ;
#9863=CARTESIAN_POINT ( 'NONE',  ( 6.490407510521211343, 45.94148377923586679, -11.84091971732770610 ) ) ;
#9864=CYLINDRICAL_SURFACE ( 'NONE', #913, 13.50000000000000000 ) ;
#9865=CARTESIAN_POINT ( 'NONE',  ( 0.2181349388514764176, 31.17215667195195650, -13.49823986759029815 ) ) ;
#9866=CARTESIAN_POINT ( 'NONE',  ( -2.469137722265373203, 56.59112983379784367, 13.27265035157923023 ) ) ;
#9868=CARTESIAN_POINT ( 'NONE',  ( -1.774006486033653518, 50.61634266422996120, 13.38478036720835362 ) ) ;
#9869=CARTESIAN_POINT ( 'NONE',  ( 13.16963777937186642, 33.32355251092941018, 3.006075874452558416 ) ) ;
#9874=CARTESIAN_POINT ( 'NONE',  ( -13.49566855491535122, 61.91587976523243952, -0.4058878017242047997 ) ) ;
#9875=ORIENTED_EDGE ( 'NONE', *, *, #13127, .T. ) ;
#9877=CARTESIAN_POINT ( 'NONE',  ( -12.72868174054197432, 43.76761864562406146, -4.497864774813045585 ) ) ;
#9879=CIRCLE ( 'NONE', #5349, 6.000000000000001776 ) ;
#9881=CARTESIAN_POINT ( 'NONE',  ( 4.171729424061791924, 34.03000000000000114, -12.83926296998457239 ) ) ;
#9882=CARTESIAN_POINT ( 'NONE',  ( 13.49999999999999822, 44.27999999999999403, 4.386415899144237684 ) ) ;
#9883=CARTESIAN_POINT ( 'NONE',  ( -4.810843242447075063, 46.35328194274109137, -12.61654248971126258 ) ) ;
#9884=CARTESIAN_POINT ( 'NONE',  ( -2.881285544132592857, 67.28364482974733107, -13.18897454037147376 ) ) ;
#9886=ADVANCED_BREP_SHAPE_REPRESENTATION ( '', ( #8814, #16654 ), #5681 ) ;
#9887=CARTESIAN_POINT ( 'NONE',  ( 6.416313580321896914, 53.91553844827561193, 11.87812472618375281 ) ) ;
#9888=AXIS2_PLACEMENT_3D ( 'NONE', #10714, #16080, #3988 ) ;
#9889=ORIENTED_EDGE ( 'NONE', *, *, #17050, .T. ) ;
#9890=CARTESIAN_POINT ( 'NONE',  ( -0.3906627798091588111, 64.19404671379548688, -13.49436755410429889 ) ) ;
#9891=ORIENTED_EDGE ( 'NONE', *, *, #8401, .F. ) ;
#9892=CARTESIAN_POINT ( 'NONE',  ( -5.364550830651251268, 34.37421519030890238, -12.38897206134628703 ) ) ;
#9894=CARTESIAN_POINT ( 'NONE',  ( 11.84730513591649448, 78.19030449563439333, 6.472368050555079577 ) ) ;
#9896=CARTESIAN_POINT ( 'NONE',  ( -10.92172942406178926, 36.62999999999999545, -7.935100905948389460 ) ) ;
#9897=CARTESIAN_POINT ( 'NONE',  ( 12.69466205804307002, 72.26397838323447331, 4.593265921401764373 ) ) ;
#9898=EDGE_CURVE ( 'NONE', #6584, #6493, #9019, .T. ) ;
#9900=CARTESIAN_POINT ( 'NONE',  ( 2.607531440858944223E-15, 58.17999999999999261, -14.19474002721660355 ) ) ;
#9901=CARTESIAN_POINT ( 'NONE',  ( -9.271824160874588827, 52.54222379914162389, -9.814342718050605541 ) ) ;
#9902=CARTESIAN_POINT ( 'NONE',  ( -3.636496289402153081, 41.32999999999999829, -11.19198476289190936 ) ) ;
#9903=CARTESIAN_POINT ( 'NONE',  ( 2.607531440858944223E-15, 60.17999999999999972, -14.19474002721660355 ) ) ;
#9904=CARTESIAN_POINT ( 'NONE',  ( 2.027675135001143936, 50.75292237657222216, 13.34755061297746082 ) ) ;
#9906=CARTESIAN_POINT ( 'NONE',  ( 11.64349391773129128, 69.17573428589047069, 6.832218660565160917 ) ) ;
#9907=CARTESIAN_POINT ( 'NONE',  ( -4.129649858159847753, 37.32848282291750763, -12.85297598121887397 ) ) ;
#9908=CARTESIAN_POINT ( 'NONE',  ( -10.92172942406179104, 73.23000000000000398, 7.935100905948387684 ) ) ;
#9910=CARTESIAN_POINT ( 'NONE',  ( -12.59327613556072833, 73.75357011053149847, -4.864702328253065033 ) ) ;
#9911=CARTESIAN_POINT ( 'NONE',  ( -1.739642266260832848, 76.24253143227396379, -13.38915460456405349 ) ) ;
#9912=DIRECTION ( 'NONE',  ( 0.000000000000000000, 0.000000000000000000, -1.000000000000000000 ) ) ;
#9916=CARTESIAN_POINT ( 'NONE',  ( 9.520470885617717371, 34.72999999999999687, -6.917026985038131848 ) ) ;
#9918=CARTESIAN_POINT ( 'NONE',  ( -10.77958242724814575, 32.23934130396135345, 8.159047414433960199 ) ) ;
#9919=CARTESIAN_POINT ( 'NONE',  ( 6.634635836420705424, 74.92436317536002832, 11.76700430428859612 ) ) ;
#9922=CARTESIAN_POINT ( 'NONE',  ( 11.76794919243112325, 31.27999999999998693, 3.823638476888996607 ) ) ;
#9923=CARTESIAN_POINT ( 'NONE',  ( 4.171729424061791924, 81.03000000000000114, -12.83926296998457239 ) ) ;
#9924=CARTESIAN_POINT ( 'NONE',  ( 10.71722923847700315, 51.74181331124376726, -8.212034718187664950 ) ) ;
#9925=DIRECTION ( 'NONE',  ( 0.000000000000000000, -1.000000000000000000, 0.000000000000000000 ) ) ;
#9927=CARTESIAN_POINT ( 'NONE',  ( 1.653273178848926472E-15, 3.999999999999961808, 13.50000000000000000 ) ) ;
#9929=CARTESIAN_POINT ( 'NONE',  ( 3.564950917667821351, 62.80727969005073419, 13.05038946788975984 ) ) ;
#9930=CARTESIAN_POINT ( 'NONE',  ( -8.891200544363830713E-16, 46.67999999999999972, 13.50000000000000000 ) ) ;
#9931=CARTESIAN_POINT ( 'NONE',  ( 10.27029722546964763, 48.76660342709478613, -8.769633602492632463 ) ) ;
#9934=CARTESIAN_POINT ( 'NONE',  ( -7.272992578804307939, 65.47999999999998977, -10.01041549318727064 ) ) ;
#9938=ORIENTED_EDGE ( 'NONE', *, *, #8401, .T. ) ;
#9939=CARTESIAN_POINT ( 'NONE',  ( -1.200094164391137586, 43.22314455631953223, -13.44841224794836343 ) ) ;
#9940=CARTESIAN_POINT ( 'NONE',  ( 6.767892274116773521, 80.93000000001259764, -11.68099457092376348 ) ) ;
#9942=DIRECTION ( 'NONE',  ( -0.000000000000000000, -1.000000000000000000, -0.000000000000000000 ) ) ;
#9944=CARTESIAN_POINT ( 'NONE',  ( 7.591558717369741416, 65.96485550035102108, 11.16641294781561378 ) ) ;
#9945=CARTESIAN_POINT ( 'NONE',  ( 11.76850315208348796, 57.18434826636972446, 6.628006218653733406 ) ) ;
#9946=CARTESIAN_POINT ( 'NONE',  ( -9.520470885617715595, 56.63000000000000256, -6.917026985038136289 ) ) ;
#9947=CARTESIAN_POINT ( 'NONE',  ( 7.272992578804311492, 67.87999999999999545, -10.01041549318726709 ) ) ;
#9948=CARTESIAN_POINT ( 'NONE',  ( -13.30473318507969438, 46.84958455783641540, -2.288076029142007695 ) ) ;
#9949=CARTESIAN_POINT ( 'NONE',  ( 9.548081290227049323, 45.80397646740897244, -9.544521494561665875 ) ) ;
#9952=CARTESIAN_POINT ( 'NONE',  ( 7.160989524558149633, 30.91366021522728147, -11.45163515356361650 ) ) ;
#9953=CARTESIAN_POINT ( 'NONE',  ( -11.07142767505757419, 56.22114726484812763, 7.724863410134291897 ) ) ;
#9955=CARTESIAN_POINT ( 'NONE',  ( 8.929833117994236957, 33.02572749855196577, 10.12741600962044153 ) ) ;
#9957=CARTESIAN_POINT ( 'NONE',  ( 8.544410748096753494, 39.85237042391017326, -10.45276505990612215 ) ) ;
#9959=CARTESIAN_POINT ( 'NONE',  ( -11.07323960031809484, 62.22103888625681378, 7.722276753161360752 ) ) ;
#9963=CARTESIAN_POINT ( 'NONE',  ( 10.67437249253150355, 48.11583226118976597, 8.265000984528860783 ) ) ;
#9965=CARTESIAN_POINT ( 'NONE',  ( 0.000000000000000000, 80.93000000000000682, -13.50000000000000000 ) ) ;
#9966=CARTESIAN_POINT ( 'NONE',  ( -8.691771469529815392E-16, 32.67999999999999261, 14.19474002721660355 ) ) ;
#9967=CARTESIAN_POINT ( 'NONE',  ( -13.49999999999999822, 39.77999999999998693, -4.386415899144240349 ) ) ;
#9968=CARTESIAN_POINT ( 'NONE',  ( -5.667667140658918967, 46.38572788627769938, -12.25425454852370422 ) ) ;
#9969=CARTESIAN_POINT ( 'NONE',  ( -11.07701847939493689, 67.63915826389134622, -7.717748835311455835 ) ) ;
#9971=( BOUNDED_CURVE ( )  B_SPLINE_CURVE ( 2, ( #9429, #5532, #11005, #13808, #8276, #14778, #302, #16189, #2668, #13722, #5712, #8100, #13465 ),
 .UNSPECIFIED., .F., .F. ) 
 B_SPLINE_CURVE_WITH_KNOTS ( ( 3, 2, 2, 2, 2, 2, 3 ),
 ( 0.5972222222222222099, 0.5999999999999999778, 0.6055555555555555136, 0.6111111111111111605, 0.6166666666666666963, 0.6222222222222222321, 0.6250000000000000000 ),
 .UNSPECIFIED. ) 
 CURVE ( )  GEOMETRIC_REPRESENTATION_ITEM ( )  RATIONAL_B_SPLINE_CURVE ( ( 0.9755282581475768211, 0.9755282581475768211, 1.000000000000000000, 0.9510565162951535312, 1.000000000000000000, 0.9510565162951535312, 1.000000000000000000, 0.9510565162951535312, 1.000000000000000000, 0.9510565162951535312, 1.000000000000000000, 0.9755282581475768211, 0.9755282581475768211 ) ) 
 REPRESENTATION_ITEM ( '' )  );
#9972=CARTESIAN_POINT ( 'NONE',  ( 6.589847531046439499, 53.92267567950827356, 11.78235791658461018 ) ) ;
#9973=EDGE_CURVE ( 'NONE', #1729, #14883, #5841, .T. ) ;
#9974=ORIENTED_EDGE ( 'NONE', *, *, #12859, .T. ) ;
#9975=CARTESIAN_POINT ( 'NONE',  ( -6.821948058657442360, 64.43206303487275477, -11.66090654277045147 ) ) ;
#9976=ORIENTED_EDGE ( 'NONE', *, *, #3408, .T. ) ;
#9978=CARTESIAN_POINT ( 'NONE',  ( -9.272717293934437777, 34.54199207297656216, -9.829925356530168301 ) ) ;
#9980=LINE ( 'NONE', #14269, #416 ) ;
#9982=FACE_OUTER_BOUND ( 'NONE', #12069, .T. ) ;
#9983=CARTESIAN_POINT ( 'NONE',  ( -13.50000000000000000, 36.92999999999999972, -3.306546357697853733E-15 ) ) ;
#9984=CARTESIAN_POINT ( 'NONE',  ( 12.82313912373315468, 72.27809372985406355, 4.222047920560166645 ) ) ;
#9986=CARTESIAN_POINT ( 'NONE',  ( 2.607531440858944223E-15, 64.18000000000000682, -14.19474002721660355 ) ) ;
#9987=CARTESIAN_POINT ( 'NONE',  ( -7.191928855478868066, 52.44777283673647617, -11.43442037222222396 ) ) ;
#9989=CARTESIAN_POINT ( 'NONE',  ( -3.636496289402153081, 38.32999999999999829, -11.19198476289190936 ) ) ;
#9991=CARTESIAN_POINT ( 'NONE',  ( 10.92172942406179104, 53.72999999999999687, -7.935100905948385908 ) ) ;
#9992=CARTESIAN_POINT ( 'NONE',  ( 1.882898711538667502, 50.74770853775734736, 13.36896204807974975 ) ) ;
#9994=CARTESIAN_POINT ( 'NONE',  ( 3.556863673587017161, 68.80789220201475587, 13.02300793823324554 ) ) ;
#9997=CARTESIAN_POINT ( 'NONE',  ( -13.34960103463238568, 73.85960930300998939, -2.009550310400444850 ) ) ;
#9998=CARTESIAN_POINT ( 'NONE',  ( -2.380313741584730192, 76.26558729244737833, -13.28849608079124600 ) ) ;
#10000=CARTESIAN_POINT ( 'NONE',  ( -8.891200544363830713E-16, 64.67999999999999261, 13.50000000000000000 ) ) ;
#10003=CARTESIAN_POINT ( 'NONE',  ( 3.636496289402157078, 38.03000000000000114, -11.19198476289190936 ) ) ;
#10004=UNCERTAINTY_MEASURE_WITH_UNIT (LENGTH_MEASURE( 1.000000000000000082E-05 ), #15008, 'distance_accuracy_value', 'NONE');
#10006=CARTESIAN_POINT ( 'NONE',  ( -9.397593110749021150, 32.31148091487975194, 9.692029560030380964 ) ) ;
#10007=CARTESIAN_POINT ( 'NONE',  ( 7.473239715704042219, 74.95973476016609993, 11.24660702021163061 ) ) ;
#10009=CARTESIAN_POINT ( 'NONE',  ( -8.691771469529815392E-16, 79.67999999999997840, 14.19474002721660355 ) ) ;
#10010=LINE ( 'NONE', #8333, #12378 ) ;
#10011=DIRECTION ( 'NONE',  ( 0.000000000000000000, -1.000000000000000000, 0.000000000000000000 ) ) ;
#10012=CARTESIAN_POINT ( 'NONE',  ( 8.199628251150381075, 36.86814087517738159, -10.72470370097659398 ) ) ;
#10013=ADVANCED_FACE ( 'NONE', ( #7162 ), #7246, .T. ) ;
#10014=CARTESIAN_POINT ( 'NONE',  ( -4.171729424061787483, 69.32999999999999829, -12.83926296998457417 ) ) ;
#10016=CARTESIAN_POINT ( 'NONE',  ( 2.670759995370414419, 62.77599826986443787, 13.23319200665662265 ) ) ;
#10017=CARTESIAN_POINT ( 'NONE',  ( 5.457920679380044326, 41.87780726792447439, 12.34751621698460156 ) ) ;
#10018=CARTESIAN_POINT ( 'NONE',  ( 13.08319187888859325, 48.54904885850037743, -3.341727267560921977 ) ) ;
#10021=CARTESIAN_POINT ( 'NONE',  ( 3.636496289402157078, 71.03000000000000114, -11.19198476289190936 ) ) ;
#10026=CARTESIAN_POINT ( 'NONE',  ( 0.8512332319012331228, 76.14939279630267777, -13.47313715764315312 ) ) ;
#10029=AXIS2_PLACEMENT_3D ( 'NONE', #9634, #10768, #16131 ) ;
#10030=CARTESIAN_POINT ( 'NONE',  ( 12.89805136966890053, 66.28698917251486478, 3.986448665878211894 ) ) ;
#10031=CARTESIAN_POINT ( 'NONE',  ( 2.607531440858944223E-15, 79.17999999999997840, -14.19474002721660355 ) ) ;
#10032=CARTESIAN_POINT ( 'NONE',  ( 2.272985001014427788E-15, 53.17999999999999972, -12.37355403259654985 ) ) ;
#10033=CARTESIAN_POINT ( 'NONE',  ( 13.50000000000000355, 32.57999999999999119, -4.386415899144233244 ) ) ;
#10034=CARTESIAN_POINT ( 'NONE',  ( 3.636496289402154414, 57.82999999999999829, 11.19198476289190936 ) ) ;
#10035=CARTESIAN_POINT ( 'NONE',  ( -11.15932890281731815, 46.64414198115739651, -7.597908150188835030 ) ) ;
#10036=CARTESIAN_POINT ( 'NONE',  ( 10.56300723442443434, 45.75040630519399798, -8.406898149203419379 ) ) ;
#10037=CARTESIAN_POINT ( 'NONE',  ( 5.256946664302129868, 69.98959847328292483, -12.43489626292463690 ) ) ;
#10038=CARTESIAN_POINT ( 'NONE',  ( 11.61781901815139406, 30.68619861389073122, -6.878981689902905039 ) ) ;
#10039=CARTESIAN_POINT ( 'NONE',  ( -12.29415991002589337, 55.72589537594633669, -5.581494872401155050 ) ) ;
#10041=FACE_OUTER_BOUND ( 'NONE', #3475, .T. ) ;
#10042=CARTESIAN_POINT ( 'NONE',  ( 4.183988668469575956, 32.83044184657291709, 12.83530497071244625 ) ) ;
#10043=CARTESIAN_POINT ( 'NONE',  ( 2.914149619088002741, 43.07521792508150327, -13.18172077187604074 ) ) ;
#10044=CARTESIAN_POINT ( 'NONE',  ( 11.95191583910591326, 39.66185494719976390, -6.277078602806502872 ) ) ;
#10046=CARTESIAN_POINT ( 'NONE',  ( -11.12255880151802145, 62.21805859032765795, 7.651163739834599298 ) ) ;
#10050=CARTESIAN_POINT ( 'NONE',  ( 11.67577013789725271, 48.17798356650521185, 6.776969691758181646 ) ) ;
#10051=DIRECTION ( 'NONE',  ( 8.659560562354952580E-17, 0.7071067811865460184, -0.7071067811865490160 ) ) ;
#10052=CARTESIAN_POINT ( 'NONE',  ( 2.607531440858944223E-15, 37.17999999999999972, -14.19474002721660355 ) ) ;
#10053=CARTESIAN_POINT ( 'NONE',  ( 13.50000000000000000, 38.42999999999999972, 1.653273178848926867E-15 ) ) ;
#10055=CARTESIAN_POINT ( 'NONE',  ( -2.429978037473502273, 46.26737343488397869, -13.27956662434927537 ) ) ;
#10056=DIRECTION ( 'NONE',  ( 0.000000000000000000, 0.000000000000000000, -1.000000000000000000 ) ) ;
#10058=VECTOR ( 'NONE', #13936, 1000.000000000000000 ) ;
#10059=EDGE_CURVE ( 'NONE', #7647, #11272, #2501, .T. ) ;
#10060=CARTESIAN_POINT ( 'NONE',  ( 10.69437805966615151, 54.11696481419528482, 8.238956478643013170 ) ) ;
#10061=ORIENTED_EDGE ( 'NONE', *, *, #5823, .T. ) ;
#10062=CARTESIAN_POINT ( 'NONE',  ( -5.956643919577332191, 64.39723371421132470, -12.11484513224996817 ) ) ;
#10064=CARTESIAN_POINT ( 'NONE',  ( 5.469506025976357044, 66.98182939450360607, -12.34254299208515704 ) ) ;
#10065=CARTESIAN_POINT ( 'NONE',  ( -8.704249455524918133, 34.51507978907589091, -10.32029972064792567 ) ) ;
#10067=CARTESIAN_POINT ( 'NONE',  ( 2.446671206298333789, 77.76795475725374729, 13.27830564658316170 ) ) ;
#10068=CARTESIAN_POINT ( 'NONE',  ( 4.171729424061789260, 46.82999999999999829, 12.83926296998457417 ) ) ;
#10071=CARTESIAN_POINT ( 'NONE',  ( 10.67780330962509616, 72.11603026634840319, 8.260421498307383814 ) ) ;
#10073=CARTESIAN_POINT ( 'NONE',  ( 10.92172942406179104, 66.73000000000000398, -7.935100905948385908 ) ) ;
#10074=CARTESIAN_POINT ( 'NONE',  ( -9.971012074513973644, 52.57671928602155731, -9.134421619915956470 ) ) ;
#10075=CARTESIAN_POINT ( 'NONE',  ( 9.520470885617717371, 34.72999999999999687, -6.917026985038131848 ) ) ;
#10076=CARTESIAN_POINT ( 'NONE',  ( -10.92172942406179104, 55.23000000000000398, 7.935100905948387684 ) ) ;
#10079=CARTESIAN_POINT ( 'NONE',  ( -1.193958653162214389, 68.63708644905558742, 13.44710585900690525 ) ) ;
#10083=CARTESIAN_POINT ( 'NONE',  ( -13.13316445793458698, 73.81725464365611344, -3.175556518140508100 ) ) ;
#10084=AXIS2_PLACEMENT_3D ( 'NONE', #9691, #11094, #1439 ) ;
#10088=CARTESIAN_POINT ( 'NONE',  ( 11.76794919243112325, 37.28000000000000114, 3.823638476888997051 ) ) ;
#10090=CARTESIAN_POINT ( 'NONE',  ( -7.287599271325371220, 32.40820039520880158, 11.36473193426337680 ) ) ;
#10091=CARTESIAN_POINT ( 'NONE',  ( 3.229257234301759816, 74.79610684415503385, 13.10849085500428224 ) ) ;
#10092=CARTESIAN_POINT ( 'NONE',  ( -0.3097317755527617678, 53.66886317309062093, 13.49645795284958716 ) ) ;
#10095=CARTESIAN_POINT ( 'NONE',  ( 9.520470885617715595, 31.12999999999999901, 6.917026985038134512 ) ) ;
#10096=CARTESIAN_POINT ( 'NONE',  ( 11.72376580509998512, 51.67863134643251755, -6.693536803949124092 ) ) ;
#10097=LINE ( 'NONE', #6030, #13230 ) ;
#10098=CARTESIAN_POINT ( 'NONE',  ( 7.321629298432528188, 36.90676912180014568, -11.34569854295486202 ) ) ;
#10099=CARTESIAN_POINT ( 'NONE',  ( -13.49999999999999822, 70.07999999999999829, 4.386415899144235020 ) ) ;
#10101=CARTESIAN_POINT ( 'NONE',  ( 0.6841847586525967584, 62.70460016233664646, 13.48383326463766529 ) ) ;
#10102=CARTESIAN_POINT ( 'NONE',  ( 0.000000000000000000, 80.93000000000000682, 0.000000000000000000 ) ) ;
#10103=CARTESIAN_POINT ( 'NONE',  ( 13.23629157939490675, 48.52372149559199954, -2.655358675363076237 ) ) ;
#10105=VERTEX_POINT ( 'NONE', #14997 ) ;
#10106=CARTESIAN_POINT ( 'NONE',  ( 11.76794919243112325, 64.43000000000000682, 1.441158131103945434E-15 ) ) ;
#10112=CARTESIAN_POINT ( 'NONE',  ( 5.912581530857422329, 65.89548293010727775, 12.13714109508869221 ) ) ;
#10113=CARTESIAN_POINT ( 'NONE',  ( 8.343458848123583849, 78.88000000000000966, -11.48378591275253768 ) ) ;
#10115=CARTESIAN_POINT ( 'NONE',  ( 9.520470885617715595, 52.12999999999999545, 6.917026985038134512 ) ) ;
#10116=CARTESIAN_POINT ( 'NONE',  ( -9.701085253511761763, 46.56373681230299866, -9.388382066297427997 ) ) ;
#10117=CARTESIAN_POINT ( 'NONE',  ( 13.08346865036885731, 45.54843980811354953, -3.328194816465799288 ) ) ;
#10120=CARTESIAN_POINT ( 'NONE',  ( 12.02455442308676759, 30.65625020179192717, -6.136782126200483134 ) ) ;
#10121=CARTESIAN_POINT ( 'NONE',  ( -12.88168228059477727, 56.07516734758430488, 4.043721559897264228 ) ) ;
#10122=CARTESIAN_POINT ( 'NONE',  ( -2.177972351186602040, 50.60165681262385107, 13.32324697659018575 ) ) ;
#10123=CARTESIAN_POINT ( 'NONE',  ( 9.340143388868789032, 33.04566569248647312, 9.748318470567989280 ) ) ;
#10124=CARTESIAN_POINT ( 'NONE',  ( 3.131226932223059034, 43.06742001594902547, -13.13221980506242303 ) ) ;
#10125=CARTESIAN_POINT ( 'NONE',  ( 10.26973110394399846, 39.76645578949973014, -8.762594870586800866 ) ) ;
#10127=CARTESIAN_POINT ( 'NONE',  ( -13.47444954086344815, 61.90133406425022145, -0.8302180661310076815 ) ) ;
#10132=CARTESIAN_POINT ( 'NONE',  ( 10.28365721251559606, 48.09423968048177045, 8.748761603325048597 ) ) ;
#10133=CARTESIAN_POINT ( 'NONE',  ( 4.708533875543480463, 58.01043352540193609, -12.65229227841353676 ) ) ;
#10134=CARTESIAN_POINT ( 'NONE',  ( 9.473773279193389740, 78.80763578817767723, -9.618192038280239942 ) ) ;
#10135=CARTESIAN_POINT ( 'NONE',  ( 11.76794919243112680, 82.58000000000001251, -3.823638476888993942 ) ) ;
#10136=CARTESIAN_POINT ( 'NONE',  ( -13.49999999999999822, 40.07999999999999829, 4.386415899144235908 ) ) ;
#10138=AXIS2_PLACEMENT_3D ( 'NONE', #327, #7144, #13919 ) ;
#10139=CARTESIAN_POINT ( 'NONE',  ( -9.620323683735932718, 46.55968297308034209, -9.470975885656756077 ) ) ;
#10143=CARTESIAN_POINT ( 'NONE',  ( 2.625108261242528052, 53.77444720219749286, 13.24532092722070509 ) ) ;
#10144=ORIENTED_EDGE ( 'NONE', *, *, #381, .F. ) ;
#10146=EDGE_LOOP ( 'NONE', ( #3227, #11615, #7929, #14762 ) ) ;
#10148=CARTESIAN_POINT ( 'NONE',  ( -5.820456496121892975, 34.39186628428911519, -12.18180719480813146 ) ) ;
#10152=CARTESIAN_POINT ( 'NONE',  ( 4.704097590039896026, 77.84933813905681177, 12.65644523216417028 ) ) ;
#10153=DIRECTION ( 'NONE',  ( 0.000000000000000000, 0.000000000000000000, -1.000000000000000000 ) ) ;
#10154=CARTESIAN_POINT ( 'NONE',  ( 0.000000000000000000, 0.000000000000000000, 0.000000000000000000 ) ) ;
#10156=CARTESIAN_POINT ( 'NONE',  ( 13.41671563044160642, 72.37743211696324863, 1.501316902429144839 ) ) ;
#10158=CARTESIAN_POINT ( 'NONE',  ( -13.49999999999999822, 55.78000000000000114, -4.386415899144240349 ) ) ;
#10159=CARTESIAN_POINT ( 'NONE',  ( -2.287575323369731795, 52.26225204508322975, -13.30505731867491903 ) ) ;
#10161=CARTESIAN_POINT ( 'NONE',  ( -8.343458848123582072, 52.37999999999999545, 11.48378591275254124 ) ) ;
#10165=CARTESIAN_POINT ( 'NONE',  ( -1.124720807883521134, 68.63959828170268906, 13.45321750979929831 ) ) ;
#10169=CARTESIAN_POINT ( 'NONE',  ( -5.188624757180122060, 65.49247307178023902, 12.46307245499054517 ) ) ;
#10174=CARTESIAN_POINT ( 'NONE',  ( 11.76794919243112680, 37.58000000000000540, -3.823638476888993942 ) ) ;
#10175=CARTESIAN_POINT ( 'NONE',  ( -3.168841352280721502, 40.29393185182132697, -13.12324853033191374 ) ) ;
#10176=CARTESIAN_POINT ( 'NONE',  ( -13.02011563133146765, 31.80264107109495697, -3.568385494409815450 ) ) ;
#10177=CARTESIAN_POINT ( 'NONE',  ( 3.677119991341980754, 74.81221565746179181, 12.98956592640999830 ) ) ;
#10179=CARTESIAN_POINT ( 'NONE',  ( 2.607531440858944223E-15, 84.17999999999999261, -14.19474002721660355 ) ) ;
#10180=CARTESIAN_POINT ( 'NONE',  ( 12.63933979188332479, 51.60176062895381932, -4.743111560129607440 ) ) ;
#10181=CARTESIAN_POINT ( 'NONE',  ( -13.49989394954305588, 37.94506420804570013, 0.4415588883962403011 ) ) ;
#10182=CARTESIAN_POINT ( 'NONE',  ( 8.534433506530605840, 36.85283109795096834, -10.46091794006641074 ) ) ;
#10184=CARTESIAN_POINT ( 'NONE',  ( -0.009181258512500184085, 49.18033011924610776, -13.49999765788927064 ) ) ;
#10185=CARTESIAN_POINT ( 'NONE',  ( -4.319557087832021303, 80.52465274632413639, 12.79068498944547905 ) ) ;
#10186=CARTESIAN_POINT ( 'NONE',  ( 13.49542268721398486, 48.41792802572773979, 0.3515307404469304453 ) ) ;
#10189=EDGE_LOOP ( 'NONE', ( #12512, #16305 ) ) ;
#10190=CARTESIAN_POINT ( 'NONE',  ( 7.272992578804308828, 63.97999999999999687, 10.01041549318726886 ) ) ;
#10192=CARTESIAN_POINT ( 'NONE',  ( -12.50000000000000000, 98.93000000000002103, 1.224646799147353059E-15 ) ) ;
#10195=CARTESIAN_POINT ( 'NONE',  ( 3.184420153851656110, 76.06550818570755723, -13.12039170739967098 ) ) ;
#10197=CARTESIAN_POINT ( 'NONE',  ( 4.412288822437548497, 65.83840567029228907, 12.76607370684300236 ) ) ;
#10199=CARTESIAN_POINT ( 'NONE',  ( 13.50000000000000355, 81.57999999999998408, -4.386415899144233244 ) ) ;
#10200=CARTESIAN_POINT ( 'NONE',  ( 11.76794919243112325, 46.42999999999999972, 1.441158131103945434E-15 ) ) ;
#10201=CARTESIAN_POINT ( 'NONE',  ( -11.06704697272087579, 59.22141069247929579, 7.731141691505153624 ) ) ;
#10202=CARTESIAN_POINT ( 'NONE',  ( 12.98058781010997009, 45.29739780767026502, 3.708848460215144804 ) ) ;
#10203=CARTESIAN_POINT ( 'NONE',  ( 9.404160778349385907, 69.81134698545751860, -9.693570510553916719 ) ) ;
#10204=CARTESIAN_POINT ( 'NONE',  ( 4.822590792482460920, 80.85373989299547759, 12.61238363178463118 ) ) ;
#10205=CARTESIAN_POINT ( 'NONE',  ( 13.47269901431903705, 30.46011270062681575, -0.8715263847070852110 ) ) ;
#10206=CARTESIAN_POINT ( 'NONE',  ( -10.91251700311249984, 56.23059369663675255, 7.948489508437808659 ) ) ;
#10207=CARTESIAN_POINT ( 'NONE',  ( -3.918493925263932809, 50.53910349840194272, 12.91881581933787615 ) ) ;
#10210=CARTESIAN_POINT ( 'NONE',  ( 11.11374454754978203, 39.71854023908382914, -7.664195384031204483 ) ) ;
#10211=ORIENTED_EDGE ( 'NONE', *, *, #1885, .F. ) ;
#10212=CARTESIAN_POINT ( 'NONE',  ( -13.41912378192338906, 61.98242377346405618, 1.505696609645044370 ) ) ;
#10217=CARTESIAN_POINT ( 'NONE',  ( 11.64509123620695341, 48.17585162153407197, 6.829551714163834220 ) ) ;
#10218=CARTESIAN_POINT ( 'NONE',  ( 5.350032676027314693, 57.98638694014967143, -12.39911101267510141 ) ) ;
#10219=CARTESIAN_POINT ( 'NONE',  ( 10.87629897145368929, 78.73263608150857351, -7.997304871519990144 ) ) ;
#10220=CARTESIAN_POINT ( 'NONE',  ( -9.520470885617717371, 81.22999999999998977, 6.917026985038133624 ) ) ;
#10221=CARTESIAN_POINT ( 'NONE',  ( 13.49999999999999822, 38.27999999999999403, 4.386415899144237684 ) ) ;
#10223=CYLINDRICAL_SURFACE ( 'NONE', #10707, 13.50000000000000000 ) ;
#10224=PLANE ( 'NONE',  #4298 ) ;
#10226=CARTESIAN_POINT ( 'NONE',  ( -8.891200544363830713E-16, 79.67999999999999261, 13.50000000000000000 ) ) ;
#10227=CARTESIAN_POINT ( 'NONE',  ( 2.848479376167694532, 34.07758484385156095, -13.19633634240523001 ) ) ;
#10228=VERTEX_POINT ( 'NONE', #1661 ) ;
#10229=CARTESIAN_POINT ( 'NONE',  ( 0.000000000000000000, 0.000000000000000000, 0.000000000000000000 ) ) ;
#10233=CARTESIAN_POINT ( 'NONE',  ( 2.692306382202049431, 67.08319488902810690, -13.22882663213062848 ) ) ;
#10236=CARTESIAN_POINT ( 'NONE',  ( -6.070109238205766644, 59.45833234045775839, 12.06637233067175785 ) ) ;
#10239=CARTESIAN_POINT ( 'NONE',  ( 12.02390709123288026, 72.65644516203032310, -6.142304361847497951 ) ) ;
#10241=CARTESIAN_POINT ( 'NONE',  ( 10.92172942406179104, 51.72999999999999687, -7.935100905948385908 ) ) ;
#10242=CARTESIAN_POINT ( 'NONE',  ( -8.866856944732615986, 52.52278280499852059, -10.17986386199988402 ) ) ;
#10246=CARTESIAN_POINT ( 'NONE',  ( -8.579405063118292318, 68.35072221898208511, 10.42323635129704229 ) ) ;
#10248=CARTESIAN_POINT ( 'NONE',  ( 0.000000000000000000, 80.93000000000000682, 0.000000000000000000 ) ) ;
#10250=CARTESIAN_POINT ( 'NONE',  ( -5.186584049524258333, 65.49254861102842540, 12.46392224160446283 ) ) ;
#10252=DIRECTION ( 'NONE',  ( 0.000000000000000000, -1.000000000000000000, 0.000000000000000000 ) ) ;
#10256=CARTESIAN_POINT ( 'NONE',  ( -2.805409333583691378, 40.28087191790951493, -13.20536015821407361 ) ) ;
#10257=AXIS2_PLACEMENT_3D ( 'NONE', #17139, #3800, #14564 ) ;
#10258=CARTESIAN_POINT ( 'NONE',  ( -13.12180246013672757, 31.81716720392802600, -3.176623397036585583 ) ) ;
#10259=CARTESIAN_POINT ( 'NONE',  ( 1.324652792791208178, 74.72762950812426652, 13.43485395247348180 ) ) ;
#10260=CARTESIAN_POINT ( 'NONE',  ( 9.404743306317577378, 60.04888379170549229, 9.685242053972840992 ) ) ;
#10263=CARTESIAN_POINT ( 'NONE',  ( -8.691771469529815392E-16, 76.68000000000000682, 14.19474002721660355 ) ) ;
#10264=CARTESIAN_POINT ( 'NONE',  ( 13.23825292412364263, 51.52337512777393158, -2.645500850496228296 ) ) ;
#10265=CARTESIAN_POINT ( 'NONE',  ( -11.19854509087375760, 38.21339351073512347, 7.539409783578506108 ) ) ;
#10266=CARTESIAN_POINT ( 'NONE',  ( 11.24391244297007120, 36.71057840753311297, -7.471579428428752223 ) ) ;
#10268=DIRECTION ( 'NONE',  ( 0.000000000000000000, -1.000000000000000000, 0.000000000000000000 ) ) ;
#10269=CARTESIAN_POINT ( 'NONE',  ( -6.693563675217492737, 77.43309452535775961, 11.72466887716232975 ) ) ;
#10271=CARTESIAN_POINT ( 'NONE',  ( -4.171729424061787483, 60.32999999999999829, -12.83926296998457417 ) ) ;
#10272=CARTESIAN_POINT ( 'NONE',  ( 5.983495836244371091, 41.89831291724665618, 12.10301303378507853 ) ) ;
#10273=CARTESIAN_POINT ( 'NONE',  ( 12.15164001199787869, 48.64617462453512076, -5.883719564323237172 ) ) ;
#10275=ORIENTED_EDGE ( 'NONE', *, *, #12615, .F. ) ;
#10276=CARTESIAN_POINT ( 'NONE',  ( -7.272992578804307939, 59.48000000000000398, -10.01041549318727064 ) ) ;
#10283=CARTESIAN_POINT ( 'NONE',  ( 8.343458848123578520, 77.97999999999998977, 11.48378591275254124 ) ) ;
#10284=CARTESIAN_POINT ( 'NONE',  ( 7.272992578804311492, 46.87999999999998835, -10.01041549318726709 ) ) ;
#10286=CARTESIAN_POINT ( 'NONE',  ( -10.69285981900389082, 59.24332124397713528, 8.245168519117006767 ) ) ;
#10287=CARTESIAN_POINT ( 'NONE',  ( 11.29577473244720132, 45.15263884231691094, 7.394358328561038363 ) ) ;
#10288=CARTESIAN_POINT ( 'NONE',  ( 1.102632182866101207, 70.14042570178519043, -13.45669853540183425 ) ) ;
#10289=CARTESIAN_POINT ( 'NONE',  ( 0.7449732705081377748, 80.70681811148803320, 13.48519498389669735 ) ) ;
#10290=CARTESIAN_POINT ( 'NONE',  ( 13.31353121000146444, 30.35142671438330098, 2.236827078041004224 ) ) ;
#10291=CARTESIAN_POINT ( 'NONE',  ( -13.46326036990713249, 55.96444472986166119, 0.9953224451197258960 ) ) ;
#10292=CARTESIAN_POINT ( 'NONE',  ( -13.47134942828595427, 49.96064118497289286, 0.8867589712405034019 ) ) ;
#10293=CARTESIAN_POINT ( 'NONE',  ( 5.649316163632027710, 63.97492181549525725, -12.26175092916859732 ) ) ;
#10294=CARTESIAN_POINT ( 'NONE',  ( 2.905705795190346219, 43.07552160509550987, -13.18358388524940317 ) ) ;
#10295=CARTESIAN_POINT ( 'NONE',  ( 11.96927535954811006, 39.66052931784707170, -6.243969760129989055 ) ) ;
#10297=CARTESIAN_POINT ( 'NONE',  ( -12.02744370554971276, 61.70390941226424530, -6.131723170855442717 ) ) ;
#10298=ORIENTED_EDGE ( 'NONE', *, *, #17466, .F. ) ;
#10299=ORIENTED_EDGE ( 'NONE', *, *, #11299, .F. ) ;
#10302=CARTESIAN_POINT ( 'NONE',  ( 11.88874087135845237, 48.19328206360869160, 6.400001648777170260 ) ) ;
#10303=CARTESIAN_POINT ( 'NONE',  ( 6.489056890134116351, 57.94152136233466877, -11.84633360268247060 ) ) ;
#10304=CARTESIAN_POINT ( 'NONE',  ( 11.65723228743481776, 78.68382482704133452, -6.824437818837509440 ) ) ;
#10305=CARTESIAN_POINT ( 'NONE',  ( -7.272992578804307939, 74.47999999999998977, -10.01041549318726886 ) ) ;
#10308=ADVANCED_FACE ( 'NONE', ( #15781 ), #7596, .T. ) ;
#10310=CARTESIAN_POINT ( 'NONE',  ( -0.3664410078159376360, 67.19317488031707342, -13.49530529745837448 ) ) ;
#10312=DIRECTION ( 'NONE',  ( -0.000000000000000000, -1.000000000000000000, -0.000000000000000000 ) ) ;
#10313=CARTESIAN_POINT ( 'NONE',  ( 5.813126995088480520, 33.96841089008475478, -12.18431645958717979 ) ) ;
#10314=ORIENTED_EDGE ( 'NONE', *, *, #7675, .T. ) ;
#10317=CARTESIAN_POINT ( 'NONE',  ( 2.747298874549415793, 67.08121722534593800, -13.21751473180457026 ) ) ;
#10319=CARTESIAN_POINT ( 'NONE',  ( 8.655293140891854975, 78.01281519178354529, 10.36031341550661899 ) ) ;
#10321=LINE ( 'NONE', #15676, #1560 ) ;
#10322=CARTESIAN_POINT ( 'NONE',  ( 7.347880794884121708E-16, 102.9300000000000068, -6.000000000000001776 ) ) ;
#10325=CARTESIAN_POINT ( 'NONE',  ( -13.49999999999999822, 50.07999999999999119, 4.386415899144235908 ) ) ;
#10326=CARTESIAN_POINT ( 'NONE',  ( -10.79414870313322083, 71.23842559514402240, 8.155184730919005531 ) ) ;
#10328=B_SPLINE_CURVE_WITH_KNOTS ( 'NONE', 3,
 ( #4693, #13776, #1675, #7090, #12474, #13861, #5766, #3174, #12644, #8598, #11150, #1847, #620, #14128, #16526, #16701, #11415, #15186, #6032, #8684, #4433, #14043, #8513, #448, #7260, #1765, #2015, #7174, #10098, #5858, #12383, #4606, #10012, #274, #12562, #533, #5685, #15448, #10182, #11757, #4863, #15533, #9206, #6373, #11498, #10440, #6118, #15799, #14558, #16874, #14299, #708, #15618, #3526, #7442, #5132, #961, #10266, #3704, #15886, #7525, #14213, #4779, #7613, #3794, #1050, #17133, #3444, #12821, #16961, #5043, #8861, #4952, #2098, #12905, #11847, #6199, #789, #8941, #10355, #9121, #14383, #11585, #2185, #12989, #17222, #13075, #872, #14471, #15709, #7698, #6283, #11671, #17046, #3613, #2359, #9027, #2272, #7792, #13163, #6462, #10523, #17394, #1483, #2707, #2533, #1304, #1137, #14728, #8136, #10957, #2617, #9643, #14903, #7961, #6548, #5481, #2797, #11927, #13250, #17308, #8047, #5310, #16231, #13331, #8228, #10693, #16059, #7873, #15974, #3967, #14645, #13589, #3877, #76, #9465, #9379, #5221, #6635, #1222, #12014, #10607, #9293, #13414, #6718, #12096, #17478, #13501, #5392, #10777, #14812, #6900, #4232, #16141, #1391, #12273, #4051, #9553, #10863, #6806, #12184, #4140, #170, #5575, #16325, #2441, #12456, #11303, #8493, #4914, #7241, #13931, #2885, #13757, #11133, #8317 ),
 .UNSPECIFIED., .F., .F.,
 ( 4, 2, 2, 2, 1, 1, 1, 2, 2, 2, 1, 1, 1, 1, 2, 2, 2, 2, 2, 1, 1, 2, 2, 1, 2, 2, 2, 2, 1, 2, 2, 1, 2, 2, 2, 1, 1, 2, 2, 2, 1, 1, 2, 2, 2, 2, 2, 2, 2, 1, 2, 2, 1, 2, 2, 2, 2, 2, 2, 1, 2, 2, 2, 2, 1, 1, 1, 2, 2, 2, 2, 2, 2, 2, 2, 2, 1, 2, 2, 2, 1, 1, 2, 2, 1, 2, 2, 2, 2, 2, 1, 1, 2, 2, 1, 2, 2, 2, 1, 1, 1, 2, 2, 4 ),
 ( 0.8578524185686006165, 0.8579098628542002336, 0.8579242239256001934, 0.8579385849970000422, 0.8579673071397998507, 0.8580821957109991960, 0.8583119728533977755, 0.8587715271381948234, 0.8596906357077890304, 0.8615288528469774443, 0.8617586299893760238, 0.8618735185605752580, 0.8619309628461748751, 0.8619596849889746837, 0.8619740460603746435, 0.8619884071317744922, 0.8624479614165716512, 0.8633670699861659692, 0.8638266242709631282, 0.8639415128421624734, 0.8639989571277620906, 0.8640133181991619393, 0.8640276792705618991, 0.8640564014133617077, 0.8642861785557602872, 0.8652052871253544941, 0.8656648414101516531, 0.8658946185525502326, 0.8660095071237494668, 0.8660382292665492754, 0.8660669514093491950, 0.8661243956949488121, 0.8670435042645431301, 0.8670578653359429788, 0.8670722264073429386, 0.8671009485501427472, 0.8671583928357423643, 0.8672732814069417095, 0.8675030585493402890, 0.8679626128341374480, 0.8680200571197371762, 0.8680487792625369847, 0.8680631403339368335, 0.8680775014053367933, 0.8681923899765360275, 0.8684221671189346070, 0.8688817214037318770, 0.8698008299733261950, 0.8700306071157247745, 0.8700880514013243916, 0.8701024124727243514, 0.8701167735441242002, 0.8701454956869240087, 0.8702603842581233540, 0.8707199385429205130, 0.8716390471125148309, 0.8720986013973119899, 0.8721273235401117985, 0.8721560456829116070, 0.8722134899685113352, 0.8723283785397105694, 0.8725581556821091489, 0.8734772642517034669, 0.8739368185365007369, 0.8740517071076999711, 0.8741091513932995882, 0.8741378735360993968, 0.8741522346074993566, 0.8741665956788993164, 0.8743963728212978959, 0.8753154813908922138, 0.8757750356756893728, 0.8762345899604866428, 0.8780728070996752788, 0.8781876956708746240, 0.8782451399564742411, 0.8783025842420739693, 0.8785323613844725488, 0.8789919156692697078, 0.8799110242388641367, 0.8801408013812627162, 0.8801982456668623334, 0.8802269678096622529, 0.8802556899524620615, 0.8803705785236612957, 0.8808301328084585657, 0.8817492413780528837, 0.8822087956628501537, 0.8826683499476473127, 0.8835874585172417417, 0.8840470128020390117, 0.8842767899444375912, 0.8843055120872373998, 0.8843342342300372083, 0.8843916785156368254, 0.8845065670868361707, 0.8854256756564305997, 0.8858852299412278697, 0.8861150070836264492, 0.8862298956548257944, 0.8862873399404254116, 0.8863160620832253311, 0.8863447842260251397, 0.8872638927956195687 ),
 .UNSPECIFIED. ) ;
#10331=CARTESIAN_POINT ( 'NONE',  ( -2.066879295991422616, 68.60558311925369424, 13.34776454378817512 ) ) ;
#10333=CARTESIAN_POINT ( 'NONE',  ( 2.992242805631164515, 55.07242087184739887, -13.16446483759825625 ) ) ;
#10335=CARTESIAN_POINT ( 'NONE',  ( -7.707562987937823351, 65.39003898384051183, 11.08354747542285956 ) ) ;
#10337=CARTESIAN_POINT ( 'NONE',  ( -1.595484067438319942, 35.62263446958586144, 13.40538992109765282 ) ) ;
#10339=CARTESIAN_POINT ( 'NONE',  ( 3.636496289402157078, 32.02999999999999403, -11.19198476289190936 ) ) ;
#10340=AXIS2_PLACEMENT_3D ( 'NONE', #7810, #3546, #6393 ) ;
#10342=CARTESIAN_POINT ( 'NONE',  ( 13.49999999999999822, 80.28000000000000114, 4.386415899144236796 ) ) ;
#10343=CARTESIAN_POINT ( 'NONE',  ( -13.50004520387097173, 31.92232117734513608, -0.2162762051120299955 ) ) ;
#10344=CARTESIAN_POINT ( 'NONE',  ( 0.000000000000000000, 0.000000000000000000, 0.000000000000000000 ) ) ;
#10345=CARTESIAN_POINT ( 'NONE',  ( 11.62435398580979751, 60.17441760321225530, 6.864763562681197584 ) ) ;
#10347=CARTESIAN_POINT ( 'NONE',  ( 4.171729424061791924, 63.03000000000000114, -12.83926296998457239 ) ) ;
#10348=CARTESIAN_POINT ( 'NONE',  ( -9.520470885617715595, 56.63000000000000256, -6.917026985038136289 ) ) ;
#10350=CARTESIAN_POINT ( 'NONE',  ( -8.343458848123582072, 76.37999999999998124, 11.48378591275254124 ) ) ;
#10351=ADVANCED_FACE ( 'NONE', ( #856 ), #15691, .T. ) ;
#10352=CARTESIAN_POINT ( 'NONE',  ( 13.44076158601913029, 51.38538528069671685, 1.282844352539189936 ) ) ;
#10354=CARTESIAN_POINT ( 'NONE',  ( -13.33448719118932146, 38.00391057290926256, 2.107558467510691980 ) ) ;
#10355=CARTESIAN_POINT ( 'NONE',  ( 12.89750109184049975, 36.57316622584918520, -3.991296069496922172 ) ) ;
#10357=CARTESIAN_POINT ( 'NONE',  ( -5.262387905378953512, 74.48968593636273283, 12.43211883244449112 ) ) ;
#10358=CARTESIAN_POINT ( 'NONE',  ( -7.312194298746915067, 77.40724852587138116, 11.35038802565898486 ) ) ;
#10359=CARTESIAN_POINT ( 'NONE',  ( -4.130858764561470053, 80.53146975156121812, 12.85259012924355915 ) ) ;
#10364=CARTESIAN_POINT ( 'NONE',  ( -11.76794919243112325, 56.92999999999999972, -2.882316262207890869E-15 ) ) ;
#10368=CARTESIAN_POINT ( 'NONE',  ( 13.03682526262544350, 75.55504566543577027, -3.506206262213893421 ) ) ;
#10370=CARTESIAN_POINT ( 'NONE',  ( -4.171729424061791036, 80.53000000000000114, 12.83926296998457239 ) ) ;
#10371=CARTESIAN_POINT ( 'NONE',  ( 11.76794919243112325, 49.28000000000000114, 3.823638476888996607 ) ) ;
#10372=EDGE_CURVE ( 'NONE', #11076, #7647, #14116, .T. ) ;
#10373=CARTESIAN_POINT ( 'NONE',  ( -10.01465321359413885, 59.28001650100842568, 9.053085426433254312 ) ) ;
#10374=CARTESIAN_POINT ( 'NONE',  ( 13.49235683156874721, 45.41405812888587690, 0.4636627382355369420 ) ) ;
#10375=CARTESIAN_POINT ( 'NONE',  ( 13.17044722332754780, 69.32228747003190961, 3.042193921996489969 ) ) ;
#10376=CARTESIAN_POINT ( 'NONE',  ( -4.171729424061791036, 67.53000000000000114, 12.83926296998457239 ) ) ;
#10377=CARTESIAN_POINT ( 'NONE',  ( 13.03052044818961441, 30.55590990951756325, -3.529457494173335874 ) ) ;
#10378=CARTESIAN_POINT ( 'NONE',  ( -10.81241192308180921, 55.62348906932676584, -8.085305829502456021 ) ) ;
#10379=CARTESIAN_POINT ( 'NONE',  ( -5.503938361541620417, 50.48042196614674992, 12.32707990364577455 ) ) ;
#10380=CARTESIAN_POINT ( 'NONE',  ( 0.000000000000000000, 80.93000000000000682, 0.000000000000000000 ) ) ;
#10381=CARTESIAN_POINT ( 'NONE',  ( 4.419207061359027300, 43.02104761480173778, -12.75630134412691952 ) ) ;
#10382=CARTESIAN_POINT ( 'NONE',  ( 13.32699551091378254, 39.35439204512613287, 2.154494870127292128 ) ) ;
#10384=CARTESIAN_POINT ( 'NONE',  ( -12.11116184202662538, 70.70858905986030152, -6.028316998684753791 ) ) ;
#10385=CARTESIAN_POINT ( 'NONE',  ( -7.265637185492512806, 61.45088050927903112, -11.37811650908751915 ) ) ;
#10388=CARTESIAN_POINT ( 'NONE',  ( -11.73735425733374349, 40.68227936623591745, -6.671254634659874228 ) ) ;
#10392=CARTESIAN_POINT ( 'NONE',  ( 3.309157057342323682, 47.79898824056381557, 13.08814985599747338 ) ) ;
#10393=CARTESIAN_POINT ( 'NONE',  ( 9.127818136977767338, 57.82506099181254910, -9.960319412006729323 ) ) ;
#10394=CARTESIAN_POINT ( 'NONE',  ( 8.740260419149842974, 78.84333345805735860, -10.29113004058012315 ) ) ;
#10395=CARTESIAN_POINT ( 'NONE',  ( 2.272985001014427788E-15, 77.18000000000000682, -12.37355403259654985 ) ) ;
#10398=CARTESIAN_POINT ( 'NONE',  ( -0.7917850522838131289, 67.20846528983619805, -13.47766984953646840 ) ) ;
#10401=CARTESIAN_POINT ( 'NONE',  ( 8.524601824545214868, 33.85328496813475851, -10.46893613448600568 ) ) ;
#10402=CARTESIAN_POINT ( 'NONE',  ( -12.90183522623821766, 73.78708785609254051, -3.983866183089469715 ) ) ;
#10403=VERTEX_POINT ( 'NONE', #11654 ) ;
#10404=CARTESIAN_POINT ( 'NONE',  ( 12.50000000000000000, 98.93000000000002103, 1.224646799147353059E-15 ) ) ;
#10409=CARTESIAN_POINT ( 'NONE',  ( -1.434929399941947459, 44.62842767942802880, 13.42577741823575899 ) ) ;
#10410=CARTESIAN_POINT ( 'NONE',  ( -7.180763499379964721, 59.41272380569992606, 11.43182607564664899 ) ) ;
#10412=DIRECTION ( 'NONE',  ( -0.000000000000000000, -0.000000000000000000, 1.000000000000000000 ) ) ;
#10413=CARTESIAN_POINT ( 'NONE',  ( -8.691771469529815392E-16, 56.67999999999998550, 14.19474002721660355 ) ) ;
#10414=CARTESIAN_POINT ( 'NONE',  ( -11.83228429192144304, 71.17079610990623451, 6.499773857208959171 ) ) ;
#10416=CARTESIAN_POINT ( 'NONE',  ( -7.557983764346632327, 68.39670004143046356, 11.19912239775939433 ) ) ;
#10418=CARTESIAN_POINT ( 'NONE',  ( 3.289654790109945992, 55.06171615666674057, -13.09305896734488606 ) ) ;
#10421=CARTESIAN_POINT ( 'NONE',  ( -9.885467538893191630, 65.28675227565267392, 9.194100240487596665 ) ) ;
#10423=CARTESIAN_POINT ( 'NONE',  ( -4.873736741403357442, 35.50432647131191999, 12.59114714938776736 ) ) ;
#10427=( BOUNDED_CURVE ( )  B_SPLINE_CURVE ( 2, ( #3216, #15229, #7212, #1886, #7130, #313, #12600, #7300, #12427, #5895, #13904, #15050, #4559 ),
 .UNSPECIFIED., .F., .F. ) 
 B_SPLINE_CURVE_WITH_KNOTS ( ( 3, 2, 2, 2, 2, 2, 3 ),
 ( 0.3472222222222222099, 0.3499999999999999778, 0.3555555555555555691, 0.3611111111111111049, 0.3666666666666666408, 0.3722222222222222321, 0.3750000000000000000 ),
 .UNSPECIFIED. ) 
 CURVE ( )  GEOMETRIC_REPRESENTATION_ITEM ( )  RATIONAL_B_SPLINE_CURVE ( ( 0.9755282581475768211, 0.9755282581475768211, 1.000000000000000000, 0.9510565162951535312, 1.000000000000000000, 0.9510565162951535312, 1.000000000000000000, 0.9510565162951535312, 1.000000000000000000, 0.9510565162951535312, 1.000000000000000000, 0.9755282581475768211, 0.9755282581475768211 ) ) 
 REPRESENTATION_ITEM ( '' )  );
#10429=CARTESIAN_POINT ( 'NONE',  ( -1.245860404445607248E-06, 40.18000018109674443, -13.49999999999994316 ) ) ;
#10430=CARTESIAN_POINT ( 'NONE',  ( -13.32379211457350721, 32.00634305175220362, 2.174812285166201509 ) ) ;
#10432=CARTESIAN_POINT ( 'NONE',  ( 12.62498755182630461, 60.25550772051544612, 4.821155371132717526 ) ) ;
#10434=CARTESIAN_POINT ( 'NONE',  ( -10.00804607396390189, 53.28036437624847110, 9.060407765840576388 ) ) ;
#10436=CARTESIAN_POINT ( 'NONE',  ( -7.576616670048093940E-16, 54.67999999999999261, 12.37355403259654985 ) ) ;
#10438=CARTESIAN_POINT ( 'NONE',  ( 13.39324380192281971, 51.37084852268094437, 1.694922732828999967 ) ) ;
#10439=CARTESIAN_POINT ( 'NONE',  ( -13.47682487734259738, 37.90268679109564687, -0.7907200057638921198 ) ) ;
#10440=CARTESIAN_POINT ( 'NONE',  ( 10.29076770525271556, 36.76532346438606424, -8.737960796721409906 ) ) ;
#10442=CARTESIAN_POINT ( 'NONE',  ( -6.074181061366862977, 74.45811146783317724, 12.05629934353452093 ) ) ;
#10443=CARTESIAN_POINT ( 'NONE',  ( -12.04419590223588443, 77.15471538261230933, 6.098651071946050273 ) ) ;
#10444=CARTESIAN_POINT ( 'NONE',  ( 1.590819206443820466, 62.73723098374880891, 13.40788169120826545 ) ) ;
#10445=CARTESIAN_POINT ( 'NONE',  ( 7.500000000000000000, 108.6686507028258575, 2.034160311361953521 ) ) ;
#10447=AXIS2_PLACEMENT_3D ( 'NONE', #5972, #1958, #7382 ) ;
#10449=VERTEX_POINT ( 'NONE', #14367 ) ;
#10450=CARTESIAN_POINT ( 'NONE',  ( -3.636496289402153081, 59.32999999999999829, -11.19198476289190936 ) ) ;
#10454=EDGE_CURVE ( 'NONE', #12212, #14613, #11740, .T. ) ;
#10455=CARTESIAN_POINT ( 'NONE',  ( 4.018767646357342294, 76.03543680882090428, -12.88819257462414392 ) ) ;
#10456=CARTESIAN_POINT ( 'NONE',  ( -13.49999999999999822, 67.78000000000001535, -4.386415899144240349 ) ) ;
#10457=CARTESIAN_POINT ( 'NONE',  ( -11.76794919243112325, 45.07999999999999829, 3.823638476888994386 ) ) ;
#10459=CARTESIAN_POINT ( 'NONE',  ( -13.47710269719165588, 58.90286290043330553, -0.7859701997998082001 ) ) ;
#10460=CARTESIAN_POINT ( 'NONE',  ( 10.42107401898988250, 45.10176735786057378, 8.582029462888934646 ) ) ;
#10461=CARTESIAN_POINT ( 'NONE',  ( 11.99114687028902537, 69.65883756502691426, -6.201907584533547180 ) ) ;
#10462=CARTESIAN_POINT ( 'NONE',  ( -8.343458848123582072, 67.37999999999998124, 11.48378591275253768 ) ) ;
#10463=CARTESIAN_POINT ( 'NONE',  ( 12.17494424314613255, 30.21560166499141431, 5.835599225542421387 ) ) ;
#10464=CARTESIAN_POINT ( 'NONE',  ( -8.113100482602192187, 55.48749888713909684, -10.81048510016282371 ) ) ;
#10465=CARTESIAN_POINT ( 'NONE',  ( -8.613601466380250926, 50.34913078849175605, 10.39500302588977476 ) ) ;
#10466=CARTESIAN_POINT ( 'NONE',  ( 7.870204901766977734, 63.88288127658925220, -10.96870105014976637 ) ) ;
#10467=CARTESIAN_POINT ( 'NONE',  ( 7.482711392322309862, 42.89984591038155770, -11.23950954596197072 ) ) ;
#10468=CARTESIAN_POINT ( 'NONE',  ( 12.48936162389965254, 39.24350828422937099, 5.125161080676649661 ) ) ;
#10469=VERTEX_POINT ( 'NONE', #17032 ) ;
#10470=CARTESIAN_POINT ( 'NONE',  ( -12.76659169606017841, 70.77175795909352018, -4.389135967592094012 ) ) ;
#10471=CARTESIAN_POINT ( 'NONE',  ( -7.531934336383805828, 61.46230439911880694, -11.20387762871766313 ) ) ;
#10474=AXIS2_PLACEMENT_3D ( 'NONE', #47, #16114, #5452 ) ;
#10475=CARTESIAN_POINT ( 'NONE',  ( -6.886120549656922663, 40.43470322261091354, -11.62389360686549722 ) ) ;
#10479=DIRECTION ( 'NONE',  ( 0.000000000000000000, 0.000000000000000000, 1.000000000000000000 ) ) ;
#10480=CARTESIAN_POINT ( 'NONE',  ( 12.46436792225129508, 57.24116669652607214, 5.185512586538920665 ) ) ;
#10481=CARTESIAN_POINT ( 'NONE',  ( 3.636496289402157078, 77.03000000000000114, -11.19198476289190936 ) ) ;
#10482=CARTESIAN_POINT ( 'NONE',  ( 2.272985001014427788E-15, 80.18000000000000682, -12.37355403259654985 ) ) ;
#10483=CARTESIAN_POINT ( 'NONE',  ( -0.1736399972044732620, 47.67375642894414511, 13.49917766817768339 ) ) ;
#10487=CYLINDRICAL_SURFACE ( 'NONE', #11207, 8.999999999999998224 ) ;
#10489=CARTESIAN_POINT ( 'NONE',  ( -2.464184276881911995, 73.26860352173120816, -13.27409137780385429 ) ) ;
#10490=VERTEX_POINT ( 'NONE', #944 ) ;
#10491=VERTEX_POINT ( 'NONE', #9104 ) ;
#10496=CARTESIAN_POINT ( 'NONE',  ( -7.237748362078336939, 44.41032146096258515, 11.39663970212459176 ) ) ;
#10498=CARTESIAN_POINT ( 'NONE',  ( 11.32884907035391464, 66.70497250890650776, -7.345399851619622389 ) ) ;
#10499=CARTESIAN_POINT ( 'NONE',  ( 4.171729424061789260, 50.82999999999999829, 12.83926296998457417 ) ) ;
#10500=CARTESIAN_POINT ( 'NONE',  ( -4.802988300473575833, 71.50697978349295170, 12.61891950573222765 ) ) ;
#10504=CARTESIAN_POINT ( 'NONE',  ( -13.38959891692747917, 67.86975879323100003, -1.725407304280444754 ) ) ;
#10507=CARTESIAN_POINT ( 'NONE',  ( 6.335111093105661340, 54.94766729977810371, -11.92126117983150912 ) ) ;
#10509=CARTESIAN_POINT ( 'NONE',  ( -11.50534062751997411, 65.19367442093394516, 7.062375311795522137 ) ) ;
#10510=CARTESIAN_POINT ( 'NONE',  ( -2.138189944381199137, 43.60311857767973720, 13.50000000000001421 ) ) ;
#10511=CARTESIAN_POINT ( 'NONE',  ( -11.27144135186879659, 35.20884229997658110, 7.430021984585419403 ) ) ;
#10514=CARTESIAN_POINT ( 'NONE',  ( -11.32176554887916886, 32.20565710450659225, 7.353236199019049124 ) ) ;
#10517=CARTESIAN_POINT ( 'NONE',  ( -9.441479826001016207, 53.30963963675974071, 9.659188822020484011 ) ) ;
#10518=CIRCLE ( 'NONE', #12498, 12.00000000000000178 ) ;
#10519=CARTESIAN_POINT ( 'NONE',  ( 7.272992578804311492, 58.88000000000000256, -10.01041549318726709 ) ) ;
#10520=CARTESIAN_POINT ( 'NONE',  ( -8.343458848123576743, 72.48000000000000398, -11.48378591275254301 ) ) ;
#10521=CARTESIAN_POINT ( 'NONE',  ( 12.58419665743400628, 51.25262647264697335, 4.889168462974375906 ) ) ;
#10522=CARTESIAN_POINT ( 'NONE',  ( -9.357762247734804362, 38.31343841487202440, 9.730492229755752120 ) ) ;
#10523=CARTESIAN_POINT ( 'NONE',  ( 13.49767104495738401, 36.43897965465946953, -0.2631044504109197324 ) ) ;
#10525=DIRECTION ( 'NONE',  ( 0.000000000000000000, 0.000000000000000000, -1.000000000000000000 ) ) ;
#10526=CARTESIAN_POINT ( 'NONE',  ( -12.28277907283284698, 77.13527343425541005, 5.607119744471182443 ) ) ;
#10527=VECTOR ( 'NONE', #12908, 1000.000000000000000 ) ;
#10528=CARTESIAN_POINT ( 'NONE',  ( -11.05895565395609026, 80.22189889663263784, 7.743948080728770833 ) ) ;
#10534=CARTESIAN_POINT ( 'NONE',  ( -3.636496289402155746, 54.52999999999999403, 11.19198476289190936 ) ) ;
#10536=FACE_BOUND ( 'NONE', #4260, .T. ) ;
#10538=CARTESIAN_POINT ( 'NONE',  ( 11.90151132640803944, 75.66574786089606164, -6.376363749881278409 ) ) ;
#10540=CARTESIAN_POINT ( 'NONE',  ( -13.49999999999999822, 77.07999999999998408, 4.386415899144235908 ) ) ;
#10541=CARTESIAN_POINT ( 'NONE',  ( 2.272985001014427788E-15, 41.17999999999999972, -12.37355403259654985 ) ) ;
#10543=AXIS2_PLACEMENT_3D ( 'NONE', #15064, #9808, #13661 ) ;
#10544=CARTESIAN_POINT ( 'NONE',  ( -13.46788654291206733, 58.89779059911582237, -0.9332917827898941088 ) ) ;
#10545=EDGE_CURVE ( 'NONE', #16090, #5515, #15528, .T. ) ;
#10546=CARTESIAN_POINT ( 'NONE',  ( 8.093304213249069790, 44.98702088532150611, 10.81425868566774895 ) ) ;
#10547=CARTESIAN_POINT ( 'NONE',  ( 13.41529543626620757, 69.37743073738961641, 1.509923354937637852 ) ) ;
#10549=CARTESIAN_POINT ( 'NONE',  ( -13.49999999999999822, 66.78000000000000114, -4.386415899144240349 ) ) ;
#10551=CARTESIAN_POINT ( 'NONE',  ( -2.436326588224761114, 55.26753496234241680, -13.28513367767414977 ) ) ;
#10552=CARTESIAN_POINT ( 'NONE',  ( -10.73222887417678351, 50.24104608057613319, 8.192202916843667637 ) ) ;
#10553=CARTESIAN_POINT ( 'NONE',  ( 7.611112758387253763, 63.89427894107092953, -11.15141948763443835 ) ) ;
#10554=CARTESIAN_POINT ( 'NONE',  ( 11.14349067449326292, 42.71675866716687864, -7.620623970109671852 ) ) ;
#10555=CARTESIAN_POINT ( 'NONE',  ( 13.34721606699788232, 39.35891505498212695, 2.027891307246981079 ) ) ;
#10557=CARTESIAN_POINT ( 'NONE',  ( -9.314018664953470861, 70.54409196600954601, -9.787303825282853253 ) ) ;
#10558=CARTESIAN_POINT ( 'NONE',  ( -4.673977061459858362, 61.34833404053931361, -12.66657423768662305 ) ) ;
#10561=ORIENTED_EDGE ( 'NONE', *, *, #7493, .T. ) ;
#10564=CARTESIAN_POINT ( 'NONE',  ( 5.028978472489433749, 47.86150763825980903, 12.52835470249129735 ) ) ;
#10565=CARTESIAN_POINT ( 'NONE',  ( 13.37958125658008868, 57.49285659070703502, -1.800066904135027013 ) ) ;
#10566=CARTESIAN_POINT ( 'NONE',  ( 7.272992578804308828, 69.97999999999998977, 10.01041549318726709 ) ) ;
#10567=CARTESIAN_POINT ( 'NONE',  ( -7.272992578804307939, 80.48000000000000398, -10.01041549318726886 ) ) ;
#10568=CARTESIAN_POINT ( 'NONE',  ( -0.2850622938858722311, 47.66975023300910408, 13.49700841942235918 ) ) ;
#10571=CARTESIAN_POINT ( 'NONE',  ( -13.49999999999999822, 33.77999999999999403, -4.386415899144240349 ) ) ;
#10573=DIRECTION ( 'NONE',  ( -0.000000000000000000, -0.000000000000000000, 1.000000000000000000 ) ) ;
#10574=CARTESIAN_POINT ( 'NONE',  ( 8.419288814318939274, 33.85814146373429878, -10.55389719033477292 ) ) ;
#10575=CARTESIAN_POINT ( 'NONE',  ( -2.271044718833372222, 73.26165834582242553, -13.30761088842764295 ) ) ;
#10577=ORIENTED_EDGE ( 'NONE', *, *, #2407, .T. ) ;
#10578=CARTESIAN_POINT ( 'NONE',  ( 3.636496289402154414, 78.82999999999999829, 11.19198476289190936 ) ) ;
#10579=ORIENTED_EDGE ( 'NONE', *, *, #206, .T. ) ;
#10581=CARTESIAN_POINT ( 'NONE',  ( -6.789762389132963705, 44.42913898759260860, 11.67122559010108418 ) ) ;
#10583=CARTESIAN_POINT ( 'NONE',  ( 11.87809514247365072, 66.66774229667706209, -6.421792920400507754 ) ) ;
#10584=CARTESIAN_POINT ( 'NONE',  ( -10.92172942406178926, 46.62999999999999545, -7.935100905948389460 ) ) ;
#10585=CARTESIAN_POINT ( 'NONE',  ( -3.171773181161692268, 71.56595516633068144, 13.12211643693878216 ) ) ;
#10589=CARTESIAN_POINT ( 'NONE',  ( -13.43350214447777979, 67.88349517729756144, -1.338323814899765818 ) ) ;
#10591=CARTESIAN_POINT ( 'NONE',  ( 6.127710875979031080, 54.95599452305749821, -12.02960116012748948 ) ) ;
#10594=CARTESIAN_POINT ( 'NONE',  ( -12.55657707847996107, 65.11044514684080298, 4.970209462128218902 ) ) ;
#10595=CARTESIAN_POINT ( 'NONE',  ( -7.264233121273926841, 35.40920166682224135, 11.37991948868003611 ) ) ;
#10597=ORIENTED_EDGE ( 'NONE', *, *, #3724, .F. ) ;
#10598=CARTESIAN_POINT ( 'NONE',  ( 2.445080149700053643E-15, 51.18000000000000682, -13.50000000000000000 ) ) ;
#10600=CARTESIAN_POINT ( 'NONE',  ( -4.763038992625359569, 31.35156427714300165, -12.63378481403946552 ) ) ;
#10601=CARTESIAN_POINT ( 'NONE',  ( 1.959398577741635616, 73.10957903055695795, -13.36603894048193908 ) ) ;
#10602=CARTESIAN_POINT ( 'NONE',  ( 13.03631756181396995, 60.30489250172575311, 3.507832160399530164 ) ) ;
#10603=CARTESIAN_POINT ( 'NONE',  ( -10.95368854796565650, 53.22816082705852381, 7.891413927665784200 ) ) ;
#10604=CARTESIAN_POINT ( 'NONE',  ( 7.272992578804311492, 61.87999999999999545, -10.01041549318726709 ) ) ;
#10605=CARTESIAN_POINT ( 'NONE',  ( 6.428591458046670759, 50.91606176058002120, 11.87836298906071519 ) ) ;
#10606=CARTESIAN_POINT ( 'NONE',  ( -13.00484043580565086, 37.80058143574180463, -3.623669304979980854 ) ) ;
#10607=CARTESIAN_POINT ( 'NONE',  ( 9.206534659575176249, 36.03913477569856383, 9.873698037947086448 ) ) ;
#10609=CARTESIAN_POINT ( 'NONE',  ( -5.229807916748995034, 74.49090577273676672, 12.44584714537170633 ) ) ;
#10610=CARTESIAN_POINT ( 'NONE',  ( -9.476141181518151768, 76.55243570330306113, -9.615298271795859719 ) ) ;
#10611=CARTESIAN_POINT ( 'NONE',  ( -12.63999744390774183, 80.10245305523378079, 4.762197372853401944 ) ) ;
#10613=CARTESIAN_POINT ( 'NONE',  ( 7.500000000000000888, 102.9299999999999073, 9.367496997597653419 ) ) ;
#10616=CARTESIAN_POINT ( 'NONE',  ( 7.272992578804311492, 52.87999999999998835, -10.01041549318726886 ) ) ;
#10621=CARTESIAN_POINT ( 'NONE',  ( 3.667885382569292307, 76.04811590521021003, -12.99217945106073735 ) ) ;
#10623=CARTESIAN_POINT ( 'NONE',  ( 4.171729424061791924, 69.03000000000000114, -12.83926296998457239 ) ) ;
#10624=CARTESIAN_POINT ( 'NONE',  ( -3.636496289402155746, 42.53000000000000114, 11.19198476289190936 ) ) ;
#10625=CARTESIAN_POINT ( 'NONE',  ( -11.96482485551292285, 58.69645965844525648, -6.333484686160312904 ) ) ;
#10627=CARTESIAN_POINT ( 'NONE',  ( 2.919893365847839650, 44.78498848662554366, 13.18044854437260405 ) ) ;
#10628=CARTESIAN_POINT ( 'NONE',  ( 12.01162584235229680, 69.65724634270705451, -6.162282692494446046 ) ) ;
#10629=CARTESIAN_POINT ( 'NONE',  ( 2.138189944381238661, 58.75688142232026223, 13.50000000000000000 ) ) ;
#10630=CARTESIAN_POINT ( 'NONE',  ( 10.95321195831160743, 30.13180978604457039, 7.892151158665086541 ) ) ;
#10631=CARTESIAN_POINT ( 'NONE',  ( -10.15369422253785814, 55.58731133826776016, -8.896836259020886928 ) ) ;
#10632=CARTESIAN_POINT ( 'NONE',  ( -5.368619122948546263, 50.48560663089287459, 12.38686502221418984 ) ) ;
#10633=CARTESIAN_POINT ( 'NONE',  ( 13.47553014558564222, 63.40190322894259367, 0.8129172673421702910 ) ) ;
#10634=CARTESIAN_POINT ( 'NONE',  ( 13.01146853698397088, 42.55849631815364376, -3.598855205904288201 ) ) ;
#10635=CARTESIAN_POINT ( 'NONE',  ( 13.50321739804985732, 39.42843470989561894, 0.04034527670750228528 ) ) ;
#10637=CARTESIAN_POINT ( 'NONE',  ( -4.853172931527291567, 70.35493761421939496, -12.59957856612076021 ) ) ;
#10638=CARTESIAN_POINT ( 'NONE',  ( -1.376924736209377498, 61.22942669131018079, -13.43187964474915930 ) ) ;
#10639=AXIS2_PLACEMENT_3D ( 'NONE', #3066, #16681, #430 ) ;
#10641=ORIENTED_EDGE ( 'NONE', *, *, #2092, .T. ) ;
#10645=EDGE_CURVE ( 'NONE', #11531, #668, #14012, .T. ) ;
#10646=CARTESIAN_POINT ( 'NONE',  ( 6.624002440913375978, 47.92407202630063523, 11.76319263586970010 ) ) ;
#10648=CARTESIAN_POINT ( 'NONE',  ( 9.880830748590257784, 72.07300539084614854, 9.199255159373397106 ) ) ;
#10649=CARTESIAN_POINT ( 'NONE',  ( 13.49993779747335942, 57.43171647853688455, -0.05021896834556438538 ) ) ;
#10650=CARTESIAN_POINT ( 'NONE',  ( -11.76794919243112325, 69.08000000000001251, 3.823638476888994386 ) ) ;
#10651=CARTESIAN_POINT ( 'NONE',  ( 9.520470885617717371, 73.73000000000000398, -6.917026985038131848 ) ) ;
#10652=CARTESIAN_POINT ( 'NONE',  ( -11.36497532230790064, 47.20289303351260912, 7.286111716941032768 ) ) ;
#10655=CARTESIAN_POINT ( 'NONE',  ( -2.138189944381236884, 75.25688142232026223, -13.50000000000000000 ) ) ;
#10658=CARTESIAN_POINT ( 'NONE',  ( 11.99908723489971329, 33.65823093649722608, -6.186429237525048030 ) ) ;
#10659=CARTESIAN_POINT ( 'NONE',  ( -9.649170248876741240, 73.56114326775332302, -9.441584397305010867 ) ) ;
#10660=ORIENTED_EDGE ( 'NONE', *, *, #6794, .F. ) ;
#10662=CARTESIAN_POINT ( 'NONE',  ( -7.272992578804307939, 74.47999999999998977, -10.01041549318727064 ) ) ;
#10663=VERTEX_POINT ( 'NONE', #6772 ) ;
#10665=CARTESIAN_POINT ( 'NONE',  ( -10.15272881233574331, 44.27273562141181174, 8.897895435131198738 ) ) ;
#10666=EDGE_CURVE ( 'NONE', #13385, #1377, #13011, .T. ) ;
#10668=CARTESIAN_POINT ( 'NONE',  ( -8.343458848123582072, 47.37999999999998835, 11.48378591275254124 ) ) ;
#10669=CARTESIAN_POINT ( 'NONE',  ( -5.685284667237421985, 71.47340530370703959, 12.24467241409343110 ) ) ;
#10671=CARTESIAN_POINT ( 'NONE',  ( -12.81927299732829795, 68.08231120825506366, 4.232820650394039319 ) ) ;
#10673=CARTESIAN_POINT ( 'NONE',  ( 10.54836534261182912, 54.75121614555988714, -8.425092043074821291 ) ) ;
#10676=CARTESIAN_POINT ( 'NONE',  ( -13.45796656469188335, 64.89315254009517275, -1.064987061088984222 ) ) ;
#10677=CARTESIAN_POINT ( 'NONE',  ( -9.611889644271915500, 35.30078168614076617, 9.481849804571114149 ) ) ;
#10678=VERTEX_POINT ( 'NONE', #285 ) ;
#10679=CARTESIAN_POINT ( 'NONE',  ( 10.92172942406178926, 50.13000000000000256, 7.935100905948387684 ) ) ;
#10681=CARTESIAN_POINT ( 'NONE',  ( -10.71852365211889335, 31.61759523208409917, -8.219185043125531109 ) ) ;
#10684=CARTESIAN_POINT ( 'NONE',  ( 3.225602179493814781, 59.79598290809182259, 13.10898689560911379 ) ) ;
#10686=CARTESIAN_POINT ( 'NONE',  ( -11.12850500992075808, 53.21771862217647708, 7.643148398810014399 ) ) ;
#10687=CARTESIAN_POINT ( 'NONE',  ( 7.272992578804308828, 48.97999999999999687, 10.01041549318726709 ) ) ;
#10689=CARTESIAN_POINT ( 'NONE',  ( 8.343458848123583849, 65.87999999999999545, -11.48378591275253768 ) ) ;
#10690=CARTESIAN_POINT ( 'NONE',  ( 11.13837427305282191, 51.14299245685476336, 7.631533066694935030 ) ) ;
#10692=CARTESIAN_POINT ( 'NONE',  ( -8.103196614201737091, 37.48751268113657176, -10.79762506269431199 ) ) ;
#10693=CARTESIAN_POINT ( 'NONE',  ( 11.16073815863965812, 36.14426946062943813, 7.595459063093625396 ) ) ;
#10695=CARTESIAN_POINT ( 'NONE',  ( -0.6513326186324287503, 74.65658052450302762, 13.48429236608166448 ) ) ;
#10696=CARTESIAN_POINT ( 'NONE',  ( -13.47320743554847589, 76.96033088227574126, 0.8785557905998884198 ) ) ;
#10697=CARTESIAN_POINT ( 'NONE',  ( -9.234617383006181512, 80.31946446022799080, 9.849864266179150007 ) ) ;
#10699=CARTESIAN_POINT ( 'NONE',  ( 7.499999999999998224, 107.9394166107542787, 5.548846425319428732 ) ) ;
#10701=CARTESIAN_POINT ( 'NONE',  ( -11.76794919243112325, 48.07999999999999119, 3.823638476888994830 ) ) ;
#10706=CARTESIAN_POINT ( 'NONE',  ( 12.45777842108767608, 75.61978625587052250, -5.214092426080158660 ) ) ;
#10707=AXIS2_PLACEMENT_3D ( 'NONE', #4910, #8902, #9166 ) ;
#10709=CARTESIAN_POINT ( 'NONE',  ( -9.520470885617715595, 38.62999999999999545, -6.917026985038136289 ) ) ;
#10710=CARTESIAN_POINT ( 'NONE',  ( -7.774974083674261571, 41.38732224484842703, 11.04531834479223917 ) ) ;
#10711=CARTESIAN_POINT ( 'NONE',  ( -9.145099759719814259, 58.53607511944338881, -9.932359848896243903 ) ) ;
#10713=CARTESIAN_POINT ( 'NONE',  ( 6.296202951178191398, 44.91078442072279842, 11.94188463877171458 ) ) ;
#10714=CARTESIAN_POINT ( 'NONE',  ( 0.000000000000000000, -1.200000000000000030E-05, 0.000000000000000000 ) ) ;
#10715=EDGE_CURVE ( 'NONE', #7293, #13128, #2491, .T. ) ;
#10716=CARTESIAN_POINT ( 'NONE',  ( -12.08201809334919830, 55.70826805169760831, -6.022897540302621699 ) ) ;
#10717=CARTESIAN_POINT ( 'NONE',  ( -13.27145342533492212, 49.84287066452262849, -2.473646717969534503 ) ) ;
#10718=CARTESIAN_POINT ( 'NONE',  ( 10.96675222851313514, 63.72739450245582304, -7.884886543510749135 ) ) ;
#10719=CARTESIAN_POINT ( 'NONE',  ( 5.656850990071720986, 42.97450686619443871, -12.25765484162504215 ) ) ;
#10720=CARTESIAN_POINT ( 'NONE',  ( 13.48307184846283491, 39.45330054262541353, -0.6758713956733961581 ) ) ;
#10721=VERTEX_POINT ( 'NONE', #8168 ) ;
#10722=CARTESIAN_POINT ( 'NONE',  ( -5.553750751693518062, 70.38149911725399477, -12.30503917794814939 ) ) ;
#10723=CARTESIAN_POINT ( 'NONE',  ( -0.5774508230433464950, 61.20074394919704730, -13.49036888543782275 ) ) ;
#10728=CARTESIAN_POINT ( 'NONE',  ( 4.789765888146141570, 61.00743788133880230, -12.62174563288985141 ) ) ;
#10732=CARTESIAN_POINT ( 'NONE',  ( 11.56040206224664502, 57.68997124128148357, -6.971880404141066911 ) ) ;
#10733=CARTESIAN_POINT ( 'NONE',  ( 7.272992578804311492, 64.87999999999999545, -10.01041549318726709 ) ) ;
#10734=CARTESIAN_POINT ( 'NONE',  ( -11.76794919243112325, 72.07999999999999829, 3.823638476888994386 ) ) ;
#10735=CARTESIAN_POINT ( 'NONE',  ( -6.839096004689836583, 47.42708027506941448, 11.64121267617738553 ) ) ;
#10737=CARTESIAN_POINT ( 'NONE',  ( -8.343458848123578520, 45.47999999999998977, -11.48378591275254124 ) ) ;
#10741=CARTESIAN_POINT ( 'NONE',  ( -13.49999999999999822, 39.77999999999998693, -4.386415899144240349 ) ) ;
#10742=CARTESIAN_POINT ( 'NONE',  ( 12.05830588875037712, 33.65359821999817314, -6.070472308088694646 ) ) ;
#10743=CARTESIAN_POINT ( 'NONE',  ( -3.658860937772914212, 73.31156020023337305, -12.99472133403736152 ) ) ;
#10745=VERTEX_POINT ( 'NONE', #4262 ) ;
#10746=CARTESIAN_POINT ( 'NONE',  ( -9.520470885617717371, 78.23000000000000398, 6.917026985038133624 ) ) ;
#10749=CARTESIAN_POINT ( 'NONE',  ( -4.276945109164544512, 44.52621246546315348, 12.80489214357455197 ) ) ;
#10751=CARTESIAN_POINT ( 'NONE',  ( -8.343458848123576743, 40.47999999999999687, -11.48378591275254301 ) ) ;
#10752=CARTESIAN_POINT ( 'NONE',  ( -13.49952901374136083, 70.92525494836556277, -0.1387502169606815439 ) ) ;
#10753=VECTOR ( 'NONE', #5854, 1000.000000000000000 ) ;
#10756=CARTESIAN_POINT ( 'NONE',  ( -13.40586589714901322, 67.87439773989004266, -1.595217673327048447 ) ) ;
#10759=CARTESIAN_POINT ( 'NONE',  ( 13.49702819973023615, 54.44026504364671126, -0.2991497332704560752 ) ) ;
#10761=CARTESIAN_POINT ( 'NONE',  ( -12.92775954166086549, 64.79065094487656040, -3.889038681538313114 ) ) ;
#10762=CARTESIAN_POINT ( 'NONE',  ( -12.94307868198818845, 34.79255189543185622, -3.838412397159299605 ) ) ;
#10765=CARTESIAN_POINT ( 'NONE',  ( 0.000000000000000000, 80.93000000000000682, 0.000000000000000000 ) ) ;
#10766=CARTESIAN_POINT ( 'NONE',  ( -5.471302638117776063, 31.37832158213074862, -12.34159723640939887 ) ) ;
#10767=CARTESIAN_POINT ( 'NONE',  ( 5.935702408891331494, 72.96359331791715874, -12.12507858477615308 ) ) ;
#10768=DIRECTION ( 'NONE',  ( 1.000000000000000000, 8.673617379884035472E-17, 0.000000000000000000 ) ) ;
#10770=CARTESIAN_POINT ( 'NONE',  ( -5.697279727035623687, 53.47290833051743419, 12.24689732723735425 ) ) ;
#10771=CARTESIAN_POINT ( 'NONE',  ( -3.636496289402155746, 45.53000000000000114, 11.19198476289190936 ) ) ;
#10773=CARTESIAN_POINT ( 'NONE',  ( 10.92172942406178926, 71.12999999999999545, 7.935100905948387684 ) ) ;
#10774=CARTESIAN_POINT ( 'NONE',  ( 5.061740244522564325, 50.86273991812466022, 12.51519464505669887 ) ) ;
#10775=CARTESIAN_POINT ( 'NONE',  ( -13.21301978975160729, 37.83156230358514449, -2.785450445402589015 ) ) ;
#10777=CARTESIAN_POINT ( 'NONE',  ( 6.741550819447308385, 35.92884056994786590, 11.69833314936273894 ) ) ;
#10779=CARTESIAN_POINT ( 'NONE',  ( -11.99481679410065382, 74.15856145072713446, 6.194708363428219400 ) ) ;
#10780=CARTESIAN_POINT ( 'NONE',  ( -10.55318980305114884, 76.60867959057283372, -8.423370909350431646 ) ) ;
#10781=CARTESIAN_POINT ( 'NONE',  ( -11.69703628230260151, 79.67889527854070764, -6.754490024069266241 ) ) ;
#10783=CARTESIAN_POINT ( 'NONE',  ( 1.668451422296014508, 80.93000000000003524, 13.07629037559565610 ) ) ;
#10785=CARTESIAN_POINT ( 'NONE',  ( 11.76794919243112325, 52.28000000000000114, 3.823638476888997051 ) ) ;
#10789=CARTESIAN_POINT ( 'NONE',  ( -12.98636831301070060, 40.79815473098589962, -3.688632511342929465 ) ) ;
#10792=CARTESIAN_POINT ( 'NONE',  ( 11.33580039144190899, 75.15524277601195990, 7.331465318532246478 ) ) ;
#10793=CARTESIAN_POINT ( 'NONE',  ( 13.50000000000000000, 32.42999999999999972, 1.653273178848926867E-15 ) ) ;
#10794=CARTESIAN_POINT ( 'NONE',  ( 10.92172942406179104, 50.72999999999999687, -7.935100905948385908 ) ) ;
#10795=CARTESIAN_POINT ( 'NONE',  ( 3.636496289402154414, 39.82999999999999829, 11.19198476289190936 ) ) ;
#10796=CARTESIAN_POINT ( 'NONE',  ( -5.328320514085317150, 41.48727112542576378, 12.41054507597009149 ) ) ;
#10797=CARTESIAN_POINT ( 'NONE',  ( -8.769463355901507384, 58.51817495466201535, -10.26385875965554462 ) ) ;
#10799=AXIS2_PLACEMENT_3D ( 'NONE', #11629, #15408, #2231 ) ;
#10801=CARTESIAN_POINT ( 'NONE',  ( 10.92172942406179104, 59.73000000000000398, -7.935100905948385908 ) ) ;
#10804=CARTESIAN_POINT ( 'NONE',  ( -7.425691233511519940, 49.45773034968338777, -11.27429194107610044 ) ) ;
#10805=CARTESIAN_POINT ( 'NONE',  ( 13.22478289187903222, 63.52662974475261137, -2.734757776350366321 ) ) ;
#10806=CARTESIAN_POINT ( 'NONE',  ( 12.65298316251227284, 42.60172510704381210, -4.748097754914298640 ) ) ;
#10808=VERTEX_POINT ( 'NONE', #5513 ) ;
#10811=ORIENTED_EDGE ( 'NONE', *, *, #7215, .T. ) ;
#10812=CARTESIAN_POINT ( 'NONE',  ( -7.347982688691526043, 43.45433612642857923, -11.33561514380692792 ) ) ;
#10814=CARTESIAN_POINT ( 'NONE',  ( 12.45342510802381497, 60.62052796052494585, -5.234417581101719286 ) ) ;
#10817=CARTESIAN_POINT ( 'NONE',  ( 9.768097186728329717, 72.06720429639440795, 9.318491340992334671 ) ) ;
#10818=CARTESIAN_POINT ( 'NONE',  ( 13.47581130843072650, 57.39853584928295049, 0.9114065446593455633 ) ) ;
#10819=CARTESIAN_POINT ( 'NONE',  ( -3.636496289402155746, 69.53000000000001535, 11.19198476289190936 ) ) ;
#10820=CARTESIAN_POINT ( 'NONE',  ( 11.76794919243112680, 79.57999999999999829, -3.823638476888993942 ) ) ;
#10821=CARTESIAN_POINT ( 'NONE',  ( -9.976789923895726275, 47.28199978130749059, 9.094920084438699703 ) ) ;
#10823=CARTESIAN_POINT ( 'NONE',  ( 4.171729424061789260, 73.83000000000001251, 12.83926296998457417 ) ) ;
#10824=CARTESIAN_POINT ( 'NONE',  ( 8.343458848123580296, 37.97999999999999687, 11.48378591275253768 ) ) ;
#10825=CARTESIAN_POINT ( 'NONE',  ( -2.138189944381230223, 76.60311857767973720, 13.50000000000000178 ) ) ;
#10827=CARTESIAN_POINT ( 'NONE',  ( -2.138189944381240881, 40.60311857767972299, 13.49999999999999822 ) ) ;
#10828=CARTESIAN_POINT ( 'NONE',  ( 13.37800033110732478, 33.36627688407902070, 1.820700357919406542 ) ) ;
#10829=CARTESIAN_POINT ( 'NONE',  ( -5.415842637199018483, 73.37609553661370398, -12.37091407123440412 ) ) ;
#10830=ORIENTED_EDGE ( 'NONE', *, *, #4834, .T. ) ;
#10831=EDGE_LOOP ( 'NONE', ( #152, #6411, #12151, #14332 ) ) ;
#10833=CARTESIAN_POINT ( 'NONE',  ( -4.084710662422550875, 62.53312106380167990, 12.86754019334286703 ) ) ;
#10836=CARTESIAN_POINT ( 'NONE',  ( -11.20293937805184470, 44.21312063056868880, 7.532871974709584251 ) ) ;
#10837=CARTESIAN_POINT ( 'NONE',  ( -10.92172942406179104, 44.22999999999999687, 7.935100905948387684 ) ) ;
#10838=CARTESIAN_POINT ( 'NONE',  ( 13.50000000000000355, 47.57999999999999119, -4.386415899144233244 ) ) ;
#10839=CARTESIAN_POINT ( 'NONE',  ( -12.50265387745223222, 71.11554310126858525, 5.102506177351393113 ) ) ;
#10841=CARTESIAN_POINT ( 'NONE',  ( -13.45717572954313646, 67.96817528193095370, 1.102425897065126392 ) ) ;
#10843=CARTESIAN_POINT ( 'NONE',  ( 12.98222888748651727, 54.29759349226736731, 3.703881015682214617 ) ) ;
#10845=CARTESIAN_POINT ( 'NONE',  ( -11.88702157392819814, 64.69325053915714818, -6.399122214038043488 ) ) ;
#10847=CARTESIAN_POINT ( 'NONE',  ( -13.35126160523930139, 34.99999482559385200, 1.998514373049085746 ) ) ;
#10851=CARTESIAN_POINT ( 'NONE',  ( -4.344788714333951418, 31.33625517492832913, -12.78223156099206470 ) ) ;
#10852=CARTESIAN_POINT ( 'NONE',  ( 4.710849725239000030, 73.01037628082356434, -12.65146089665251417 ) ) ;
#10853=CARTESIAN_POINT ( 'NONE',  ( -1.545162525932825686E-06, 79.18000005555833809, -13.49999999999990941 ) ) ;
#10856=CARTESIAN_POINT ( 'NONE',  ( -10.92172942406178926, 76.63000000000000966, -7.935100905948389460 ) ) ;
#10857=CARTESIAN_POINT ( 'NONE',  ( -13.25030927750719023, 52.83740350991146784, -2.625255815485765254 ) ) ;
#10858=CARTESIAN_POINT ( 'NONE',  ( -3.636496289402153081, 47.32999999999999829, -11.19198476289190936 ) ) ;
#10859=CARTESIAN_POINT ( 'NONE',  ( -13.49999999999999822, 64.07999999999999829, 4.386415899144235908 ) ) ;
#10860=CARTESIAN_POINT ( 'NONE',  ( 10.71528539912113587, 51.11814703885590916, 8.211795539909561015 ) ) ;
#10861=CARTESIAN_POINT ( 'NONE',  ( -8.262753881998353478, 37.49471052164448537, -10.67663033658361194 ) ) ;
#10862=CIRCLE ( 'NONE', #5516, 12.00000000000000178 ) ;
#10863=CARTESIAN_POINT ( 'NONE',  ( 4.171617934058110322, 35.82999575861108355, 12.83930447791230733 ) ) ;
#10865=CARTESIAN_POINT ( 'NONE',  ( -12.20819043409092686, 74.14144561344353690, 5.764729960070299697 ) ) ;
#10866=CARTESIAN_POINT ( 'NONE',  ( -13.31362382857851401, 76.85144516294874961, -2.236570268612275481 ) ) ;
#10867=CARTESIAN_POINT ( 'NONE',  ( -11.99286688454158423, 80.15883121440852221, 6.202559419596111567 ) ) ;
#10870=CARTESIAN_POINT ( 'NONE',  ( 0.000000000000000000, 108.9300000000000068, 0.000000000000000000 ) ) ;
#10872=CARTESIAN_POINT ( 'NONE',  ( -7.272992578804310604, 48.38000000000000256, 10.01041549318726886 ) ) ;
#10876=CARTESIAN_POINT ( 'NONE',  ( -9.271068558427053574, 40.54190090920804579, -9.832000470486038424 ) ) ;
#10877=CARTESIAN_POINT ( 'NONE',  ( -2.754321577462427229, 34.27903524419202341, -13.21604803840751075 ) ) ;
#10878=CARTESIAN_POINT ( 'NONE',  ( 13.42050293043087628, 75.37783193970557249, 1.493644694584513877 ) ) ;
#10881=( BOUNDED_CURVE ( )  B_SPLINE_CURVE ( 2, ( #328, #5824, #1902, #16405, #4306, #11291, #9983, #9718, #9896, #15330, #3142, #1645, #1732 ),
 .UNSPECIFIED., .F., .F. ) 
 B_SPLINE_CURVE_WITH_KNOTS ( ( 3, 2, 2, 2, 2, 2, 3 ),
 ( 0.8750000000000000000, 0.8777777777777777679, 0.8833333333333333037, 0.8888888888888888395, 0.8944444444444444864, 0.9000000000000000222, 0.9027777777777777901 ),
 .UNSPECIFIED. ) 
 CURVE ( )  GEOMETRIC_REPRESENTATION_ITEM ( )  RATIONAL_B_SPLINE_CURVE ( ( 0.9755282581475768211, 0.9755282581475768211, 1.000000000000000000, 0.9510565162951535312, 1.000000000000000000, 0.9510565162951535312, 1.000000000000000000, 0.9510565162951535312, 1.000000000000000000, 0.9510565162951535312, 1.000000000000000000, 0.9755282581475768211, 0.9755282581475768211 ) ) 
 REPRESENTATION_ITEM ( '' )  );
#10882=CARTESIAN_POINT ( 'NONE',  ( 3.636496289402157078, 32.02999999999999403, -11.19198476289190936 ) ) ;
#10883=CARTESIAN_POINT ( 'NONE',  ( -9.328174606224918008, 41.31489523830415322, 9.758853723763433408 ) ) ;
#10884=CARTESIAN_POINT ( 'NONE',  ( -5.766677717960000393, 58.38977191998154126, -12.20636860387775968 ) ) ;
#10886=CARTESIAN_POINT ( 'NONE',  ( 4.819556118089159291, 44.85366279358599684, 12.61109904234389134 ) ) ;
#10888=CARTESIAN_POINT ( 'NONE',  ( 11.27030629789887151, 30.15099789552461118, 7.433993972937317452 ) ) ;
#10889=CARTESIAN_POINT ( 'NONE',  ( 4.178864255851000829E-14, 61.67999999999999261, 13.50000000000000000 ) ) ;
#10890=CARTESIAN_POINT ( 'NONE',  ( -11.11345371158683193, 49.64136890623429821, -7.664617922830998076 ) ) ;
#10891=CARTESIAN_POINT ( 'NONE',  ( 13.43761406456407492, 63.38425578468477539, 1.321427766813064730 ) ) ;
#10892=CARTESIAN_POINT ( 'NONE',  ( 12.41764327119240008, 42.23685895187078643, 5.297586243279120310 ) ) ;
#10893=CARTESIAN_POINT ( 'NONE',  ( 1.767417051738310985, 49.11645020481132917, -13.49999950439118379 ) ) ;
#10895=CARTESIAN_POINT ( 'NONE',  ( -3.095780066046758261, 70.29131268516505315, -13.14851532330129480 ) ) ;
#10896=CARTESIAN_POINT ( 'NONE',  ( -2.138189944381240881, 49.60311857767973009, 13.49999999999999822 ) ) ;
#10899=CARTESIAN_POINT ( 'NONE',  ( -11.10089580902282158, 43.64063000482338595, -7.682467894417619902 ) ) ;
#10900=CARTESIAN_POINT ( 'NONE',  ( -7.500000000000000000, 104.2024577724304208, -9.199283337799345261 ) ) ;
#10901=CARTESIAN_POINT ( 'NONE',  ( 10.46746661683255653, 60.75568857945317092, -8.525446913291563789 ) ) ;
#10906=CARTESIAN_POINT ( 'NONE',  ( 9.849129003214182276, 66.78863070281131797, -9.232880278536482521 ) ) ;
#10907=CARTESIAN_POINT ( 'NONE',  ( 4.773345198892768870, 56.85194987062286032, 12.62857154888958888 ) ) ;
#10908=CARTESIAN_POINT ( 'NONE',  ( 9.520470885617717371, 73.73000000000000398, -6.917026985038131848 ) ) ;
#10909=CARTESIAN_POINT ( 'NONE',  ( 9.520470885617717371, 70.73000000000000398, -6.917026985038131848 ) ) ;
#10910=CARTESIAN_POINT ( 'NONE',  ( -9.897695747161748159, 47.28611403347316866, 9.180720129038011379 ) ) ;
#10911=DIRECTION ( 'NONE',  ( 0.000000000000000000, -1.000000000000000000, 0.000000000000000000 ) ) ;
#10914=CARTESIAN_POINT ( 'NONE',  ( -2.762017976112265849, 56.58058146214491302, 13.21593017864399933 ) ) ;
#10918=CARTESIAN_POINT ( 'NONE',  ( 13.22184478347566206, 33.52670040130352902, -2.737004561010502268 ) ) ;
#10924=CARTESIAN_POINT ( 'NONE',  ( -13.47797578622742698, 40.90339952845120308, -0.7708587157098785170 ) ) ;
#10927=CARTESIAN_POINT ( 'NONE',  ( -13.32560535323595907, 44.00666090964475075, 2.189336705854063148 ) ) ;
#10930=CARTESIAN_POINT ( 'NONE',  ( 4.171729424061789260, 47.82999999999999829, 12.83926296998457417 ) ) ;
#10931=CARTESIAN_POINT ( 'NONE',  ( 4.171729424061789260, 46.82999999999999829, 12.83926296998457417 ) ) ;
#10932=CARTESIAN_POINT ( 'NONE',  ( -13.49604125154532852, 70.91871731678214985, -0.3286502116883691649 ) ) ;
#10934=CARTESIAN_POINT ( 'NONE',  ( -5.633048038538731817, 67.38456837596503135, -12.26866196724357216 ) ) ;
#10936=CARTESIAN_POINT ( 'NONE',  ( 13.01147089442868499, 54.55850596185721457, -3.599127685514930342 ) ) ;
#10938=CARTESIAN_POINT ( 'NONE',  ( -11.53528178546093130, 64.66812037823611092, -7.019368641623308314 ) ) ;
#10941=CARTESIAN_POINT ( 'NONE',  ( -11.86977617365307225, 34.69196684977737277, -6.431069432459339374 ) ) ;
#10942=ORIENTED_EDGE ( 'NONE', *, *, #2407, .F. ) ;
#10943=CARTESIAN_POINT ( 'NONE',  ( 13.36905443401149540, 78.36436234710785698, 1.879137346049587487 ) ) ;
#10945=CARTESIAN_POINT ( 'NONE',  ( -7.980211593510496471, 31.48200763573738570, -10.88882779094767983 ) ) ;
#10946=CARTESIAN_POINT ( 'NONE',  ( 3.672445938696736967, 73.04794425685443571, -12.99169412694102199 ) ) ;
#10947=CARTESIAN_POINT ( 'NONE',  ( 6.632128238234288986, 59.92444508611708898, 11.75866641223520759 ) ) ;
#10949=CARTESIAN_POINT ( 'NONE',  ( 8.343458848123583849, 69.87999999999999545, -11.48378591275253768 ) ) ;
#10950=CARTESIAN_POINT ( 'NONE',  ( -13.31348943002978125, 53.00938470406190106, 2.264923173904857201 ) ) ;
#10951=B_SPLINE_CURVE_WITH_KNOTS ( 'NONE', 3,
 ( #11352, #14071, #3207, #4721, #9868, #1874, #564, #15218, #647, #3114, #10122, #1957, #7381, #12759, #8799, #477, #8542, #2044, #391, #11266, #12848, #11524, #10207, #15561, #3471, #2558, #10632, #6489, #10379, #3820, #3902, #13017, #11783, #9234, #898, #15997, #5160, #14409, #6310, #13190, #14324, #11872, #16987, #10465, #8968, #14670, #17335, #11696, #2213, #3642, #15826, #14588, #10552, #17072, #6575, #9320, #15733, #15911, #2468, #11611, #12930, #5246, #13276, #3730, #17247, #9056, #7901, #988, #11956, #7640, #814, #4976, #2297, #7725, #6225, #13101, #6400, #4891, #17159, #5071, #1164, #10292, #9148, #15644, #3554, #14495, #2382, #7818, #1075, #6922, #2821, #1414, #12299, #6657, #6831, #278, #5687, #17417, #16082, #5332, #10717, #5598, #11066, #3990, #1245, #4256, #13439, #2732, #8075, #9578, #1593, #13525, #13356, #9491, #15096, #13694, #12208, #10980, #9406, #102, #5507, #16440, #10890, #193, #1326, #7988, #16259, #4166, #12038, #6742, #14754, #2908, #14929, #2643, #8250, #12122, #16350, #13613, #1506, #9665, #11, #5415, #10804, #16166, #4342, #8338, #9751, #15016, #7010, #4076, #14838, #8160, #12387, #8515, #15276, #3089, #4608, #14131, #8600, #8425, #4521, #6034, #4435, #535, #1767, #5768, #12564, #12735, #711, #13952, #1933, #13865, #10184, #1849, #16702 ),
 .UNSPECIFIED., .F., .F.,
 ( 4, 2, 2, 2, 2, 1, 1, 2, 2, 2, 1, 2, 2, 2, 2, 2, 2, 1, 2, 2, 2, 2, 2, 2, 1, 1, 1, 1, 2, 2, 2, 1, 1, 1, 2, 2, 2, 2, 1, 2, 2, 2, 2, 2, 1, 2, 2, 1, 1, 1, 2, 2, 2, 1, 2, 2, 2, 2, 1, 2, 2, 1, 1, 2, 2, 2, 2, 1, 2, 2, 2, 1, 1, 1, 1, 1, 1, 1, 1, 2, 2, 2, 2, 2, 2, 2, 2, 1, 1, 2, 2, 2, 2, 2, 2, 2, 2, 2, 2, 1, 1, 1, 1, 2, 4 ),
 ( 0.5931508481644109931, 0.5940699344761732892, 0.5945294776320543262, 0.5945869205265394974, 0.5946156419737820276, 0.5946443634210246687, 0.5947592492099949002, 0.5949890207879354742, 0.5954485639438166222, 0.5956783355217571962, 0.5957932213107275388, 0.5958506642052125990, 0.5958793856524552401, 0.5959081070996977703, 0.5968271934114600663, 0.5970569649894006403, 0.5971144078838857006, 0.5971718507783708718, 0.5972867365673412143, 0.5977462797232223624, 0.5986653660349846584, 0.5995844523467469545, 0.5995988130703682195, 0.5996131737939895956, 0.5996418952412321257, 0.5996993381357172970, 0.5998142239246876395, 0.6000439955026282135, 0.6005035386585094725, 0.6014226249702718796, 0.6018821681261531387, 0.6019970539151234812, 0.6020544968096086524, 0.6020832182568511826, 0.6020975789804724476, 0.6021119397040937127, 0.6023417112820343977, 0.6041798839055592119, 0.6044096554834998969, 0.6045245412724701284, 0.6046394270614404709, 0.6050989702173216189, 0.6060180565290841370, 0.6069371428408465441, 0.6070520286298167756, 0.6071094715243019468, 0.6071381929715445880, 0.6071669144187871181, 0.6073966859967276921, 0.6078562291526089512, 0.6083157723084902102, 0.6083444937557327403, 0.6083732152029753815, 0.6084306580974604417, 0.6085455438864307842, 0.6087753154643713582, 0.6092348586202526173, 0.6094646301981931913, 0.6095795159871635338, 0.6096082374344060639, 0.6096225981580273290, 0.6096369588816485940, 0.6096944017761337653, 0.6115325743996586905, 0.6119921175555398385, 0.6121070033445101810, 0.6121644462389953523, 0.6122218891334805235, 0.6124516607114210975, 0.6133707470231835046, 0.6133994684704260347, 0.6134281899176685648, 0.6134856328121537361, 0.6136005186011240786, 0.6138302901790646526, 0.6142898333349458007, 0.6145196049128863747, 0.6145770478073715459, 0.6146057692546140760, 0.6146201299782353411, 0.6146344907018566062, 0.6147493764908269487, 0.6152089196467082077, 0.6161280059584706148, 0.6170470922702331329, 0.6171045351647183042, 0.6171332566119608343, 0.6171619780592034754, 0.6172768638481737069, 0.6175066354261143919, 0.6179661785819955400, 0.6188852648937579470, 0.6193448080496392061, 0.6195745796275797801, 0.6198043512055204651, 0.6207234375172828722, 0.6216425238290452793, 0.6221020669849264273, 0.6223318385628671123, 0.6224467243518373438, 0.6225041672463225151, 0.6225328886935651562, 0.6225472494171864213, 0.6225544297789969983, 0.6225616101408076863 ),
 .UNSPECIFIED. ) ;
#10952=CARTESIAN_POINT ( 'NONE',  ( 2.272985001014427788E-15, 44.17999999999998550, -12.37355403259654985 ) ) ;
#10953=CARTESIAN_POINT ( 'NONE',  ( -8.691771469529815392E-16, 67.68000000000000682, 14.19474002721660355 ) ) ;
#10955=CARTESIAN_POINT ( 'NONE',  ( 11.90994820305756718, 69.66503421312197020, -6.356414413265706997 ) ) ;
#10956=CARTESIAN_POINT ( 'NONE',  ( -13.39266229628177918, 37.86830100434433177, -1.771454170845632614 ) ) ;
#10957=CARTESIAN_POINT ( 'NONE',  ( 13.31123005953295113, 36.35096708053784198, 2.249764498763733744 ) ) ;
#10959=CARTESIAN_POINT ( 'NONE',  ( -8.405755648187358986, 74.35874387436902566, 10.56379513576823825 ) ) ;
#10960=CARTESIAN_POINT ( 'NONE',  ( -13.49157297123065113, 76.94640455294563708, 0.4769767824848614723 ) ) ;
#10963=CARTESIAN_POINT ( 'NONE',  ( -10.79499759444871465, 80.92999999999997840, 5.634798678241480729 ) ) ;
#10966=CARTESIAN_POINT ( 'NONE',  ( -7.272992578804307939, 50.47999999999999687, -10.01041549318727064 ) ) ;
#10969=CARTESIAN_POINT ( 'NONE',  ( 12.17225613010915630, 75.21553104833439818, 5.838516313590356610 ) ) ;
#10971=CIRCLE ( 'NONE', #10138, 8.999999999999994671 ) ;
#10972=CARTESIAN_POINT ( 'NONE',  ( 9.520470885617717371, 31.72999999999999332, -6.917026985038131848 ) ) ;
#10973=CARTESIAN_POINT ( 'NONE',  ( -5.731539176755555687, 41.47177041787331575, 12.23222747491296403 ) ) ;
#10974=CARTESIAN_POINT ( 'NONE',  ( -3.535167248572977261, 58.30710965717599947, -13.03526438387624964 ) ) ;
#10975=CARTESIAN_POINT ( 'NONE',  ( 4.618812367767958449, 44.84625946610768921, 12.68529031168209009 ) ) ;
#10976=CARTESIAN_POINT ( 'NONE',  ( -8.343458848123582072, 55.37999999999998835, 11.48378591275253768 ) ) ;
#10978=CARTESIAN_POINT ( 'NONE',  ( -8.343458848123578520, 57.48000000000000398, -11.48378591275254124 ) ) ;
#10979=EDGE_CURVE ( 'NONE', #4213, #10745, #14469, .T. ) ;
#10980=CARTESIAN_POINT ( 'NONE',  ( -11.52230132989533651, 49.66675174565017414, -7.055497591694980919 ) ) ;
#10981=CARTESIAN_POINT ( 'NONE',  ( 11.50794140772470442, 63.69349671364791021, -7.058136192068576342 ) ) ;
#10982=CARTESIAN_POINT ( 'NONE',  ( 9.471282408482009529, 42.05193615182220412, 9.629884418960235948 ) ) ;
#10983=CARTESIAN_POINT ( 'NONE',  ( 3.785595641572113985E-06, 49.17999986388394973, -13.49999999999946887 ) ) ;
#10985=VERTEX_POINT ( 'NONE', #7885 ) ;
#10986=CARTESIAN_POINT ( 'NONE',  ( -2.363332742774242767, 70.26497115792561488, -13.29196632392810429 ) ) ;
#10989=CARTESIAN_POINT ( 'NONE',  ( -8.845124509614564090, 43.52173457442797400, -10.19943598800505846 ) ) ;
#10991=CARTESIAN_POINT ( 'NONE',  ( 11.61166856071877795, 60.68652284347961512, -6.886578250901779441 ) ) ;
#10992=SHAPE_REPRESENTATION ( 'Top rod', ( #16654 ), #5681 ) ;
#10995=CARTESIAN_POINT ( 'NONE',  ( 11.44624021849559270, 66.69747484006249749, -7.161096640856107420 ) ) ;
#10996=CARTESIAN_POINT ( 'NONE',  ( 8.472248300915232733, 57.00428603186374232, 10.51143461932150736 ) ) ;
#10997=CARTESIAN_POINT ( 'NONE',  ( 11.76794919243112680, 55.58000000000000540, -3.823638476888993942 ) ) ;
#10998=CARTESIAN_POINT ( 'NONE',  ( 9.520470885617717371, 67.73000000000000398, -6.917026985038131848 ) ) ;
#10999=CARTESIAN_POINT ( 'NONE',  ( -2.563398806372461536, 47.58790005324861738, 13.26025254451834456 ) ) ;
#11001=CARTESIAN_POINT ( 'NONE',  ( 13.49999999999999822, 74.28000000000000114, 4.386415899144236796 ) ) ;
#11005=CARTESIAN_POINT ( 'NONE',  ( -4.171729424061791036, 52.53000000000000114, 12.83926296998457239 ) ) ;
#11006=CARTESIAN_POINT ( 'NONE',  ( 13.48617201663203780, 33.45105711750449728, -0.6112691538384680268 ) ) ;
#11010=ORIENTED_EDGE ( 'NONE', *, *, #10715, .F. ) ;
#11011=CARTESIAN_POINT ( 'NONE',  ( -5.632579572119366773, 62.47544819939797378, 12.26882833910524617 ) ) ;
#11013=CARTESIAN_POINT ( 'NONE',  ( -13.32942039305800819, 41.00505323559917770, 2.139340077664309892 ) ) ;
#11016=CARTESIAN_POINT ( 'NONE',  ( -13.47749323749192740, 43.95689747672926018, 0.7792445917878014772 ) ) ;
#11018=CARTESIAN_POINT ( 'NONE',  ( 4.171729424061789260, 35.82999999999999119, 12.83926296998457417 ) ) ;
#11019=CARTESIAN_POINT ( 'NONE',  ( 13.50000000000000355, 44.58000000000000540, -4.386415899144233244 ) ) ;
#11020=CARTESIAN_POINT ( 'NONE',  ( -13.49688162372039990, 70.92003375154399691, -0.2904274958478991753 ) ) ;
#11022=CARTESIAN_POINT ( 'NONE',  ( -10.91250422740056614, 67.62945040754487991, -7.948069400918766902 ) ) ;
#11025=CARTESIAN_POINT ( 'NONE',  ( 13.42879437376425500, 54.37163056846146247, 1.680570053129028629 ) ) ;
#11026=CARTESIAN_POINT ( 'NONE',  ( -2.624842932224632719, 64.27450954149531981, -13.24583211552917739 ) ) ;
#11028=CARTESIAN_POINT ( 'NONE',  ( -11.85197915507875521, 34.69064970905623824, -6.463791718503999917 ) ) ;
#11030=CARTESIAN_POINT ( 'NONE',  ( 13.42225261468230713, 78.37947749321138247, 1.448575772764510328 ) ) ;
#11034=CARTESIAN_POINT ( 'NONE',  ( 11.20647886694230522, 72.71291404450818163, -7.527623646720101647 ) ) ;
#11035=CARTESIAN_POINT ( 'NONE',  ( 0.03691118140029227973, 79.17867285846638481, -13.49996200175932692 ) ) ;
#11037=CARTESIAN_POINT ( 'NONE',  ( 4.171729424061791924, 73.03000000000000114, -12.83926296998457239 ) ) ;
#11038=CARTESIAN_POINT ( 'NONE',  ( -11.20932835276732575, 52.64727559639315757, -7.523361188747804462 ) ) ;
#11039=ADVANCED_FACE ( 'NONE', ( #8952, #10536 ), #14394, .F. ) ;
#11040=CARTESIAN_POINT ( 'NONE',  ( -11.76794919243112325, 44.77999999999998693, -3.823638476888998827 ) ) ;
#11042=CARTESIAN_POINT ( 'NONE',  ( 0.4447399503994752812, 50.69609182596189356, 13.49999999964396302 ) ) ;
#11043=CARTESIAN_POINT ( 'NONE',  ( 11.07943945917226181, 69.13930839722881672, 7.714844222956088515 ) ) ;
#11047=CARTESIAN_POINT ( 'NONE',  ( -13.12364411654131402, 74.04252074095533942, 3.167980043827653525 ) ) ;
#11048=CARTESIAN_POINT ( 'NONE',  ( -8.341416350532403712, 76.49767382419285866, -10.64073998737741533 ) ) ;
#11049=CARTESIAN_POINT ( 'NONE',  ( -4.085520694688061560, 79.32684323223975298, -12.86729062109435340 ) ) ;
#11054=CARTESIAN_POINT ( 'NONE',  ( 7.272992578804308828, 51.97999999999998977, 10.01041549318726886 ) ) ;
#11056=CARTESIAN_POINT ( 'NONE',  ( -4.494282199184345572, 32.51830724862094257, 12.72999398840573448 ) ) ;
#11057=CARTESIAN_POINT ( 'NONE',  ( 13.47046671447611921, 75.39302779519800879, 1.059546044154582312 ) ) ;
#11059=CARTESIAN_POINT ( 'NONE',  ( 9.520470885617715595, 34.13000000000000256, 6.917026985038134512 ) ) ;
#11060=CARTESIAN_POINT ( 'NONE',  ( -12.54844231482822003, 41.11082418795689364, 4.978620826851912540 ) ) ;
#11061=CARTESIAN_POINT ( 'NONE',  ( -2.347235880096729677, 58.26439793459769589, -13.29438112138644712 ) ) ;
#11065=CARTESIAN_POINT ( 'NONE',  ( -0.5497339802477337889, 55.19976638620128995, -13.48880876228390591 ) ) ;
#11066=CARTESIAN_POINT ( 'NONE',  ( -13.26384252841972966, 49.84140379325150150, -2.514066362863750292 ) ) ;
#11067=AXIS2_PLACEMENT_3D ( 'NONE', #9310, #6477, #12112 ) ;
#11068=CARTESIAN_POINT ( 'NONE',  ( 10.38695722535535104, 63.09982902898799040, 8.626549733017945698 ) ) ;
#11069=CARTESIAN_POINT ( 'NONE',  ( 13.48620919108931382, 42.40890622764071338, 0.6106556734208694603 ) ) ;
#11072=CARTESIAN_POINT ( 'NONE',  ( -11.76794919243112325, 72.07999999999999829, 3.823638476888994830 ) ) ;
#11073=CARTESIAN_POINT ( 'NONE',  ( -4.128382448430371277, 70.32844985923892978, -12.85360630656942504 ) ) ;
#11076=VERTEX_POINT ( 'NONE', #15720 ) ;
#11077=CARTESIAN_POINT ( 'NONE',  ( -2.247839795003510055, 43.26082400849369947, -13.31154558271445509 ) ) ;
#11078=CARTESIAN_POINT ( 'NONE',  ( -7.500000000000000000, 106.5806336763438935, 7.726132535793189149 ) ) ;
#11079=CARTESIAN_POINT ( 'NONE',  ( 6.401920825618216959, 60.94496828387899257, -11.88551464368857680 ) ) ;
#11082=CARTESIAN_POINT ( 'NONE',  ( 13.25906685095921489, 66.33919486957000800, 2.577579219623620244 ) ) ;
#11083=CARTESIAN_POINT ( 'NONE',  ( 1.401137238041307853, 56.73038022015892778, 13.42714289984223797 ) ) ;
#11085=CARTESIAN_POINT ( 'NONE',  ( -7.576616670048093940E-16, 57.67999999999999261, 12.37355403259654985 ) ) ;
#11086=CARTESIAN_POINT ( 'NONE',  ( 2.272985001014427788E-15, 68.18000000000000682, -12.37355403259654985 ) ) ;
#11087=AXIS2_PLACEMENT_3D ( 'NONE', #15664, #15492, #10056 ) ;
#11088=CARTESIAN_POINT ( 'NONE',  ( -13.24853700240426058, 46.83817720085215086, -2.602182145016867842 ) ) ;
#11091=CARTESIAN_POINT ( 'NONE',  ( 11.26921262112964683, 30.70896170274106396, -7.433369082940963324 ) ) ;
#11092=CARTESIAN_POINT ( 'NONE',  ( -8.617953050394065784, 56.34892783574404262, 10.39139140008484574 ) ) ;
#11094=DIRECTION ( 'NONE',  ( -1.000000000000000000, -1.734723475976807094E-16, -0.000000000000000000 ) ) ;
#11095=CARTESIAN_POINT ( 'NONE',  ( 6.741542013777170439, 32.92885702970292527, 11.69833832118984773 ) ) ;
#11097=CARTESIAN_POINT ( 'NONE',  ( 1.287047813695933574, 40.13382801857486015, -13.44065531857610019 ) ) ;
#11100=AXIS2_PLACEMENT_3D ( 'NONE', #10102, #8778, #14134 ) ;
#11102=CARTESIAN_POINT ( 'NONE',  ( -13.49677891199997504, 43.94321173900256383, 0.3859101346687785483 ) ) ;
#11104=CARTESIAN_POINT ( 'NONE',  ( -4.171729424061791036, 35.53000000000000114, 12.83926296998457239 ) ) ;
#11105=ADVANCED_FACE ( 'NONE', ( #3807 ), #15811, .T. ) ;
#11106=AXIS2_PLACEMENT_3D ( 'NONE', #844, #14445, #12792 ) ;
#11107=CARTESIAN_POINT ( 'NONE',  ( -6.314785314735273047, 46.41152104994968397, -11.93203815175650462 ) ) ;
#11108=CARTESIAN_POINT ( 'NONE',  ( -11.69000891540406073, 67.67898000483805276, -6.752419532946158931 ) ) ;
#11110=CARTESIAN_POINT ( 'NONE',  ( 11.73858346217181037, 54.18242075136932812, 6.667783194025956206 ) ) ;
#11112=CARTESIAN_POINT ( 'NONE',  ( -5.878827033754383535, 64.39416732176437108, -12.15275301167633870 ) ) ;
#11114=CARTESIAN_POINT ( 'NONE',  ( -11.47022446788024830, 35.19602096309857586, 7.119919174184125232 ) ) ;
#11116=CARTESIAN_POINT ( 'NONE',  ( 11.71436862115008637, 78.18064915872857057, 6.711522305461322446 ) ) ;
#11119=CARTESIAN_POINT ( 'NONE',  ( 4.654787199579893731, 73.01242072379346837, -12.67213584933875836 ) ) ;
#11120=CARTESIAN_POINT ( 'NONE',  ( 2.519697212011065446, 79.08940101069002537, -13.26277544837490296 ) ) ;
#11122=CARTESIAN_POINT ( 'NONE',  ( -8.343458848123582072, 62.37999999999998835, 11.48378591275254124 ) ) ;
#11123=CARTESIAN_POINT ( 'NONE',  ( 13.50000000000000355, 50.58000000000000540, -4.386415899144233244 ) ) ;
#11124=CARTESIAN_POINT ( 'NONE',  ( -13.50515042037184976, 52.92788077079702447, -0.05679620317202376673 ) ) ;
#11126=CARTESIAN_POINT ( 'NONE',  ( -11.76794919243112325, 41.77999999999999403, -3.823638476888998827 ) ) ;
#11128=CARTESIAN_POINT ( 'NONE',  ( -4.171729424061791036, 58.53000000000000114, 12.83926296998457239 ) ) ;
#11129=CARTESIAN_POINT ( 'NONE',  ( 1.564284005194032989, 50.73624596681315779, 13.40908526793743505 ) ) ;
#11131=CARTESIAN_POINT ( 'NONE',  ( 10.96292031448879989, 69.13240560544066682, 7.878467101911673431 ) ) ;
#11132=CARTESIAN_POINT ( 'NONE',  ( 6.750022862106053623, 29.92926176209967437, 11.69132975161703669 ) ) ;
#11133=CARTESIAN_POINT ( 'NONE',  ( 0.4450047276655222372, 35.69605895621225500, 13.49999999987117683 ) ) ;
#11135=CARTESIAN_POINT ( 'NONE',  ( -10.07304411609868922, 74.27699509055480576, 8.989944076744466273 ) ) ;
#11136=CARTESIAN_POINT ( 'NONE',  ( -7.164914557665265527, 76.44660487377331037, -11.44177756266805268 ) ) ;
#11137=CARTESIAN_POINT ( 'NONE',  ( 0.000000000000000000, 80.93000000000000682, 0.000000000000000000 ) ) ;
#11140=CARTESIAN_POINT ( 'NONE',  ( 3.636496289402157078, 41.02999999999999403, -11.19198476289190936 ) ) ;
#11142=CARTESIAN_POINT ( 'NONE',  ( -7.134497763750654364, 32.41468128586360820, 11.46076502362460836 ) ) ;
#11143=CARTESIAN_POINT ( 'NONE',  ( 13.32613498935721807, 75.35421527273051368, 2.159664486192276467 ) ) ;
#11145=CARTESIAN_POINT ( 'NONE',  ( 9.520470885617715595, 31.12999999999999901, 6.917026985038134512 ) ) ;
#11146=CARTESIAN_POINT ( 'NONE',  ( -13.49999999999999822, 82.08000000000001251, 4.386415899144235908 ) ) ;
#11148=CARTESIAN_POINT ( 'NONE',  ( 7.620118401036991784, 51.89386994708977596, -11.14470155242018912 ) ) ;
#11149=CARTESIAN_POINT ( 'NONE',  ( -0.4450088281291025294, 38.66413328918902437, 13.50000000012805756 ) ) ;
#11150=CARTESIAN_POINT ( 'NONE',  ( 0.7721810585093080714, 37.15227321576206521, -13.48105077863768742 ) ) ;
#11153=CARTESIAN_POINT ( 'NONE',  ( 7.321132905710702410, 62.95323300269863154, 11.34287645249957777 ) ) ;
#11154=CARTESIAN_POINT ( 'NONE',  ( 13.48357555260946228, 42.45296674144867666, -0.6662799819680408353 ) ) ;
#11155=CARTESIAN_POINT ( 'NONE',  ( 6.511591735624385535, 48.94067668905481838, -11.83699345231539546 ) ) ;
#11159=CARTESIAN_POINT ( 'NONE',  ( -7.272992578804310604, 63.37999999999999545, 10.01041549318726886 ) ) ;
#11160=CARTESIAN_POINT ( 'NONE',  ( -0.5895600827330491622, 70.20119840546840351, -13.49999998549911773 ) ) ;
#11164=CARTESIAN_POINT ( 'NONE',  ( -8.945013995349350822, 43.52648452866512230, -10.11178031813171785 ) ) ;
#11165=CARTESIAN_POINT ( 'NONE',  ( -7.500000000000000000, 108.6229112031126505, -2.544524385544284062 ) ) ;
#11166=CARTESIAN_POINT ( 'NONE',  ( 6.420329193139213686, 60.94422300306127482, -11.87558703656385184 ) ) ;
#11170=CARTESIAN_POINT ( 'NONE',  ( 9.980110855971577877, 66.07825710158466848, 9.092675784874080236 ) ) ;
#11171=CARTESIAN_POINT ( 'NONE',  ( 11.01769831327593074, 57.13567825725026950, 7.805250006001219987 ) ) ;
#11172=CARTESIAN_POINT ( 'NONE',  ( -7.272992578804310604, 63.37999999999998835, 10.01041549318726709 ) ) ;
#11173=CARTESIAN_POINT ( 'NONE',  ( -4.171729424061787483, 33.32999999999999829, -12.83926296998457417 ) ) ;
#11174=CARTESIAN_POINT ( 'NONE',  ( 3.636496289402157078, 71.03000000000000114, -11.19198476289190936 ) ) ;
#11175=CARTESIAN_POINT ( 'NONE',  ( -13.31651195430729828, 46.85210362530030892, -2.218283652183269172 ) ) ;
#11176=CARTESIAN_POINT ( 'NONE',  ( 8.201072769536251528, 45.86863449535839266, -10.74934398742807495 ) ) ;
#11178=CARTESIAN_POINT ( 'NONE',  ( 8.348315818218853934, 30.86137531282033208, -10.60922870909750593 ) ) ;
#11179=CARTESIAN_POINT ( 'NONE',  ( -5.838732723835591720, 56.46738623871877394, 12.17296727378241350 ) ) ;
#11181=DIRECTION ( 'NONE',  ( 0.000000000000000000, -1.000000000000000000, 0.000000000000000000 ) ) ;
#11182=CARTESIAN_POINT ( 'NONE',  ( 10.96333157205655873, 33.13238853848653775, 7.878424145257830524 ) ) ;
#11184=CARTESIAN_POINT ( 'NONE',  ( 3.273252351246041414, 40.06251456520496390, -13.10396545777065747 ) ) ;
#11187=CARTESIAN_POINT ( 'NONE',  ( -10.11974732110556374, 62.27491796265164226, 8.946316878496988423 ) ) ;
#11189=ORIENTED_EDGE ( 'NONE', *, *, #3486, .T. ) ;
#11191=CARTESIAN_POINT ( 'NONE',  ( -11.11006920932890196, 44.21883285313256806, 7.669478262804471314 ) ) ;
#11193=CARTESIAN_POINT ( 'NONE',  ( 10.92172942406178926, 36.12999999999999545, 7.935100905948387684 ) ) ;
#11194=CARTESIAN_POINT ( 'NONE',  ( 10.92172942406179104, 47.73000000000000398, -7.935100905948385908 ) ) ;
#11196=CARTESIAN_POINT ( 'NONE',  ( -8.219743528356605822, 46.49234792102033964, -10.74582137773523449 ) ) ;
#11197=CARTESIAN_POINT ( 'NONE',  ( -7.992194457595993562, 67.48253745615919286, -10.88025959043272373 ) ) ;
#11199=CARTESIAN_POINT ( 'NONE',  ( 9.413837210981146342, 54.04933858495957111, 9.676282647599792952 ) ) ;
#11200=CARTESIAN_POINT ( 'NONE',  ( -8.082238262464676026, 64.48655149555420962, -10.81439697735142502 ) ) ;
#11203=CARTESIAN_POINT ( 'NONE',  ( -10.37171067933893376, 34.59884894902187824, -8.642314730309303528 ) ) ;
#11205=CARTESIAN_POINT ( 'NONE',  ( 13.47859327190760759, 78.39933782603816326, 0.8769525335675483202 ) ) ;
#11207=AXIS2_PLACEMENT_3D ( 'NONE', #13379, #2403, #14693 ) ;
#11209=CARTESIAN_POINT ( 'NONE',  ( 11.97746557486279251, 72.19970894202896261, 6.240527775782743092 ) ) ;
#11211=CARTESIAN_POINT ( 'NONE',  ( -4.171729424061787483, 64.32999999999999829, -12.83926296998457417 ) ) ;
#11212=CARTESIAN_POINT ( 'NONE',  ( -0.6196722084519333817, 71.65772062913328000, 13.48668984471889587 ) ) ;
#11213=CARTESIAN_POINT ( 'NONE',  ( -7.272992578804307939, 35.47999999999999687, -10.01041549318726886 ) ) ;
#11214=CARTESIAN_POINT ( 'NONE',  ( -10.92172942406178926, 54.62999999999999545, -7.935100905948389460 ) ) ;
#11217=CARTESIAN_POINT ( 'NONE',  ( 3.549402833027860638, 68.80762806818306387, 13.02504335811066305 ) ) ;
#11219=CARTESIAN_POINT ( 'NONE',  ( -8.343458848123582072, 79.37999999999999545, 11.48378591275253768 ) ) ;
#11221=CARTESIAN_POINT ( 'NONE',  ( -11.44226849560644155, 73.66214175551372989, -7.164337856285095896 ) ) ;
#11222=CARTESIAN_POINT ( 'NONE',  ( -1.931361406942186720, 76.24943241617928891, -13.36225245988610588 ) ) ;
#11229=CARTESIAN_POINT ( 'NONE',  ( 11.76794919243112325, 37.42999999999999972, 1.441158131103945434E-15 ) ) ;
#11231=CARTESIAN_POINT ( 'NONE',  ( -4.425713338080228709, 32.52081085309985298, 12.75399470283292658 ) ) ;
#11232=CARTESIAN_POINT ( 'NONE',  ( 1.295514318413480082, 74.72657971910703623, 13.43770740680674969 ) ) ;
#11234=CARTESIAN_POINT ( 'NONE',  ( 7.272992578804311492, 31.87999999999999545, -10.01041549318726709 ) ) ;
#11235=CARTESIAN_POINT ( 'NONE',  ( -2.383599452370637195, 58.26570543616674058, -13.28790837415479231 ) ) ;
#11240=CARTESIAN_POINT ( 'NONE',  ( 11.55360894227645474, 63.16957824287888457, 6.983155331944742805 ) ) ;
#11241=CARTESIAN_POINT ( 'NONE',  ( 13.46927589499868816, 42.39849010613973235, 0.9131328280806061404 ) ) ;
#11242=CARTESIAN_POINT ( 'NONE',  ( 11.79887646993529948, 48.67349572257840862, -6.571923756045907616 ) ) ;
#11244=ORIENTED_EDGE ( 'NONE', *, *, #17031, .T. ) ;
#11245=CARTESIAN_POINT ( 'NONE',  ( 2.272985001014427393E-15, 71.17999999999999261, -12.37355403259654807 ) ) ;
#11251=CARTESIAN_POINT ( 'NONE',  ( -7.499999999999999112, 108.4800942032927509, -3.560038493048083730 ) ) ;
#11254=CARTESIAN_POINT ( 'NONE',  ( 13.14794202937746093, 66.31858931631785481, 3.143476922865568568 ) ) ;
#11255=CARTESIAN_POINT ( 'NONE',  ( 4.440672829457194659, 56.83962754305976262, 12.75201459754448230 ) ) ;
#11256=CARTESIAN_POINT ( 'NONE',  ( -11.76794919243112325, 57.07999999999999829, 3.823638476888994386 ) ) ;
#11257=CARTESIAN_POINT ( 'NONE',  ( 10.92172942406178926, 32.12999999999999545, 7.935100905948387684 ) ) ;
#11258=CARTESIAN_POINT ( 'NONE',  ( 7.272992578804311492, 70.87999999999998124, -10.01041549318726709 ) ) ;
#11259=CARTESIAN_POINT ( 'NONE',  ( -11.32938012359942981, 46.65483419514092844, -7.341333998329178989 ) ) ;
#11261=CARTESIAN_POINT ( 'NONE',  ( 9.153496884233396358, 45.82344744250357849, -9.922878119584453316 ) ) ;
#11263=CARTESIAN_POINT ( 'NONE',  ( 11.23155463829053247, 30.71129247825936304, -7.490173329162382210 ) ) ;
#11265=CARTESIAN_POINT ( 'NONE',  ( -5.554567472103006942, 56.47846890177030588, 12.30434293202147167 ) ) ;
#11266=CARTESIAN_POINT ( 'NONE',  ( -3.811337859253840943, 50.54295824350852939, 12.95086203090105670 ) ) ;
#11267=CARTESIAN_POINT ( 'NONE',  ( 1.308231877209349081, 32.72703918382474342, 13.43647239758811374 ) ) ;
#11269=CARTESIAN_POINT ( 'NONE',  ( 13.47604474945591058, 39.45782905736723478, -0.8059756131630804177 ) ) ;
#11270=ORIENTED_EDGE ( 'NONE', *, *, #15700, .F. ) ;
#11271=CARTESIAN_POINT ( 'NONE',  ( -9.114618562460469420, 62.32545052674210240, 9.962813353323715759 ) ) ;
#11272=VERTEX_POINT ( 'NONE', #13366 ) ;
#11274=CARTESIAN_POINT ( 'NONE',  ( 10.72853415096860275, 48.11889978472238738, 8.194428814822611429 ) ) ;
#11276=CARTESIAN_POINT ( 'NONE',  ( 13.50000000000000000, 36.42999999999999972, 1.653273178848926867E-15 ) ) ;
#11277=CARTESIAN_POINT ( 'NONE',  ( -8.343458848123582072, 40.37999999999998835, 11.48378591275254124 ) ) ;
#11279=CARTESIAN_POINT ( 'NONE',  ( -10.15340906302686719, 67.58731543087333193, -8.897236675027087927 ) ) ;
#11281=CARTESIAN_POINT ( 'NONE',  ( 6.729357836367587886, 53.92846635459285665, 11.70346878396139445 ) ) ;
#11283=CARTESIAN_POINT ( 'NONE',  ( -0.4537535686862056439, 64.19631530089112914, -13.49237553831279612 ) ) ;
#11284=ORIENTED_EDGE ( 'NONE', *, *, #4346, .T. ) ;
#11286=CARTESIAN_POINT ( 'NONE',  ( -11.34489072193997394, 34.65565179922739247, -7.320614711993081336 ) ) ;
#11288=CARTESIAN_POINT ( 'NONE',  ( 13.50002729581672867, 78.43731220364004741, -0.2171257608274307360 ) ) ;
#11289=CARTESIAN_POINT ( 'NONE',  ( 2.138189944381238661, 46.75688142232026934, 13.50000000000000000 ) ) ;
#11290=FACE_OUTER_BOUND ( 'NONE', #14597, .T. ) ;
#11291=CARTESIAN_POINT ( 'NONE',  ( -13.49999999999999822, 37.07999999999999829, 4.386415899144235020 ) ) ;
#11292=CARTESIAN_POINT ( 'NONE',  ( 13.37264497842671673, 72.36533816201536240, 1.850009941757990717 ) ) ;
#11294=CARTESIAN_POINT ( 'NONE',  ( 13.49999999999999822, 66.28000000000001535, 4.386415899144237684 ) ) ;
#11295=CARTESIAN_POINT ( 'NONE',  ( -1.010931998681471075E-07, 71.67999718330101189, 13.49999999999999822 ) ) ;
#11297=CARTESIAN_POINT ( 'NONE',  ( -7.272992578804307939, 41.47999999999999687, -10.01041549318726886 ) ) ;
#11298=CARTESIAN_POINT ( 'NONE',  ( -8.691771469529815392E-16, 58.67999999999998550, 14.19474002721660355 ) ) ;
#11299=EDGE_CURVE ( 'NONE', #5905, #16027, #13036, .T. ) ;
#11300=CARTESIAN_POINT ( 'NONE',  ( 1.629909063141895542, 50.73860606154746478, 13.40135283676167965 ) ) ;
#11302=CARTESIAN_POINT ( 'NONE',  ( 5.029451273018744395, 68.86152500203888849, 12.52818279675859792 ) ) ;
#11303=CARTESIAN_POINT ( 'NONE',  ( 1.768248422467277647, 35.74357465886849639, 13.38469673118040504 ) ) ;
#11305=CARTESIAN_POINT ( 'NONE',  ( -11.47705729850806122, 73.66444291895690810, -7.108385984861816276 ) ) ;
#11312=CARTESIAN_POINT ( 'NONE',  ( -7.576616670048093940E-16, 42.67999999999999261, 12.37355403259654807 ) ) ;
#11314=CARTESIAN_POINT ( 'NONE',  ( -11.28923155001206347, 32.20771843106157206, 7.402935447327149809 ) ) ;
#11315=B_SPLINE_CURVE_WITH_KNOTS ( 'NONE', 3,
 ( #4098, #7200, #3204, #1703, #5969, #9865, #3295, #299, #15122, #4547, #13805, #7116, #8709, #12503, #3020, #14069, #16553, #388, #562, #8451, #5794, #7379, #12757, #16641, #1617, #1789, #16463, #8624, #9952, #15216, #13976, #2930, #5709, #11178, #12586, #15388, #4460, #3112, #8361, #1954, #12412, #7033, #15037, #13718, #8540, #645, #4632, #5884, #6055, #13890, #9688, #4278, #475, #1871, #11263, #7287, #11091, #15300, #12670, #11350, #11438, #16725, #9776, #4367, #10038, #13015, #4718, #15473, #896, #8796, #14154, #6486, #2295, #6223, #10120, #2042, #1073, #15731, #3384, #7723, #7466, #16899, #10377, #12846, #3552, #11609, #8883, #4888, #9146, #15642, #735, #6143, #5068, #11522, #16810, #4803, #10205, #15558, #2210, #3469, #3639, #6308, #14238, #2123, #7549, #985, #11693, #12927, #17070, #16985, #812, #10290, #8966, #7815, #14322, #4974, #7638, #9053, #14407, #13099, #6398, #11781, #17157, #14493, #10463, #15823, #3728, #2380, #13188, #10888, #5244, #9489, #10630, #13274, #2556, #9404, #8158, #14835, #15995, #5505, #8248, #16257, #8, #3899, #9317, #13522, #1412 ),
 .UNSPECIFIED., .F., .F.,
 ( 4, 2, 2, 2, 1, 1, 2, 2, 2, 2, 1, 1, 1, 2, 2, 2, 2, 2, 1, 2, 2, 1, 1, 2, 2, 2, 2, 1, 2, 2, 1, 1, 2, 1, 2, 2, 2, 2, 2, 2, 1, 1, 2, 2, 1, 1, 1, 2, 2, 2, 1, 2, 2, 1, 1, 2, 2, 2, 2, 1, 1, 1, 2, 2, 2, 2, 2, 2, 2, 2, 1, 1, 2, 2, 2, 2, 2, 2, 2, 2, 2, 2, 2, 2, 2, 4 ),
 ( 0.9754977937536480903, 0.9755935054967979081, 0.9756413613683727615, 0.9756652893041601882, 0.9756892172399477259, 0.9758806407262472504, 0.9762634876988464105, 0.9770291816440448418, 0.9785605695344414823, 0.9793262634796398025, 0.9795176869659394381, 0.9796133987090892559, 0.9796612545806641092, 0.9796851825164515359, 0.9797091104522390737, 0.9800919574248382338, 0.9808576513700365540, 0.9816233453152349853, 0.9817190570583846920, 0.9817310210262785164, 0.9817429849941722297, 0.9817669129299596564, 0.9818147688015345098, 0.9820061922878341454, 0.9823890392604333055, 0.9831547332056317368, 0.9835375801782308969, 0.9837290036645305324, 0.9837529316003179591, 0.9837768595361053858, 0.9838247154076803502, 0.9839204271508300570, 0.9846861210960283772, 0.9847339769676032306, 0.9847579049033906573, 0.9847818328391780840, 0.9848775445823279018, 0.9850689680686274263, 0.9854518150412265864, 0.9856432385275261110, 0.9857389502706759288, 0.9857868061422507822, 0.9857897971342242105, 0.9857927881261976388, 0.9857987701101444955, 0.9858107340780382088, 0.9858346620138257466, 0.9862175089864250177, 0.9869832029316235600, 0.9877488968768222133, 0.9877967527483971777, 0.9878206806841846044, 0.9878326446520783177, 0.9878446086199720311, 0.9879403203631218489, 0.9881317438494214844, 0.9885145908220207556, 0.9892802847672194089, 0.9896631317398186800, 0.9897588434829684978, 0.9898066993545434622, 0.9898306272903308889, 0.9898425912582246022, 0.9898545552261183156, 0.9900459787124179512, 0.9908116726576166045, 0.9915773666028151467, 0.9917687900891147823, 0.9918645018322646001, 0.9918884297680521378, 0.9919123577038395645, 0.9919602135754144179, 0.9923430605480138000, 0.9938744484384109956, 0.9942572954110103778, 0.9946401423836096489, 0.9954058363288083022, 0.9957886833014075734, 0.9959801067877072089, 0.9961715302740068445, 0.9969372242192054978, 0.9977029181644041511, 0.9978943416507037867, 0.9980857651370034223, 0.9984686121096026934, 1.000000000000000000 ),
 .UNSPECIFIED. ) ;
#11316=CARTESIAN_POINT ( 'NONE',  ( 5.984812564823209335, 74.89834532313686566, 12.10097681524328195 ) ) ;
#11318=CARTESIAN_POINT ( 'NONE',  ( -4.171729424061787483, 84.32999999999999829, -12.83926296998457417 ) ) ;
#11320=CARTESIAN_POINT ( 'NONE',  ( 9.114567266466451656, 51.82565792604705024, -9.971525571875499594 ) ) ;
#11322=DIRECTION ( 'NONE',  ( 0.000000000000000000, -1.000000000000000000, 0.000000000000000000 ) ) ;
#11323=B_SPLINE_CURVE_WITH_KNOTS ( 'NONE', 3,
 ( #13229, #11995, #2167, #11737, #6532, #6264, #10333, #1204, #13059, #17289, #17114, #3594, #10418, #5113, #15953, #5201, #15687, #1032, #2421, #6442, #14364, #6615, #2511, #3775, #17377, #7773, #7592, #12971, #9101, #11911, #15776, #10591, #9006, #13144, #10507, #5019, #16037, #3687, #3859, #11825, #853, #15868, #11651, #17028, #9188, #4933, #2252, #14453, #9273, #2340, #14536, #7855, #3946, #14626, #7941, #5291, #10673, #236, #16483, #8383, #13483, #4121, #6786, #2775, #7053, #13568, #8027, #13396, #2955, #4032, #14710, #9446, #14794, #17457, #147, #2598, #8296, #12434, #4387, #12165, #13653, #16396, #10936, #2686, #14974, #9535, #16210, #8117, #1460, #5729, #1284, #4210, #10759, #6698, #14879, #1636, #2865, #1371, #57, #11025, #4299, #15055, #5553, #1547, #5460, #9711, #8206, #13738, #16122, #10843, #6966, #6880, #12252, #320, #16303, #9623, #11110, #12345, #5642, #12078, #5371, #7487, #12868, #756, #4652, #7138, #7307, #4480, #8730, #10060, #3223, #14088, #8472, #5816, #1805, #12692, #3405, #8558, #495, #13822, #6165, #11199, #3132, #15410, #7219, #12606, #8819, #5902, #13911, #2062, #4565, #11281, #6078, #16658, #9972, #16575, #580, #15236, #9887, #15319, #8644, #1975, #3316, #13997, #7399, #1723, #1892, #5990, #11373, #14178, #16744, #12780, #12524, #11545, #408, #667, #11459, #16835, #4738, #10143, #15494, #16922, #9798, #15144 ),
 .UNSPECIFIED., .F., .F.,
 ( 4, 2, 2, 2, 1, 1, 1, 2, 2, 1, 2, 1, 1, 1, 2, 2, 2, 2, 2, 1, 1, 1, 2, 2, 2, 2, 1, 1, 2, 2, 1, 2, 2, 2, 2, 1, 1, 1, 1, 1, 1, 1, 2, 2, 1, 2, 2, 2, 2, 1, 2, 2, 1, 1, 2, 2, 2, 2, 1, 2, 2, 2, 2, 2, 2, 2, 1, 1, 2, 2, 2, 2, 2, 2, 2, 2, 2, 2, 2, 2, 1, 1, 1, 2, 2, 2, 1, 1, 1, 2, 2, 2, 1, 1, 2, 2, 1, 2, 2, 2, 2, 1, 1, 1, 1, 1, 1, 2, 2, 2, 2, 2, 4 ),
 ( 0.5049162376868217006, 0.5058378572734049117, 0.5067594768599881228, 0.5069898817566339533, 0.5071050842049568130, 0.5071626854291182429, 0.5071914860411990134, 0.5072058863472392876, 0.5072202866532796728, 0.5076810964465712228, 0.5081419062398627728, 0.5082571086881857436, 0.5083147099123471735, 0.5083435105244278329, 0.5083579108304682181, 0.5083723111365086034, 0.5086027160331543229, 0.5090635258264457619, 0.5092939307230914814, 0.5094091331714143411, 0.5094667343955757710, 0.5094955350076564304, 0.5095099353136968157, 0.5095243356197372009, 0.5104459552063200789, 0.5113675747929029569, 0.5118283845861943959, 0.5119435870345172557, 0.5120011882586786855, 0.5120299888707593450, 0.5120587894828401154, 0.5122891943794857239, 0.5132108139660684909, 0.5132684151902299208, 0.5132972158023106912, 0.5133260164143913507, 0.5134412188627142104, 0.5136716237593599299, 0.5141324335526512579, 0.5143628384492969774, 0.5144780408976198371, 0.5145068415097004966, 0.5145212418157408818, 0.5145284419687611299, 0.5145356421217812670, 0.5145932433459426969, 0.5150540531392339139, 0.5159756727258163478, 0.5168972923123987817, 0.5170124947607216415, 0.5170268950667619157, 0.5170412953728023009, 0.5170700959848829603, 0.5171276972090443902, 0.5173581021056899987, 0.5178189118989813267, 0.5187405314855637606, 0.5192013412788549775, 0.5194317461755006970, 0.5194893473996620159, 0.5195469486238234458, 0.5196621510721463055, 0.5215053902453112844, 0.5219662000386025014, 0.5220238012627639312, 0.5220382015688043165, 0.5220526018748445907, 0.5220814024869253611, 0.5221966049352481098, 0.5224270098318937183, 0.5233486294184762633, 0.5242702490050588082, 0.5245006539017044167, 0.5246158563500272765, 0.5247310587983501362, 0.5251918685916413532, 0.5256526783849325701, 0.5257678808332554299, 0.5257822811392958151, 0.5257894812923159522, 0.5257966814453360893, 0.5258254820574168598, 0.5258830832815782896, 0.5261134881782240091, 0.5270351077648066651, 0.5270927089889680950, 0.5271503102131295249, 0.5272655126614523846, 0.5274959175580981041, 0.5279567273513894321, 0.5288783469379721991, 0.5293391567312635271, 0.5294543591795863868, 0.5295119604037478167, 0.5295407610158285872, 0.5295551613218688614, 0.5295695616279092466, 0.5297999665245549661, 0.5307215861111376221, 0.5307791873352990519, 0.5308367885594604818, 0.5309519910077833416, 0.5311823959044290611, 0.5316432056977203890, 0.5318736105943661086, 0.5319888130426889683, 0.5320176136547696277, 0.5320320139608100130, 0.5320464142668503982, 0.5321040154910118281, 0.5325648252843031560, 0.5334864448708860341, 0.5344080644574688010 ),
 .UNSPECIFIED. ) ;
#11326=CARTESIAN_POINT ( 'NONE',  ( 11.65849161655502542, 63.17672869437035388, 6.808066451784101858 ) ) ;
#11327=CARTESIAN_POINT ( 'NONE',  ( -11.52888015854957793, 80.93000000000003524, 3.329402692645399675 ) ) ;
#11328=CARTESIAN_POINT ( 'NONE',  ( 12.26390295534138097, 48.63671511653366508, -5.643290960661551559 ) ) ;
#11331=CARTESIAN_POINT ( 'NONE',  ( 11.76794919243112325, 70.28000000000000114, 3.823638476888997051 ) ) ;
#11336=CARTESIAN_POINT ( 'NONE',  ( -0.4672551503964261221, 43.19680077074366409, -13.49191230240068151 ) ) ;
#11337=CARTESIAN_POINT ( 'NONE',  ( 3.590940523862469647, 80.93000000000002103, -12.80902731135813255 ) ) ;
#11340=CARTESIAN_POINT ( 'NONE',  ( 5.739335732908509513, 65.88870427065418767, 12.21924884404352873 ) ) ;
#11341=CARTESIAN_POINT ( 'NONE',  ( 13.49999999999999822, 81.27999999999998693, 4.386415899144237684 ) ) ;
#11342=CARTESIAN_POINT ( 'NONE',  ( -9.520470885617717371, 63.23000000000001108, 6.917026985038133624 ) ) ;
#11344=CARTESIAN_POINT ( 'NONE',  ( 3.636496289402157078, 62.03000000000000114, -11.19198476289190936 ) ) ;
#11345=ADVANCED_FACE ( 'NONE', ( #463 ), #2919, .T. ) ;
#11346=CARTESIAN_POINT ( 'NONE',  ( -11.22710358024347066, 46.64834459066621264, -7.497684075563164185 ) ) ;
#11347=CARTESIAN_POINT ( 'NONE',  ( 11.77153775093140453, 45.67521517251212515, -6.609237642556685444 ) ) ;
#11348=CARTESIAN_POINT ( 'NONE',  ( 0.4427203256037225421, 70.16408690274822391, -13.49318835613360079 ) ) ;
#11349=AXIS2_PLACEMENT_3D ( 'NONE', #4269, #13879, #13795 ) ;
#11350=CARTESIAN_POINT ( 'NONE',  ( 11.30690640946770387, 30.70661390184433870, -7.375942793261094366 ) ) ;
#11351=CARTESIAN_POINT ( 'NONE',  ( -12.81049166330523370, 55.77383991625395510, -4.351154996992983470 ) ) ;
#11352=CARTESIAN_POINT ( 'NONE',  ( 2.894739436579920166E-06, 50.68008041434205069, 13.49999999999938005 ) ) ;
#11353=CARTESIAN_POINT ( 'NONE',  ( 13.26911237221029083, 33.34238326213255732, 2.487181046264572259 ) ) ;
#11354=B_SPLINE_CURVE_WITH_KNOTS ( 'NONE', 3,
 ( #9940, #2742, #11428, #11337, #17060, #13003, #5957, #7366, #11684, #12746, #11599, #8786, #4964, #7539, #14228, #16976, #15548, #3373, #16714, #3460, #547, #4706, #3190, #16799, #14143, #15462, #15632, #802 ),
 .UNSPECIFIED., .F., .F.,
 ( 4, 2, 2, 2, 2, 2, 2, 2, 2, 2, 2, 2, 2, 4 ),
 ( 0.000000000000000000, 0.002887961676758743750, 0.004331942515138114541, 0.005775923353517485766, 0.007219904191896856123, 0.008663885030276227348, 0.01155184670703496633, 0.01299582754541433668, 0.01443980838379370357, 0.01588378922217307393, 0.01732777006055244429, 0.02021573173731117806, 0.02165971257569054842, 0.02310369341406991878 ),
 .UNSPECIFIED. ) ;
#11355=CARTESIAN_POINT ( 'NONE',  ( 1.227961615663091699, 43.13597886236095746, -13.44709991383356495 ) ) ;
#11356=CARTESIAN_POINT ( 'NONE',  ( 10.37184659297094846, 39.76092788044618231, -8.641630322754368265 ) ) ;
#11358=CARTESIAN_POINT ( 'NONE',  ( -12.78755855970386968, 62.08593128313325593, 4.328318190136370980 ) ) ;
#11359=ORIENTED_EDGE ( 'NONE', *, *, #3866, .T. ) ;
#11360=CARTESIAN_POINT ( 'NONE',  ( -13.03040177922608933, 40.80407172380693481, -3.529905272466287602 ) ) ;
#11363=CARTESIAN_POINT ( 'NONE',  ( 11.72395686480903798, 48.18137790691303479, 6.693342665092507637 ) ) ;
#11365=CARTESIAN_POINT ( 'NONE',  ( 2.974383071351499819, 58.07333263741331564, -13.17907237816856814 ) ) ;
#11366=CARTESIAN_POINT ( 'NONE',  ( 13.50000000000000000, 33.42999999999999261, 1.653273178848926867E-15 ) ) ;
#11367=CARTESIAN_POINT ( 'NONE',  ( 10.92172942406179104, 38.73000000000000398, -7.935100905948385908 ) ) ;
#11368=CARTESIAN_POINT ( 'NONE',  ( 8.549612433556128696E-08, 65.68000242247177312, 13.49999999999999822 ) ) ;
#11370=FACE_OUTER_BOUND ( 'NONE', #1289, .T. ) ;
#11373=CARTESIAN_POINT ( 'NONE',  ( 3.927706695870254894, 53.82098454782523334, 12.91925010199899404 ) ) ;
#11374=ORIENTED_EDGE ( 'NONE', *, *, #10545, .T. ) ;
#11375=CARTESIAN_POINT ( 'NONE',  ( -5.598125747105554773, 64.38316814361185436, -12.28681845237412240 ) ) ;
#11377=CARTESIAN_POINT ( 'NONE',  ( 5.253982477109049753, 66.98991576002745774, -12.43579786932437514 ) ) ;
#11378=CARTESIAN_POINT ( 'NONE',  ( -5.489207653998832370, 34.37901037099156554, -12.33365157413798308 ) ) ;
#11380=CARTESIAN_POINT ( 'NONE',  ( 10.30926263822041733, 78.09576994560912055, 8.718911663792482614 ) ) ;
#11382=DIRECTION ( 'NONE',  ( 0.000000000000000000, 0.000000000000000000, 1.000000000000000000 ) ) ;
#11384=CARTESIAN_POINT ( 'NONE',  ( 11.80346242492321274, 72.67293280733154859, -6.552678632547006998 ) ) ;
#11386=CARTESIAN_POINT ( 'NONE',  ( 13.50000000000000355, 63.57999999999999829, -4.386415899144233244 ) ) ;
#11387=CARTESIAN_POINT ( 'NONE',  ( -6.092287277825001901, 52.40267620124564729, -12.04843092496792778 ) ) ;
#11388=CIRCLE ( 'NONE', #3756, 6.000000000000000000 ) ;
#11389=CARTESIAN_POINT ( 'NONE',  ( 11.76794919243112325, 43.28000000000000114, 3.823638476888996607 ) ) ;
#11391=CARTESIAN_POINT ( 'NONE',  ( 10.92172942406179104, 59.73000000000000398, -7.935100905948385908 ) ) ;
#11394=CARTESIAN_POINT ( 'NONE',  ( -4.359978608474780692, 68.52319895195806509, 12.77656657477075619 ) ) ;
#11398=CARTESIAN_POINT ( 'NONE',  ( -13.47669604685034273, 73.95737517794891858, 0.7929544294831025741 ) ) ;
#11399=CARTESIAN_POINT ( 'NONE',  ( -4.681627421645250919, 76.34857381001411625, -12.66224289353729482 ) ) ;
#11404=CARTESIAN_POINT ( 'NONE',  ( -9.520470885617717371, 36.22999999999999687, 6.917026985038133624 ) ) ;
#11406=CARTESIAN_POINT ( 'NONE',  ( -12.50000000000000000, 98.93000000000002103, 1.224646799147353059E-15 ) ) ;
#11407=CARTESIAN_POINT ( 'NONE',  ( -5.430539838780684470, 32.48335489466801818, 12.36597437050387605 ) ) ;
#11408=CARTESIAN_POINT ( 'NONE',  ( 0.6357631489675421577, 74.70282378747322127, 13.48670659248960391 ) ) ;
#11411=CARTESIAN_POINT ( 'NONE',  ( -10.92172942406179104, 79.23000000000000398, 7.935100905948387684 ) ) ;
#11412=CARTESIAN_POINT ( 'NONE',  ( 13.39742027234894373, 51.37205055260678677, 1.661267672429425080 ) ) ;
#11413=CARTESIAN_POINT ( 'NONE',  ( -3.953315691120589559, 38.53792859346052779, 12.90880018502329740 ) ) ;
#11414=AXIS2_PLACEMENT_3D ( 'NONE', #11406, #12725, #2259 ) ;
#11415=CARTESIAN_POINT ( 'NONE',  ( 5.257186988432292374, 36.98950229088148944, -12.43479488390594234 ) ) ;
#11418=CARTESIAN_POINT ( 'NONE',  ( 11.99276598793104220, 63.20099088703636170, 6.208637428856185636 ) ) ;
#11419=CARTESIAN_POINT ( 'NONE',  ( 0.7454762885463678268, 41.70680463810530370, 13.47968111932929425 ) ) ;
#11420=CARTESIAN_POINT ( 'NONE',  ( 13.22392818312517981, 48.52595923520821941, -2.716232255608545199 ) ) ;
#11423=CARTESIAN_POINT ( 'NONE',  ( -3.636496289402153081, 71.32999999999999829, -11.19198476289190936 ) ) ;
#11427=CARTESIAN_POINT ( 'NONE',  ( -1.516382701837864061E-05, 43.18000056530163278, -13.49999999999148237 ) ) ;
#11428=CARTESIAN_POINT ( 'NONE',  ( 4.992525441478825599, 80.92999999999999261, -12.45192268195328644 ) ) ;
#11431=CARTESIAN_POINT ( 'NONE',  ( 5.638822662700721189, 65.88478960647121596, 12.26611570875842361 ) ) ;
#11433=CARTESIAN_POINT ( 'NONE',  ( 9.520470885617715595, 46.12999999999999545, 6.917026985038134512 ) ) ;
#11434=CARTESIAN_POINT ( 'NONE',  ( -13.33009014538846060, 46.85508354669458697, -2.135410199497755457 ) ) ;
#11435=CARTESIAN_POINT ( 'NONE',  ( 13.00530806322553801, 45.55934659475123993, -3.622166112361987711 ) ) ;
#11436=CARTESIAN_POINT ( 'NONE',  ( 8.581308343826755447, 69.85066467472573493, -10.42246601472090184 ) ) ;
#11438=CARTESIAN_POINT ( 'NONE',  ( 11.32201783469629319, 30.70566325776308148, -7.352740184045440053 ) ) ;
#11439=CARTESIAN_POINT ( 'NONE',  ( -12.75462880676983346, 56.08956944644259579, 4.424037827898520625 ) ) ;
#11441=CARTESIAN_POINT ( 'NONE',  ( 12.74964865169902595, 33.26969396973853321, 4.447817866060830738 ) ) ;
#11442=CARTESIAN_POINT ( 'NONE',  ( 0.02127179003657111989, 43.17923766543314912, -13.49998428890246238 ) ) ;
#11443=CARTESIAN_POINT ( 'NONE',  ( 8.276543950180441200, 39.86464973345010065, -10.66536639688594157 ) ) ;
#11445=CARTESIAN_POINT ( 'NONE',  ( -13.47504669145713052, 61.95844030485035603, 0.8236179170182681419 ) ) ;
#11447=EDGE_CURVE ( 'NONE', #14369, #16090, #11354, .T. ) ;
#11450=CARTESIAN_POINT ( 'NONE',  ( 11.44020875125550418, 48.16198584060624199, 7.171056752996642025 ) ) ;
#11451=CARTESIAN_POINT ( 'NONE',  ( 2.429919961663213446, 58.09262903994793703, -13.27951469578883170 ) ) ;
#11452=CARTESIAN_POINT ( 'NONE',  ( 4.962992231027985923, 79.00097767184028896, -12.55463077525622850 ) ) ;
#11453=CARTESIAN_POINT ( 'NONE',  ( -3.636496289402153081, 77.32999999999999829, -11.19198476289190936 ) ) ;
#11454=CARTESIAN_POINT ( 'NONE',  ( -13.49999999999999822, 42.77999999999999403, -4.386415899144240349 ) ) ;
#11455=CARTESIAN_POINT ( 'NONE',  ( -1.080702808754571365, 46.21883424019694075, -13.45909926978481685 ) ) ;
#11456=CARTESIAN_POINT ( 'NONE',  ( -0.6268641640632613976, 67.20253659941207047, -13.48655692365852765 ) ) ;
#11459=CARTESIAN_POINT ( 'NONE',  ( 3.249354579472210958, 53.79684832599942723, 13.10312257493411892 ) ) ;
#11460=ORIENTED_EDGE ( 'NONE', *, *, #3366, .F. ) ;
#11461=DIRECTION ( 'NONE',  ( 0.000000000000000000, -1.000000000000000000, 0.000000000000000000 ) ) ;
#11462=ORIENTED_EDGE ( 'NONE', *, *, #7558, .F. ) ;
#11463=CARTESIAN_POINT ( 'NONE',  ( 2.856314228632829799, 67.07729655047123174, -13.19448560150985550 ) ) ;
#11464=CARTESIAN_POINT ( 'NONE',  ( -4.429559070322160785, 34.33932522792037645, -12.75305594940425813 ) ) ;
#11467=CARTESIAN_POINT ( 'NONE',  ( 2.224888343446056904, 77.75999185975226169, 13.31734366878287190 ) ) ;
#11468=CARTESIAN_POINT ( 'NONE',  ( -1.167348460861534098, 59.63805143168455203, 13.45207174649093140 ) ) ;
#11471=CARTESIAN_POINT ( 'NONE',  ( 13.50427256397625442, 72.45803527614656048, -0.8161559238757217782 ) ) ;
#11474=CARTESIAN_POINT ( 'NONE',  ( -8.343458848123582072, 53.37999999999998835, 11.48378591275254124 ) ) ;
#11475=CARTESIAN_POINT ( 'NONE',  ( -8.818712758598348245, 52.52050123826117556, -10.22156924380393761 ) ) ;
#11477=CARTESIAN_POINT ( 'NONE',  ( -10.92172942406178926, 51.62999999999999545, -7.935100905948389460 ) ) ;
#11481=CARTESIAN_POINT ( 'NONE',  ( -1.221649949217112674, 68.63608161155467258, 13.44461842710221866 ) ) ;
#11483=CARTESIAN_POINT ( 'NONE',  ( 13.50000000000000355, 71.57999999999999829, -4.386415899144233244 ) ) ;
#11486=CARTESIAN_POINT ( 'NONE',  ( -10.26088610336786999, 65.26697153941822194, 8.775667508859029908 ) ) ;
#11487=DIRECTION ( 'NONE',  ( 0.000000000000000000, 0.000000000000000000, -1.000000000000000000 ) ) ;
#11488=CARTESIAN_POINT ( 'NONE',  ( 0.000000000000000000, 108.9300000000000068, 0.000000000000000000 ) ) ;
#11490=CARTESIAN_POINT ( 'NONE',  ( -7.272992578804307939, 41.48000000000000398, -10.01041549318727064 ) ) ;
#11491=CARTESIAN_POINT ( 'NONE',  ( -4.020198640976432536, 40.32452907086292271, -12.88802636581765171 ) ) ;
#11492=CARTESIAN_POINT ( 'NONE',  ( -11.47301210480950573, 32.19583706789580901, 7.115409834509677012 ) ) ;
#11494=CARTESIAN_POINT ( 'NONE',  ( -0.3977526850660704771, 53.66569853454892325, 13.49421918269976572 ) ) ;
#11495=CARTESIAN_POINT ( 'NONE',  ( -8.343458848123576743, 78.47999999999998977, -11.48378591275254301 ) ) ;
#11496=CARTESIAN_POINT ( 'NONE',  ( 12.72736902482333932, 51.59255635549924079, -4.502454855677821222 ) ) ;
#11497=CARTESIAN_POINT ( 'NONE',  ( -12.51208461251463788, 38.11435409805191199, 5.070052519584926642 ) ) ;
#11498=CARTESIAN_POINT ( 'NONE',  ( 10.20673554080668310, 36.76984911407893719, -8.836287964642385973 ) ) ;
#11502=CARTESIAN_POINT ( 'NONE',  ( -3.972390705872383965, 80.53716609899321099, 12.90244840476221633 ) ) ;
#11503=CARTESIAN_POINT ( 'NONE',  ( 5.833048919164877333, 41.89238145366736887, 12.17567392941536397 ) ) ;
#11504=CARTESIAN_POINT ( 'NONE',  ( 13.49629668835036789, 48.41912274314424991, 0.3168857007667773007 ) ) ;
#11507=CARTESIAN_POINT ( 'NONE',  ( 2.272985001014427393E-15, 68.18000000000000682, -12.37355403259654807 ) ) ;
#11509=CARTESIAN_POINT ( 'NONE',  ( 2.138189944381200469, 57.10311857767973720, -13.50000000000001421 ) ) ;
#11512=CARTESIAN_POINT ( 'NONE',  ( 0.2986627873522048060, 76.16926118795059608, -13.50000000000000355 ) ) ;
#11514=CARTESIAN_POINT ( 'NONE',  ( 4.823391606894267269, 65.85361332035319037, 12.61649015956374065 ) ) ;
#11516=CARTESIAN_POINT ( 'NONE',  ( 9.520470885617717371, 49.72999999999999687, -6.917026985038131848 ) ) ;
#11518=CARTESIAN_POINT ( 'NONE',  ( -13.09214566475795571, 59.04778350712611257, 3.306315388002783351 ) ) ;
#11519=CARTESIAN_POINT ( 'NONE',  ( 13.21252823081788641, 45.52825912558844834, -2.779356458002163688 ) ) ;
#11520=CARTESIAN_POINT ( 'NONE',  ( 2.196737167881437358, 70.10124606214743892, -13.32735827648023985 ) ) ;
#11521=ADVANCED_FACE ( 'NONE', ( #6044 ), #8874, .T. ) ;
#11522=CARTESIAN_POINT ( 'NONE',  ( 13.37271033652606178, 30.49610245274473641, -1.890770679655365827 ) ) ;
#11523=CARTESIAN_POINT ( 'NONE',  ( -13.41558627325511921, 55.87683987596568613, -1.528904511477074069 ) ) ;
#11524=CARTESIAN_POINT ( 'NONE',  ( -3.880351607964129368, 50.54047666460265731, 12.93032359281371946 ) ) ;
#11525=DIRECTION ( 'NONE',  ( 0.000000000000000000, 0.000000000000000000, -1.000000000000000000 ) ) ;
#11526=DIRECTION ( 'NONE',  ( 0.000000000000000000, -1.000000000000000000, 0.000000000000000000 ) ) ;
#11527=CARTESIAN_POINT ( 'NONE',  ( 13.00990400852149698, 39.55870865720761742, -3.604563544963208521 ) ) ;
#11528=VERTEX_POINT ( 'NONE', #13964 ) ;
#11529=CARTESIAN_POINT ( 'NONE',  ( -13.42561672413123119, 61.87950532278058091, -1.455403704591293534 ) ) ;
#11530=VERTEX_POINT ( 'NONE', #1860 ) ;
#11531=VERTEX_POINT ( 'NONE', #7274 ) ;
#11534=CARTESIAN_POINT ( 'NONE',  ( 7.608556374808001621, 57.89437078001525094, -11.15259761450094267 ) ) ;
#11535=CARTESIAN_POINT ( 'NONE',  ( 10.85989957991099963, 78.73358321125698467, -8.019560153188759699 ) ) ;
#11536=CARTESIAN_POINT ( 'NONE',  ( 11.76794919243112325, 82.43000000000000682, 1.441158131103945434E-15 ) ) ;
#11537=CARTESIAN_POINT ( 'NONE',  ( -7.272992578804307939, 83.47999999999998977, -10.01041549318726886 ) ) ;
#11539=B_SPLINE_CURVE_WITH_KNOTS ( 'NONE', 3,
 ( #11698, #11613, #6059, #11442, #14326, #2215, #4807, #3473, #5973, #2046, #16989, #11355, #7470, #16729, #13019, #3300, #16815, #4893, #10294, #4636, #10043, #17074, #12850, #10124, #6312, #649, #15477, #8713, #15646, #12761, #4978, #15392, #10381, #7383, #3388, #14073, #1960, #739, #8801, #6402, #10719, #13441, #11785, #17161, #13358, #12040, #10467, #1166, #2560, #6577, #14497, #9236, #5248, #6744, #9322, #7990, #7820, #11958, #1247, #2384, #17249, #15828, #4078, #13, #3732, #11874, #16168, #5162, #16084, #10554, #14756, #13278, #17419, #3992, #6659, #7903, #9150, #5334, #5073, #9408, #15913, #3822, #17337, #2470, #2646, #8077, #1328, #13192, #15999, #12124, #1077, #10806, #5417, #9493, #2299, #14590, #6491, #10634, #7727, #13103, #3904, #14672, #990, #7095, #13615, #8163, #4168, #452, #8427, #11154, #8340, #13867, #1679, #16530, #5862, #11069, #4258, #4437, #1769, #13527, #4344, #8517, #11241, #195, #12479, #365, #1596, #16619, #9753, #4523, #15190, #280, #13780, #12301, #9844, #2910, #7178, #10892, #8253, #15098, #6924, #5770, #1416, #6834, #12210, #16442, #3091, #104, #2823, #5509, #12566, #14840, #2734, #2997, #16261, #16352, #9580, #14931, #1508, #7012, #5600, #10982, #9668, #15018, #13696, #12389, #5689, #16791, #14047, #7530, #2191, #7264, #3180, #13954, #8688, #8946, #10272, #11503, #3531, #15453, #15279, #3451, #10017, #7358, #15623, #11676, #7618, #713, #6124, #12995, #3362, #8866, #15365, #16879, #14304, #12648, #12737, #1935, #625, #15539, #6289, #537, #14218, #6036, #11419, #4697, #5947, #794, #877, #17052 ),
 .UNSPECIFIED., .F., .F.,
 ( 4, 2, 1, 1, 1, 1, 2, 2, 2, 2, 1, 1, 2, 2, 1, 2, 2, 2, 2, 2, 1, 2, 1, 1, 2, 2, 1, 2, 2, 2, 2, 2, 2, 2, 2, 2, 2, 2, 1, 1, 1, 1, 1, 2, 2, 1, 2, 1, 1, 2, 2, 1, 1, 2, 2, 2, 2, 2, 2, 2, 1, 1, 2, 2, 2, 2, 2, 1, 1, 1, 2, 1, 2, 2, 2, 2, 2, 1, 1, 2, 2, 2, 2, 2, 2, 1, 1, 2, 2, 2, 2, 2, 2, 2, 1, 2, 2, 2, 2, 2, 2, 1, 2, 2, 2, 2, 2, 1, 2, 2, 1, 1, 2, 1, 2, 2, 1, 1, 1, 2, 2, 2, 2, 2, 4 ),
 ( 0.7402069710304320926, 0.7402141279982914490, 0.7402212849661509164, 0.7402355989018696292, 0.7402642267733071657, 0.7403214825161822388, 0.7404359940019324959, 0.7406650169734327882, 0.7411230629164335948, 0.7420391548024349859, 0.7421536662881852431, 0.7422109220310603162, 0.7422252359667790289, 0.7422395499024978527, 0.7422681777739353892, 0.7424972007454357925, 0.7429552466884364881, 0.7431842696599368914, 0.7432415254028119644, 0.7432987811456871485, 0.7434132926314372947, 0.7438713385744381013, 0.7441003615459383935, 0.7442148730316886507, 0.7442435009031261872, 0.7442721287745637238, 0.7443293845174387968, 0.7447874304604396034, 0.7457035223464411056, 0.7461615682894418011, 0.7462760797751919473, 0.7463905912609422044, 0.7466196142324426077, 0.7475357061184439988, 0.7479937520614448054, 0.7482227750329450977, 0.7482800307758202818, 0.7483372865186953549, 0.7484517980044455010, 0.7489098439474461966, 0.7491388669189465999, 0.7492533784046967460, 0.7493106341475718191, 0.7493392620190093556, 0.7493535759547281794, 0.7493678898904470032, 0.7502839817764483943, 0.7503412375193234674, 0.7503483944871829348, 0.7503519729711125574, 0.7503555514550422911, 0.7503698653907610039, 0.7503984932621985404, 0.7505130047479487976, 0.7507420277194492009, 0.7512000736624500075, 0.7521161655484517317, 0.7523451885199521350, 0.7523738163913896715, 0.7523881303271084953, 0.7524024442628272080, 0.7524597000057023921, 0.7525742114914525382, 0.7530322574344533448, 0.7539483493204549580, 0.7544063952634557646, 0.7544636510063309487, 0.7545209067492060218, 0.7546354182349561679, 0.7548644412064565712, 0.7553224871494573778, 0.7553797428923325619, 0.7554083707637700984, 0.7554369986352076349, 0.7555515101209577811, 0.7557805330924581844, 0.7562385790354591020, 0.7563530905212092481, 0.7564103462640843212, 0.7564389741355218577, 0.7564676020069595053, 0.7566966249784599086, 0.7585288087504631349, 0.7587578317219635382, 0.7587864595934010747, 0.7588150874648386113, 0.7588723432077136843, 0.7589868546934639415, 0.7594449006364647481, 0.7603609925224663613, 0.7608190384654671679, 0.7610480614369676822, 0.7610766893084052187, 0.7611053171798427552, 0.7611625729227178283, 0.7612770844084680855, 0.7621931762944698097, 0.7631092681804716449, 0.7633382911519720482, 0.7633955468948471212, 0.7634241747662847688, 0.7634528026377223053, 0.7635673141234724515, 0.7640253600664732581, 0.7649414519524749823, 0.7653994978954757888, 0.7656285208669761921, 0.7656857766098513762, 0.7657144044812889128, 0.7657287184170076255, 0.7657430323527264493, 0.7658575438384767065, 0.7667736357244784307, 0.7672316816674793483, 0.7674607046389797516, 0.7674750185746985753, 0.7674893325104173991, 0.7675179603818549356, 0.7675752161247300087, 0.7676897276104802659, 0.7686058194964821011, 0.7690638654394830187, 0.7691783769252332759, 0.7692928884109835330, 0.7695219113824839363 ),
 .UNSPECIFIED. ) ;
#11542=CARTESIAN_POINT ( 'NONE',  ( 8.343458848123583849, 41.88000000000000256, -11.48378591275253768 ) ) ;
#11543=CARTESIAN_POINT ( 'NONE',  ( -8.891200544363830713E-16, 34.67999999999999261, 13.50000000000000000 ) ) ;
#11545=CARTESIAN_POINT ( 'NONE',  ( 3.280751270289125721, 53.79795775059116636, 13.09529373139613817 ) ) ;
#11547=CARTESIAN_POINT ( 'NONE',  ( 1.653273178848926472E-15, 80.93000000000000682, 13.50000000000000000 ) ) ;
#11549=CARTESIAN_POINT ( 'NONE',  ( 1.109228931819516317, 67.14015256849161517, -13.46182782856074134 ) ) ;
#11553=CARTESIAN_POINT ( 'NONE',  ( -1.516382701837864061E-05, 43.18000056530163278, -13.49999999999148237 ) ) ;
#11554=CARTESIAN_POINT ( 'NONE',  ( -4.866239539597595254, 59.50453715926928311, 12.60008563178253382 ) ) ;
#11557=CARTESIAN_POINT ( 'NONE',  ( 13.37582773222545462, 72.36614543582099657, 1.826812634724402251 ) ) ;
#11560=CARTESIAN_POINT ( 'NONE',  ( 4.171729424061791924, 58.03000000000000114, -12.83926296998457239 ) ) ;
#11561=CARTESIAN_POINT ( 'NONE',  ( -1.099254190772257944, 52.21949712129632815, -13.46198568913586158 ) ) ;
#11562=EDGE_CURVE ( 'NONE', #3478, #8302, #3950, .T. ) ;
#11564=AXIS2_PLACEMENT_3D ( 'NONE', #6655, #11870, #12206 ) ;
#11566=CARTESIAN_POINT ( 'NONE',  ( -4.375457956215162980, 68.52263673597026639, 12.77127380410037460 ) ) ;
#11568=CARTESIAN_POINT ( 'NONE',  ( 13.50000000000000000, 71.43000000000000682, 1.653273178848926867E-15 ) ) ;
#11570=CARTESIAN_POINT ( 'NONE',  ( -1.755979736915106670, 65.61690310277927551, 13.38701199797056596 ) ) ;
#11574=EDGE_LOOP ( 'NONE', ( #11593, #5139, #10811, #14937 ) ) ;
#11575=CARTESIAN_POINT ( 'NONE',  ( 2.272985001014427393E-15, 32.17999999999999972, -12.37355403259654807 ) ) ;
#11576=CARTESIAN_POINT ( 'NONE',  ( 0.000000000000000000, 88.93000000000000682, 0.000000000000000000 ) ) ;
#11577=CARTESIAN_POINT ( 'NONE',  ( -2.757875465074077770, 40.27916169625384413, -13.21535913837822918 ) ) ;
#11578=CARTESIAN_POINT ( 'NONE',  ( -12.73613204840894575, 32.09161058603033467, 4.477490723709251164 ) ) ;
#11579=CARTESIAN_POINT ( 'NONE',  ( 4.363973203552268920, 74.83691680965836213, 12.79366461543962785 ) ) ;
#11580=CARTESIAN_POINT ( 'NONE',  ( 10.64851715830567969, 60.11437978181223230, 8.298139595169439886 ) ) ;
#11583=CARTESIAN_POINT ( 'NONE',  ( 13.49703212424635090, 51.44014129662132717, -0.2960093095830344523 ) ) ;
#11584=CARTESIAN_POINT ( 'NONE',  ( -10.98823275438732594, 38.22618272328060840, 7.843141453616995662 ) ) ;
#11585=CARTESIAN_POINT ( 'NONE',  ( 13.02171738018827973, 36.55712068918894886, -3.561963326260443985 ) ) ;
#11587=CARTESIAN_POINT ( 'NONE',  ( -13.49999999999999822, 69.78000000000000114, -4.386415899144240349 ) ) ;
#11588=CARTESIAN_POINT ( 'NONE',  ( -0.4449605378473073247, 77.66411776958061353, 13.50000000002665779 ) ) ;
#11590=DIRECTION ( 'NONE',  ( -0.000000000000000000, -1.000000000000000000, -0.000000000000000000 ) ) ;
#11591=CARTESIAN_POINT ( 'NONE',  ( 12.06997253147024907, 48.65274548705490076, -6.050138844817690931 ) ) ;
#11593=ORIENTED_EDGE ( 'NONE', *, *, #5182, .F. ) ;
#11594=CARTESIAN_POINT ( 'NONE',  ( 11.76794919243112325, 61.27999999999999403, 3.823638476888997051 ) ) ;
#11599=CARTESIAN_POINT ( 'NONE',  ( -1.218708134003366972, 80.92999999999994998, -12.93996086231559950 ) ) ;
#11602=CARTESIAN_POINT ( 'NONE',  ( -13.49999999999999822, 79.78000000000001535, -4.386415899144240349 ) ) ;
#11603=CARTESIAN_POINT ( 'NONE',  ( -7.576616670048093940E-16, 51.68000000000000682, 12.37355403259654985 ) ) ;
#11605=CARTESIAN_POINT ( 'NONE',  ( -13.47788786600996858, 58.90332777413669874, -0.7723891097661439442 ) ) ;
#11606=CARTESIAN_POINT ( 'NONE',  ( 11.46114320549623322, 45.16339242848184199, 7.133879970484350963 ) ) ;
#11607=DIRECTION ( 'NONE',  ( 0.000000000000000000, 0.000000000000000000, -1.000000000000000000 ) ) ;
#11609=CARTESIAN_POINT ( 'NONE',  ( 13.06885327976965350, 30.55053021910186573, -3.384549578735317699 ) ) ;
#11610=CARTESIAN_POINT ( 'NONE',  ( -13.26782536342165386, 55.84215906510630134, -2.493279635214634471 ) ) ;
#11611=CARTESIAN_POINT ( 'NONE',  ( -11.03304771478256718, 50.22344490325513533, 7.779581208127924086 ) ) ;
#11612=CARTESIAN_POINT ( 'NONE',  ( 3.389914706142906464, 64.05807598113629808, -13.07065644264653237 ) ) ;
#11613=CARTESIAN_POINT ( 'NONE',  ( 0.003459163312698950409, 43.17987605612985647, -13.50000000389382748 ) ) ;
#11614=CARTESIAN_POINT ( 'NONE',  ( 13.17317126124304139, 39.53500463294717093, -2.964159239871142937 ) ) ;
#11615=ORIENTED_EDGE ( 'NONE', *, *, #15163, .T. ) ;
#11617=CARTESIAN_POINT ( 'NONE',  ( -6.997891731511667324, 61.43956589088693221, -11.54533655814920046 ) ) ;
#11618=ORIENTED_EDGE ( 'NONE', *, *, #5116, .T. ) ;
#11619=VERTEX_POINT ( 'NONE', #7254 ) ;
#11623=CARTESIAN_POINT ( 'NONE',  ( 10.27722599705290740, 57.76617510714760328, -8.759151267258511453 ) ) ;
#11624=CARTESIAN_POINT ( 'NONE',  ( 9.860830236870366861, 78.78814180884941720, -9.230709546527805287 ) ) ;
#11625=CARTESIAN_POINT ( 'NONE',  ( -11.76794919243112325, 74.78000000000000114, -3.823638476888998827 ) ) ;
#11626=CARTESIAN_POINT ( 'NONE',  ( 3.636496289402157078, 83.03000000000000114, -11.19198476289190936 ) ) ;
#11628=CARTESIAN_POINT ( 'NONE',  ( 2.138189944381242213, 42.10311857767972299, -13.49999999999999822 ) ) ;
#11629=CARTESIAN_POINT ( 'NONE',  ( 0.000000000000000000, 80.93000000000000682, 0.000000000000000000 ) ) ;
#11632=CARTESIAN_POINT ( 'NONE',  ( 6.796988989821601379, 33.92896228189544416, -11.67543111795051480 ) ) ;
#11638=CARTESIAN_POINT ( 'NONE',  ( 3.524474397628260203, 77.80665974831858023, 13.03877614333868351 ) ) ;
#11639=CARTESIAN_POINT ( 'NONE',  ( -7.174930598646008129, 59.41297086956210194, 11.43548786726982769 ) ) ;
#11642=LINE ( 'NONE', #17105, #8292 ) ;
#11643=CARTESIAN_POINT ( 'NONE',  ( 9.756437614077082543, 72.06660688249944258, 9.330710072649175402 ) ) ;
#11644=CARTESIAN_POINT ( 'NONE',  ( 13.49999999999999822, 54.27999999999999403, 4.386415899144237684 ) ) ;
#11645=CARTESIAN_POINT ( 'NONE',  ( -5.787687467190007595, 71.46940676660642566, 12.19642108145509418 ) ) ;
#11649=CARTESIAN_POINT ( 'NONE',  ( 2.582823892810359290, 68.77289463184231977, 13.25273780715061456 ) ) ;
#11651=CARTESIAN_POINT ( 'NONE',  ( 8.971056075657596551, 54.83247871843056487, -10.09135430922370347 ) ) ;
#11653=CARTESIAN_POINT ( 'NONE',  ( -9.725010589135534289, 65.29500619405467887, 9.363680539315007323 ) ) ;
#11654=CARTESIAN_POINT ( 'NONE',  ( -12.50000000000000000, 98.93000000000002103, 9.000000000000000000 ) ) ;
#11655=CARTESIAN_POINT ( 'NONE',  ( -7.020346476131678060, 35.41948706349571552, 11.53104520956814305 ) ) ;
#11661=CARTESIAN_POINT ( 'NONE',  ( -11.83717302900882551, 31.68955936364634951, -6.490870104775230409 ) ) ;
#11662=CARTESIAN_POINT ( 'NONE',  ( 0.000000000000000000, 80.93000000000000682, 0.000000000000000000 ) ) ;
#11663=CARTESIAN_POINT ( 'NONE',  ( 13.49992669839407178, 60.43171412446871216, -0.05011807936940589070 ) ) ;
#11665=CARTESIAN_POINT ( 'NONE',  ( 10.92172942406179104, 62.73000000000001108, -7.935100905948385908 ) ) ;
#11666=CARTESIAN_POINT ( 'NONE',  ( 2.272985001014427788E-15, 56.17999999999999972, -12.37355403259654985 ) ) ;
#11668=CARTESIAN_POINT ( 'NONE',  ( -4.171729424061791036, 73.53000000000000114, 12.83926296998457239 ) ) ;
#11669=CARTESIAN_POINT ( 'NONE',  ( 13.24054410806451720, 51.52295701284848661, -2.634018347425864714 ) ) ;
#11670=CARTESIAN_POINT ( 'NONE',  ( -13.41433228084396312, 37.98342063485497277, 1.534182904327553443 ) ) ;
#11671=CARTESIAN_POINT ( 'NONE',  ( 13.41223885496773427, 36.48523552608328657, -1.585925835905837689 ) ) ;
#11673=CARTESIAN_POINT ( 'NONE',  ( -3.493226371046825651, 74.55439642829867353, 13.04022828054566041 ) ) ;
#11674=CARTESIAN_POINT ( 'NONE',  ( -11.60036162406280980, 77.18758477582102273, 6.922111537354720845 ) ) ;
#11675=CARTESIAN_POINT ( 'NONE',  ( 0.2536749733826671460, 62.68912121125626413, 13.49762152966559903 ) ) ;
#11676=CARTESIAN_POINT ( 'NONE',  ( 5.430970834852819173, 41.87677223918051084, 12.35939327805447263 ) ) ;
#11680=CARTESIAN_POINT ( 'NONE',  ( 7.272992578804311492, 61.87999999999999545, -10.01041549318726886 ) ) ;
#11684=CARTESIAN_POINT ( 'NONE',  ( 0.2248552520821813783, 80.93000000000000682, -13.08843060417381210 ) ) ;
#11686=CARTESIAN_POINT ( 'NONE',  ( 4.171729424061789260, 80.82999999999999829, 12.83926296998457417 ) ) ;
#11687=CARTESIAN_POINT ( 'NONE',  ( -7.576616670048093940E-16, 48.67999999999999261, 12.37355403259654985 ) ) ;
#11689=CARTESIAN_POINT ( 'NONE',  ( -13.21743544613662813, 59.02708992862847737, 2.747696697556875733 ) ) ;
#11690=CARTESIAN_POINT ( 'NONE',  ( 10.40464366657246487, 45.10088306759819687, 8.601957922238709031 ) ) ;
#11691=CARTESIAN_POINT ( 'NONE',  ( 13.37950080006454989, 69.36708149302486959, 1.803377588645109775 ) ) ;
#11692=CARTESIAN_POINT ( 'NONE',  ( -2.875760791593931984E-14, 76.17999999999999261, -13.50000000000000000 ) ) ;
#11693=CARTESIAN_POINT ( 'NONE',  ( 13.50382142429054255, 30.41741325757080716, 0.3602961522248570025 ) ) ;
#11695=CARTESIAN_POINT ( 'NONE',  ( -8.561537994842248978, 55.50809341652116302, -10.44924880110730392 ) ) ;
#11696=CARTESIAN_POINT ( 'NONE',  ( -9.186396683897722681, 50.32198487252506425, 9.897154769051333290 ) ) ;
#11698=CARTESIAN_POINT ( 'NONE',  ( -1.516382701837864061E-05, 43.18000056530163278, -13.49999999999148237 ) ) ;
#11699=CARTESIAN_POINT ( 'NONE',  ( 7.311509977803601679, 38.95289584714333841, 11.35082926183423702 ) ) ;
#11700=ORIENTED_EDGE ( 'NONE', *, *, #14287, .T. ) ;
#11701=CARTESIAN_POINT ( 'NONE',  ( -12.30392646493007014, 61.72675570561128211, -5.559945461151370338 ) ) ;
#11703=ORIENTED_EDGE ( 'NONE', *, *, #12169, .T. ) ;
#11704=CARTESIAN_POINT ( 'NONE',  ( -8.194307551003054968, 40.49162043279464029, -10.72866187828134876 ) ) ;
#11705=ORIENTED_EDGE ( 'NONE', *, *, #7092, .T. ) ;
#11708=CARTESIAN_POINT ( 'NONE',  ( 4.973974161897672275, 47.85944346994435961, 12.55031192319891531 ) ) ;
#11709=CARTESIAN_POINT ( 'NONE',  ( 1.102885466463079389, 58.14037304227331049, -13.46176891591130698 ) ) ;
#11710=CARTESIAN_POINT ( 'NONE',  ( 10.15633907889109544, 78.77269066048498303, -8.904669665069901541 ) ) ;
#11711=CARTESIAN_POINT ( 'NONE',  ( 11.76794919243112325, 76.28000000000000114, 3.823638476888996607 ) ) ;
#11712=CARTESIAN_POINT ( 'NONE',  ( -8.691771469529815392E-16, 37.67999999999999261, 14.19474002721660355 ) ) ;
#11713=CARTESIAN_POINT ( 'NONE',  ( 9.520470885617715595, 82.13000000000000966, 6.917026985038134512 ) ) ;
#11716=EDGE_CURVE ( 'NONE', #15567, #19, #14439, .T. ) ;
#11717=CARTESIAN_POINT ( 'NONE',  ( 0.000000000000000000, 80.93000000000000682, 0.000000000000000000 ) ) ;
#11719=DIRECTION ( 'NONE',  ( -1.000000000000000000, -1.734723475976807094E-16, -0.000000000000000000 ) ) ;
#11720=CARTESIAN_POINT ( 'NONE',  ( 5.975311483674380142, 33.96202926739386641, -12.10592502158520922 ) ) ;
#11721=CARTESIAN_POINT ( 'NONE',  ( -13.35309327176764604, 73.86044722355309489, -1.986183259433068615 ) ) ;
#11723=CARTESIAN_POINT ( 'NONE',  ( -7.499999999999999112, 102.9300000000000068, 9.367496997597601904 ) ) ;
#11724=ORIENTED_EDGE ( 'NONE', *, *, #6562, .T. ) ;
#11727=CARTESIAN_POINT ( 'NONE',  ( -7.230983158322074722, 59.41059414015147411, 11.40016698628919123 ) ) ;
#11728=DIRECTION ( 'NONE',  ( -1.000000000000000000, -8.673617379884035472E-17, 0.000000000000000000 ) ) ;
#11730=CARTESIAN_POINT ( 'NONE',  ( 13.50000000000000355, 51.57999999999999829, -4.386415899144233244 ) ) ;
#11731=CARTESIAN_POINT ( 'NONE',  ( -3.039585127116079200, 71.57070844762461093, 13.15361936645533092 ) ) ;
#11734=CARTESIAN_POINT ( 'NONE',  ( -3.962338278797073343, 68.53759793175959203, 12.90602271434200077 ) ) ;
#11737=CARTESIAN_POINT ( 'NONE',  ( 2.065461445335230017, 55.10580354823416371, -13.34947176806445590 ) ) ;
#11739=CARTESIAN_POINT ( 'NONE',  ( -7.603109958011293301, 65.39459751660324116, 11.15547822810680856 ) ) ;
#11740=LINE ( 'NONE', #3512, #2792 ) ;
#11741=CARTESIAN_POINT ( 'NONE',  ( -9.443773158109223687, 35.30916239436312054, 9.647063514268658935 ) ) ;
#11743=CARTESIAN_POINT ( 'NONE',  ( 8.050216715958701030, 31.03187307936175188, 8.940658242654157206 ) ) ;
#11746=CARTESIAN_POINT ( 'NONE',  ( -2.405887066621936299, 40.26649426164142653, -13.28772887298001848 ) ) ;
#11747=CARTESIAN_POINT ( 'NONE',  ( -13.08398228043214218, 31.81151393346248213, -3.329647435564872193 ) ) ;
#11749=CARTESIAN_POINT ( 'NONE',  ( 13.05092373128589678, 60.30692759104906742, 3.453064110984449098 ) ) ;
#11751=CARTESIAN_POINT ( 'NONE',  ( -7.552751977303077346, 53.39683216713059011, 11.19100968736766255 ) ) ;
#11752=CARTESIAN_POINT ( 'NONE',  ( 11.76794919243112325, 55.27999999999998693, 3.823638476888996607 ) ) ;
#11753=CARTESIAN_POINT ( 'NONE',  ( -13.49999999999999822, 76.07999999999999829, 4.386415899144235908 ) ) ;
#11754=CARTESIAN_POINT ( 'NONE',  ( 12.24683778235814735, 51.63890018789970782, -5.702013043655419722 ) ) ;
#11756=CARTESIAN_POINT ( 'NONE',  ( -13.18940372997155563, 38.03370036661469555, 2.928436094923779986 ) ) ;
#11757=CARTESIAN_POINT ( 'NONE',  ( 9.040794826975059095, 36.82921390846524901, -10.03951093010358697 ) ) ;
#11759=CARTESIAN_POINT ( 'NONE',  ( -0.6196373872324472121, 74.65772012599740037, 13.48577371833401095 ) ) ;
#11761=CARTESIAN_POINT ( 'NONE',  ( -12.00653703015586515, 77.15764966734894870, 6.172573912317796285 ) ) ;
#11762=CARTESIAN_POINT ( 'NONE',  ( -8.343458848123582072, 61.38000000000000256, 11.48378591275253768 ) ) ;
#11764=ORIENTED_EDGE ( 'NONE', *, *, #5501, .F. ) ;
#11767=CARTESIAN_POINT ( 'NONE',  ( 11.76794919243112680, 61.57999999999999829, -3.823638476888993942 ) ) ;
#11770=CARTESIAN_POINT ( 'NONE',  ( 7.895834936963976425, 75.88172377336412922, -10.95133422968197578 ) ) ;
#11771=VECTOR ( 'NONE', #7663, 1000.000000000000000 ) ;
#11772=CARTESIAN_POINT ( 'NONE',  ( 2.138189944381242213, 33.10311857767972299, -13.49999999999999822 ) ) ;
#11773=CARTESIAN_POINT ( 'NONE',  ( -13.49999999999999822, 68.07999999999998408, 4.386415899144235908 ) ) ;
#11774=CARTESIAN_POINT ( 'NONE',  ( -11.76794919243112325, 38.92999999999999972, -2.882316262207890869E-15 ) ) ;
#11776=CARTESIAN_POINT ( 'NONE',  ( -11.05161298094616384, 59.22233715161402756, 7.753204029402317232 ) ) ;
#11778=CARTESIAN_POINT ( 'NONE',  ( 9.435697569393814987, 45.05040745589252538, 9.656000601265819938 ) ) ;
#11779=CARTESIAN_POINT ( 'NONE',  ( 13.10046565438790900, 69.54592110386441561, -3.260037864952345377 ) ) ;
#11780=CARTESIAN_POINT ( 'NONE',  ( 2.452460625982255227, 80.76816317512970045, 13.29106717814962835 ) ) ;
#11781=CARTESIAN_POINT ( 'NONE',  ( 12.75594003600799908, 30.26868555994605359, 4.481693421996284954 ) ) ;
#11782=CARTESIAN_POINT ( 'NONE',  ( -4.048254027269543087, 55.32555987908665429, -12.87879573082893714 ) ) ;
#11783=CARTESIAN_POINT ( 'NONE',  ( -5.602506701022878843, 50.47661089226183151, 12.28261366399036980 ) ) ;
#11784=CARTESIAN_POINT ( 'NONE',  ( 5.344403403599800484, 63.98653430214261562, -12.39707219021102347 ) ) ;
#11785=CARTESIAN_POINT ( 'NONE',  ( 5.813490055168404780, 42.96841201847881564, -12.18495851764158111 ) ) ;
#11786=CARTESIAN_POINT ( 'NONE',  ( 12.95529851766885265, 39.29347969363125515, 3.812543400925126669 ) ) ;
#11788=CARTESIAN_POINT ( 'NONE',  ( 1.653273178848926472E-15, 80.93000000000000682, 13.50000000000000000 ) ) ;
#11789=CARTESIAN_POINT ( 'NONE',  ( -5.360921580443687162, 70.37408821014601301, -12.39000541084428875 ) ) ;
#11790=CARTESIAN_POINT ( 'NONE',  ( -11.53742970777352106, 61.66777873792855758, -7.029701866567251933 ) ) ;
#11792=EDGE_LOOP ( 'NONE', ( #11270, #17187, #5716, #10597 ) ) ;
#11793=CARTESIAN_POINT ( 'NONE',  ( -8.101227806547106169, 40.48742319736930995, -10.79914935875280868 ) ) ;
#11794=VERTEX_POINT ( 'NONE', #2522 ) ;
#11797=CARTESIAN_POINT ( 'NONE',  ( 5.060896339973242064, 47.86270747902148059, 12.51549536631464754 ) ) ;
#11798=CARTESIAN_POINT ( 'NONE',  ( 12.77833647190731092, 57.27053577403307827, 4.428673400738554200 ) ) ;
#11799=CARTESIAN_POINT ( 'NONE',  ( 12.15329104187025955, 78.64596498996522200, -5.877850047516828269 ) ) ;
#11800=ADVANCED_FACE ( 'NONE', ( #13240 ), #15964, .T. ) ;
#11801=CARTESIAN_POINT ( 'NONE',  ( -11.76794919243112325, 77.92999999999999261, -2.882316262207890869E-15 ) ) ;
#11802=CARTESIAN_POINT ( 'NONE',  ( -11.76794919243112325, 74.78000000000000114, -3.823638476888998827 ) ) ;
#11804=CARTESIAN_POINT ( 'NONE',  ( 0.000000000000000000, 75.00000000000000000, 5.000000000000000000 ) ) ;
#11806=CARTESIAN_POINT ( 'NONE',  ( 2.445080149700053643E-15, 63.17999999999998550, -13.50000000000000000 ) ) ;
#11809=CARTESIAN_POINT ( 'NONE',  ( -13.37510790282587081, 73.86589262026581082, -1.834146428142618301 ) ) ;
#11810=EDGE_LOOP ( 'NONE', ( #7827, #11700, #1638, #3845 ) ) ;
#11817=CARTESIAN_POINT ( 'NONE',  ( -5.930465559976500600, 44.46394333671532451, 12.13728569908712451 ) ) ;
#11819=CARTESIAN_POINT ( 'NONE',  ( 9.909898397854359331, 66.78548077375248226, -9.167550852036580267 ) ) ;
#11820=CARTESIAN_POINT ( 'NONE',  ( 10.92172942406178926, 54.12999999999999545, 7.935100905948387684 ) ) ;
#11821=CARTESIAN_POINT ( 'NONE',  ( -3.239062113971910684, 71.56354731355079934, 13.10570111947281369 ) ) ;
#11823=CARTESIAN_POINT ( 'NONE',  ( -13.49575779976988343, 67.94255581264309285, 0.3657745621878383813 ) ) ;
#11825=CARTESIAN_POINT ( 'NONE',  ( 7.886035413494550284, 54.88256797924555030, -10.96628294449290308 ) ) ;
#11829=CARTESIAN_POINT ( 'NONE',  ( -11.44341903511235792, 65.19769748763089012, 7.162640882872341130 ) ) ;
#11831=CARTESIAN_POINT ( 'NONE',  ( -4.326545005012490286, 35.52442011644006925, 12.78817203166833316 ) ) ;
#11832=ORIENTED_EDGE ( 'NONE', *, *, #17256, .T. ) ;
#11834=CARTESIAN_POINT ( 'NONE',  ( -2.851258122864091415, 40.28252070923673500, -13.19546944467250960 ) ) ;
#11835=CARTESIAN_POINT ( 'NONE',  ( -12.87226159753149268, 32.07661166022045052, 4.082475368119833803 ) ) ;
#11836=CARTESIAN_POINT ( 'NONE',  ( 0.5300433235337840276, 73.16094159698265287, -13.48959140114411781 ) ) ;
#11837=CARTESIAN_POINT ( 'NONE',  ( 11.64793254230706232, 60.17604334945948352, 6.824638435576549256 ) ) ;
#11840=CARTESIAN_POINT ( 'NONE',  ( -3.336379296991717869, 53.56006013931011722, 13.08240930115279710 ) ) ;
#11842=CARTESIAN_POINT ( 'NONE',  ( 11.76794919243112325, 61.42999999999999972, 1.441158131103945434E-15 ) ) ;
#11844=CARTESIAN_POINT ( 'NONE',  ( 13.49999999999999822, 74.28000000000000114, 4.386415899144237684 ) ) ;
#11845=CARTESIAN_POINT ( 'NONE',  ( 13.02289043530450208, 51.30254417723856619, 3.567633519790383900 ) ) ;
#11846=CARTESIAN_POINT ( 'NONE',  ( -11.60693306515659984, 38.18798383908444549, 6.929076632654524559 ) ) ;
#11847=CARTESIAN_POINT ( 'NONE',  ( 12.13964550287791866, 36.64708739272366245, -5.907247546172663455 ) ) ;
#11849=CARTESIAN_POINT ( 'NONE',  ( -5.165543354712239577, 74.49330207109468915, 12.47278248272050050 ) ) ;
#11850=CARTESIAN_POINT ( 'NONE',  ( -12.13837278097153849, 77.14717783657690120, 5.908462373232763909 ) ) ;
#11851=CARTESIAN_POINT ( 'NONE',  ( -6.434411898208869829, 80.44366145310867466, 11.86853559793800450 ) ) ;
#11852=CARTESIAN_POINT ( 'NONE',  ( 7.500000000000000888, 104.9266221009244191, -8.932545650451682917 ) ) ;
#11857=CARTESIAN_POINT ( 'NONE',  ( 7.272992578804308828, 54.98000000000000398, 10.01041549318726886 ) ) ;
#11859=CARTESIAN_POINT ( 'NONE',  ( 13.49999999999999822, 56.27999999999999403, 4.386415899144236796 ) ) ;
#11861=CARTESIAN_POINT ( 'NONE',  ( 10.71234848535828199, 75.74200647849511370, -8.215984252163476498 ) ) ;
#11863=CARTESIAN_POINT ( 'NONE',  ( 13.50000000000000000, 68.43000000000000682, 1.653273178848926867E-15 ) ) ;
#11864=CARTESIAN_POINT ( 'NONE',  ( 4.171729424061791924, 70.03000000000000114, -12.83926296998457239 ) ) ;
#11865=CARTESIAN_POINT ( 'NONE',  ( 3.636496289402157078, 38.03000000000000114, -11.19198476289190936 ) ) ;
#11866=DIRECTION ( 'NONE',  ( 0.000000000000000000, -1.000000000000000000, 0.000000000000000000 ) ) ;
#11867=CARTESIAN_POINT ( 'NONE',  ( -13.21369905157459890, 59.02775396092354043, 2.765669001886426059 ) ) ;
#11868=CARTESIAN_POINT ( 'NONE',  ( 9.058805526620455240, 45.03196713883374969, 10.00967056491867524 ) ) ;
#11869=CARTESIAN_POINT ( 'NONE',  ( 12.88435061792157832, 69.28518360341051618, 4.034773658741488411 ) ) ;
#11870=DIRECTION ( 'NONE',  ( 0.000000000000000000, -1.000000000000000000, 0.000000000000000000 ) ) ;
#11871=CARTESIAN_POINT ( 'NONE',  ( -4.007836095776672991, 55.32410577306614385, -12.89143502976331312 ) ) ;
#11872=CARTESIAN_POINT ( 'NONE',  ( -8.587248194232895315, 50.35035759758954299, 10.41677944331643602 ) ) ;
#11874=CARTESIAN_POINT ( 'NONE',  ( 10.52133674883681813, 42.75279131939787902, -8.462481817991241329 ) ) ;
#11875=CARTESIAN_POINT ( 'NONE',  ( 10.04801546086567399, 39.08131876964824158, 9.027590569278633126 ) ) ;
#11877=CARTESIAN_POINT ( 'NONE',  ( -6.953862414529842439, 70.43748566701286506, -11.58376311006115422 ) ) ;
#11878=CARTESIAN_POINT ( 'NONE',  ( -9.987088467865099517, 61.57852760064511699, -9.083992418538327840 ) ) ;
#11885=CARTESIAN_POINT ( 'NONE',  ( 0.6915575771887298995, 47.70484266932048456, 13.50000000000285461 ) ) ;
#11886=ADVANCED_FACE ( 'NONE', ( #2434, #12981 ), #9284, .F. ) ;
#11887=CARTESIAN_POINT ( 'NONE',  ( 12.45313895046523811, 57.24012120377358315, 5.212443691823386516 ) ) ;
#11888=CARTESIAN_POINT ( 'NONE',  ( -3.636496289402153081, 71.32999999999999829, -11.19198476289190936 ) ) ;
#11889=CARTESIAN_POINT ( 'NONE',  ( 2.272985001014427788E-15, 74.17999999999997840, -12.37355403259654985 ) ) ;
#11890=CARTESIAN_POINT ( 'NONE',  ( -0.3885106188271407746, 47.66603124818684734, 13.49448874308720114 ) ) ;
#11891=CARTESIAN_POINT ( 'NONE',  ( 10.92172942406179104, 41.72999999999999687, -7.935100905948385908 ) ) ;
#11892=DIRECTION ( 'NONE',  ( -6.302562568933760152E-16, -1.000000000000000000, -0.000000000000000000 ) ) ;
#11894=CARTESIAN_POINT ( 'NONE',  ( 2.138189944381280405, 43.75688142232026223, 13.49999999999998579 ) ) ;
#11895=CARTESIAN_POINT ( 'NONE',  ( 7.448728434142215526, 33.90129485598647108, -11.26199948916008786 ) ) ;
#11896=CARTESIAN_POINT ( 'NONE',  ( -2.293477329192559644, 73.26246498174589306, -13.30375830701482087 ) ) ;
#11902=CARTESIAN_POINT ( 'NONE',  ( -9.960433271135549660, 44.28289197857108661, 9.113836154488136998 ) ) ;
#11904=CARTESIAN_POINT ( 'NONE',  ( 9.771573629660572635, 66.79262956996798550, -9.315150575223826834 ) ) ;
#11905=CARTESIAN_POINT ( 'NONE',  ( 4.171729424061791924, 40.02999999999999403, -12.83926296998457239 ) ) ;
#11906=CARTESIAN_POINT ( 'NONE',  ( -10.23977083959674061, 71.26919422278727723, 8.841254286924575823 ) ) ;
#11908=CARTESIAN_POINT ( 'NONE',  ( -11.89252447053387307, 68.16661037567293135, 6.393518228508523471 ) ) ;
#11910=AXIS2_PLACEMENT_3D ( 'NONE', #10192, #2109, #7536 ) ;
#11911=CARTESIAN_POINT ( 'NONE',  ( 5.839258915127627070, 54.96742705686380503, -12.17263519449883091 ) ) ;
#11913=CARTESIAN_POINT ( 'NONE',  ( -12.92492960912350597, 65.06980143740064193, 3.900769340635460214 ) ) ;
#11914=CARTESIAN_POINT ( 'NONE',  ( -1.609292034251611714, 35.62213402059252587, 13.40373931015559172 ) ) ;
#11917=DIRECTION ( 'NONE',  ( 0.000000000000000000, 1.000000000000000000, 0.000000000000000000 ) ) ;
#11919=CARTESIAN_POINT ( 'NONE',  ( -5.519902694494632556, 31.38019316832627581, -12.31995397698188022 ) ) ;
#11920=DIRECTION ( 'NONE',  ( 0.000000000000000000, 0.000000000000000000, 1.000000000000000000 ) ) ;
#11921=CARTESIAN_POINT ( 'NONE',  ( 11.63721506080949020, 60.17530159522576838, 6.842919234061048073 ) ) ;
#11922=CARTESIAN_POINT ( 'NONE',  ( -3.892879492245595152, 53.54002628341550718, 12.92654989019562883 ) ) ;
#11923=CARTESIAN_POINT ( 'NONE',  ( 11.76794919243112680, 58.57999999999999119, -3.823638476888993942 ) ) ;
#11924=CARTESIAN_POINT ( 'NONE',  ( -10.92172942406179104, 73.23000000000000398, 7.935100905948387684 ) ) ;
#11925=CARTESIAN_POINT ( 'NONE',  ( 10.68360996784106121, 51.11635650885985882, 8.252908712777312417 ) ) ;
#11926=CARTESIAN_POINT ( 'NONE',  ( -13.10880650276811465, 37.81520070515529142, -3.229914644386858491 ) ) ;
#11927=CARTESIAN_POINT ( 'NONE',  ( 13.04805342603775742, 36.30564934951262757, 3.492309041391611579 ) ) ;
#11930=CARTESIAN_POINT ( 'NONE',  ( -6.108332572802023464, 74.45675329115508134, 12.03905252150416771 ) ) ;
#11931=CARTESIAN_POINT ( 'NONE',  ( -2.202876632959991809, 77.60068045598771391, 13.32638450149024045 ) ) ;
#11932=CARTESIAN_POINT ( 'NONE',  ( -12.00843261896035052, 79.70224609130038118, -6.172195262188137299 ) ) ;
#11934=DIRECTION ( 'NONE',  ( 0.000000000000000000, -1.000000000000000000, 0.000000000000000000 ) ) ;
#11937=ORIENTED_EDGE ( 'NONE', *, *, #12229, .F. ) ;
#11938=CARTESIAN_POINT ( 'NONE',  ( -7.272992578804310604, 57.37999999999999545, 10.01041549318726886 ) ) ;
#11943=CARTESIAN_POINT ( 'NONE',  ( 6.388575815097190969, 75.94550667101978547, -11.89345360526400341 ) ) ;
#11944=CARTESIAN_POINT ( 'NONE',  ( 13.50000000000000355, 32.57999999999999119, -4.386415899144233244 ) ) ;
#11945=CARTESIAN_POINT ( 'NONE',  ( 10.92172942406178926, 75.12999999999999545, 7.935100905948387684 ) ) ;
#11946=CARTESIAN_POINT ( 'NONE',  ( -7.272992578804307939, 44.47999999999999687, -10.01041549318726886 ) ) ;
#11949=CARTESIAN_POINT ( 'NONE',  ( -10.61093645061555257, 58.61191818804664422, -8.349755948771326430 ) ) ;
#11950=DIRECTION ( 'NONE',  ( 0.000000000000000000, 0.000000000000000000, 1.000000000000000000 ) ) ;
#11951=CARTESIAN_POINT ( 'NONE',  ( 10.80743988185431270, 69.73672264826443268, -8.091202902239265526 ) ) ;
#11954=CARTESIAN_POINT ( 'NONE',  ( -11.75435161585808785, 55.68303527114955642, -6.650987819685640901 ) ) ;
#11955=EDGE_CURVE ( 'NONE', #1729, #12392, #5255, .T. ) ;
#11956=CARTESIAN_POINT ( 'NONE',  ( -12.68856319678013733, 50.09667819037224490, 4.610493161354706437 ) ) ;
#11957=CARTESIAN_POINT ( 'NONE',  ( 13.38071212497846751, 63.49259793051759004, -1.791777274255796248 ) ) ;
#11958=CARTESIAN_POINT ( 'NONE',  ( 9.938623679662498489, 42.78404089153169565, -9.138168626435373199 ) ) ;
#11959=CARTESIAN_POINT ( 'NONE',  ( 11.09090470402770201, 39.14001624768924614, 7.697158664951603946 ) ) ;
#11960=EDGE_LOOP ( 'NONE', ( #14976, #12082 ) ) ;
#11961=CARTESIAN_POINT ( 'NONE',  ( -9.884595526216783057, 70.57320152317427642, -9.194823709309879689 ) ) ;
#11962=CARTESIAN_POINT ( 'NONE',  ( -10.06711309424234990, 61.58274721441556210, -8.994624661598212612 ) ) ;
#11968=CARTESIAN_POINT ( 'NONE',  ( 3.106396304733963554, 61.06830536267598575, -13.13775590234083879 ) ) ;
#11970=CARTESIAN_POINT ( 'NONE',  ( 13.39815693410163000, 57.37226897754249677, 1.655122989353433605 ) ) ;
#11971=CARTESIAN_POINT ( 'NONE',  ( -7.576616670048093940E-16, 72.68000000000000682, 12.37355403259654985 ) ) ;
#11972=CARTESIAN_POINT ( 'NONE',  ( -9.520470885617715595, 74.62999999999999545, -6.917026985038136289 ) ) ;
#11973=CARTESIAN_POINT ( 'NONE',  ( -11.35926100027876551, 47.20325402242907842, 7.295012114585781582 ) ) ;
#11974=CARTESIAN_POINT ( 'NONE',  ( 4.171729424061791924, 39.03000000000000114, -12.83926296998457239 ) ) ;
#11979=CARTESIAN_POINT ( 'NONE',  ( 1.117928010715994125, 34.13984769869428249, -13.46164090031036054 ) ) ;
#11980=CARTESIAN_POINT ( 'NONE',  ( -3.636291849404581722, 73.31075916562413397, -13.00105766639911131 ) ) ;
#11981=ORIENTED_EDGE ( 'NONE', *, *, #8720, .T. ) ;
#11983=CARTESIAN_POINT ( 'NONE',  ( -11.76794919243112325, 75.08000000000001251, 3.823638476888994830 ) ) ;
#11987=CARTESIAN_POINT ( 'NONE',  ( -4.198563671053442192, 44.52903422088949270, 12.83079698937739721 ) ) ;
#11989=CARTESIAN_POINT ( 'NONE',  ( 13.50000000000000355, 39.57999999999998408, -4.386415899144233244 ) ) ;
#11990=CARTESIAN_POINT ( 'NONE',  ( -3.129712353247879442, 71.56746715821304861, 13.13221255258535258 ) ) ;
#11991=CLOSED_SHELL ( 'NONE', ( #1244, #8180, #4618, #4641, #12453, #15504, #2931, #6333, #9619, #3684, #11800, #12772, #9216, #16572, #13225, #1714, #10351, #12502, #13343, #2589, #11105, #5058, #4993, #11521, #519, #15525, #2952, #15406, #8797, #10013, #8298, #16063, #15848, #6733, #14666, #6241, #11345, #9703, #13304, #13748, #10308, #15947, #5358, #1524, #1444, #7537, #7054, #9115, #1366, #16614, #1344, #16593, #11039, #13561, #11886, #5683, #2335, #2138, #17428, #9183, #13769, #6079 ) ) ;
#11993=CARTESIAN_POINT ( 'NONE',  ( -13.49018641668098617, 67.94809635601976083, 0.5259755334716053055 ) ) ;
#11995=CARTESIAN_POINT ( 'NONE',  ( 0.5919370610761245377, 55.15871612706705918, -13.49999999834249387 ) ) ;
#11997=CARTESIAN_POINT ( 'NONE',  ( -13.47392021138490215, 64.90062200235198020, -0.8468760602646752123 ) ) ;
#11998=CARTESIAN_POINT ( 'NONE',  ( -9.401475381598739745, 35.31127215530875674, 9.688255670132432940 ) ) ;
#12000=ORIENTED_EDGE ( 'NONE', *, *, #12859, .F. ) ;
#12002=CARTESIAN_POINT ( 'NONE',  ( -9.286222281767340547, 31.54266391133846881, -9.816746840912003336 ) ) ;
#12005=CARTESIAN_POINT ( 'NONE',  ( 3.358410185994296082, 59.80067827238347888, 13.07579168776377010 ) ) ;
#12007=CARTESIAN_POINT ( 'NONE',  ( -11.05360854115534863, 53.22221651762638572, 7.750340433578712052 ) ) ;
#12009=CARTESIAN_POINT ( 'NONE',  ( -11.76794919243112325, 51.07999999999999829, 3.823638476888994386 ) ) ;
#12011=CARTESIAN_POINT ( 'NONE',  ( -13.50000000000000000, 66.93000000000000682, -3.306546357697853733E-15 ) ) ;
#12012=CARTESIAN_POINT ( 'NONE',  ( 3.316253209170452632, 50.79922521005602221, 13.08634827626489638 ) ) ;
#12013=CARTESIAN_POINT ( 'NONE',  ( -10.17240047902380873, 37.58838810588826362, -8.875558754972354691 ) ) ;
#12014=CARTESIAN_POINT ( 'NONE',  ( 9.214156735519342334, 36.03950685236531370, 9.866582668058638816 ) ) ;
#12018=CARTESIAN_POINT ( 'NONE',  ( -13.29873604195502601, 76.84834518085253308, -2.322416864990943353 ) ) ;
#12019=CARTESIAN_POINT ( 'NONE',  ( -8.740861150229537913, 80.34329372878345055, 10.29062010435449359 ) ) ;
#12023=CARTESIAN_POINT ( 'NONE',  ( -7.576616670048093940E-16, 51.68000000000000682, 12.37355403259654807 ) ) ;
#12027=CARTESIAN_POINT ( 'NONE',  ( 13.49999999999999822, 35.28000000000000114, 4.386415899144236796 ) ) ;
#12028=CARTESIAN_POINT ( 'NONE',  ( 10.56020146213972311, 75.75055865699756907, -8.410247565123782465 ) ) ;
#12029=CARTESIAN_POINT ( 'NONE',  ( 2.445080149700053643E-15, 33.17999999999999261, -13.50000000000000000 ) ) ;
#12031=CARTESIAN_POINT ( 'NONE',  ( -11.76794919243112325, 36.08000000000000540, 3.823638476888994386 ) ) ;
#12032=CARTESIAN_POINT ( 'NONE',  ( -4.258041676676088017, 41.52689555004522504, 12.81095024554207740 ) ) ;
#12033=CARTESIAN_POINT ( 'NONE',  ( -8.534716217167439112, 58.50719729932798430, -10.46066808379417701 ) ) ;
#12034=DIRECTION ( 'NONE',  ( 0.000000000000000000, 1.000000000000000000, 0.000000000000000000 ) ) ;
#12035=CARTESIAN_POINT ( 'NONE',  ( 2.138189944381220897, 60.10311857767972299, -13.50000000000000355 ) ) ;
#12037=CARTESIAN_POINT ( 'NONE',  ( -6.432409982582727892, 55.41626211658963541, -11.87138287464854258 ) ) ;
#12038=CARTESIAN_POINT ( 'NONE',  ( -10.15313977396370504, 49.58728767534731219, -8.897419797724348101 ) ) ;
#12039=CARTESIAN_POINT ( 'NONE',  ( 9.916447128233048858, 63.78514480093842565, -9.160676570550608133 ) ) ;
#12040=CARTESIAN_POINT ( 'NONE',  ( 6.825507540484397673, 42.92779699185432918, -11.65901476425138839 ) ) ;
#12041=CARTESIAN_POINT ( 'NONE',  ( 13.31319243190779389, 39.35139063027423845, 2.238058999171629981 ) ) ;
#12044=CARTESIAN_POINT ( 'NONE',  ( -10.95763016649321919, 70.63148440308884801, -7.897661228886724061 ) ) ;
#12051=CARTESIAN_POINT ( 'NONE',  ( 4.764356863092740646, 61.00836482418741014, -12.63134666390240213 ) ) ;
#12053=CARTESIAN_POINT ( 'NONE',  ( 7.954458010882204277, 71.98083086217984317, 10.90864659553976956 ) ) ;
#12054=CARTESIAN_POINT ( 'NONE',  ( 12.33862782127885716, 57.22973384493053572, 5.479451552045422780 ) ) ;
#12055=CARTESIAN_POINT ( 'NONE',  ( 9.520470885617717371, 67.73000000000000398, -6.917026985038131848 ) ) ;
#12056=CARTESIAN_POINT ( 'NONE',  ( -9.520470885617717371, 72.23000000000000398, 6.917026985038133624 ) ) ;
#12058=CARTESIAN_POINT ( 'NONE',  ( -3.653058138417871081, 47.54865290029032110, 12.99660501964011594 ) ) ;
#12059=CARTESIAN_POINT ( 'NONE',  ( 0.000000000000000000, 102.9300000000000068, 0.000000000000000000 ) ) ;
#12061=CARTESIAN_POINT ( 'NONE',  ( -10.92172942406179104, 34.22999999999999687, 7.935100905948387684 ) ) ;
#12063=LINE ( 'NONE', #5183, #17116 ) ;
#12064=CARTESIAN_POINT ( 'NONE',  ( 12.99666601036235036, 33.56048209808822236, -3.652216699307488046 ) ) ;
#12065=CARTESIAN_POINT ( 'NONE',  ( -1.717801689700091616, 73.24174962197940886, -13.39190774218556612 ) ) ;
#12067=ORIENTED_EDGE ( 'NONE', *, *, #9795, .T. ) ;
#12068=CARTESIAN_POINT ( 'NONE',  ( 9.520470885617715595, 73.12999999999999545, 6.917026985038134512 ) ) ;
#12069=EDGE_LOOP ( 'NONE', ( #8435, #15586, #3225, #9157 ) ) ;
#12073=CARTESIAN_POINT ( 'NONE',  ( -8.691771469529815392E-16, 41.67999999999998550, 14.19474002721660355 ) ) ;
#12074=CARTESIAN_POINT ( 'NONE',  ( -13.37080425425743968, 70.99696510027449392, 1.915368337129497833 ) ) ;
#12076=CARTESIAN_POINT ( 'NONE',  ( -12.71100910673158246, 67.76566160515973536, -4.549615297461226504 ) ) ;
#12078=CARTESIAN_POINT ( 'NONE',  ( 11.66531418640665407, 54.17725219472052345, 6.794926229372841853 ) ) ;
#12079=DIRECTION ( 'NONE',  ( 0.000000000000000000, 0.000000000000000000, -1.000000000000000000 ) ) ;
#12080=CARTESIAN_POINT ( 'NONE',  ( -13.28285221338691890, 64.84474501369872712, -2.423398101427317819 ) ) ;
#12081=CARTESIAN_POINT ( 'NONE',  ( -12.88515085615131639, 35.07508799605628980, 4.041843465557555248 ) ) ;
#12082=ORIENTED_EDGE ( 'NONE', *, *, #15601, .F. ) ;
#12083=DIRECTION ( 'NONE',  ( 0.000000000000000000, 0.000000000000000000, -1.000000000000000000 ) ) ;
#12084=CARTESIAN_POINT ( 'NONE',  ( -6.905685108143932105, 31.43550380796823873, -11.61237663357330341 ) ) ;
#12085=CARTESIAN_POINT ( 'NONE',  ( 4.867973651388805223, 73.00457954580815567, -12.59203443152197721 ) ) ;
#12087=CARTESIAN_POINT ( 'NONE',  ( 3.238893374653856849, 59.79645227764538618, 13.10570931148826013 ) ) ;
#12089=CARTESIAN_POINT ( 'NONE',  ( -11.95953986185622320, 53.16127550200973673, 6.262611427032776845 ) ) ;
#12091=CARTESIAN_POINT ( 'NONE',  ( 3.636496289402157078, 47.02999999999999403, -11.19198476289190936 ) ) ;
#12092=SHAPE_DEFINITION_REPRESENTATION ( #6503, #10992 ) ;
#12093=CARTESIAN_POINT ( 'NONE',  ( 2.607531440858944223E-15, 69.18000000000000682, -14.19474002721660355 ) ) ;
#12094=CARTESIAN_POINT ( 'NONE',  ( 11.77664224129239834, 51.18329203575517283, 6.664799459490041933 ) ) ;
#12095=CARTESIAN_POINT ( 'NONE',  ( -6.481058573409227641, 37.41816792217149157, -11.84851559884859462 ) ) ;
#12096=CARTESIAN_POINT ( 'NONE',  ( 8.224471913408319068, 35.99288207254014083, 10.71476016740036563 ) ) ;
#12098=CARTESIAN_POINT ( 'NONE',  ( -11.29150227822014152, 74.20758383959375237, 7.399465225293304194 ) ) ;
#12099=CARTESIAN_POINT ( 'NONE',  ( -12.51871653938473195, 76.74630541835415443, -5.052900597489689893 ) ) ;
#12100=CARTESIAN_POINT ( 'NONE',  ( -13.45670837459887359, 79.96812659038552340, 1.102554880423010308 ) ) ;
#12102=CARTESIAN_POINT ( 'NONE',  ( 7.500000000000000888, 107.2300670966469625, 6.927727048493004247 ) ) ;
#12105=CARTESIAN_POINT ( 'NONE',  ( -3.636496289402155746, 48.52999999999999403, 11.19198476289190936 ) ) ;
#12109=CARTESIAN_POINT ( 'NONE',  ( -12.01298688515180757, 40.70272110868870641, -6.163212580704716892 ) ) ;
#12111=CARTESIAN_POINT ( 'NONE',  ( 5.701800690820812534, 75.97265264077142888, -12.23843519416455550 ) ) ;
#12112=DIRECTION ( 'NONE',  ( 0.000000000000000000, 0.000000000000000000, -1.000000000000000000 ) ) ;
#12113=( BOUNDED_CURVE ( )  B_SPLINE_CURVE ( 2, ( #8756, #12804, #1998, #15094, #1913, #11483, #11568, #16858, #8843, #3244, #14199, #2081, #8667 ),
 .UNSPECIFIED., .F., .F. ) 
 B_SPLINE_CURVE_WITH_KNOTS ( ( 3, 2, 2, 2, 2, 2, 3 ),
 ( 0.2361111111111111049, 0.2388888888888889006, 0.2444444444444444364, 0.2500000000000000000, 0.2555555555555555358, 0.2611111111111111271, 0.2638888888888888951 ),
 .UNSPECIFIED. ) 
 CURVE ( )  GEOMETRIC_REPRESENTATION_ITEM ( )  RATIONAL_B_SPLINE_CURVE ( ( 0.9755282581475765991, 0.9755282581475765991, 1.000000000000000000, 0.9510565162951535312, 1.000000000000000000, 0.9510565162951535312, 1.000000000000000000, 0.9510565162951535312, 1.000000000000000000, 0.9510565162951535312, 1.000000000000000000, 0.9755282581475768211, 0.9755282581475768211 ) ) 
 REPRESENTATION_ITEM ( '' )  );
#12114=CARTESIAN_POINT ( 'NONE',  ( -7.576616670048093940E-16, 39.67999999999999261, 12.37355403259654985 ) ) ;
#12115=CARTESIAN_POINT ( 'NONE',  ( -11.18038004580210121, 41.21451517937148878, 7.566320479137822019 ) ) ;
#12116=CARTESIAN_POINT ( 'NONE',  ( -5.755473554220444932, 58.38933414821598689, -12.21165709677288014 ) ) ;
#12118=FACE_OUTER_BOUND ( 'NONE', #6232, .T. ) ;
#12122=CARTESIAN_POINT ( 'NONE',  ( -9.962969835881040126, 49.57729431268386122, -9.110904113917294822 ) ) ;
#12123=CARTESIAN_POINT ( 'NONE',  ( 13.40375923506036315, 63.48631738253013168, -1.615599257011282042 ) ) ;
#12124=CARTESIAN_POINT ( 'NONE',  ( 12.20577700513132946, 42.64168893067194688, -5.771419099262523389 ) ) ;
#12125=CARTESIAN_POINT ( 'NONE',  ( 4.286075472464928815, 38.83412300064772893, 12.80155259534364376 ) ) ;
#12126=ORIENTED_EDGE ( 'NONE', *, *, #15163, .F. ) ;
#12129=ORIENTED_EDGE ( 'NONE', *, *, #8957, .F. ) ;
#12133=CARTESIAN_POINT ( 'NONE',  ( 8.763194653383337140, 60.84238623439762961, -10.27162055150819064 ) ) ;
#12135=CARTESIAN_POINT ( 'NONE',  ( 10.57835835680828929, 72.11049049234127040, 8.387854446822782251 ) ) ;
#12136=CARTESIAN_POINT ( 'NONE',  ( 11.70212564305006353, 57.68033890375173200, -6.734146581967513256 ) ) ;
#12137=CARTESIAN_POINT ( 'NONE',  ( 7.272992578804311492, 67.87999999999999545, -10.01041549318726709 ) ) ;
#12138=CARTESIAN_POINT ( 'NONE',  ( -7.272992578804310604, 78.38000000000000966, 10.01041549318726709 ) ) ;
#12139=CARTESIAN_POINT ( 'NONE',  ( -4.903230271211689306, 47.50310532243074135, 12.58596196147269808 ) ) ;
#12141=CARTESIAN_POINT ( 'NONE',  ( 10.92172942406179104, 74.73000000000000398, -7.935100905948385908 ) ) ;
#12143=CARTESIAN_POINT ( 'NONE',  ( -13.49999999999999822, 76.07999999999999829, 4.386415899144235020 ) ) ;
#12146=VECTOR ( 'NONE', #2948, 1000.000000000000000 ) ;
#12147=CARTESIAN_POINT ( 'NONE',  ( 11.27325719286469230, 33.70873714612665140, -7.427241792320101510 ) ) ;
#12148=CARTESIAN_POINT ( 'NONE',  ( -5.014217190436002447, 73.36095352106737266, -12.53426255818751933 ) ) ;
#12149=ORIENTED_EDGE ( 'NONE', *, *, #6438, .F. ) ;
#12151=ORIENTED_EDGE ( 'NONE', *, *, #15881, .T. ) ;
#12154=ORIENTED_EDGE ( 'NONE', *, *, #4516, .F. ) ;
#12158=CARTESIAN_POINT ( 'NONE',  ( -8.691771469529815392E-16, 47.67999999999999972, 14.19474002721660355 ) ) ;
#12159=CARTESIAN_POINT ( 'NONE',  ( -13.49999999999999822, 49.07999999999999829, 4.386415899144235908 ) ) ;
#12160=CARTESIAN_POINT ( 'NONE',  ( -13.39839221111840750, 70.87233709335372112, -1.653208847849865215 ) ) ;
#12163=CARTESIAN_POINT ( 'NONE',  ( -12.07707027602519112, 68.15293157428645543, 6.055626961436693101 ) ) ;
#12165=CARTESIAN_POINT ( 'NONE',  ( 12.98848230150326621, 54.56155940439027319, -3.680959392705737798 ) ) ;
#12168=CARTESIAN_POINT ( 'NONE',  ( -13.46209291828269983, 64.89500517973988281, -1.010990238245216943 ) ) ;
#12169=EDGE_CURVE ( 'NONE', #2917, #5695, #16362, .T. ) ;
#12170=CARTESIAN_POINT ( 'NONE',  ( -12.47073097209211667, 35.11824904818834625, 5.170595160201629348 ) ) ;
#12174=CARTESIAN_POINT ( 'NONE',  ( -10.97962057844975270, 31.63274308883676156, -7.866999682609990607 ) ) ;
#12175=CARTESIAN_POINT ( 'NONE',  ( 5.975404689433335470, 72.96202560524248781, -12.10557300981717610 ) ) ;
#12179=CARTESIAN_POINT ( 'NONE',  ( -12.78222371368175914, 52.77349219538730551, -4.343505285234531499 ) ) ;
#12180=CARTESIAN_POINT ( 'NONE',  ( 7.272992578804311492, 46.87999999999998835, -10.01041549318726709 ) ) ;
#12181=CARTESIAN_POINT ( 'NONE',  ( -13.49999999999999822, 66.78000000000001535, -4.386415899144240349 ) ) ;
#12182=CARTESIAN_POINT ( 'NONE',  ( 3.303023401292605854, 50.79875792230046017, 13.08969376897518266 ) ) ;
#12183=CARTESIAN_POINT ( 'NONE',  ( -11.52100015834348490, 37.66715461419663313, -7.042761957645991444 ) ) ;
#12184=CARTESIAN_POINT ( 'NONE',  ( 4.071488193451239468, 35.82639234911870574, 12.87155199998092314 ) ) ;
#12186=CARTESIAN_POINT ( 'NONE',  ( -11.27694939588988099, 74.20849020820207897, 7.421620996757082978 ) ) ;
#12187=CARTESIAN_POINT ( 'NONE',  ( -9.953402372925438613, 76.57636814536873260, -9.131542486324162766 ) ) ;
#12188=EDGE_CURVE ( 'NONE', #13982, #13489, #3149, .T. ) ;
#12189=CARTESIAN_POINT ( 'NONE',  ( -6.552499304188867058, 79.42106022813749178, -11.80367691769144578 ) ) ;
#12190=CARTESIAN_POINT ( 'NONE',  ( -10.16154112308408664, 80.92999999999997840, 6.935345943047934725 ) ) ;
#12193=CARTESIAN_POINT ( 'NONE',  ( -7.576616670048093940E-16, 45.67999999999999261, 12.37355403259654807 ) ) ;
#12197=CARTESIAN_POINT ( 'NONE',  ( -11.90770218001530978, 40.69479922003479544, -6.360556165360144121 ) ) ;
#12200=CARTESIAN_POINT ( 'NONE',  ( 10.23922769745222006, 75.09193609827978833, 8.798267285036342145 ) ) ;
#12202=CARTESIAN_POINT ( 'NONE',  ( -2.104796621658385103, 41.60471069576241376, 13.35964989392017266 ) ) ;
#12203=CARTESIAN_POINT ( 'NONE',  ( -4.329453876402491019, 58.33570365221549281, -12.78742087842741881 ) ) ;
#12204=CARTESIAN_POINT ( 'NONE',  ( 3.025992313210662754, 44.78877108066809853, 13.15667717828717365 ) ) ;
#12205=CARTESIAN_POINT ( 'NONE',  ( 0.000000000000000000, 80.93000000000000682, 0.000000000000000000 ) ) ;
#12206=DIRECTION ( 'NONE',  ( 0.000000000000000000, -0.000000000000000000, -1.000000000000000000 ) ) ;
#12207=DIRECTION ( 'NONE',  ( 0.000000000000000000, 0.000000000000000000, -1.000000000000000000 ) ) ;
#12208=CARTESIAN_POINT ( 'NONE',  ( -11.75516853449998855, 49.68309035655853734, -6.649812433528813571 ) ) ;
#12209=CARTESIAN_POINT ( 'NONE',  ( 13.47201310395382201, 63.39998930646792275, 0.8689103304181599041 ) ) ;
#12210=CARTESIAN_POINT ( 'NONE',  ( 12.21953790584814570, 42.21938887054512435, 5.740768505231178764 ) ) ;
#12212=VERTEX_POINT ( 'NONE', #12403 ) ;
#12217=CARTESIAN_POINT ( 'NONE',  ( -7.856066726180596760, 43.47605057973713372, -11.00250018620803161 ) ) ;
#12218=CARTESIAN_POINT ( 'NONE',  ( -7.499999999999999112, 107.2300670966469340, -6.927727048493005135 ) ) ;
#12219=CARTESIAN_POINT ( 'NONE',  ( 9.199277144405600737, 60.82129824580783861, -9.880725865329580415 ) ) ;
#12220=( BOUNDED_CURVE ( )  B_SPLINE_CURVE ( 2, ( #13840, #7154, #12539, #12884, #8751, #3423, #16938, #937, #3505, #14277, #1993, #772, #3590 ),
 .UNSPECIFIED., .F., .F. ) 
 B_SPLINE_CURVE_WITH_KNOTS ( ( 3, 2, 2, 2, 2, 2, 3 ),
 ( 0.1249999999999999861, 0.1277777777777777679, 0.1333333333333333315, 0.1388888888888888951, 0.1444444444444444309, 0.1499999999999999944, 0.1527777777777777624 ),
 .UNSPECIFIED. ) 
 CURVE ( )  GEOMETRIC_REPRESENTATION_ITEM ( )  RATIONAL_B_SPLINE_CURVE ( ( 0.9755282581475768211, 0.9755282581475768211, 1.000000000000000000, 0.9510565162951535312, 1.000000000000000000, 0.9510565162951535312, 1.000000000000000000, 0.9510565162951535312, 1.000000000000000000, 0.9510565162951535312, 1.000000000000000000, 0.9755282581475768211, 0.9755282581475765991 ) ) 
 REPRESENTATION_ITEM ( '' )  );
#12222=CIRCLE ( 'NONE', #4883, 8.999999999999998224 ) ;
#12223=CARTESIAN_POINT ( 'NONE',  ( 7.614339970345533892, 71.96589283257024761, 11.14773206480789902 ) ) ;
#12224=CARTESIAN_POINT ( 'NONE',  ( 11.63364995522154111, 66.68500620773784249, -6.849007341775995350 ) ) ;
#12225=CARTESIAN_POINT ( 'NONE',  ( 5.049197031033813232, 56.86226893306975683, 12.52026344672814773 ) ) ;
#12226=CARTESIAN_POINT ( 'NONE',  ( 11.76794919243112325, 70.28000000000000114, 3.823638476888996607 ) ) ;
#12227=CARTESIAN_POINT ( 'NONE',  ( 11.76794919243112325, 64.43000000000000682, 1.441158131103945434E-15 ) ) ;
#12228=CARTESIAN_POINT ( 'NONE',  ( -11.35148106077255292, 47.20374464058922825, 7.307114632781469332 ) ) ;
#12229=EDGE_CURVE ( 'NONE', #16027, #15567, #894, .T. ) ;
#12233=CARTESIAN_POINT ( 'NONE',  ( -3.432968479904499937, 56.55653457480887170, 13.05682199246169439 ) ) ;
#12235=CARTESIAN_POINT ( 'NONE',  ( -10.92172942406178926, 39.62999999999999545, -7.935100905948389460 ) ) ;
#12236=CARTESIAN_POINT ( 'NONE',  ( 13.05193165377879971, 33.55293093225556333, -3.449255337325025650 ) ) ;
#12238=CARTESIAN_POINT ( 'NONE',  ( -1.245860404445607248E-06, 40.18000018109674443, -13.49999999999994316 ) ) ;
#12240=CARTESIAN_POINT ( 'NONE',  ( -2.502312991112111806, 62.59002693677476259, 13.26656818365915846 ) ) ;
#12242=CARTESIAN_POINT ( 'NONE',  ( -13.47712500954352421, 40.90289342314857635, -0.7855927258160574356 ) ) ;
#12244=CARTESIAN_POINT ( 'NONE',  ( -11.97926611549661935, 44.15976937875102948, 6.224998469355170094 ) ) ;
#12246=CARTESIAN_POINT ( 'NONE',  ( -10.92172942406178926, 43.62999999999999545, -7.935100905948389460 ) ) ;
#12247=CARTESIAN_POINT ( 'NONE',  ( 10.92172942406178926, 47.12999999999999545, 7.935100905948387684 ) ) ;
#12248=CARTESIAN_POINT ( 'NONE',  ( -12.90636597786267004, 71.07200195134710441, 3.959650672786486414 ) ) ;
#12250=CARTESIAN_POINT ( 'NONE',  ( -8.282215288612736259, 67.49552574882251577, -10.66482282856927988 ) ) ;
#12252=CARTESIAN_POINT ( 'NONE',  ( 12.61908122025767831, 54.25491345416680389, 4.836902432757269388 ) ) ;
#12253=CARTESIAN_POINT ( 'NONE',  ( -12.93929638727112774, 64.79209698274094364, -3.850488161051479175 ) ) ;
#12256=CARTESIAN_POINT ( 'NONE',  ( -12.15349527366901583, 34.71354853195965262, -5.893693796836648957 ) ) ;
#12258=CARTESIAN_POINT ( 'NONE',  ( 12.77063822339987986, 78.27209968102339133, 4.380528554209194958 ) ) ;
#12260=CARTESIAN_POINT ( 'NONE',  ( -10.19389412933198891, 31.58943635166178865, -8.850721524905974746 ) ) ;
#12261=CARTESIAN_POINT ( 'NONE',  ( 10.30697988259215059, 72.76444513209375486, -8.718751012341657614 ) ) ;
#12263=CARTESIAN_POINT ( 'NONE',  ( 5.014896044935506225, 59.86097445767614289, 12.53416570668548147 ) ) ;
#12265=CARTESIAN_POINT ( 'NONE',  ( -8.691771469529815392E-16, 71.68000000000000682, 14.19474002721660355 ) ) ;
#12266=CARTESIAN_POINT ( 'NONE',  ( -11.37807240653128105, 52.65795867555990384, -7.266101496908787816 ) ) ;
#12267=CARTESIAN_POINT ( 'NONE',  ( -9.520470885617717371, 45.22999999999999687, 6.917026985038133624 ) ) ;
#12268=CARTESIAN_POINT ( 'NONE',  ( -10.92172942406179104, 70.23000000000000398, 7.935100905948387684 ) ) ;
#12271=CARTESIAN_POINT ( 'NONE',  ( 10.89610398280023595, 69.73159480780164188, -7.971896094627922480 ) ) ;
#12272=CARTESIAN_POINT ( 'NONE',  ( -5.373303095793861672, 37.37454771265330322, -12.38528482517545015 ) ) ;
#12273=CARTESIAN_POINT ( 'NONE',  ( 4.326442524531895373, 35.83557250899896474, 12.78850620315103015 ) ) ;
#12275=CARTESIAN_POINT ( 'NONE',  ( -6.199815743880803254, 74.45309725584640148, 11.99228407210806147 ) ) ;
#12277=CARTESIAN_POINT ( 'NONE',  ( -12.53661919023033811, 76.74802840221525457, -5.008329300253832272 ) ) ;
#12278=CARTESIAN_POINT ( 'NONE',  ( -12.79019475395541505, 80.08649566584584534, 4.342692408574423624 ) ) ;
#12280=DIRECTION ( 'NONE',  ( 0.000000000000000000, -1.000000000000000000, 0.000000000000000000 ) ) ;
#12281=CARTESIAN_POINT ( 'NONE',  ( -7.686450350235888962, 80.93000000000003524, 9.894994522812504911 ) ) ;
#12284=CARTESIAN_POINT ( 'NONE',  ( 11.76794919243112325, 43.28000000000000114, 3.823638476888997051 ) ) ;
#12286=CARTESIAN_POINT ( 'NONE',  ( -5.574510941783231033, 40.38230122635308561, -12.29535200136428053 ) ) ;
#12287=CARTESIAN_POINT ( 'NONE',  ( -2.720355926141545755, 34.27781377822991971, -13.22308644890100027 ) ) ;
#12288=CARTESIAN_POINT ( 'NONE',  ( 13.48856620667041817, 75.44918483557830768, -0.5573347285596893519 ) ) ;
#12290=( NAMED_UNIT ( * ) PLANE_ANGLE_UNIT ( ) SI_UNIT ( $, .RADIAN. ) );
#12291=CARTESIAN_POINT ( 'NONE',  ( -10.79260502828427448, 41.23832797851595444, 8.135719096258426930 ) ) ;
#12293=CARTESIAN_POINT ( 'NONE',  ( -8.793690106930448280, 58.51931832914060294, -10.24309792423728638 ) ) ;
#12294=CARTESIAN_POINT ( 'NONE',  ( 5.517797477233192360, 44.87981964034685234, 12.33095150429005571 ) ) ;
#12296=DIRECTION ( 'NONE',  ( 0.000000000000000000, -1.000000000000000000, 0.000000000000000000 ) ) ;
#12298=CARTESIAN_POINT ( 'NONE',  ( -13.49999999999999822, 58.07999999999999119, 4.386415899144235020 ) ) ;
#12299=CARTESIAN_POINT ( 'NONE',  ( -13.46636358844568804, 49.89703890068803105, -0.9552207532122933831 ) ) ;
#12300=CARTESIAN_POINT ( 'NONE',  ( 12.71497711639302430, 63.59386036163260059, -4.536661660007360375 ) ) ;
#12301=CARTESIAN_POINT ( 'NONE',  ( 13.27852674175506387, 42.34417970882014970, 2.437829359112944960 ) ) ;
#12302=CARTESIAN_POINT ( 'NONE',  ( 1.360536668025988272, 38.72891990362956705, 13.43129604877473326 ) ) ;
#12303=ORIENTED_EDGE ( 'NONE', *, *, #14837, .F. ) ;
#12308=CARTESIAN_POINT ( 'NONE',  ( -5.664360417381419488, 43.38578491710213569, -12.25418510808193240 ) ) ;
#12309=CARTESIAN_POINT ( 'NONE',  ( -7.500000000000000000, 108.7397976749054891, -0.4943161440816168373 ) ) ;
#12310=CARTESIAN_POINT ( 'NONE',  ( 13.19392137637406925, 60.53158643750810342, -2.870547323392556915 ) ) ;
#12314=CARTESIAN_POINT ( 'NONE',  ( 13.38999116389189936, 66.49008748670826208, -1.721341902523813472 ) ) ;
#12315=CARTESIAN_POINT ( 'NONE',  ( 2.437340764247437175, 56.76768723153878682, 13.28085166176790288 ) ) ;
#12316=CARTESIAN_POINT ( 'NONE',  ( 11.76794919243112325, 58.42999999999999261, 1.441158131103945434E-15 ) ) ;
#12317=CARTESIAN_POINT ( 'NONE',  ( -4.171729424061787483, 36.32999999999999829, -12.83926296998457417 ) ) ;
#12318=CARTESIAN_POINT ( 'NONE',  ( 3.636496289402157078, 65.03000000000000114, -11.19198476289190936 ) ) ;
#12319=CARTESIAN_POINT ( 'NONE',  ( -7.060864377102370248, 47.41778540159006639, 11.50630388396855075 ) ) ;
#12320=CARTESIAN_POINT ( 'NONE',  ( 2.785878927130813844E-06, 56.68007738487546732, 13.49999999999942979 ) ) ;
#12323=CARTESIAN_POINT ( 'NONE',  ( -8.656036233252274670, 56.34715074576422467, 10.35972221486941791 ) ) ;
#12325=CARTESIAN_POINT ( 'NONE',  ( -10.92172942406179104, 40.23000000000000398, 7.935100905948387684 ) ) ;
#12326=CARTESIAN_POINT ( 'NONE',  ( 11.60125947145433045, 33.68733103568060017, -6.906614582173877359 ) ) ;
#12329=CARTESIAN_POINT ( 'NONE',  ( -5.609107424940139808, 62.47635901954124904, 12.27957684733320320 ) ) ;
#12330=( BOUNDED_CURVE ( )  B_SPLINE_CURVE ( 2, ( #12437, #8386, #240, #323, #16214, #5646, #1375, #14885, #2780, #8210, #13572, #1464, #9626 ),
 .UNSPECIFIED., .F., .F. ) 
 B_SPLINE_CURVE_WITH_KNOTS ( ( 3, 2, 2, 2, 2, 2, 3 ),
 ( 0.3750000000000000000, 0.3777777777777777679, 0.3833333333333333592, 0.3888888888888888951, 0.3944444444444444309, 0.4000000000000000222, 0.4027777777777777901 ),
 .UNSPECIFIED. ) 
 CURVE ( )  GEOMETRIC_REPRESENTATION_ITEM ( )  RATIONAL_B_SPLINE_CURVE ( ( 0.9755282581475768211, 0.9755282581475768211, 1.000000000000000000, 0.9510565162951535312, 1.000000000000000000, 0.9510565162951535312, 1.000000000000000000, 0.9510565162951535312, 1.000000000000000000, 0.9510565162951535312, 1.000000000000000000, 0.9755282581475768211, 0.9755282581475768211 ) ) 
 REPRESENTATION_ITEM ( '' )  );
#12331=ORIENTED_EDGE ( 'NONE', *, *, #16246, .F. ) ;
#12334=EDGE_CURVE ( 'NONE', #10449, #8975, #1608, .T. ) ;
#12335=CARTESIAN_POINT ( 'NONE',  ( -13.46460360472914886, 43.89619422539368543, -0.9770138388471342195 ) ) ;
#12337=CIRCLE ( 'NONE', #7835, 8.999999999999998224 ) ;
#12338=CARTESIAN_POINT ( 'NONE',  ( -4.171729424061791036, 38.52999999999999403, 12.83926296998457239 ) ) ;
#12339=CARTESIAN_POINT ( 'NONE',  ( 10.92172942406179104, 44.72999999999999687, -7.935100905948385908 ) ) ;
#12340=CARTESIAN_POINT ( 'NONE',  ( -13.47028805993524259, 70.89819967500132236, -0.9202425323688597780 ) ) ;
#12342=CARTESIAN_POINT ( 'NONE',  ( -10.97285289887956417, 67.63299039756994091, -7.864268408584646153 ) ) ;
#12344=B_SPLINE_CURVE_WITH_KNOTS ( 'NONE', 3,
 ( #10853, #16221, #11035, #4133, #14894, #1647, #6237, #3567, #7063, #13747, #12445, #4818, #15657, #330, #8483, #5739, #11120, #14169, #15572, #8982, #16494, #15156, #14337, #12861, #4399, #15488, #9810, #3054, #7147, #11452, #750, #16999, #825, #12771, #2226, #7655, #3483, #13031, #3398, #13834, #915, #8897, #1734, #2056, #660, #8811, #14252, #10394, #6069, #6324, #16826, #4733, #10134, #11624, #11710, #7480, #6158, #11535, #10219, #17087, #16913, #2140, #7565, #12942, #4905, #10304, #4992, #2964, #8394, #11799, #7741, #3659, #2313, #9071, #15749, #13116, #1004, #6415, #17176, #14424, #5087, #16488, #14889, #14979, #15062, #16666, #9629, #4395, #3140, #4573, #153, #8479, #13918, #12350, #4485, #413, #16309, #12440, #13659, #5559, #6972, #244, #11288, #5649, #11205, #8213, #11030, #1553, #16402, #2783, #4304, #9716, #13575, #15152, #10943, #1730, #2960, #9805, #13743, #326, #4216, #5821, #1467, #16580, #6886, #12258, #8565, #2871, #8303, #3050, #8390, #7143, #1643, #7059, #9894, #5910, #5735, #11116, #15242, #13830, #503, #12529, #1812, #7226, #12612, #1982, #8912, #14005, #1898, #11380, #17017, #2241, #8739, #16752, #8651, #4746, #15590, #17102, #7316, #10319, #12700, #15417, #4660, #7407, #8995, #12789, #14097, #7669, #10152, #675, #6252, #3324, #3231, #587, #11638, #6087, #10067, #11467, #16843, #4921, #2069, #15674, #13048, #3582, #8826 ),
 .UNSPECIFIED., .F., .F.,
 ( 4, 2, 1, 1, 1, 2, 2, 2, 2, 1, 2, 2, 1, 2, 1, 1, 1, 2, 2, 1, 2, 2, 2, 1, 1, 1, 2, 2, 2, 2, 2, 2, 2, 2, 2, 2, 2, 1, 2, 2, 1, 1, 1, 1, 1, 2, 2, 1, 2, 2, 2, 2, 2, 2, 1, 1, 1, 2, 2, 1, 2, 2, 1, 2, 2, 1, 1, 1, 2, 2, 2, 2, 2, 1, 2, 2, 1, 1, 2, 2, 2, 2, 2, 1, 1, 1, 1, 1, 1, 1, 1, 1, 2, 2, 1, 2, 2, 2, 2, 2, 1, 1, 2, 2, 2, 1, 2, 2, 2, 2, 2, 2, 2, 4 ),
 ( 0.03433471828737562348, 0.03436343981862335223, 0.03439216134987107404, 0.03444960441236652460, 0.03456449053735742571, 0.03479426278733922795, 0.03525380728730283242, 0.03571335178726643689, 0.03594312403724823912, 0.03605801016223914024, 0.03608673169348686205, 0.03611545322473459080, 0.03617289628723004830, 0.03709198528715729193, 0.03755152978712091028, 0.03778130203710271945, 0.03783874509959817695, 0.03785310586522203785, 0.03786746663084590570, 0.03789618816209362751, 0.03801107428708454944, 0.03893016328701191797, 0.03938970778697560571, 0.03950459391196652764, 0.03956203697446198514, 0.03959075850570972083, 0.03960511927133358867, 0.03961948003695744958, 0.03984925228693930732, 0.04076834128686672443, 0.04122788578683042604, 0.04145765803681228379, 0.04168743028679414153, 0.04260651928672155864, 0.04306606378668526025, 0.04312350684918071775, 0.04318094991167618218, 0.04329583603666711106, 0.04352560828664896186, 0.04444469728657637897, 0.04467446953655822978, 0.04478935566154915865, 0.04484679872404462309, 0.04487552025529235183, 0.04488988102091621968, 0.04489347121232218490, 0.04489706140372815013, 0.04490424178654011528, 0.04536378628650494099, 0.04628287528643459242, 0.04651264753641700528, 0.04662753366140821171, 0.04665625519265600984, 0.04666343557546796805, 0.04667061595827991238, 0.04668497672390381492, 0.04674241978639941120, 0.04720196428636422303, 0.04812105328629383283, 0.04835082553627623181, 0.04840826859877183502, 0.04846571166126743824, 0.04858059778625863773, 0.04904014228622343569, 0.04995923128615303854, 0.05007411741114424497, 0.05013156047363984125, 0.05016028200488764632, 0.05017464277051153498, 0.05018900353613543752, 0.05041877578611784344, 0.05087832028608266222, 0.05179740928601228589, 0.05191229541100348538, 0.05192665617662738792, 0.05194101694225129046, 0.05196973847349908859, 0.05202718153599469181, 0.05225695378597709773, 0.05271649828594189569, 0.05363558728587150548, 0.05369303034836710176, 0.05372175187961490683, 0.05375047341086270497, 0.05386535953585390446, 0.05409513178583630344, 0.05455467628580110140, 0.05501422078576589242, 0.05524399303574828446, 0.05535887916073949089, 0.05541632222323508716, 0.05544504375448289224, 0.05545222413729483657, 0.05545940452010678090, 0.05547376528573066956, 0.05639285428565964098, 0.05685239878562411975, 0.05708217103560635913, 0.05719705716059747536, 0.05722577869184525962, 0.05725450022309304388, 0.05731194328558860546, 0.05823103228551756994, 0.05915012128544652747, 0.06006921028537549889, 0.06052875478533997766, 0.06064364091033110082, 0.06075852703532222399, 0.06098829928530446337, 0.06190738828523344173, 0.06236693278519793437, 0.06259670503518018070, 0.06282647728516242702, 0.06374556628509139844 ),
 .UNSPECIFIED. ) ;
#12345=CARTESIAN_POINT ( 'NONE',  ( 11.71143458302510965, 54.18049042001842963, 6.715257056421563675 ) ) ;
#12346=CARTESIAN_POINT ( 'NONE',  ( -10.26110598144033403, 64.59313657883589599, -8.772856892074198498 ) ) ;
#12348=CARTESIAN_POINT ( 'NONE',  ( -13.43241235626039831, 34.88232143987041667, -1.376510585871620229 ) ) ;
#12349=ORIENTED_EDGE ( 'NONE', *, *, #17031, .F. ) ;
#12350=CARTESIAN_POINT ( 'NONE',  ( 13.35186508744918576, 78.50178817042122148, -2.050551861675898646 ) ) ;
#12351=CARTESIAN_POINT ( 'NONE',  ( 7.500000000000000888, 102.9299999999999073, 9.367496997597653419 ) ) ;
#12353=CARTESIAN_POINT ( 'NONE',  ( 11.17057654354756657, 72.71510454181631644, -7.580829038184448088 ) ) ;
#12356=CARTESIAN_POINT ( 'NONE',  ( 10.92172942406179104, 69.73000000000000398, -7.935100905948385908 ) ) ;
#12357=CARTESIAN_POINT ( 'NONE',  ( -12.56842791742744758, 52.75088463843982822, -4.935720490616978928 ) ) ;
#12358=CARTESIAN_POINT ( 'NONE',  ( -9.520470885617715595, 47.62999999999999545, -6.917026985038136289 ) ) ;
#12359=CARTESIAN_POINT ( 'NONE',  ( 10.92172942406178926, 68.12999999999999545, 7.935100905948387684 ) ) ;
#12361=CARTESIAN_POINT ( 'NONE',  ( 9.980839278485152732, 69.07821623398331212, 9.090265664844007887 ) ) ;
#12362=CARTESIAN_POINT ( 'NONE',  ( -0.5739585204448709455, 37.20062488901800890, -13.49031863273558507 ) ) ;
#12365=CARTESIAN_POINT ( 'NONE',  ( -6.131838958729160183, 74.45581572403800408, 12.02710268997748067 ) ) ;
#12366=CARTESIAN_POINT ( 'NONE',  ( -13.36244170316012081, 76.86246845120821547, -1.928779065015713279 ) ) ;
#12373=CARTESIAN_POINT ( 'NONE',  ( 7.272992578804308828, 48.97999999999999687, 10.01041549318726886 ) ) ;
#12375=CARTESIAN_POINT ( 'NONE',  ( -2.701716699869450178, 34.27714333493316445, -13.22690816007884784 ) ) ;
#12376=CARTESIAN_POINT ( 'NONE',  ( 13.46309567844158117, 75.46468981469040216, -1.002245987159475549 ) ) ;
#12378=VECTOR ( 'NONE', #1673, 1000.000000000000000 ) ;
#12379=CARTESIAN_POINT ( 'NONE',  ( -7.272992578804310604, 33.38000000000000256, 10.01041549318726709 ) ) ;
#12380=CARTESIAN_POINT ( 'NONE',  ( -11.21531812396516514, 41.21235424446476969, 7.514485397707633574 ) ) ;
#12381=CARTESIAN_POINT ( 'NONE',  ( -0.5901369808829292074, 58.20121914870583169, -13.50000000000000178 ) ) ;
#12383=CARTESIAN_POINT ( 'NONE',  ( 7.961489030491042840, 36.87882774062229174, -10.90288674562418869 ) ) ;
#12385=B_SPLINE_CURVE_WITH_KNOTS ( 'NONE', 3,
 ( #2214, #8969, #815, #17073, #15912, #16903, #14410, #8886, #4806, #7641, #17248, #989, #6226, #11612, #3731, #14496, #4977, #15734, #15562, #899, #11784, #3643, #6490, #14241, #16988, #7726, #10293, #15645, #5161, #9057, #2298, #10553, #17160, #5072, #7819, #10466, #15827, #2126, #13191, #12931, #7552, #1076, #3821, #9235, #14589, #7469, #12849, #738, #15998, #12039, #12, #13614, #1246, #10718, #1165, #194, #1327, #6576, #14755, #8161, #10981, #1507, #3903, #13357, #2733, #17418, #5333, #6923, #16083, #6658, #12300, #2644, #3991, #16260, #9407, #8076, #9321, #10805, #7989, #14671, #13440, #2559, #1415, #14839, #6743, #6833, #11957, #12123, #5416, #16167, #5599, #4077, #9492, #17336, #16351, #10633, #13526, #12209, #103, #5508, #10891, #2822, #4167, #4257, #9579, #7902, #2469, #14930, #8252, #9667, #13277, #5247, #3090, #12565, #7094, #11418, #12478, #11326, #8516, #4696, #7263, #2909, #13695, #11240, #7011, #12388, #15017, #536, #4436, #8339, #279, #16790, #13953, #1594, #5946, #5688, #16704, #11068, #8687, #13779, #6035, #364, #13866, #7357, #1768, #16441, #4343, #3270, #9752, #15097, #2996, #8426, #1678, #5769, #11153, #16529, #624, #9843, #15189, #1850, #7177, #14046, #451, #12647, #5861, #16618, #4522, #9929, #4609, #10016, #15278, #1934, #3179, #8601, #15364, #12736, #14303, #13168, #17051, #17226, #10444, #9033, #15538, #10101, #15622, #6288, #15452, #8777, #11675, #2020, #7446, #3361, #13079 ),
 .UNSPECIFIED., .F., .F.,
 ( 4, 2, 2, 1, 2, 2, 1, 1, 1, 2, 2, 1, 2, 2, 1, 1, 2, 2, 2, 2, 2, 1, 1, 2, 2, 2, 2, 2, 2, 1, 1, 2, 2, 1, 1, 1, 2, 2, 1, 2, 2, 2, 2, 2, 1, 1, 2, 2, 2, 1, 2, 2, 1, 1, 2, 2, 2, 2, 2, 1, 2, 2, 2, 1, 2, 2, 1, 2, 2, 2, 2, 2, 2, 1, 2, 2, 2, 2, 2, 1, 1, 1, 1, 2, 1, 1, 1, 2, 2, 1, 1, 2, 2, 2, 2, 2, 2, 1, 1, 2, 2, 2, 1, 2, 2, 1, 2, 2, 2, 2, 2, 1, 1, 2, 2, 4 ),
 ( 0.3284481763819381284, 0.3293659151444585653, 0.3302836539069789468, 0.3303410125796364949, 0.3303553522478008819, 0.3303696919159652690, 0.3303983712522940430, 0.3305130885976090838, 0.3307425232882391652, 0.3312013926694993837, 0.3321191314320198207, 0.3322338487773348614, 0.3322625281136636355, 0.3322768677818280225, 0.3322912074499924096, 0.3323485661226499022, 0.3325780008132800947, 0.3330368701945404797, 0.3339546089570611942, 0.3341840436476913867, 0.3342127229840201608, 0.3342414023203489348, 0.3342987609930064830, 0.3344134783383215792, 0.3348723477195819642, 0.3357900864821026787, 0.3360195211727328712, 0.3360768798453904194, 0.3361055591817191934, 0.3361342385180479675, 0.3362489558633630637, 0.3367078252446234488, 0.3376255640071442743, 0.3378549986977744668, 0.3379697160430895631, 0.3379983953794183371, 0.3380055652135005584, 0.3380127350475827241, 0.3380270747157471112, 0.3380844333884046593, 0.3385433027696648223, 0.3394610415321852592, 0.3399199109134454777, 0.3399772695861030258, 0.3400346282587605184, 0.3401493456040756147, 0.3403787802947056962, 0.3412965190572261331, 0.3417553884384863516, 0.3418127471111438997, 0.3418270867793082868, 0.3418414264474726183, 0.3418701057838013924, 0.3419848231291164331, 0.3422142578197465146, 0.3431319965822668405, 0.3435908659635270590, 0.3437055833088420997, 0.3437629419814995924, 0.3438203006541571405, 0.3440497353447872220, 0.3449674741073075479, 0.3458852128698278738, 0.3459425715424854220, 0.3459712508788141960, 0.3459999302151429146, 0.3461146475604579553, 0.3463440822510880923, 0.3468029516323482553, 0.3477206903948685812, 0.3481795597761287442, 0.3482082391124575182, 0.3482369184487862923, 0.3482942771214438404, 0.3484089944667588812, 0.3486384291573890182, 0.3490972985386492922, 0.3493267332292794292, 0.3493410728974438162, 0.3493554125656082032, 0.3493840919019369773, 0.3494414505745945254, 0.3495561679199096772, 0.3500150373011700622, 0.3502444719918003102, 0.3503591893371154065, 0.3504165480097729546, 0.3504452273461017286, 0.3504523971801839499, 0.3504595670142661157, 0.3504739066824305027, 0.3513916454449503290, 0.3523093842074701554, 0.3525388188981000703, 0.3526535362434150556, 0.3526678759115794426, 0.3526822155797438296, 0.3527108949160725482, 0.3527682535887300408, 0.3532271229699898707, 0.3541448617325096415, 0.3559803392575490721, 0.3560090185938777907, 0.3560233582620421777, 0.3560376979302065648, 0.3560950566028640019, 0.3562097739481789871, 0.3564392086388087910, 0.3568980780200685099, 0.3573569474013282288, 0.3575863820919580882, 0.3576437407646155808, 0.3576724201009442994, 0.3576867597691086309, 0.3577010994372730179, 0.3578158167825879477 ),
 .UNSPECIFIED. ) ;
#12386=CARTESIAN_POINT ( 'NONE',  ( 0.000000000000000000, 80.93000000000000682, 0.000000000000000000 ) ) ;
#12387=CARTESIAN_POINT ( 'NONE',  ( -4.816349661276159821, 49.35356466364647332, -12.61319266799936223 ) ) ;
#12388=CARTESIAN_POINT ( 'NONE',  ( 11.49974279481918948, 63.16598485185204481, 7.071657227356595854 ) ) ;
#12389=CARTESIAN_POINT ( 'NONE',  ( 8.386380085766983683, 42.00036598867336579, 10.57921543981575851 ) ) ;
#12390=CARTESIAN_POINT ( 'NONE',  ( 0.8900221435513422374, 38.71200720458531919, 13.47797817745645865 ) ) ;
#12392=VERTEX_POINT ( 'NONE', #976 ) ;
#12393=CARTESIAN_POINT ( 'NONE',  ( 9.520470885617715595, 76.13000000000000966, 6.917026985038134512 ) ) ;
#12397=ORIENTED_EDGE ( 'NONE', *, *, #10372, .F. ) ;
#12398=EDGE_CURVE ( 'NONE', #12392, #39, #5059, .T. ) ;
#12399=CARTESIAN_POINT ( 'NONE',  ( -2.284164177028834342, 43.26213011653167939, -13.30536795550864149 ) ) ;
#12400=CARTESIAN_POINT ( 'NONE',  ( -7.499999999999998224, 108.6199039925686662, 2.572187159835563897 ) ) ;
#12401=CARTESIAN_POINT ( 'NONE',  ( 11.56739400518585192, 60.68949195955414666, -6.960273062025671642 ) ) ;
#12403=CARTESIAN_POINT ( 'NONE',  ( 0.000000000000000000, 0.000000000000000000, 9.500000000000021316 ) ) ;
#12404=CARTESIAN_POINT ( 'NONE',  ( 13.42937308305210919, 66.38180020187820674, 1.390829281587693478 ) ) ;
#12405=CARTESIAN_POINT ( 'NONE',  ( 1.463318478726158389, 56.73261554528513528, 13.42046002623553669 ) ) ;
#12406=CARTESIAN_POINT ( 'NONE',  ( -7.272992578804307939, 59.48000000000000398, -10.01041549318726886 ) ) ;
#12407=CARTESIAN_POINT ( 'NONE',  ( 11.76794919243112325, 67.43000000000000682, 1.441158131103945434E-15 ) ) ;
#12408=CARTESIAN_POINT ( 'NONE',  ( -12.95528734819502503, 47.06741981842274924, 3.836386419411801807 ) ) ;
#12410=CARTESIAN_POINT ( 'NONE',  ( -13.49999999999999822, 46.07999999999999829, 4.386415899144235020 ) ) ;
#12411=CYLINDRICAL_SURFACE ( 'NONE', #15296, 13.50000000000000000 ) ;
#12412=CARTESIAN_POINT ( 'NONE',  ( 9.037365757593402549, 30.82912645640030647, -10.03076112684414589 ) ) ;
#12413=CARTESIAN_POINT ( 'NONE',  ( -5.572576793242300042, 56.47777282521396813, 12.29619502175249401 ) ) ;
#12416=CARTESIAN_POINT ( 'NONE',  ( 1.324280721486043255, 32.72761620803525062, 13.43490005586108360 ) ) ;
#12418=CARTESIAN_POINT ( 'NONE',  ( 3.652837425045026176, 40.04880968999665214, -13.00149846498695005 ) ) ;
#12421=CARTESIAN_POINT ( 'NONE',  ( -2.064298368984843535, 62.60577758412497218, 13.34129268682456981 ) ) ;
#12423=EDGE_CURVE ( 'NONE', #3781, #17339, #1929, .T. ) ;
#12426=CARTESIAN_POINT ( 'NONE',  ( -11.19741182518031053, 44.21346306567002671, 7.541088250378106039 ) ) ;
#12427=CARTESIAN_POINT ( 'NONE',  ( 10.92172942406178926, 65.12999999999999545, 7.935100905948387684 ) ) ;
#12428=CARTESIAN_POINT ( 'NONE',  ( -4.171729424061791036, 32.52999999999999403, 12.83926296998457239 ) ) ;
#12429=CARTESIAN_POINT ( 'NONE',  ( -8.691771469529815392E-16, 43.67999999999998550, 14.19474002721660355 ) ) ;
#12430=CARTESIAN_POINT ( 'NONE',  ( -6.327032371063140204, 46.41202214260281522, -11.92554859961118119 ) ) ;
#12431=CARTESIAN_POINT ( 'NONE',  ( -3.712474928015834230, 67.31306499987073266, -12.98134956584450350 ) ) ;
#12433=( BOUNDED_CURVE ( )  B_SPLINE_CURVE ( 2, ( #17156, #4973, #10376, #10462, #15822, #15908, #17245, #10549, #3817, #14584, #2465, #7897, #13273 ),
 .UNSPECIFIED., .F., .F. ) 
 B_SPLINE_CURVE_WITH_KNOTS ( ( 3, 2, 2, 2, 2, 2, 3 ),
 ( 0.3194444444444444198, 0.3222222222222222432, 0.3277777777777777790, 0.3333333333333333148, 0.3388888888888889062, 0.3444444444444444420, 0.3472222222222222099 ),
 .UNSPECIFIED. ) 
 CURVE ( )  GEOMETRIC_REPRESENTATION_ITEM ( )  RATIONAL_B_SPLINE_CURVE ( ( 0.9755282581475768211, 0.9755282581475765991, 1.000000000000000000, 0.9510565162951535312, 1.000000000000000000, 0.9510565162951535312, 1.000000000000000000, 0.9510565162951535312, 1.000000000000000000, 0.9510565162951535312, 1.000000000000000000, 0.9755282581475768211, 0.9755282581475768211 ) ) 
 REPRESENTATION_ITEM ( '' )  );
#12434=CARTESIAN_POINT ( 'NONE',  ( 12.95352307866690111, 54.56613520967127329, -3.803420169897604008 ) ) ;
#12435=CARTESIAN_POINT ( 'NONE',  ( -5.827146427730992784, 64.39213759910121837, -12.17765789728212766 ) ) ;
#12436=EDGE_LOOP ( 'NONE', ( #13199, #8015, #11618, #12781 ) ) ;
#12437=CARTESIAN_POINT ( 'NONE',  ( -8.891200544363830713E-16, 64.67999999999999261, 13.50000000000000000 ) ) ;
#12438=CARTESIAN_POINT ( 'NONE',  ( -13.49990086529558830, 34.94504141492947724, 0.4412720814781904144 ) ) ;
#12440=CARTESIAN_POINT ( 'NONE',  ( 13.46864404905786117, 78.46180393935253505, -0.9198462106560619800 ) ) ;
#12442=VECTOR ( 'NONE', #10051, 1000.000000000000114 ) ;
#12444=CARTESIAN_POINT ( 'NONE',  ( 8.010861774722636497, 72.87662127041942028, -10.86656001248561587 ) ) ;
#12445=CARTESIAN_POINT ( 'NONE',  ( 1.758123048363891883, 79.11681026432344765, -13.38681728492156431 ) ) ;
#12447=CARTESIAN_POINT ( 'NONE',  ( 10.92172942406178926, 66.12999999999999545, 7.935100905948387684 ) ) ;
#12448=CARTESIAN_POINT ( 'NONE',  ( -13.20937656505621227, 53.02849338733904716, 2.786178234548895905 ) ) ;
#12449=CARTESIAN_POINT ( 'NONE',  ( 9.520470885617715595, 40.12999999999999545, 6.917026985038134512 ) ) ;
#12451=CARTESIAN_POINT ( 'NONE',  ( -10.92172942406179104, 61.22999999999999687, 7.935100905948387684 ) ) ;
#12452=CARTESIAN_POINT ( 'NONE',  ( -7.499999999999996447, 88.93000000000000682, -12.00000000000000178 ) ) ;
#12453=ADVANCED_FACE ( 'NONE', ( #2723 ), #9136, .T. ) ;
#12454=CARTESIAN_POINT ( 'NONE',  ( 5.752805971757215531, 68.88911494562405835, 12.22037727962858611 ) ) ;
#12456=CARTESIAN_POINT ( 'NONE',  ( 1.948779282392957057, 35.75006106732994482, 13.35913770969951564 ) ) ;
#12458=CARTESIAN_POINT ( 'NONE',  ( -10.46266594696475316, 74.25595380999331496, 8.531279792551288210 ) ) ;
#12459=CARTESIAN_POINT ( 'NONE',  ( -4.671281222091343999, 76.34819209519075400, -12.66606340400099562 ) ) ;
#12462=CARTESIAN_POINT ( 'NONE',  ( -11.52888015854957793, 80.93000000000003524, 3.329402692645399675 ) ) ;
#12465=CARTESIAN_POINT ( 'NONE',  ( -11.76794919243112325, 35.92999999999999972, -2.882316262207890869E-15 ) ) ;
#12467=CARTESIAN_POINT ( 'NONE',  ( -9.257301361965243558, 32.31846096236034782, 9.826932714272743397 ) ) ;
#12468=CARTESIAN_POINT ( 'NONE',  ( 12.22812538439530528, 75.22023328956014154, 5.720436177748926987 ) ) ;
#12470=CARTESIAN_POINT ( 'NONE',  ( -11.76794919243112325, 33.07999999999998408, 3.823638476888994386 ) ) ;
#12471=CARTESIAN_POINT ( 'NONE',  ( 4.558948942910276969, 52.01595162841300635, -12.70712274664167474 ) ) ;
#12474=CARTESIAN_POINT ( 'NONE',  ( 0.1004344462107467778, 37.17638874791335013, -13.49962723151365296 ) ) ;
#12475=CARTESIAN_POINT ( 'NONE',  ( -7.291143994141260196E-08, 47.67999796853253258, 13.49999999999999822 ) ) ;
#12477=AXIS2_PLACEMENT_3D ( 'NONE', #10344, #7950, #864 ) ;
#12478=CARTESIAN_POINT ( 'NONE',  ( 11.73819402979808046, 63.18233018420252023, 6.670510071192460089 ) ) ;
#12479=CARTESIAN_POINT ( 'NONE',  ( 13.44060992811053623, 42.38566405594722397, 1.278966233340825154 ) ) ;
#12483=CARTESIAN_POINT ( 'NONE',  ( 11.76794919243112325, 76.42999999999999261, 1.441158131103945434E-15 ) ) ;
#12487=ORIENTED_EDGE ( 'NONE', *, *, #7738, .F. ) ;
#12488=CARTESIAN_POINT ( 'NONE',  ( -9.800337745008080859, 43.56848657308245976, -9.294634735303336726 ) ) ;
#12489=CARTESIAN_POINT ( 'NONE',  ( -7.499999999999998224, 108.7258046340737963, 1.043242051446487517 ) ) ;
#12490=CARTESIAN_POINT ( 'NONE',  ( 9.464546292035263875, 60.80808485042920353, -9.627110977571010864 ) ) ;
#12493=CARTESIAN_POINT ( 'NONE',  ( 10.07262787396443748, 66.08313066052312479, 8.989075947907759101 ) ) ;
#12494=CARTESIAN_POINT ( 'NONE',  ( 8.577460307545479168, 57.00915232730558557, 10.42567900465104280 ) ) ;
#12495=CARTESIAN_POINT ( 'NONE',  ( 11.76794919243112325, 58.28000000000000114, 3.823638476888996607 ) ) ;
#12496=CARTESIAN_POINT ( 'NONE',  ( 10.92172942406178926, 35.13000000000000256, 7.935100905948387684 ) ) ;
#12497=CARTESIAN_POINT ( 'NONE',  ( 7.272992578804308828, 66.98000000000000398, 10.01041549318726709 ) ) ;
#12498=AXIS2_PLACEMENT_3D ( 'NONE', #12386, #276, #12207 ) ;
#12499=CARTESIAN_POINT ( 'NONE',  ( -12.57615766451182537, 46.75189198415294101, -4.908197936080784807 ) ) ;
#12500=CARTESIAN_POINT ( 'NONE',  ( 11.82910594196685850, 45.67102758238960547, -6.505590469736891812 ) ) ;
#12502=ADVANCED_FACE ( 'NONE', ( #14746 ), #2372, .T. ) ;
#12503=CARTESIAN_POINT ( 'NONE',  ( 2.919510057594956187, 31.07524303651355169, -13.20096495093523004 ) ) ;
#12507=CARTESIAN_POINT ( 'NONE',  ( 0.2224977522097629223, 32.68807153545635913, 13.49999999993604760 ) ) ;
#12508=CARTESIAN_POINT ( 'NONE',  ( -1.844924112955495524E-14, 72.18000000000000682, -13.50000000000000000 ) ) ;
#12510=ORIENTED_EDGE ( 'NONE', *, *, #8935, .T. ) ;
#12511=CARTESIAN_POINT ( 'NONE',  ( -13.46962982805347231, 61.96129992434394040, 0.9054387881791874371 ) ) ;
#12512=ORIENTED_EDGE ( 'NONE', *, *, #16969, .T. ) ;
#12513=AXIS2_PLACEMENT_3D ( 'NONE', #14286, #10252, #3159 ) ;
#12516=CARTESIAN_POINT ( 'NONE',  ( -12.80129509359390738, 43.77561004955722268, -4.287691323260377274 ) ) ;
#12518=CARTESIAN_POINT ( 'NONE',  ( -13.49999999999999822, 38.07999999999999829, 4.386415899144235908 ) ) ;
#12519=CARTESIAN_POINT ( 'NONE',  ( -10.92172942406179104, 46.22999999999999687, 7.935100905948387684 ) ) ;
#12520=EDGE_CURVE ( 'NONE', #717, #10228, #3649, .T. ) ;
#12521=CARTESIAN_POINT ( 'NONE',  ( -5.471725549333255501, 46.37816455119584447, -12.34359373141929872 ) ) ;
#12522=CARTESIAN_POINT ( 'NONE',  ( -5.584685134716633748, 67.38269536530388848, -12.29070702121700620 ) ) ;
#12524=CARTESIAN_POINT ( 'NONE',  ( 3.294022803995052762, 53.79842651621079597, 13.09196167790783605 ) ) ;
#12525=CARTESIAN_POINT ( 'NONE',  ( -3.061294706506703545, 64.29016813706658695, -13.14846668619222392 ) ) ;
#12527=CARTESIAN_POINT ( 'NONE',  ( -5.592873841450387573, 34.38301124043937307, -12.28706942924041989 ) ) ;
#12529=CARTESIAN_POINT ( 'NONE',  ( 10.68121621590718995, 78.11601607104590528, 8.257274610802166848 ) ) ;
#12532=CARTESIAN_POINT ( 'NONE',  ( 12.57737074227892826, 72.25174867838231307, 4.912843465583652147 ) ) ;
#12534=CARTESIAN_POINT ( 'NONE',  ( -8.343458848123576743, 58.47999999999998977, -11.48378591275254301 ) ) ;
#12535=CARTESIAN_POINT ( 'NONE',  ( -13.19435882288848028, 53.03109597840953171, 2.856512463374823341 ) ) ;
#12536=CARTESIAN_POINT ( 'NONE',  ( 7.272992578804308828, 36.97999999999998977, 10.01041549318726709 ) ) ;
#12538=CARTESIAN_POINT ( 'NONE',  ( 10.92172942406178926, 56.13000000000000256, 7.935100905948387684 ) ) ;
#12539=CARTESIAN_POINT ( 'NONE',  ( 4.171729424061791924, 78.03000000000000114, -12.83926296998457239 ) ) ;
#12541=CARTESIAN_POINT ( 'NONE',  ( 3.562763415993998262, 68.80810093510450542, 13.02139636752514207 ) ) ;
#12542=CARTESIAN_POINT ( 'NONE',  ( -3.048821793079171893, 37.28962259733035012, -13.15181977963969651 ) ) ;
#12543=CARTESIAN_POINT ( 'NONE',  ( -2.138189944381247098, 72.25688142232026223, -13.49999999999999645 ) ) ;
#12545=CARTESIAN_POINT ( 'NONE',  ( -11.59403592772097547, 73.67225474520861894, -6.918110984581458567 ) ) ;
#12546=CARTESIAN_POINT ( 'NONE',  ( -8.762708921790252958, 76.51760276393278559, -10.27614992352630274 ) ) ;
#12549=CYLINDRICAL_SURFACE ( 'NONE', #12797, 13.50000000000000000 ) ;
#12552=CARTESIAN_POINT ( 'NONE',  ( -11.76794919243112325, 35.77999999999999403, -3.823638476888998827 ) ) ;
#12554=CARTESIAN_POINT ( 'NONE',  ( 1.628308837847167748E-06, 32.68004529479373588, 13.49999999999980460 ) ) ;
#12555=CARTESIAN_POINT ( 'NONE',  ( 13.47305538128101077, 75.45974515404770955, -0.8610043160690442621 ) ) ;
#12558=CARTESIAN_POINT ( 'NONE',  ( 11.76794919243112680, 34.57999999999999829, -3.823638476888993942 ) ) ;
#12559=CARTESIAN_POINT ( 'NONE',  ( 8.050218389484046000, 31.03187319105529340, 8.940655939244130934 ) ) ;
#12560=CARTESIAN_POINT ( 'NONE',  ( 10.14124484132416626, 51.77333499035184872, -8.911260184641234261 ) ) ;
#12562=CARTESIAN_POINT ( 'NONE',  ( 8.267901496158602370, 36.86504151979552546, -10.67201748973769782 ) ) ;
#12564=CARTESIAN_POINT ( 'NONE',  ( -0.3617901473021373771, 49.19299986674817404, -13.49533619113506688 ) ) ;
#12565=CARTESIAN_POINT ( 'NONE',  ( 12.47474062557478192, 63.24199196955865432, 5.166233987108326708 ) ) ;
#12566=CARTESIAN_POINT ( 'NONE',  ( 10.89469735476495416, 42.12845549515284205, 7.973421550594564700 ) ) ;
#12567=CARTESIAN_POINT ( 'NONE',  ( 10.70081124441169784, 48.74267151870439108, -8.230608850174302660 ) ) ;
#12569=VERTEX_POINT ( 'NONE', #6648 ) ;
#12570=CARTESIAN_POINT ( 'NONE',  ( 11.76794919243112680, 67.57999999999998408, -3.823638476888993942 ) ) ;
#12574=VERTEX_POINT ( 'NONE', #17409 ) ;
#12575=CARTESIAN_POINT ( 'NONE',  ( -9.182998036710223744, 43.53789999169043057, -9.897881256833889196 ) ) ;
#12579=CARTESIAN_POINT ( 'NONE',  ( 8.206140411365607790, 65.99215479700292519, 10.71966715772747669 ) ) ;
#12580=CARTESIAN_POINT ( 'NONE',  ( 1.580573102785959083, 56.73683176799062267, 13.40744280352419437 ) ) ;
#12581=CARTESIAN_POINT ( 'NONE',  ( 11.76794919243112680, 58.57999999999999119, -3.823638476888993942 ) ) ;
#12582=CARTESIAN_POINT ( 'NONE',  ( -11.76794919243112325, 65.93000000000000682, -2.882316262207890869E-15 ) ) ;
#12583=CARTESIAN_POINT ( 'NONE',  ( -13.49125618869725862, 46.94671107676184363, 0.4858370549406775818 ) ) ;
#12584=CARTESIAN_POINT ( 'NONE',  ( 6.997088715578399842, 45.92049188004365590, -11.54634344188570161 ) ) ;
#12586=CARTESIAN_POINT ( 'NONE',  ( 8.352825653922046456, 30.86116902798444173, -10.60567559741120469 ) ) ;
#12587=CARTESIAN_POINT ( 'NONE',  ( -4.507315936713728988, 56.51790915384739833, 12.73940224085357009 ) ) ;
#12588=CARTESIAN_POINT ( 'NONE',  ( 4.171729424061789260, 52.83000000000000540, 12.83926296998457417 ) ) ;
#12589=CARTESIAN_POINT ( 'NONE',  ( 3.595939032899281074, 32.80928899092024409, 13.01768941633015686 ) ) ;
#12592=VERTEX_POINT ( 'NONE', #8066 ) ;
#12593=CARTESIAN_POINT ( 'NONE',  ( -8.680814540994266082, 62.34599070752307171, 10.33893831029611121 ) ) ;
#12598=CARTESIAN_POINT ( 'NONE',  ( 11.62831264688102451, 48.17469404744644379, 6.858106635231019155 ) ) ;
#12600=CARTESIAN_POINT ( 'NONE',  ( 13.50000000000000000, 65.43000000000000682, 1.653273178848926867E-15 ) ) ;
#12601=CARTESIAN_POINT ( 'NONE',  ( -13.49999999999999822, 34.78000000000000114, -4.386415899144240349 ) ) ;
#12604=CARTESIAN_POINT ( 'NONE',  ( -5.666818938165120834, 67.38588027987705686, -12.25310711623839133 ) ) ;
#12606=CARTESIAN_POINT ( 'NONE',  ( 8.670433428822322597, 54.01357483247397795, 10.35003895964909226 ) ) ;
#12608=CARTESIAN_POINT ( 'NONE',  ( -3.191717032724610714, 64.29480952879987399, -13.11732287425230581 ) ) ;
#12610=CARTESIAN_POINT ( 'NONE',  ( -9.604335505081937896, 34.55882025099123922, -9.493374980285292253 ) ) ;
#12612=CARTESIAN_POINT ( 'NONE',  ( 10.47449681190867210, 78.10467755407360357, 8.516757727679493684 ) ) ;
#12615=EDGE_CURVE ( 'NONE', #10808, #7754, #14208, .T. ) ;
#12617=CARTESIAN_POINT ( 'NONE',  ( 11.86550600985247250, 72.66835694352569419, -6.439119142892169023 ) ) ;
#12619=CARTESIAN_POINT ( 'NONE',  ( -4.171729424061791036, 59.53000000000000114, 12.83926296998457239 ) ) ;
#12620=CARTESIAN_POINT ( 'NONE',  ( -5.806291557865342234, 52.39132149430719210, -12.18757512875381721 ) ) ;
#12621=CARTESIAN_POINT ( 'NONE',  ( -3.636496289402155746, 36.53000000000000114, 11.19198476289190936 ) ) ;
#12622=CARTESIAN_POINT ( 'NONE',  ( -8.343458848123576743, 60.47999999999999687, -11.48378591275254301 ) ) ;
#12623=CARTESIAN_POINT ( 'NONE',  ( 1.522075781121807969, 50.73472822943448080, 13.41392177511433559 ) ) ;
#12625=CARTESIAN_POINT ( 'NONE',  ( 9.736523788050917005, 69.06556698226975755, 9.351906487042457528 ) ) ;
#12626=CYLINDRICAL_SURFACE ( 'NONE', #16900, 5.000000000000000000 ) ;
#12629=CARTESIAN_POINT ( 'NONE',  ( -13.22250539961364169, 73.83308068845481387, -2.742208778312596795 ) ) ;
#12630=CARTESIAN_POINT ( 'NONE',  ( -2.875760791593931984E-14, 76.17999999999999261, -13.50000000000000000 ) ) ;
#12635=CARTESIAN_POINT ( 'NONE',  ( -11.76794919243112325, 41.78000000000000114, -3.823638476888998827 ) ) ;
#12639=CARTESIAN_POINT ( 'NONE',  ( -7.169881344235224496, 32.41318569726487908, 11.43868762491521451 ) ) ;
#12641=CARTESIAN_POINT ( 'NONE',  ( 11.76794919243112325, 31.27999999999998693, 3.823638476888996607 ) ) ;
#12642=CARTESIAN_POINT ( 'NONE',  ( 1.963551943317787263, 52.10952655783576404, -13.36279640122861423 ) ) ;
#12643=CARTESIAN_POINT ( 'NONE',  ( -4.076052042102673134, 38.53349475998775375, 12.87062638305022411 ) ) ;
#12644=CARTESIAN_POINT ( 'NONE',  ( 0.2077865973656172205, 37.17252950262063393, -13.49854835976931078 ) ) ;
#12645=CARTESIAN_POINT ( 'NONE',  ( -8.343458848123582072, 70.37999999999999545, 11.48378591275253768 ) ) ;
#12646=CARTESIAN_POINT ( 'NONE',  ( 0.000000000000000000, 108.9300000000000068, -12.00000000000000178 ) ) ;
#12647=CARTESIAN_POINT ( 'NONE',  ( 6.600044012045160891, 62.92306809907158538, 11.77869433798020715 ) ) ;
#12648=CARTESIAN_POINT ( 'NONE',  ( 3.074525348032466798, 41.79056361433298861, 13.14524077292679749 ) ) ;
#12649=CARTESIAN_POINT ( 'NONE',  ( 10.61485236059771786, 48.74751858167648066, -8.341608621204406049 ) ) ;
#12652=CARTESIAN_POINT ( 'NONE',  ( 11.76794919243112325, 67.43000000000000682, 1.441158131103945434E-15 ) ) ;
#12656=CARTESIAN_POINT ( 'NONE',  ( -0.5621853200489609348, 43.20021404884155203, -13.48847943194547483 ) ) ;
#12661=CARTESIAN_POINT ( 'NONE',  ( 8.311444000958445599, 65.99692735864155679, 10.63876800420476698 ) ) ;
#12662=CARTESIAN_POINT ( 'NONE',  ( -13.49999999999999822, 82.78000000000001535, -4.386415899144240349 ) ) ;
#12663=CARTESIAN_POINT ( 'NONE',  ( 11.76794919243112325, 61.27999999999999403, 3.823638476888996607 ) ) ;
#12664=CARTESIAN_POINT ( 'NONE',  ( 6.750022565184456980, 31.92926174983937671, 11.69132992304556673 ) ) ;
#12665=CARTESIAN_POINT ( 'NONE',  ( 11.76794919243112680, 61.57999999999999829, -3.823638476888993942 ) ) ;
#12666=CARTESIAN_POINT ( 'NONE',  ( -12.53713441344856072, 46.74807280042572444, -5.007212535617639126 ) ) ;
#12667=CARTESIAN_POINT ( 'NONE',  ( 6.273726922098238568, 45.95023082440073381, -11.95538543147346822 ) ) ;
#12668=CARTESIAN_POINT ( 'NONE',  ( 8.093548673611641320, 69.87292072123501896, -10.80485039633414601 ) ) ;
#12670=CARTESIAN_POINT ( 'NONE',  ( 11.28924783770012219, 30.70771545723502172, -7.402899756116059216 ) ) ;
#12673=CARTESIAN_POINT ( 'NONE',  ( -13.36489353327162632, 55.86322898162038086, -1.909449360262173379 ) ) ;
#12675=CARTESIAN_POINT ( 'NONE',  ( 12.51119357652121344, 33.24557417593518238, 5.072678182924500234 ) ) ;
#12677=CARTESIAN_POINT ( 'NONE',  ( 8.190820164315349317, 39.86853779885616689, -10.73135278157234396 ) ) ;
#12679=CARTESIAN_POINT ( 'NONE',  ( -13.46074512384716115, 61.89434089339735579, -1.032255895472621088 ) ) ;
#12680=EDGE_LOOP ( 'NONE', ( #10314, #15584, #3844, #10660 ) ) ;
#12681=CARTESIAN_POINT ( 'NONE',  ( -13.21933525180101121, 40.83269136074343919, -2.754417799056112059 ) ) ;
#12684=CARTESIAN_POINT ( 'NONE',  ( 13.01373734262449311, 48.30174901136457066, 3.592500545224007968 ) ) ;
#12686=CARTESIAN_POINT ( 'NONE',  ( -10.92172942406179104, 35.22999999999999687, 7.935100905948387684 ) ) ;
#12688=CARTESIAN_POINT ( 'NONE',  ( -0.03222258848736525572, 46.18115845073967307, -13.49996702218131261 ) ) ;
#12692=CARTESIAN_POINT ( 'NONE',  ( 10.55718600268835772, 54.10925673300133099, 8.414815218569547284 ) ) ;
#12695=CARTESIAN_POINT ( 'NONE',  ( -10.08098277730616310, 64.58357994695883519, -8.980069834276186214 ) ) ;
#12698=CARTESIAN_POINT ( 'NONE',  ( -10.16207160523757835, 34.58782041647135941, -8.887247792507393385 ) ) ;
#12700=CARTESIAN_POINT ( 'NONE',  ( 8.623259911401813582, 78.01131858175091338, 10.38704685952772699 ) ) ;
#12704=CARTESIAN_POINT ( 'NONE',  ( 11.31643680712456401, 72.15395803400841146, 7.362692955525563576 ) ) ;
#12706=CARTESIAN_POINT ( 'NONE',  ( -13.49999999999999822, 65.07999999999999829, 4.386415899144235908 ) ) ;
#12707=CARTESIAN_POINT ( 'NONE',  ( -5.794542289981962746, 52.39086140184792129, -12.19316736257134437 ) ) ;
#12708=CARTESIAN_POINT ( 'NONE',  ( 3.636496289402157078, 35.03000000000000114, -11.19198476289190936 ) ) ;
#12710=CARTESIAN_POINT ( 'NONE',  ( -8.691771469529815392E-16, 55.67999999999999972, 14.19474002721660355 ) ) ;
#12713=CARTESIAN_POINT ( 'NONE',  ( 9.990009898246189124, 69.07869612477813348, 9.080182975746776464 ) ) ;
#12715=EDGE_CURVE ( 'NONE', #4556, #14181, #1367, .T. ) ;
#12716=DIRECTION ( 'NONE',  ( 0.000000000000000000, 0.000000000000000000, -1.000000000000000000 ) ) ;
#12718=CARTESIAN_POINT ( 'NONE',  ( -10.55719944458992998, 73.60929019257851280, -8.414036521270118030 ) ) ;
#12720=CARTESIAN_POINT ( 'NONE',  ( -11.76794919243112325, 80.92999999999767624, -5.919446256302011733E-11 ) ) ;
#12724=CARTESIAN_POINT ( 'NONE',  ( -7.272992578804310604, 42.37999999999999545, 10.01041549318726886 ) ) ;
#12725=DIRECTION ( 'NONE',  ( 1.000000000000000000, 0.000000000000000000, 0.000000000000000000 ) ) ;
#12726=CARTESIAN_POINT ( 'NONE',  ( -11.26568359562893029, 32.20920359819594125, 7.438710005716663964 ) ) ;
#12727=CARTESIAN_POINT ( 'NONE',  ( 5.795435194651767041, 74.89090867474413926, 12.19293766284020997 ) ) ;
#12728=CYLINDRICAL_SURFACE ( 'NONE', #8270, 13.50000000000000000 ) ;
#12729=CARTESIAN_POINT ( 'NONE',  ( -4.171729424061791036, 79.53000000000000114, 12.83926296998457239 ) ) ;
#12730=CARTESIAN_POINT ( 'NONE',  ( 2.775048885307294100, 52.08055395342481120, -13.21813026032616456 ) ) ;
#12734=CARTESIAN_POINT ( 'NONE',  ( 0.000000000000000000, 80.93000000000000682, 0.000000000000000000 ) ) ;
#12735=CARTESIAN_POINT ( 'NONE',  ( -0.2547729068321639145, 49.18915660688823976, -13.49793348477203203 ) ) ;
#12736=CARTESIAN_POINT ( 'NONE',  ( 2.567202442714003219, 62.77235785574046645, 13.25368192155630709 ) ) ;
#12737=CARTESIAN_POINT ( 'NONE',  ( 3.053862296787171360, 41.78983512861384497, 13.15006426398930550 ) ) ;
#12738=CARTESIAN_POINT ( 'NONE',  ( 10.67465755508037617, 48.74414866033003335, -8.264490526360749101 ) ) ;
#12741=CARTESIAN_POINT ( 'NONE',  ( 9.520470885617715595, 64.12999999999999545, 6.917026985038134512 ) ) ;
#12746=CARTESIAN_POINT ( 'NONE',  ( -0.7362654489741128350, 80.93000000000000682, -13.00758670407025086 ) ) ;
#12748=CARTESIAN_POINT ( 'NONE',  ( 5.706916115397674183, 65.88744019540719421, 12.23443642958042687 ) ) ;
#12750=CARTESIAN_POINT ( 'NONE',  ( -11.76794919243112325, 50.77999999999998693, -3.823638476888998827 ) ) ;
#12751=CARTESIAN_POINT ( 'NONE',  ( -9.520470885617717371, 57.23000000000000398, 6.917026985038133624 ) ) ;
#12752=CARTESIAN_POINT ( 'NONE',  ( -12.97183641456126502, 46.79586893643946865, -3.748799059863759275 ) ) ;
#12753=CARTESIAN_POINT ( 'NONE',  ( 12.62323547485571851, 45.60479695812286138, -4.831092889884269326 ) ) ;
#12754=CARTESIAN_POINT ( 'NONE',  ( 5.666431094655353107, 69.97415835491503344, -12.25323033163396680 ) ) ;
#12755=AXIS2_PLACEMENT_3D ( 'NONE', #6935, #13709, #5784 ) ;
#12757=CARTESIAN_POINT ( 'NONE',  ( 5.837233680499599231, 30.96745156617631523, -12.17279074635751535 ) ) ;
#12758=CARTESIAN_POINT ( 'NONE',  ( -12.15097179258997073, 55.71389053688777437, -5.882769356534193861 ) ) ;
#12759=CARTESIAN_POINT ( 'NONE',  ( -2.759338081070636051, 50.58068028277337191, 13.21652401455469850 ) ) ;
#12760=CARTESIAN_POINT ( 'NONE',  ( 13.29140006584865574, 33.34684006576951276, 2.364050045256024468 ) ) ;
#12761=CARTESIAN_POINT ( 'NONE',  ( 4.264411549263888546, 43.02666127736967638, -12.80881877248479128 ) ) ;
#12762=CARTESIAN_POINT ( 'NONE',  ( 11.16754829665910798, 39.71527879939828409, -7.585325781705508419 ) ) ;
#12764=CARTESIAN_POINT ( 'NONE',  ( -13.45264947251579102, 61.96924832227834656, 1.132187044750279536 ) ) ;
#12770=CARTESIAN_POINT ( 'NONE',  ( 8.312300566215480302, 57.86311205854902795, -10.64140145696314121 ) ) ;
#12771=CARTESIAN_POINT ( 'NONE',  ( 5.638949650228808785, 78.97550847713628741, -12.27579838479350194 ) ) ;
#12772=ADVANCED_FACE ( 'NONE', ( #1841 ), #12728, .T. ) ;
#12773=CARTESIAN_POINT ( 'NONE',  ( 3.636496289402154414, 75.83000000000001251, 11.19198476289190936 ) ) ;
#12774=CARTESIAN_POINT ( 'NONE',  ( 13.50000000000000355, 41.57999999999999119, -4.386415899144233244 ) ) ;
#12776=CARTESIAN_POINT ( 'NONE',  ( -4.302195761316967015, 46.33469344025497350, -12.79681310502842884 ) ) ;
#12780=CARTESIAN_POINT ( 'NONE',  ( 3.313926305061611455, 53.79912973232266893, 13.08694846433931858 ) ) ;
#12781=ORIENTED_EDGE ( 'NONE', *, *, #1130, .T. ) ;
#12785=CARTESIAN_POINT ( 'NONE',  ( 2.000359907488380884, 67.10810958415484606, -13.35850880710533772 ) ) ;
#12786=CARTESIAN_POINT ( 'NONE',  ( -8.288051004685030421, 34.49586041775943102, -10.65699721998313976 ) ) ;
#12789=CARTESIAN_POINT ( 'NONE',  ( 5.969853497853632618, 77.89748442894395453, 12.11621569323665781 ) ) ;
#12792=DIRECTION ( 'NONE',  ( 0.000000000000000000, 0.000000000000000000, 1.000000000000000000 ) ) ;
#12793=CARTESIAN_POINT ( 'NONE',  ( 12.17897594257505034, 72.64436298052412155, -5.840729639915025473 ) ) ;
#12795=CARTESIAN_POINT ( 'NONE',  ( 4.171729424061789260, 62.82999999999999829, 12.83926296998457417 ) ) ;
#12796=CARTESIAN_POINT ( 'NONE',  ( -0.5918238176221393143, 52.20127980115676536, -13.49999999999999822 ) ) ;
#12797=AXIS2_PLACEMENT_3D ( 'NONE', #8673, #6187, #435 ) ;
#12798=CARTESIAN_POINT ( 'NONE',  ( 11.76794919243112325, 34.28000000000000114, 3.823638476888996607 ) ) ;
#12800=CARTESIAN_POINT ( 'NONE',  ( -13.49999999999999822, 60.78000000000000114, -4.386415899144240349 ) ) ;
#12802=CARTESIAN_POINT ( 'NONE',  ( 3.479075845151533564, 68.80513213033660236, 13.04407958699342096 ) ) ;
#12804=CARTESIAN_POINT ( 'NONE',  ( 2.138189944381231555, 72.10311857767972299, -13.50000000000000178 ) ) ;
#12806=CARTESIAN_POINT ( 'NONE',  ( -13.46101605912647337, 73.89364307768008189, -1.052211620652566681 ) ) ;
#12807=CARTESIAN_POINT ( 'NONE',  ( -9.269880003010733560, 76.54218929687127115, -9.814641767077731060 ) ) ;
#12809=CARTESIAN_POINT ( 'NONE',  ( -7.499999999999999112, 102.9299999999999073, -9.367496997597655195 ) ) ;
#12810=ORIENTED_EDGE ( 'NONE', *, *, #744, .F. ) ;
#12811=CARTESIAN_POINT ( 'NONE',  ( 3.636496289402154414, 33.82999999999999829, 11.19198476289190936 ) ) ;
#12813=CARTESIAN_POINT ( 'NONE',  ( -9.816093411897769627, 32.29071182833408926, 9.278652180130679383 ) ) ;
#12814=CARTESIAN_POINT ( 'NONE',  ( 1.061297819423365540, 74.71813576689515912, 13.45990699938060331 ) ) ;
#12817=CARTESIAN_POINT ( 'NONE',  ( 0.1963306558083189324, 30.65984393938648722, 13.47512034797125580 ) ) ;
#12818=CARTESIAN_POINT ( 'NONE',  ( 12.61419996821527789, 51.60431945238178741, -4.809772638418851720 ) ) ;
#12820=CARTESIAN_POINT ( 'NONE',  ( -12.47471083728540719, 38.11787751918529921, 5.160988080696901292 ) ) ;
#12821=CARTESIAN_POINT ( 'NONE',  ( 11.96006256146126390, 36.66123345659914889, -6.261549132648513094 ) ) ;
#12825=CARTESIAN_POINT ( 'NONE',  ( -2.138189944381257757, 60.25688142232026934, -13.49999999999999289 ) ) ;
#12826=CARTESIAN_POINT ( 'NONE',  ( -11.76349012782661951, 80.93000000000003524, 2.235278043115120461 ) ) ;
#12827=CARTESIAN_POINT ( 'NONE',  ( 12.26213682806825567, 48.63686586570011627, -5.647125736108378646 ) ) ;
#12830=ORIENTED_EDGE ( 'NONE', *, *, #13515, .T. ) ;
#12831=CARTESIAN_POINT ( 'NONE',  ( -11.76794919243112325, 62.92999999999999972, -2.882316262207890869E-15 ) ) ;
#12836=CARTESIAN_POINT ( 'NONE',  ( 0.9520164539180778762, 76.14576922985241936, -13.46646205020914699 ) ) ;
#12840=CARTESIAN_POINT ( 'NONE',  ( 11.86519348393725970, 66.19162581074351692, 6.439609381232799024 ) ) ;
#12841=CARTESIAN_POINT ( 'NONE',  ( -13.49999999999999822, 80.07999999999998408, 4.386415899144235908 ) ) ;
#12842=CARTESIAN_POINT ( 'NONE',  ( 11.76794919243112325, 49.42999999999999972, 1.441158131103945434E-15 ) ) ;
#12843=CARTESIAN_POINT ( 'NONE',  ( -9.954157355241310512, 59.28317716132346504, 9.119471290265320107 ) ) ;
#12844=CARTESIAN_POINT ( 'NONE',  ( 10.52479684053763620, 45.75252738753766124, -8.454649685126563341 ) ) ;
#12845=CARTESIAN_POINT ( 'NONE',  ( 8.136481847135470957, 69.87099141200431518, -10.77264556894015257 ) ) ;
#12846=CARTESIAN_POINT ( 'NONE',  ( 13.04595580355921136, 30.55377996617673375, -3.472152230004342144 ) ) ;
#12847=CARTESIAN_POINT ( 'NONE',  ( -13.30909409913599006, 55.85048046686320333, -2.263500039713061796 ) ) ;
#12848=CARTESIAN_POINT ( 'NONE',  ( -3.859537734194087744, 50.54122529663226260, 12.93654704252784882 ) ) ;
#12849=CARTESIAN_POINT ( 'NONE',  ( 9.846585001760786326, 63.78875900491937045, -9.235520396473821947 ) ) ;
#12850=CARTESIAN_POINT ( 'NONE',  ( 3.028015045671256900, 43.07112457749870060, -13.15637380351495089 ) ) ;
#12851=CARTESIAN_POINT ( 'NONE',  ( 12.04987116223745147, 39.65426265503597136, -6.087320985860698030 ) ) ;
#12852=ORIENTED_EDGE ( 'NONE', *, *, #15881, .F. ) ;
#12853=CARTESIAN_POINT ( 'NONE',  ( -13.20951207043308351, 61.83148949826453844, -2.786434271337515867 ) ) ;
#12854=ORIENTED_EDGE ( 'NONE', *, *, #12423, .F. ) ;
#12855=ORIENTED_EDGE ( 'NONE', *, *, #11299, .T. ) ;
#12858=CARTESIAN_POINT ( 'NONE',  ( 13.08213917803373327, 48.31138509259425717, 3.332853635039773721 ) ) ;
#12859=EDGE_CURVE ( 'NONE', #149, #225, #4175, .T. ) ;
#12860=CARTESIAN_POINT ( 'NONE',  ( 10.49489484557887664, 57.75417860629620037, -8.491615491609847410 ) ) ;
#12861=CARTESIAN_POINT ( 'NONE',  ( 4.440276171078080480, 79.02008338065117243, -12.75216793947442895 ) ) ;
#12862=CARTESIAN_POINT ( 'NONE',  ( 2.272985001014427788E-15, 80.18000000000000682, -12.37355403259654985 ) ) ;
#12868=CARTESIAN_POINT ( 'NONE',  ( 11.54936908542054219, 54.16929694213506252, 6.991207511958483778 ) ) ;
#12871=EDGE_LOOP ( 'NONE', ( #12067, #14615, #9608, #13364 ) ) ;
#12872=CARTESIAN_POINT ( 'NONE',  ( 5.334058230349888241, 66.98693642648522939, -12.40152507886732458 ) ) ;
#12874=CYLINDRICAL_SURFACE ( 'NONE', #15920, 13.50000000000000000 ) ;
#12875=CARTESIAN_POINT ( 'NONE',  ( -0.3076292557609190959, 59.66893862671528126, 13.49651329554702883 ) ) ;
#12877=CYLINDRICAL_SURFACE ( 'NONE', #11106, 8.999999999999998224 ) ;
#12878=CARTESIAN_POINT ( 'NONE',  ( 11.48707053576665160, 72.16510984276516183, 7.092083023523681362 ) ) ;
#12881=CARTESIAN_POINT ( 'NONE',  ( 2.607531440858944223E-15, 49.17999999999999972, -14.19474002721660355 ) ) ;
#12882=CARTESIAN_POINT ( 'NONE',  ( -11.20412284216293664, 52.64695269834547275, -7.531112085699138703 ) ) ;
#12883=CARTESIAN_POINT ( 'NONE',  ( -13.49999999999999822, 52.07999999999999119, 4.386415899144235908 ) ) ;
#12884=CARTESIAN_POINT ( 'NONE',  ( 8.343458848123583849, 77.88000000000000966, -11.48378591275253768 ) ) ;
#12885=CARTESIAN_POINT ( 'NONE',  ( 1.801739650404782012, 68.74478696605716266, 13.37942991408443660 ) ) ;
#12890=CARTESIAN_POINT ( 'NONE',  ( -2.506966426393243630, 65.58985874448374886, 13.26518509152382030 ) ) ;
#12891=CARTESIAN_POINT ( 'NONE',  ( -11.64508433789041675, 80.92999999999999261, -2.787474072191427510 ) ) ;
#12894=VERTEX_POINT ( 'NONE', #2162 ) ;
#12895=CARTESIAN_POINT ( 'NONE',  ( 4.171729424061791924, 51.03000000000000114, -12.83926296998457239 ) ) ;
#12896=CARTESIAN_POINT ( 'NONE',  ( -4.345187459725349477, 40.33626392346928213, -12.78162779989500031 ) ) ;
#12897=CARTESIAN_POINT ( 'NONE',  ( -12.71943797413999988, 31.76515268481853838, -4.567396653572560083 ) ) ;
#12898=CARTESIAN_POINT ( 'NONE',  ( 3.539998177671969781, 74.80728451192426576, 13.02775590127090943 ) ) ;
#12899=CARTESIAN_POINT ( 'NONE',  ( 12.05005302082176044, 60.20532830390902035, 6.102261332639054459 ) ) ;
#12902=CARTESIAN_POINT ( 'NONE',  ( 4.171729424061791924, 72.03000000000000114, -12.83926296998457239 ) ) ;
#12903=CARTESIAN_POINT ( 'NONE',  ( 13.49014888215909203, 51.44774366630825568, -0.5156731279918199684 ) ) ;
#12904=CARTESIAN_POINT ( 'NONE',  ( -8.992785922287852785, 38.33140772955672304, 10.07305468610416987 ) ) ;
#12905=CARTESIAN_POINT ( 'NONE',  ( 12.05351726939188062, 36.65397582186106717, -6.080038080744102125 ) ) ;
#12907=EDGE_CURVE ( 'NONE', #12392, #11794, #6509, .T. ) ;
#12908=DIRECTION ( 'NONE',  ( 0.000000000000000000, -1.000000000000000000, 0.000000000000000000 ) ) ;
#12909=CARTESIAN_POINT ( 'NONE',  ( -4.484750243281778737, 77.51863919606381614, 12.74519890846088899 ) ) ;
#12910=CYLINDRICAL_SURFACE ( 'NONE', #11100, 13.50000000000000000 ) ;
#12911=CARTESIAN_POINT ( 'NONE',  ( 13.17195031443938547, 48.53499887136660362, -2.961669012155129010 ) ) ;
#12914=CARTESIAN_POINT ( 'NONE',  ( 3.636496289402157078, 62.03000000000000114, -11.19198476289190936 ) ) ;
#12919=CARTESIAN_POINT ( 'NONE',  ( 1.293831188543124400, 76.13348380643110147, -13.43844946783898031 ) ) ;
#12921=CARTESIAN_POINT ( 'NONE',  ( 4.171729424061789260, 77.82999999999999829, 12.83926296998457417 ) ) ;
#12922=CARTESIAN_POINT ( 'NONE',  ( 7.272992578804308828, 51.97999999999998977, 10.01041549318726709 ) ) ;
#12923=CARTESIAN_POINT ( 'NONE',  ( -13.50510647780722095, 58.92757876024586494, -0.06544038226817162907 ) ) ;
#12924=CARTESIAN_POINT ( 'NONE',  ( 11.88858366554402757, 45.19312755830633677, 6.405256951248860631 ) ) ;
#12925=CARTESIAN_POINT ( 'NONE',  ( 5.622204590887941222, 69.97583870266406336, -12.27358394821601273 ) ) ;
#12926=CARTESIAN_POINT ( 'NONE',  ( 1.753268986668952691E-06, 80.68004880551006863, 13.49999999999977263 ) ) ;
#12927=CARTESIAN_POINT ( 'NONE',  ( 13.48213564506632522, 30.40254256736282557, 0.7883542253392303856 ) ) ;
#12928=CARTESIAN_POINT ( 'NONE',  ( -13.47515042673155428, 55.90172887063787499, -0.8194478264856674965 ) ) ;
#12930=CARTESIAN_POINT ( 'NONE',  ( -11.08263705370628749, 50.22048702777903628, 7.709197264984768871 ) ) ;
#12931=CARTESIAN_POINT ( 'NONE',  ( 8.560836630084285304, 63.85167834306816559, -10.44139667627318069 ) ) ;
#12933=CARTESIAN_POINT ( 'NONE',  ( 12.66463686987026271, 39.60059382856163523, -4.718913685864155383 ) ) ;
#12935=CARTESIAN_POINT ( 'NONE',  ( -7.353569438412593584, 61.45463544861350869, -11.32146132068871580 ) ) ;
#12940=CARTESIAN_POINT ( 'NONE',  ( 9.541952228206893594, 48.05573085917402665, 9.550091761750962860 ) ) ;
#12941=CARTESIAN_POINT ( 'NONE',  ( 10.04127278578228477, 57.77887113727757651, -9.033026199713900084 ) ) ;
#12942=CARTESIAN_POINT ( 'NONE',  ( 11.13970935207611568, 78.71701762036461503, -7.626765219171713461 ) ) ;
#12943=CARTESIAN_POINT ( 'NONE',  ( 11.76794919243112325, 76.42999999999999261, 1.441158131103945434E-15 ) ) ;
#12944=CARTESIAN_POINT ( 'NONE',  ( 2.272985001014427788E-15, 83.17999999999999261, -12.37355403259654985 ) ) ;
#12951=CARTESIAN_POINT ( 'NONE',  ( -10.92172942406178926, 78.63000000000000966, -7.935100905948389460 ) ) ;
#12952=CARTESIAN_POINT ( 'NONE',  ( 8.246725363360754457, 33.86600348702350516, -10.68840209571144939 ) ) ;
#12961=DIRECTION ( 'NONE',  ( 0.000000000000000000, -0.000000000000000000, 1.000000000000000000 ) ) ;
#12963=CARTESIAN_POINT ( 'NONE',  ( 2.443868322553949479, 71.76788406128898146, 13.27695547668219866 ) ) ;
#12964=CARTESIAN_POINT ( 'NONE',  ( 13.50000000000000355, 54.57999999999999119, -4.386415899144233244 ) ) ;
#12965=CARTESIAN_POINT ( 'NONE',  ( -0.4388680196204213790, 71.66422011136278059, 13.49292316262332214 ) ) ;
#12967=VECTOR ( 'NONE', #14585, 1000.000000000000000 ) ;
#12969=CARTESIAN_POINT ( 'NONE',  ( -11.63268444319199624, 68.18495566772109839, 6.850846920013293762 ) ) ;
#12971=CARTESIAN_POINT ( 'NONE',  ( 5.390530401168515340, 54.98489645169363627, -12.37944730132690196 ) ) ;
#12973=CARTESIAN_POINT ( 'NONE',  ( 8.549612433556128696E-08, 65.68000242247177312, 13.49999999999999822 ) ) ;
#12975=CARTESIAN_POINT ( 'NONE',  ( -11.21669893531349160, 35.21226868908650687, 7.512399413318213703 ) ) ;
#12978=CARTESIAN_POINT ( 'NONE',  ( -11.76794919243112325, 32.92999999999999972, -2.882316262207890869E-15 ) ) ;
#12979=CARTESIAN_POINT ( 'NONE',  ( -5.257100738639275406, 40.37012037508893769, -12.43485227326261011 ) ) ;
#12980=CARTESIAN_POINT ( 'NONE',  ( -11.86009848853153947, 31.69125030478712191, -6.448902088085707973 ) ) ;
#12981=FACE_BOUND ( 'NONE', #15131, .T. ) ;
#12982=CARTESIAN_POINT ( 'NONE',  ( 11.88531977884646196, 60.19299833890768525, 6.407369536219499118 ) ) ;
#12984=CARTESIAN_POINT ( 'NONE',  ( 4.178864255851000829E-14, 61.67999999999999261, 13.50000000000000000 ) ) ;
#12986=CARTESIAN_POINT ( 'NONE',  ( 4.171729424061789260, 73.83000000000001251, 12.83926296998457417 ) ) ;
#12987=CARTESIAN_POINT ( 'NONE',  ( 12.05091702511513851, 51.65458203422696926, -6.096857118557952759 ) ) ;
#12988=CARTESIAN_POINT ( 'NONE',  ( -10.33299960000793050, 38.26336937052408871, 8.690946034728787239 ) ) ;
#12989=CARTESIAN_POINT ( 'NONE',  ( 13.04240740954509015, 36.55426163316852239, -3.485073724549926588 ) ) ;
#12992=( BOUNDED_CURVE ( )  B_SPLINE_CURVE ( 2, ( #13609, #14925, #9403, #10976, #13691, #1323, #9575, #8335, #7, #7007, #190, #17414, #15994 ),
 .UNSPECIFIED., .F., .F. ) 
 B_SPLINE_CURVE_WITH_KNOTS ( ( 3, 2, 2, 2, 2, 2, 3 ),
 ( 0.5416666666666666297, 0.5444444444444443976, 0.5500000000000000444, 0.5555555555555555802, 0.5611111111111111160, 0.5666666666666666519, 0.5694444444444444198 ),
 .UNSPECIFIED. ) 
 CURVE ( )  GEOMETRIC_REPRESENTATION_ITEM ( )  RATIONAL_B_SPLINE_CURVE ( ( 0.9755282581475768211, 0.9755282581475768211, 1.000000000000000000, 0.9510565162951535312, 1.000000000000000000, 0.9510565162951535312, 1.000000000000000000, 0.9510565162951535312, 1.000000000000000000, 0.9510565162951535312, 1.000000000000000000, 0.9755282581475768211, 0.9755282581475768211 ) ) 
 REPRESENTATION_ITEM ( '' )  );
#12993=CARTESIAN_POINT ( 'NONE',  ( -10.79460918060730990, 77.23732893913023645, 8.107729363714126336 ) ) ;
#12994=CARTESIAN_POINT ( 'NONE',  ( -3.066993958782973095, 80.56964720549299841, 13.15436491285448106 ) ) ;
#12995=CARTESIAN_POINT ( 'NONE',  ( 3.833221879840224222, 41.81748144897261454, 12.94619382350246184 ) ) ;
#12996=ORIENTED_EDGE ( 'NONE', *, *, #14449, .T. ) ;
#13000=CARTESIAN_POINT ( 'NONE',  ( -7.576616670048093940E-16, 57.67999999999999261, 12.37355403259654807 ) ) ;
#13002=DIRECTION ( 'NONE',  ( 0.000000000000000000, -1.000000000000000000, 0.000000000000000000 ) ) ;
#13003=CARTESIAN_POINT ( 'NONE',  ( 2.150159292860549076, 80.92999999999997840, -13.03677673010519733 ) ) ;
#13006=CARTESIAN_POINT ( 'NONE',  ( -8.343458848123576743, 82.47999999999997556, -11.48378591275254301 ) ) ;
#13008=CARTESIAN_POINT ( 'NONE',  ( -7.272992578804307939, 50.47999999999999687, -10.01041549318726886 ) ) ;
#13010=CARTESIAN_POINT ( 'NONE',  ( -11.20034620794313440, 59.21330483900249675, 7.537432996273548014 ) ) ;
#13011=B_SPLINE_CURVE_WITH_KNOTS ( 'NONE', 3,
 ( #5118, #2850, #3779, #15872, #2761, #12421, #13642, #41, #5446, #15046, #2941, #132, #12240, #9191, #8193, #1536, #4377, #13555, #15132, #8370, #8105, #10833, #16195, #7043, #4107, #1446, #308, #5538, #16291, #13727, #9609, #12329, #13470, #224, #11011, #16382, #1625, #5717, #9785, #7776, #13149, #1037, #1712, #16562, #12593, #569, #14161, #1795, #11271, #7125, #742, #11187, #1879, #3303, #7294, #15223, #9959, #5976, #7473, #10046, #8716, #8459, #3029, #15307, #1963, #16648, #6062, #4469, #8632, #11358, #484, #16907, #5892, #16818, #13983, #10212, #12764, #7386, #13813, #7207, #4555, #396, #12511, #11445, #3212, #5803, #9874, #4810, #652, #3121, #4726, #8547, #10127, #13898, #2049, #12679, #11529, #15480, #3391, #8804, #16732, #4639, #12853, #15395, #14076, #6152, #7731, #13022, #14245, #11701, #3826, #2303, #14501, #16992, #10297, #819, #17253, #11790, #4897, #15832, #14415, #14329, #14594, #15917, #17167, #9240, #3648, #3476, #15565, #4982, #2388, #17078, #1082, #15649, #9062, #13107, #7645, #11962, #904, #11878, #994, #6406, #5077, #8890, #2130, #10471, #7556, #12935, #5252, #6495, #10385, #6230, #11617, #17341, #7824, #3559, #5166, #8973, #10558, #2218, #2474, #3737, #15739, #6315, #9154, #7907, #13196, #13282, #1170, #6581, #17423, #10638, #5338, #10723, #13362, #9412 ),
 .UNSPECIFIED., .F., .F.,
 ( 4, 2, 2, 1, 2, 2, 1, 2, 2, 1, 2, 2, 1, 1, 2, 2, 2, 1, 2, 2, 2, 2, 2, 2, 2, 2, 1, 1, 1, 2, 2, 1, 1, 1, 2, 2, 2, 2, 2, 2, 2, 1, 2, 2, 2, 2, 2, 2, 1, 1, 1, 2, 1, 2, 2, 1, 1, 2, 2, 2, 1, 1, 1, 1, 2, 2, 2, 2, 2, 2, 2, 1, 2, 2, 1, 2, 2, 2, 2, 2, 2, 2, 1, 2, 2, 2, 1, 2, 2, 1, 2, 2, 2, 2, 1, 2, 2, 1, 2, 2, 2, 2, 4 ),
 ( 0.3578158167825879477, 0.3587362859346358013, 0.3591965205106597558, 0.3593115791546657722, 0.3593691084766687527, 0.3593978731376702429, 0.3594266377986717331, 0.3596567550866837104, 0.3605772242387316195, 0.3606059888997331098, 0.3606203712302338271, 0.3606347535607346000, 0.3606922828827375804, 0.3608073415267435968, 0.3610374588147555741, 0.3614976933907795287, 0.3617278106787915060, 0.3618428693227974668, 0.3618716339837989571, 0.3619003986448004473, 0.3619579279668034832, 0.3624181625428274378, 0.3633386316948752914, 0.3642591008469232006, 0.3643741594909292170, 0.3644029241519307072, 0.3644316888129321974, 0.3644892181349351779, 0.3647193354229471551, 0.3651795699989711652, 0.3661000391510190743, 0.3665602737270430289, 0.3667903910150550617, 0.3668479203370580422, 0.3668766849980595324, 0.3669054496590610226, 0.3670205083030670390, 0.3688614466071628017, 0.3693216811831867008, 0.3693792105051897368, 0.3694367398271927172, 0.3695517984711986781, 0.3697819157592106554, 0.3707023849112585645, 0.3716228540633064181, 0.3718529713513183954, 0.3718817360123198856, 0.3719105006733214314, 0.3719680299953244118, 0.3720830886393303727, 0.3725433232153543273, 0.3730035577913782818, 0.3731186164353842982, 0.3731329987658850156, 0.3731473810963857884, 0.3731761457573872787, 0.3732336750793902591, 0.3734637923674022364, 0.3743842615194501455, 0.3744130261804516357, 0.3744417908414531260, 0.3744993201634561619, 0.3746143788074621228, 0.3748444960954741001, 0.3753047306714980547, 0.3762251998235459638, 0.3766854343995698629, 0.3768004930435758792, 0.3769155516875818401, 0.3771456689755938174, 0.3780661381276417266, 0.3781236674496447070, 0.3781380497801454799, 0.3781524321106461972, 0.3781811967716476874, 0.3782962554156537038, 0.3785263727036656811, 0.3789866072796896912, 0.3792167245677016685, 0.3793317832117076849, 0.3793893125337106653, 0.3794180771947121555, 0.3794468418557136458, 0.3799070764317378224, 0.3808275455837860646, 0.3817480147358343623, 0.3818630733798403787, 0.3818918380408418689, 0.3819206027018434146, 0.3819781320238463951, 0.3822082493118584834, 0.3826684838878826600, 0.3835889530399310132, 0.3840491876159551898, 0.3842793049039672226, 0.3843943635479732945, 0.3844231282089747848, 0.3844518928699763305, 0.3845094221919793109, 0.3854298913440276086, 0.3863503604960759064, 0.3868105950721000275, 0.3872708296481242041 ),
 .UNSPECIFIED. ) ;
#13012=CARTESIAN_POINT ( 'NONE',  ( 10.47861606810065815, 45.10486826704778451, 8.511906612892380153 ) ) ;
#13013=CARTESIAN_POINT ( 'NONE',  ( 11.94609836220409349, 69.66229794021633381, -6.288142491076607499 ) ) ;
#13015=CARTESIAN_POINT ( 'NONE',  ( 11.77408743055708662, 30.67508156744361969, -6.605444128499801337 ) ) ;
#13016=CARTESIAN_POINT ( 'NONE',  ( -10.98298365945945143, 56.22644425589727035, 7.850925719499952216 ) ) ;
#13017=CARTESIAN_POINT ( 'NONE',  ( -5.569062747661596369, 50.47790839199158341, 12.29782247994843658 ) ) ;
#13019=CARTESIAN_POINT ( 'NONE',  ( 2.530352284268557295, 43.08905591751716457, -13.26307597662109927 ) ) ;
#13020=CARTESIAN_POINT ( 'NONE',  ( 7.498839979050778481, 39.89913384926502005, -11.22908298276431260 ) ) ;
#13021=EDGE_LOOP ( 'NONE', ( #4899, #4788, #1104, #3673, #8034, #9035, #7650, #14137, #570, #6517 ) ) ;
#13022=CARTESIAN_POINT ( 'NONE',  ( -12.64888242172768607, 61.75875439202012274, -4.738583482749483267 ) ) ;
#13025=CARTESIAN_POINT ( 'NONE',  ( -8.571272707445116268, 40.50886853748669836, -10.43127125671136568 ) ) ;
#13026=ORIENTED_EDGE ( 'NONE', *, *, #2873, .F. ) ;
#13029=CARTESIAN_POINT ( 'NONE',  ( 6.014033562793300369, 47.89924598142680878, 12.09241346544142104 ) ) ;
#13030=CARTESIAN_POINT ( 'NONE',  ( 11.16378927044967462, 57.71547821250464949, -7.596269605373482392 ) ) ;
#13031=CARTESIAN_POINT ( 'NONE',  ( 6.974580545495159711, 78.92141596235254042, -11.55926377139148897 ) ) ;
#13032=CARTESIAN_POINT ( 'NONE',  ( -11.76794919243112325, 80.78000000000000114, -3.823638476888998827 ) ) ;
#13033=CARTESIAN_POINT ( 'NONE',  ( 11.76794919243112325, 82.27999999999998693, 3.823638476888996607 ) ) ;
#13036=B_SPLINE_CURVE_WITH_KNOTS ( 'NONE', 3,
 ( #1690, #8172, #6931, #16359, #13535, #3007, #5518, #7105, #203, #9763, #1605, #11078, #16271, #6842, #7021, #16630, #2831, #13791, #1425, #12400, #9676, #12489, #4447, #12309, #4177, #5609, #11165, #11251, #8262, #4354, #8437, #4266, #12218, #15026, #8528, #288, #374, #9589, #14939, #10900, #9854, #1778, #13622, #5780 ),
 .UNSPECIFIED., .F., .F.,
 ( 4, 2, 2, 2, 2, 2, 2, 2, 2, 2, 2, 2, 2, 2, 2, 2, 2, 2, 2, 2, 2, 4 ),
 ( 0.03689401835950767428, 0.03766257893388839234, 0.03843113950826911041, 0.03919970008264983541, 0.03996826065703055347, 0.04073682123141127154, 0.04150538180579199654, 0.04304250295455346043, 0.04457962410331493125, 0.04611674525207640207, 0.04765386640083786596, 0.04919098754959933678, 0.05072810869836080067, 0.05226522984712227149, 0.05380235099588373537, 0.05533947214464519926, 0.05687659329340666314, 0.05764515386778738815, 0.05841371444216810621, 0.05995083559092950765, 0.06071939616531019102, 0.06148795673969087439 ),
 .UNSPECIFIED. ) ;
#13037=CARTESIAN_POINT ( 'NONE',  ( 13.50000000000000000, 41.42999999999999972, 1.653273178848926867E-15 ) ) ;
#13038=DIRECTION ( 'NONE',  ( 0.000000000000000000, -0.000000000000000000, -1.000000000000000000 ) ) ;
#13041=CARTESIAN_POINT ( 'NONE',  ( 5.544738967689208486, 33.97889555847616094, -12.31101044224262253 ) ) ;
#13042=ORIENTED_EDGE ( 'NONE', *, *, #8177, .T. ) ;
#13043=DIRECTION ( 'NONE',  ( 0.000000000000000000, -0.000000000000000000, -1.000000000000000000 ) ) ;
#13048=CARTESIAN_POINT ( 'NONE',  ( 0.8898902232607978080, 77.71204398683455850, 13.47798471056508873 ) ) ;
#13049=CARTESIAN_POINT ( 'NONE',  ( -3.352402354136216900, 59.55948517377429852, 13.07833649419892730 ) ) ;
#13052=CARTESIAN_POINT ( 'NONE',  ( -8.343458848123582072, 56.38000000000000256, 11.48378591275254124 ) ) ;
#13053=CARTESIAN_POINT ( 'NONE',  ( -6.097425033090877911, 71.45719859721984335, 12.04586506600376161 ) ) ;
#13057=CARTESIAN_POINT ( 'NONE',  ( 3.045871263339404056, 68.78958672362097104, 13.15403766504849159 ) ) ;
#13059=CARTESIAN_POINT ( 'NONE',  ( 3.169521232131934596, 55.06603785773634741, -13.12275766666495613 ) ) ;
#13061=CARTESIAN_POINT ( 'NONE',  ( -6.285214426531775977, 65.44986835950689397, 11.95462813086504106 ) ) ;
#13063=CARTESIAN_POINT ( 'NONE',  ( -11.25052883642759483, 35.21015491215516136, 7.461608953425876045 ) ) ;
#13064=CARTESIAN_POINT ( 'NONE',  ( 11.76794919243112325, 31.42999999999999972, 1.441158131103945434E-15 ) ) ;
#13065=CARTESIAN_POINT ( 'NONE',  ( -5.521256578040511620, 40.38024479432580449, -12.31935789223439492 ) ) ;
#13067=CARTESIAN_POINT ( 'NONE',  ( -13.48148663984154894, 31.90541497078363520, -0.7088848451981341059 ) ) ;
#13069=CARTESIAN_POINT ( 'NONE',  ( 11.72855914400952315, 60.18170760815687714, 6.685430133444309142 ) ) ;
#13071=CARTESIAN_POINT ( 'NONE',  ( -7.148322466681692688, 53.41409683114213891, 11.45214043970867301 ) ) ;
#13072=CARTESIAN_POINT ( 'NONE',  ( -11.76794919243112325, 56.92999999999999972, -2.882316262207890869E-15 ) ) ;
#13073=CARTESIAN_POINT ( 'NONE',  ( 13.40257667448758916, 51.37355437458653995, 1.618959382087582721 ) ) ;
#13074=CARTESIAN_POINT ( 'NONE',  ( -13.47552119200681808, 37.90193867599817423, -0.8126124652662984893 ) ) ;
#13075=CARTESIAN_POINT ( 'NONE',  ( 13.05049472663724330, 36.55313275038592025, -3.454688345068896105 ) ) ;
#13078=CARTESIAN_POINT ( 'NONE',  ( -4.945268273999643860, 77.50155154180465900, 12.56911554149012922 ) ) ;
#13079=CARTESIAN_POINT ( 'NONE',  ( 4.299690572160308814E-08, 62.68000119825558869, 13.49999999999999822 ) ) ;
#13080=CARTESIAN_POINT ( 'NONE',  ( 0.000000000000000000, 102.9300000000000068, -12.00000000000000178 ) ) ;
#13081=ORIENTED_EDGE ( 'NONE', *, *, #9524, .T. ) ;
#13086=CARTESIAN_POINT ( 'NONE',  ( -9.520470885617717371, 60.22999999999999687, 6.917026985038133624 ) ) ;
#13090=CARTESIAN_POINT ( 'NONE',  ( 8.252097576776698418, 75.86575466930307243, -10.68462399792931805 ) ) ;
#13092=CARTESIAN_POINT ( 'NONE',  ( 2.607531440858944223E-15, 73.17999999999999261, -14.19474002721660355 ) ) ;
#13093=CARTESIAN_POINT ( 'NONE',  ( 2.272985001014427788E-15, 47.17999999999999972, -12.37355403259654985 ) ) ;
#13095=CARTESIAN_POINT ( 'NONE',  ( -13.46060157357587705, 58.96570155535383861, 1.031214257062757156 ) ) ;
#13096=CARTESIAN_POINT ( 'NONE',  ( 13.48827146342498118, 45.41039300781007171, 0.5693795367556682141 ) ) ;
#13097=CARTESIAN_POINT ( 'NONE',  ( 10.26325473544014244, 69.76683747837135741, -8.770540033709549377 ) ) ;
#13098=CARTESIAN_POINT ( 'NONE',  ( 1.651742348007693817, 80.73938956827036861, 13.39882440897573090 ) ) ;
#13099=CARTESIAN_POINT ( 'NONE',  ( 13.19255495532672384, 30.32843427499656741, 2.870686787867847922 ) ) ;
#13100=CARTESIAN_POINT ( 'NONE',  ( -9.894286701644787740, 55.57365333309054733, -9.185706287943689929 ) ) ;
#13101=CARTESIAN_POINT ( 'NONE',  ( -13.44902317320591223, 49.97066846970101039, 1.172593465884237185 ) ) ;
#13103=CARTESIAN_POINT ( 'NONE',  ( 13.02724366109965359, 42.55636079357457646, -3.541529992081969169 ) ) ;
#13104=CARTESIAN_POINT ( 'NONE',  ( 12.73078937444389958, 39.26766722070165372, 4.496366551774039877 ) ) ;
#13106=CARTESIAN_POINT ( 'NONE',  ( -12.78543602905191356, 70.77384588509148955, -4.334193518847205162 ) ) ;
#13107=CARTESIAN_POINT ( 'NONE',  ( -10.07944169913838550, 61.58339775250015435, -8.980808011171538041 ) ) ;
#13110=CARTESIAN_POINT ( 'NONE',  ( -10.31701163439258195, 40.59603470620067611, -8.706927762819312022 ) ) ;
#13116=CARTESIAN_POINT ( 'NONE',  ( 12.19413841524875686, 78.64259250466695050, -5.792494143745500423 ) ) ;
#13117=CARTESIAN_POINT ( 'NONE',  ( -7.272992578804307939, 80.48000000000000398, -10.01041549318726886 ) ) ;
#13118=CARTESIAN_POINT ( 'NONE',  ( -11.76794919243112325, 83.93000000000000682, -2.882316262207890869E-15 ) ) ;
#13119=CARTESIAN_POINT ( 'NONE',  ( 0.000000000000000000, 80.93000000000000682, 0.000000000000000000 ) ) ;
#13123=DIRECTION ( 'NONE',  ( -1.000000000000000000, -0.000000000000000000, -0.000000000000000000 ) ) ;
#13124=CARTESIAN_POINT ( 'NONE',  ( 9.380613467790862359, 33.81254506432511420, -9.717859427143588746 ) ) ;
#13125=CARTESIAN_POINT ( 'NONE',  ( -13.41322977063805411, 73.87657456906511300, -1.534601281563461317 ) ) ;
#13127=EDGE_CURVE ( 'NONE', #14678, #12894, #6809, .T. ) ;
#13128=VERTEX_POINT ( 'NONE', #9774 ) ;
#13129=LINE ( 'NONE', #11547, #14574 ) ;
#13131=VERTEX_POINT ( 'NONE', #6942 ) ;
#13134=CARTESIAN_POINT ( 'NONE',  ( -5.485275766071775660E-07, 44.67998473833578998, 13.49999999999997691 ) ) ;
#13135=FACE_OUTER_BOUND ( 'NONE', #397, .T. ) ;
#13136=DIRECTION ( 'NONE',  ( 9.637352644315600173E-17, -1.000000000000000000, 0.000000000000000000 ) ) ;
#13137=CARTESIAN_POINT ( 'NONE',  ( 11.61487935108414860, 66.68628431109220855, -6.880802064610810120 ) ) ;
#13138=CARTESIAN_POINT ( 'NONE',  ( -10.92172942406178926, 52.62999999999999545, -7.935100905948389460 ) ) ;
#13139=CARTESIAN_POINT ( 'NONE',  ( -5.359544901455636001, 71.48597326161704757, 12.39102907241780827 ) ) ;
#13140=VECTOR ( 'NONE', #9301, 1000.000000000000000 ) ;
#13142=CARTESIAN_POINT ( 'NONE',  ( 2.924053257345435538E-06, 68.68008145904181561, 13.49999999999936584 ) ) ;
#13144=CARTESIAN_POINT ( 'NONE',  ( 6.308629901301857856, 54.94873493297386347, -11.93532085539004051 ) ) ;
#13147=CARTESIAN_POINT ( 'NONE',  ( -2.514869812877075006, 65.58957455577544238, 13.26368900418464492 ) ) ;
#13149=CARTESIAN_POINT ( 'NONE',  ( -7.881676343575944266, 62.38282404488849409, 10.98390370778267311 ) ) ;
#13150=CARTESIAN_POINT ( 'NONE',  ( -1.388180886794196711, 35.63013967225546708, 13.42855345809681289 ) ) ;
#13154=CARTESIAN_POINT ( 'NONE',  ( -13.47846937990238914, 31.96028432000488095, 0.8791170498727822746 ) ) ;
#13155=CARTESIAN_POINT ( 'NONE',  ( 0.4269699266103727520, 73.16464788207684933, -13.49334228634718258 ) ) ;
#13156=CARTESIAN_POINT ( 'NONE',  ( 9.324401936112977296, 60.04491477143539413, 9.762614344302546598 ) ) ;
#13158=CARTESIAN_POINT ( 'NONE',  ( -0.5897042632328444167, 53.65879917600137361, 13.48805907082272704 ) ) ;
#13159=CARTESIAN_POINT ( 'NONE',  ( -9.520470885617717371, 54.23000000000000398, 6.917026985038133624 ) ) ;
#13160=CARTESIAN_POINT ( 'NONE',  ( 13.22767550596827313, 51.52528944818870116, -2.697998014972899927 ) ) ;
#13162=CARTESIAN_POINT ( 'NONE',  ( -11.13964547656885706, 38.21702771554652855, 7.626358909834451971 ) ) ;
#13163=CARTESIAN_POINT ( 'NONE',  ( 13.49038636612923803, 36.44758377910591207, -0.5111530726713751083 ) ) ;
#13166=CARTESIAN_POINT ( 'NONE',  ( -10.66896271836897725, 77.24446959830603987, 8.271838784292951274 ) ) ;
#13168=CARTESIAN_POINT ( 'NONE',  ( 2.435030327634469582, 62.76764002089962702, 13.27876764330338588 ) ) ;
#13169=CARTESIAN_POINT ( 'NONE',  ( 7.500000000000000000, 103.9536021580775014, -9.261711852864907613 ) ) ;
#13173=CARTESIAN_POINT ( 'NONE',  ( 7.272992578804311492, 58.88000000000000256, -10.01041549318726886 ) ) ;
#13177=CARTESIAN_POINT ( 'NONE',  ( 8.496523779928633502, 75.85456680855661205, -10.49111029357017344 ) ) ;
#13179=CARTESIAN_POINT ( 'NONE',  ( 13.50000000000000355, 68.57999999999998408, -4.386415899144233244 ) ) ;
#13180=CARTESIAN_POINT ( 'NONE',  ( 3.311465905292703571, 65.79890599816108931, 13.08767270555769535 ) ) ;
#13181=CARTESIAN_POINT ( 'NONE',  ( -4.171729424061787483, 70.32999999999999829, -12.83926296998457417 ) ) ;
#13182=CARTESIAN_POINT ( 'NONE',  ( 11.76794919243112325, 40.27999999999998693, 3.823638476888996607 ) ) ;
#13184=CARTESIAN_POINT ( 'NONE',  ( -12.81629044767723258, 59.08368428406883766, 4.264882000424433883 ) ) ;
#13185=CARTESIAN_POINT ( 'NONE',  ( 12.88521962934911969, 45.28541850008814151, 4.028261922845268295 ) ) ;
#13186=CARTESIAN_POINT ( 'NONE',  ( 13.22000464319502910, 69.52673859052352157, -2.737438834081824979 ) ) ;
#13187=CARTESIAN_POINT ( 'NONE',  ( 3.708978301276113054, 80.81333388317378308, 12.98124409862539252 ) ) ;
#13188=CARTESIAN_POINT ( 'NONE',  ( 11.37079320667167082, 30.15738796711680081, 7.279353378998085766 ) ) ;
#13189=CARTESIAN_POINT ( 'NONE',  ( -10.11932462375468589, 55.58550355030939727, -8.935858638386630304 ) ) ;
#13190=CARTESIAN_POINT ( 'NONE',  ( -8.561306179327837995, 50.35156287121731822, 10.43811098430223971 ) ) ;
#13191=CARTESIAN_POINT ( 'NONE',  ( 8.352964853697221415, 63.86126407894886370, -10.60947463986401296 ) ) ;
#13192=CARTESIAN_POINT ( 'NONE',  ( 12.03319936400606771, 42.65557395139708063, -6.120239074458291739 ) ) ;
#13193=CARTESIAN_POINT ( 'NONE',  ( 11.13553297422662425, 39.14273495546231629, 7.632164570861474928 ) ) ;
#13195=CARTESIAN_POINT ( 'NONE',  ( -8.467238370142107229, 70.50394589295852654, -10.52029779368665352 ) ) ;
#13196=CARTESIAN_POINT ( 'NONE',  ( -3.992645158735599775, 61.32355938215374636, -12.89609062310873711 ) ) ;
#13198=ORIENTED_EDGE ( 'NONE', *, *, #3547, .T. ) ;
#13199=ORIENTED_EDGE ( 'NONE', *, *, #9029, .F. ) ;
#13202=CARTESIAN_POINT ( 'NONE',  ( 0.000000000000000000, 102.9300000000000068, 6.000000000000001776 ) ) ;
#13203=CARTESIAN_POINT ( 'NONE',  ( 13.39541892358324482, 57.37148616028263604, 1.677126579065239209 ) ) ;
#13204=APPLICATION_CONTEXT ( 'automotive_design' ) ;
#13205=CARTESIAN_POINT ( 'NONE',  ( -3.636496289402153081, 68.32999999999999829, -11.19198476289190936 ) ) ;
#13206=CARTESIAN_POINT ( 'NONE',  ( -3.636496289402155746, 75.53000000000000114, 11.19198476289190936 ) ) ;
#13211=LINE ( 'NONE', #8988, #2988 ) ;
#13212=CARTESIAN_POINT ( 'NONE',  ( 5.803585914168436943, 33.96878461091537815, -12.18886560664654439 ) ) ;
#13213=CARTESIAN_POINT ( 'NONE',  ( -4.772267704801665289, 73.35190717389953363, -12.62917378417867553 ) ) ;
#13214=ORIENTED_EDGE ( 'NONE', *, *, #6562, .F. ) ;
#13216=CARTESIAN_POINT ( 'NONE',  ( 7.272992578804311492, 79.87999999999999545, -10.01041549318726886 ) ) ;
#13217=VERTEX_POINT ( 'NONE', #8360 ) ;
#13219=CARTESIAN_POINT ( 'NONE',  ( -9.654787189692980220, 44.29874787832478944, 9.440553263455338850 ) ) ;
#13221=CARTESIAN_POINT ( 'NONE',  ( 13.34696669401933811, 66.50124740785342681, -2.033240060188988618 ) ) ;
#13223=CARTESIAN_POINT ( 'NONE',  ( 13.50000000000000355, 57.57999999999999829, -4.386415899144233244 ) ) ;
#13224=CARTESIAN_POINT ( 'NONE',  ( -11.83441462683018308, 71.17064391044787897, 6.495893364519336188 ) ) ;
#13225=ADVANCED_FACE ( 'NONE', ( #214 ), #12411, .T. ) ;
#13227=CARTESIAN_POINT ( 'NONE',  ( -13.49996152797187854, 67.91463075201109234, -0.4484004657480521461 ) ) ;
#13229=CARTESIAN_POINT ( 'NONE',  ( 3.780205736804012180E-08, 55.17999999864077409, -13.50000000000000000 ) ) ;
#13230=VECTOR ( 'NONE', #9925, 1000.000000000000000 ) ;
#13233=CARTESIAN_POINT ( 'NONE',  ( -13.46311281423534645, 64.89547304182495679, -0.9973165763568858644 ) ) ;
#13234=CARTESIAN_POINT ( 'NONE',  ( -1.560960962377287098, 35.62388556644654614, 13.40948977943153153 ) ) ;
#13237=CARTESIAN_POINT ( 'NONE',  ( 5.883989548015875926, 30.92926152634062475, 10.19133431864935879 ) ) ;
#13239=CARTESIAN_POINT ( 'NONE',  ( -4.184719208025596160, 31.33046874752387012, -12.83515809457515111 ) ) ;
#13240=FACE_OUTER_BOUND ( 'NONE', #15481, .T. ) ;
#13241=CARTESIAN_POINT ( 'NONE',  ( 6.789432038303849559, 59.93098817131988199, 11.66862129383769897 ) ) ;
#13243=CARTESIAN_POINT ( 'NONE',  ( -9.971704770123398731, 53.28226430956654269, 9.100406691781726565 ) ) ;
#13245=CARTESIAN_POINT ( 'NONE',  ( -3.636496289402153081, 53.33000000000000540, -11.19198476289190936 ) ) ;
#13246=CARTESIAN_POINT ( 'NONE',  ( 10.92172942406179104, 74.73000000000000398, -7.935100905948385908 ) ) ;
#13248=CARTESIAN_POINT ( 'NONE',  ( 5.029058773629547119, 50.86151010740556444, 12.52835747826576451 ) ) ;
#13249=CARTESIAN_POINT ( 'NONE',  ( -12.14893529072169009, 37.71319614887404725, -5.902479453089211070 ) ) ;
#13250=CARTESIAN_POINT ( 'NONE',  ( 12.85437900238714093, 36.28169154084510950, 4.130910386987205918 ) ) ;
#13252=CARTESIAN_POINT ( 'NONE',  ( -1.492738206771355713, 74.62634578251100947, 13.41930821191457568 ) ) ;
#13253=CARTESIAN_POINT ( 'NONE',  ( -11.80473894797548873, 77.17302640020055549, 6.558943582821462392 ) ) ;
#13254=CARTESIAN_POINT ( 'NONE',  ( -13.49997129730146028, 79.93743929743982335, 0.2167451702461970775 ) ) ;
#13256=CARTESIAN_POINT ( 'NONE',  ( 7.499999999999999112, 106.7538932235142966, 7.532295102519074526 ) ) ;
#13260=CARTESIAN_POINT ( 'NONE',  ( -11.76794919243112325, 53.77999999999999403, -3.823638476888998827 ) ) ;
#13264=CARTESIAN_POINT ( 'NONE',  ( 12.03944877831089677, 75.65508428389024687, -6.107598382801971759 ) ) ;
#13265=CARTESIAN_POINT ( 'NONE',  ( -4.023268246324633536E-14, 69.18000000000000682, -13.50000000000000000 ) ) ;
#13266=CARTESIAN_POINT ( 'NONE',  ( 0.4417390832689820357, 65.69588305743820911, 13.49284045995814374 ) ) ;
#13267=CARTESIAN_POINT ( 'NONE',  ( 4.171729424061789260, 68.82999999999999829, 12.83926296998457417 ) ) ;
#13268=CARTESIAN_POINT ( 'NONE',  ( 9.520470885617715595, 37.12999999999999545, 6.917026985038134512 ) ) ;
#13270=CARTESIAN_POINT ( 'NONE',  ( -8.668252091055315134, 58.51341961490522436, -10.34967728072912685 ) ) ;
#13271=CARTESIAN_POINT ( 'NONE',  ( 13.49636432536657793, 45.41924338305506836, 0.3133736981627452400 ) ) ;
#13272=CARTESIAN_POINT ( 'NONE',  ( 11.94743759944812744, 69.66219602205637784, -6.285597574998869952 ) ) ;
#13273=CARTESIAN_POINT ( 'NONE',  ( 2.445080149700053643E-15, 66.18000000000000682, -13.50000000000000000 ) ) ;
#13274=CARTESIAN_POINT ( 'NONE',  ( 10.89794336758623139, 30.12856905013999409, 7.968289002914518804 ) ) ;
#13275=CARTESIAN_POINT ( 'NONE',  ( -11.17210748473980253, 55.64497476832795542, -7.578533830143271643 ) ) ;
#13276=CARTESIAN_POINT ( 'NONE',  ( -11.56639327183221866, 50.19069324002893495, 6.996189293027585521 ) ) ;
#13277=CARTESIAN_POINT ( 'NONE',  ( 12.78700290053627597, 63.27388653237613170, 4.333656960051132323 ) ) ;
#13278=CARTESIAN_POINT ( 'NONE',  ( 11.17787638430055530, 42.71467156718345137, -7.570014911160897420 ) ) ;
#13279=CARTESIAN_POINT ( 'NONE',  ( 9.216665679856882676, 39.03962942028351790, 9.864241841985725401 ) ) ;
#13281=CARTESIAN_POINT ( 'NONE',  ( -5.034154520868722393, 70.36169635399654965, -12.52728796785475041 ) ) ;
#13282=CARTESIAN_POINT ( 'NONE',  ( -3.680674551539889983, 61.31232984300370958, -12.99219103675922504 ) ) ;
#13288=CARTESIAN_POINT ( 'NONE',  ( 3.458946346613236411, 61.05562364027491640, -13.05177015192364820 ) ) ;
#13289=CARTESIAN_POINT ( 'NONE',  ( 7.681080053067259605, 71.96880320796036301, 11.10186521252582104 ) ) ;
#13290=CARTESIAN_POINT ( 'NONE',  ( 13.29995246372572737, 57.34789229178345948, 2.331640294117302670 ) ) ;
#13291=CARTESIAN_POINT ( 'NONE',  ( 11.76794919243112325, 67.28000000000000114, 3.823638476888996607 ) ) ;
#13292=CARTESIAN_POINT ( 'NONE',  ( -11.76794919243112325, 77.77999999999998693, -3.823638476888998827 ) ) ;
#13297=CARTESIAN_POINT ( 'NONE',  ( 4.489225048192535539, 34.01849207910494499, -12.73175184514909830 ) ) ;
#13298=CARTESIAN_POINT ( 'NONE',  ( -7.517232062827917005, 73.46167874442537027, -11.21345962906566207 ) ) ;
#13300=VERTEX_POINT ( 'NONE', #122 ) ;
#13301=CARTESIAN_POINT ( 'NONE',  ( 11.76794919243112325, 76.28000000000000114, 3.823638476888997051 ) ) ;
#13304=ADVANCED_FACE ( 'NONE', ( #16462 ), #9864, .T. ) ;
#13305=CARTESIAN_POINT ( 'NONE',  ( -10.12090119985971626, 44.27440800199393323, 8.934056138211790454 ) ) ;
#13307=CARTESIAN_POINT ( 'NONE',  ( 12.79597734119763430, 66.58496463305510815, -4.302840019310315789 ) ) ;
#13308=CARTESIAN_POINT ( 'NONE',  ( 8.343458848123578520, 41.97999999999999687, 11.48378591275254124 ) ) ;
#13309=CARTESIAN_POINT ( 'NONE',  ( -11.83480306631655665, 71.17061613792351693, 6.495185643570378531 ) ) ;
#13311=CARTESIAN_POINT ( 'NONE',  ( -13.42521090995868427, 67.97936017792704888, 1.419127934761323928 ) ) ;
#13316=CARTESIAN_POINT ( 'NONE',  ( -12.08625417401086466, 65.15233228621843864, 6.041222395741010054 ) ) ;
#13317=CARTESIAN_POINT ( 'NONE',  ( -2.859817639333870343, 35.57722089168602508, 13.19986362302225658 ) ) ;
#13318=VERTEX_POINT ( 'NONE', #3111 ) ;
#13320=CARTESIAN_POINT ( 'NONE',  ( -2.685559703086524141, 31.27656278095842524, -13.23019760191706240 ) ) ;
#13321=CARTESIAN_POINT ( 'NONE',  ( 0.000000000000000000, 102.9300000000000068, 0.000000000000000000 ) ) ;
#13323=CARTESIAN_POINT ( 'NONE',  ( 6.476227018813886183, 59.91800028742412820, 11.84548389080563524 ) ) ;
#13325=CARTESIAN_POINT ( 'NONE',  ( -4.883725581089568557, 53.50385945949214772, 12.59343935867386044 ) ) ;
#13327=CARTESIAN_POINT ( 'NONE',  ( 9.520470885617715595, 52.12999999999999545, 6.917026985038134512 ) ) ;
#13328=CARTESIAN_POINT ( 'NONE',  ( -10.92172942406178926, 69.62999999999999545, -7.935100905948389460 ) ) ;
#13329=CARTESIAN_POINT ( 'NONE',  ( 10.82490547629966393, 51.12442037295507902, 8.066909685650703210 ) ) ;
#13330=CARTESIAN_POINT ( 'NONE',  ( -10.26118691261005367, 37.59304863723961176, -8.772592031706285098 ) ) ;
#13331=CARTESIAN_POINT ( 'NONE',  ( 11.71544674525831908, 36.17874677927314764, 6.766421350180369387 ) ) ;
#13333=CARTESIAN_POINT ( 'NONE',  ( -5.282920329015465377, 74.48891104032615829, 12.42340604607010945 ) ) ;
#13334=CARTESIAN_POINT ( 'NONE',  ( -13.29386781379963445, 76.84733676671916669, -2.350162437524830228 ) ) ;
#13336=CARTESIAN_POINT ( 'NONE',  ( -13.41783933752910585, 79.86962778622965686, -1.738652325513279973 ) ) ;
#13337=CARTESIAN_POINT ( 'NONE',  ( 7.499999999999999112, 106.0136413093990342, -8.254396200996678701 ) ) ;
#13339=CARTESIAN_POINT ( 'NONE',  ( 9.520470885617717371, 61.72999999999999687, -6.917026985038131848 ) ) ;
#13343=ADVANCED_FACE ( 'NONE', ( #15120 ), #3018, .T. ) ;
#13345=CARTESIAN_POINT ( 'NONE',  ( 11.73542858777253350, 75.67814331974577158, -6.690067788355273493 ) ) ;
#13348=CARTESIAN_POINT ( 'NONE',  ( 7.272992578804308828, 42.97999999999998977, 10.01041549318726709 ) ) ;
#13350=CARTESIAN_POINT ( 'NONE',  ( -12.78340117865951520, 58.77362691746088785, -4.339946196950513091 ) ) ;
#13351=CARTESIAN_POINT ( 'NONE',  ( 3.572953084902807053, 44.80828262693227515, 13.02032272097764576 ) ) ;
#13352=CARTESIAN_POINT ( 'NONE',  ( 13.41657896972532704, 69.37782559286166872, 1.498472742429565630 ) ) ;
#13355=CARTESIAN_POINT ( 'NONE',  ( -12.11432412061597219, 55.71088818410203203, -5.957677718900700192 ) ) ;
#13356=CARTESIAN_POINT ( 'NONE',  ( -12.10558320543248989, 49.71015782045832765, -5.975393061918390814 ) ) ;
#13357=CARTESIAN_POINT ( 'NONE',  ( 11.52526665190315391, 63.69236103524189474, -7.029820945411229260 ) ) ;
#13358=CARTESIAN_POINT ( 'NONE',  ( 6.442398735761099893, 42.94338794518161961, -11.86886155631007966 ) ) ;
#13359=CARTESIAN_POINT ( 'NONE',  ( 9.245400910555552798, 39.04103442320599271, 9.837310621197884686 ) ) ;
#13360=ORIENTED_EDGE ( 'NONE', *, *, #1130, .F. ) ;
#13361=CARTESIAN_POINT ( 'NONE',  ( -5.253428466288492693, 70.36999080376129712, -12.43590961766370562 ) ) ;
#13362=CARTESIAN_POINT ( 'NONE',  ( -0.2958543223917724507, 61.19063785939420796, -13.49999999999999467 ) ) ;
#13364=ORIENTED_EDGE ( 'NONE', *, *, #2675, .F. ) ;
#13366=CARTESIAN_POINT ( 'NONE',  ( -12.50000000000000000, 94.93000000000002103, 1.224646799147353059E-15 ) ) ;
#13367=CARTESIAN_POINT ( 'NONE',  ( 4.897649543255423232, 47.85658455420482937, 12.58047166699710040 ) ) ;
#13369=CARTESIAN_POINT ( 'NONE',  ( 2.423490671691030496, 71.76716578115846801, 13.28070271859271934 ) ) ;
#13370=CARTESIAN_POINT ( 'NONE',  ( 13.40032062549284575, 57.48717893755269870, -1.642066659324613820 ) ) ;
#13371=CARTESIAN_POINT ( 'NONE',  ( -7.576616670048093940E-16, 69.68000000000000682, 12.37355403259654985 ) ) ;
#13372=CARTESIAN_POINT ( 'NONE',  ( -11.76794919243112325, 78.07999999999999829, 3.823638476888994386 ) ) ;
#13373=CARTESIAN_POINT ( 'NONE',  ( -3.903004734176718671, 47.53966149391548157, 12.92364409840641848 ) ) ;
#13375=CARTESIAN_POINT ( 'NONE',  ( -8.343458848123582072, 46.37999999999999545, 11.48378591275253768 ) ) ;
#13379=CARTESIAN_POINT ( 'NONE',  ( 12.50000000000000000, 98.93000000000002103, 1.224646799147353059E-15 ) ) ;
#13380=CARTESIAN_POINT ( 'NONE',  ( 11.72575753619244487, 33.67872147816529349, -6.696208405594990865 ) ) ;
#13381=CARTESIAN_POINT ( 'NONE',  ( -9.709238084139839131, 73.56419381030619320, -9.379939381872517856 ) ) ;
#13383=ORIENTED_EDGE ( 'NONE', *, *, #13479, .T. ) ;
#13384=CARTESIAN_POINT ( 'NONE',  ( 9.520470885617717371, 76.73000000000000398, -6.917026985038131848 ) ) ;
#13385=VERTEX_POINT ( 'NONE', #16808 ) ;
#13388=CARTESIAN_POINT ( 'NONE',  ( -7.124923918163931447, 44.41509661022353583, 11.46745630815109429 ) ) ;
#13390=CARTESIAN_POINT ( 'NONE',  ( 8.343458848123578520, 47.97999999999999687, 11.48378591275254124 ) ) ;
#13391=CARTESIAN_POINT ( 'NONE',  ( -8.228354664486742465, 71.36683761322035480, 10.70256661444891222 ) ) ;
#13393=CARTESIAN_POINT ( 'NONE',  ( -13.47488564051851334, 67.95938883480165771, 0.8512204470096735864 ) ) ;
#13396=CARTESIAN_POINT ( 'NONE',  ( 11.54421080121787391, 54.69106169426531494, -6.998656893040053006 ) ) ;
#13398=CARTESIAN_POINT ( 'NONE',  ( -13.01035162171275772, 64.80131765794939724, -3.603924305307248055 ) ) ;
#13399=CARTESIAN_POINT ( 'NONE',  ( -12.58169653699114043, 35.10756079940100705, 4.893995670961994726 ) ) ;
#13401=ORIENTED_EDGE ( 'NONE', *, *, #4416, .T. ) ;
#13404=CARTESIAN_POINT ( 'NONE',  ( -2.369581839689028691, 31.26519794180775946, -13.29387509668438305 ) ) ;
#13405=CARTESIAN_POINT ( 'NONE',  ( 11.58782070419744592, 72.68816403396648695, -6.927154233550009366 ) ) ;
#13408=CARTESIAN_POINT ( 'NONE',  ( -2.574185747556406501, 53.58751162550813518, 13.25824297384535377 ) ) ;
#13409=CARTESIAN_POINT ( 'NONE',  ( -9.520470885617717371, 48.23000000000000398, 6.917026985038133624 ) ) ;
#13410=CARTESIAN_POINT ( 'NONE',  ( 13.50000000000000355, 65.57999999999998408, -4.386415899144233244 ) ) ;
#13411=CARTESIAN_POINT ( 'NONE',  ( 10.69206503222415527, 51.11683399389762883, 8.241953851791326002 ) ) ;
#13413=CARTESIAN_POINT ( 'NONE',  ( -12.70032077649241131, 37.76312699646079807, -4.620871474344856900 ) ) ;
#13414=CARTESIAN_POINT ( 'NONE',  ( 8.950850146857373346, 36.02672331505379333, 10.10926642398400332 ) ) ;
#13416=CARTESIAN_POINT ( 'NONE',  ( -7.804728211771945645, 74.38584041582383577, 11.02015311321599889 ) ) ;
#13418=CARTESIAN_POINT ( 'NONE',  ( -12.72587516454714240, 76.76713713515550808, -4.510395728399637427 ) ) ;
#13419=CARTESIAN_POINT ( 'NONE',  ( -13.04304625457159084, 79.80563238178049801, -3.489764737285672158 ) ) ;
#13420=CARTESIAN_POINT ( 'NONE',  ( 7.500000000000000000, 106.2113042096659257, -8.086389325435060726 ) ) ;
#13423=CARTESIAN_POINT ( 'NONE',  ( -11.76794919243112325, 50.92999999999999972, -2.882316262207890869E-15 ) ) ;
#13428=CARTESIAN_POINT ( 'NONE',  ( 6.174388639489537312, 75.95411551790840576, -12.00529625765989294 ) ) ;
#13431=CARTESIAN_POINT ( 'NONE',  ( -9.520470885617715595, 35.62999999999999545, -6.917026985038136289 ) ) ;
#13432=CARTESIAN_POINT ( 'NONE',  ( -9.845587001014646233, 41.28914020501957083, 9.247743145432201217 ) ) ;
#13433=CARTESIAN_POINT ( 'NONE',  ( -5.764196172476330204, 58.38967490561365992, -12.20754040654003880 ) ) ;
#13436=CARTESIAN_POINT ( 'NONE',  ( 0.000000000000000000, 80.93000000000000682, -13.50000000000000000 ) ) ;
#13437=CYLINDRICAL_SURFACE ( 'NONE', #8752, 13.50000000000000000 ) ;
#13438=CARTESIAN_POINT ( 'NONE',  ( -9.291548975078672612, 55.54290236572062156, -9.805807003418143708 ) ) ;
#13439=CARTESIAN_POINT ( 'NONE',  ( -12.81046799232142419, 49.77384515584038382, -4.351227976931586916 ) ) ;
#13440=CARTESIAN_POINT ( 'NONE',  ( 13.36172522450170241, 63.49744435280518928, -1.927315141226759732 ) ) ;
#13441=CARTESIAN_POINT ( 'NONE',  ( 5.678863279829545974, 42.97365145709494527, -12.24748028004784572 ) ) ;
#13442=CARTESIAN_POINT ( 'NONE',  ( 8.224463485078279845, 38.99288720330545033, 10.71476610712685051 ) ) ;
#13443=VERTEX_POINT ( 'NONE', #7198 ) ;
#13444=CARTESIAN_POINT ( 'NONE',  ( -9.891601304258150762, 70.57355540121815807, -9.187288538321107367 ) ) ;
#13451=CARTESIAN_POINT ( 'NONE',  ( 6.374620558230982503, 60.94607247059151689, -11.90018113148034473 ) ) ;
#13453=CARTESIAN_POINT ( 'NONE',  ( 9.378081481877091008, 72.04743592386726903, 9.715564754266829084 ) ) ;
#13454=CARTESIAN_POINT ( 'NONE',  ( 13.50123327339441914, 57.41482836698943970, 0.4418988847496390648 ) ) ;
#13455=CARTESIAN_POINT ( 'NONE',  ( 2.272985001014427788E-15, 71.17999999999999261, -12.37355403259654985 ) ) ;
#13456=CARTESIAN_POINT ( 'NONE',  ( -8.343458848123582072, 34.37999999999998835, 11.48378591275254124 ) ) ;
#13457=CARTESIAN_POINT ( 'NONE',  ( -3.636496289402153081, 74.33000000000001251, -11.19198476289190936 ) ) ;
#13458=CARTESIAN_POINT ( 'NONE',  ( -3.140275034707463941, 47.56712421504963118, 13.13116523590432116 ) ) ;
#13459=CARTESIAN_POINT ( 'NONE',  ( 0.000000000000000000, 75.00000000000000000, 0.000000000000000000 ) ) ;
#13465=CARTESIAN_POINT ( 'NONE',  ( 2.445080149700053643E-15, 51.18000000000000682, -13.50000000000000000 ) ) ;
#13466=CARTESIAN_POINT ( 'NONE',  ( 13.49036936581445900, 33.44756504376105255, -0.5105335361757911139 ) ) ;
#13467=CARTESIAN_POINT ( 'NONE',  ( -9.651347398433271607, 73.56125364406217670, -9.439358866893277522 ) ) ;
#13470=CARTESIAN_POINT ( 'NONE',  ( -5.611269881966371109, 62.47627512215084522, 12.27858589067506934 ) ) ;
#13472=CARTESIAN_POINT ( 'NONE',  ( -13.30519346037214135, 41.01035172162969644, 2.285875191404075579 ) ) ;
#13474=CARTESIAN_POINT ( 'NONE',  ( -0.6761224248667969672, 44.65568913397951434, 13.48306232859242293 ) ) ;
#13476=CARTESIAN_POINT ( 'NONE',  ( 13.50000000000000000, 48.42999999999999972, 1.653273178848926867E-15 ) ) ;
#13477=CARTESIAN_POINT ( 'NONE',  ( -10.92172942406179104, 43.22999999999999687, 7.935100905948387684 ) ) ;
#13478=CARTESIAN_POINT ( 'NONE',  ( -12.93260499938089403, 71.06873686804253509, 3.872692500715011921 ) ) ;
#13479=EDGE_CURVE ( 'NONE', #11794, #760, #15331, .T. ) ;
#13481=CARTESIAN_POINT ( 'NONE',  ( -12.18806906699818882, 67.71628745454681564, -5.824626418828033891 ) ) ;
#13483=CARTESIAN_POINT ( 'NONE',  ( 11.18355001832372864, 54.71426267336678961, -7.567176262528036546 ) ) ;
#13486=CARTESIAN_POINT ( 'NONE',  ( -12.73065029274041393, 64.76630363813843871, -4.537315649280014185 ) ) ;
#13488=CARTESIAN_POINT ( 'NONE',  ( -13.34685961114456099, 35.00103985169026544, 2.027643910844264763 ) ) ;
#13489=VERTEX_POINT ( 'NONE', #3685 ) ;
#13491=CARTESIAN_POINT ( 'NONE',  ( -10.13503849319200256, 31.58637571636829122, -8.918039105965791080 ) ) ;
#13492=CARTESIAN_POINT ( 'NONE',  ( 6.811485724132999131, 72.92836491868227711, -11.66693257913138382 ) ) ;
#13495=CARTESIAN_POINT ( 'NONE',  ( -13.47895445410198612, 52.90400025295915043, -0.7535177491850849618 ) ) ;
#13496=CARTESIAN_POINT ( 'NONE',  ( -11.76794919243112325, 47.77999999999999403, -3.823638476888998827 ) ) ;
#13497=CARTESIAN_POINT ( 'NONE',  ( 10.92172942406179104, 68.73000000000000398, -7.935100905948385908 ) ) ;
#13498=CARTESIAN_POINT ( 'NONE',  ( 10.61679899383538483, 51.11259005245373999, 8.339111544401394127 ) ) ;
#13500=CARTESIAN_POINT ( 'NONE',  ( -5.616158569158017144, 37.38391327537662789, -12.27641445107196105 ) ) ;
#13501=CARTESIAN_POINT ( 'NONE',  ( 7.311491871512308727, 35.95290065796121581, 11.35084104978724895 ) ) ;
#13503=CARTESIAN_POINT ( 'NONE',  ( -11.68704921467410784, 74.18220605320536265, 6.786032449176635062 ) ) ;
#13504=CARTESIAN_POINT ( 'NONE',  ( -11.20590004775074355, 76.64706285525832641, -7.528468286527173703 ) ) ;
#13505=CARTESIAN_POINT ( 'NONE',  ( -10.71293590878329205, 79.61766727756590001, -8.226627743301476059 ) ) ;
#13506=CARTESIAN_POINT ( 'NONE',  ( -7.321446643557331768, 80.92999999999996419, 10.20755442051737205 ) ) ;
#13508=CARTESIAN_POINT ( 'NONE',  ( -11.76794919243112325, 44.92999999999999972, -2.882316262207890869E-15 ) ) ;
#13512=CARTESIAN_POINT ( 'NONE',  ( -5.995934488988542199, 40.39877640253387625, -12.09682232891648468 ) ) ;
#13514=CARTESIAN_POINT ( 'NONE',  ( 10.27758411003093819, 75.09396747692687768, 8.753359694643265243 ) ) ;
#13515=EDGE_CURVE ( 'NONE', #760, #13131, #6948, .T. ) ;
#13517=CARTESIAN_POINT ( 'NONE',  ( 2.272985001014427788E-15, 38.17999999999999972, -12.37355403259654985 ) ) ;
#13518=CARTESIAN_POINT ( 'NONE',  ( -11.57650647816374700, 41.18894672448205796, 6.947845214036406425 ) ) ;
#13519=CARTESIAN_POINT ( 'NONE',  ( -11.17817305665808014, 58.64534897024895344, -7.569578125800211055 ) ) ;
#13520=CARTESIAN_POINT ( 'NONE',  ( 2.914010673256763440, 44.78477707381765782, 13.18175074847055761 ) ) ;
#13521=CARTESIAN_POINT ( 'NONE',  ( 4.171729424061789260, 58.82999999999999829, 12.83926296998457417 ) ) ;
#13522=CARTESIAN_POINT ( 'NONE',  ( 7.392150717925613179, 29.95598776866237145, 11.32059538698433165 ) ) ;
#13523=AXIS2_PLACEMENT_3D ( 'NONE', #14457, #6356, #11487 ) ;
#13525=CARTESIAN_POINT ( 'NONE',  ( -12.11427638989693101, 49.71086542188117363, -5.957774775766911723 ) ) ;
#13526=CARTESIAN_POINT ( 'NONE',  ( 13.47352731021837258, 63.40080362853115048, 0.8451059437790031659 ) ) ;
#13527=CARTESIAN_POINT ( 'NONE',  ( 13.48004015203407668, 42.40468154064383555, 0.7338770590801271254 ) ) ;
#13531=CARTESIAN_POINT ( 'NONE',  ( -13.49999999999999822, 49.07999999999999829, 4.386415899144235020 ) ) ;
#13534=CARTESIAN_POINT ( 'NONE',  ( -5.576931461581311034, 43.38239337497184067, -12.29436833682542307 ) ) ;
#13535=CARTESIAN_POINT ( 'NONE',  ( -7.499999999999998224, 104.2017679084707851, 9.199276322163095543 ) ) ;
#13537=CARTESIAN_POINT ( 'NONE',  ( 11.86384666090724416, 60.66867754764784593, -6.447385887097871304 ) ) ;
#13540=CARTESIAN_POINT ( 'NONE',  ( 7.779282341488525709, 56.97302794364081535, 11.03737104057997165 ) ) ;
#13541=CARTESIAN_POINT ( 'NONE',  ( -11.76794919243112325, 65.93000000000000682, -2.882316262207890869E-15 ) ) ;
#13542=CARTESIAN_POINT ( 'NONE',  ( 11.76794919243112325, 67.28000000000000114, 3.823638476888996607 ) ) ;
#13543=CARTESIAN_POINT ( 'NONE',  ( -4.473130523687919968, 47.51903911116670542, 12.74611812840811176 ) ) ;
#13544=CARTESIAN_POINT ( 'NONE',  ( 5.281167590608333740, 45.98876608056069415, -12.42463402102491621 ) ) ;
#13547=CARTESIAN_POINT ( 'NONE',  ( -0.8894075400429002354, 56.64828133586323133, 13.47800860622838393 ) ) ;
#13551=CARTESIAN_POINT ( 'NONE',  ( 13.48726538980810474, 33.45020437573430172, -0.5866928101883699398 ) ) ;
#13552=CARTESIAN_POINT ( 'NONE',  ( -3.847640698436238349, 73.31827516608075257, -12.94019317380912959 ) ) ;
#13555=CARTESIAN_POINT ( 'NONE',  ( -3.922215051620934645, 62.53897161928807691, 12.91767269693318276 ) ) ;
#13556=( BOUNDED_CURVE ( )  B_SPLINE_CURVE ( 2, ( #1706, #4634, #7468, #3386, #1791, #15390, #16643, #13892, #8885, #5886, #12588, #15302, #16902 ),
 .UNSPECIFIED., .F., .F. ) 
 B_SPLINE_CURVE_WITH_KNOTS ( ( 3, 2, 2, 2, 2, 2, 3 ),
 ( 0.5694444444444444198, 0.5722222222222221877, 0.5777777777777777235, 0.5833333333333333703, 0.5888888888888889062, 0.5944444444444444420, 0.5972222222222222099 ),
 .UNSPECIFIED. ) 
 CURVE ( )  GEOMETRIC_REPRESENTATION_ITEM ( )  RATIONAL_B_SPLINE_CURVE ( ( 0.9755282581475768211, 0.9755282581475768211, 1.000000000000000000, 0.9510565162951535312, 1.000000000000000000, 0.9510565162951535312, 1.000000000000000000, 0.9510565162951535312, 1.000000000000000000, 0.9510565162951535312, 1.000000000000000000, 0.9755282581475768211, 0.9755282581475768211 ) ) 
 REPRESENTATION_ITEM ( '' )  );
#13557=ORIENTED_EDGE ( 'NONE', *, *, #8002, .F. ) ;
#13560=CARTESIAN_POINT ( 'NONE',  ( -13.10259906904691896, 44.04626536728174102, 3.264601644182080875 ) ) ;
#13561=ADVANCED_FACE ( 'NONE', ( #3488 ), #7305, .F. ) ;
#13563=CARTESIAN_POINT ( 'NONE',  ( 2.607531440858944223E-15, 43.17999999999999972, -14.19474002721660355 ) ) ;
#13564=CARTESIAN_POINT ( 'NONE',  ( -13.47393936470618137, 70.95918448809980816, 0.8439462952680778507 ) ) ;
#13566=CARTESIAN_POINT ( 'NONE',  ( -13.42870403230521958, 67.88181673837877383, -1.385841348755903590 ) ) ;
#13568=CARTESIAN_POINT ( 'NONE',  ( 11.54108203963314239, 54.69126936105765679, -7.003815892991897663 ) ) ;
#13570=CARTESIAN_POINT ( 'NONE',  ( -12.71393839463805797, 65.09396562736293390, 4.539402788875312567 ) ) ;
#13572=CARTESIAN_POINT ( 'NONE',  ( -4.171729424061787483, 63.32999999999999829, -12.83926296998457417 ) ) ;
#13573=CARTESIAN_POINT ( 'NONE',  ( -13.46032330647282826, 34.89419764945687774, -1.036509372401692053 ) ) ;
#13575=CARTESIAN_POINT ( 'NONE',  ( 13.39701859097131909, 78.37195839092206029, 1.664708910713033507 ) ) ;
#13577=CARTESIAN_POINT ( 'NONE',  ( -11.52056222259168372, 31.66712582499730999, -7.043476334750435441 ) ) ;
#13578=CARTESIAN_POINT ( 'NONE',  ( 10.16376560654192218, 72.77214537080571688, -8.885750376373021453 ) ) ;
#13582=CARTESIAN_POINT ( 'NONE',  ( -4.171729424061787483, 73.33000000000001251, -12.83926296998457417 ) ) ;
#13583=CARTESIAN_POINT ( 'NONE',  ( -12.86141184943314109, 52.78247262265329454, -4.106605482048742317 ) ) ;
#13584=CARTESIAN_POINT ( 'NONE',  ( 11.76794919243112325, 46.42999999999999972, 1.441158131103945434E-15 ) ) ;
#13585=CARTESIAN_POINT ( 'NONE',  ( 2.607531440858944223E-15, 63.17999999999999972, -14.19474002721660355 ) ) ;
#13587=CARTESIAN_POINT ( 'NONE',  ( 8.069076079402949020, 50.98598018282910971, 10.82319128239823236 ) ) ;
#13588=CARTESIAN_POINT ( 'NONE',  ( -4.930242145783458874, 37.35776634295052645, -12.56953676492723204 ) ) ;
#13589=CARTESIAN_POINT ( 'NONE',  ( 10.66331449835562140, 36.11497312102070367, 8.282658568296689339 ) ) ;
#13591=CARTESIAN_POINT ( 'NONE',  ( -11.99159045330921813, 74.15881072468002344, 6.200948343019899944 ) ) ;
#13592=CARTESIAN_POINT ( 'NONE',  ( -13.49332011507778617, 76.94460881575584210, 0.4250470828855623662 ) ) ;
#13593=CARTESIAN_POINT ( 'NONE',  ( -5.572961361443443451, 79.38198842499259911, -12.30395537494314695 ) ) ;
#13595=CARTESIAN_POINT ( 'NONE',  ( 0.2248552520803865362, 80.93000000000003524, 13.08843060417372151 ) ) ;
#13597=CARTESIAN_POINT ( 'NONE',  ( 11.76794919243112325, 43.42999999999999972, 1.441158131103945434E-15 ) ) ;
#13602=CARTESIAN_POINT ( 'NONE',  ( 11.47620768244502898, 75.16437255002460915, 7.109921825326903644 ) ) ;
#13604=CARTESIAN_POINT ( 'NONE',  ( -7.272992578804307939, 32.47999999999999687, -10.01041549318726886 ) ) ;
#13605=CARTESIAN_POINT ( 'NONE',  ( -9.286236634453807426, 41.31697598119224324, 9.798817830080201574 ) ) ;
#13606=CARTESIAN_POINT ( 'NONE',  ( -12.76045986475135585, 58.77107810914377239, -4.407033307690351620 ) ) ;
#13607=CARTESIAN_POINT ( 'NONE',  ( 4.654608482077335019, 44.84757688545764154, 12.67221841744786559 ) ) ;
#13608=VECTOR ( 'NONE', #11590, 1000.000000000000000 ) ;
#13609=CARTESIAN_POINT ( 'NONE',  ( -8.891200544363830713E-16, 55.67999999999999972, 13.50000000000000000 ) ) ;
#13611=EDGE_CURVE ( 'NONE', #11272, #7647, #4022, .T. ) ;
#13613=CARTESIAN_POINT ( 'NONE',  ( -9.404872160078671328, 49.54852003193013132, -9.698209604899176384 ) ) ;
#13614=CARTESIAN_POINT ( 'NONE',  ( 10.28911076424348892, 63.76544862978350636, -8.742538089261900680 ) ) ;
#13615=CARTESIAN_POINT ( 'NONE',  ( 13.34880532577127177, 42.50252970743873249, -2.070817942779479282 ) ) ;
#13616=CARTESIAN_POINT ( 'NONE',  ( 3.534134406043794474, 49.05403510232272879, -13.14852249132305140 ) ) ;
#13620=EDGE_LOOP ( 'NONE', ( #13214, #15853, #3317, #8170 ) ) ;
#13621=CARTESIAN_POINT ( 'NONE',  ( -3.959965371964460079, 43.32238572718495107, -12.90617264008083076 ) ) ;
#13622=CARTESIAN_POINT ( 'NONE',  ( -7.500000000000001776, 103.1885367479068947, -9.367496997597607233 ) ) ;
#13623=CARTESIAN_POINT ( 'NONE',  ( 11.54232513752469202, 60.69116484201946804, -7.001836541325773489 ) ) ;
#13627=CARTESIAN_POINT ( 'NONE',  ( 13.47309748709204769, 66.46350195002293049, -0.9713120919723320368 ) ) ;
#13628=CARTESIAN_POINT ( 'NONE',  ( 3.015054115773358134, 56.78848833989679434, 13.15920921728376491 ) ) ;
#13629=CARTESIAN_POINT ( 'NONE',  ( 3.636496289402157078, 59.03000000000000114, -11.19198476289190936 ) ) ;
#13630=CARTESIAN_POINT ( 'NONE',  ( 7.272992578804308828, 69.97999999999998977, 10.01041549318726709 ) ) ;
#13631=CARTESIAN_POINT ( 'NONE',  ( -11.89520195798273328, 47.16632926303795159, 6.387517813708311287 ) ) ;
#13635=CARTESIAN_POINT ( 'NONE',  ( -2.021337026714439489, 56.60737098508230503, 13.34784511190158440 ) ) ;
#13638=CARTESIAN_POINT ( 'NONE',  ( 10.97843994255461908, 33.72687523005959065, -7.868560920089366029 ) ) ;
#13642=CARTESIAN_POINT ( 'NONE',  ( -2.117782281948723977, 62.60385290822299709, 13.33293114825980297 ) ) ;
#13645=CARTESIAN_POINT ( 'NONE',  ( -13.47586914819473414, 43.90198424617900486, -0.8086415342413884044 ) ) ;
#13647=CARTESIAN_POINT ( 'NONE',  ( 8.343458848123583849, 45.87999999999999545, -11.48378591275253768 ) ) ;
#13648=CARTESIAN_POINT ( 'NONE',  ( -13.46831384632932327, 70.96207412421891547, 0.9270688974616148048 ) ) ;
#13651=CARTESIAN_POINT ( 'NONE',  ( -4.340783059308429337, 67.33576598374806110, -12.79059142491898449 ) ) ;
#13653=CARTESIAN_POINT ( 'NONE',  ( 12.99037541014949504, 54.56130944003646022, -3.674264842619463067 ) ) ;
#13654=CARTESIAN_POINT ( 'NONE',  ( -0.4240723324158873764, 64.19524804890893677, -13.49336454334395086 ) ) ;
#13657=CARTESIAN_POINT ( 'NONE',  ( -12.71024981273410681, 34.76417616951957257, -4.593182735545670248 ) ) ;
#13659=CARTESIAN_POINT ( 'NONE',  ( 13.47158690398116043, 78.46026125564927156, -0.8756916466218195305 ) ) ;
#13661=DIRECTION ( 'NONE',  ( 0.000000000000000000, 0.000000000000000000, -1.000000000000000000 ) ) ;
#13662=CARTESIAN_POINT ( 'NONE',  ( 10.80751904294156240, 72.73667749500260982, -8.095150784743120553 ) ) ;
#13663=CARTESIAN_POINT ( 'NONE',  ( 4.690695874063101733, 59.84888257105829723, 12.65971414261017536 ) ) ;
#13665=CARTESIAN_POINT ( 'NONE',  ( -8.691771469529815392E-16, 68.68000000000000682, 14.19474002721660355 ) ) ;
#13666=CARTESIAN_POINT ( 'NONE',  ( -11.27793812523095696, 52.65156426295828140, -7.420298747894694458 ) ) ;
#13667=CARTESIAN_POINT ( 'NONE',  ( 11.76794919243112325, 49.28000000000000114, 3.823638476888996607 ) ) ;
#13668=CARTESIAN_POINT ( 'NONE',  ( 10.92172942406179104, 62.73000000000001108, -7.935100905948385908 ) ) ;
#13670=CARTESIAN_POINT ( 'NONE',  ( 11.64809207761678600, 69.17605374645687277, 6.824371320973884103 ) ) ;
#13671=LINE ( 'NONE', #1824, #16038 ) ;
#13674=CARTESIAN_POINT ( 'NONE',  ( -13.02432634260977018, 74.05675360358792148, 3.552071022051288551 ) ) ;
#13675=CARTESIAN_POINT ( 'NONE',  ( -13.48935192615955359, 76.94856188004330022, 0.5393466570965053108 ) ) ;
#13681=CARTESIAN_POINT ( 'NONE',  ( 3.636496289402157078, 44.03000000000000114, -11.19198476289190936 ) ) ;
#13683=CARTESIAN_POINT ( 'NONE',  ( -2.005948350121168566, 34.25209037325986827, -13.35772390745884231 ) ) ;
#13684=CARTESIAN_POINT ( 'NONE',  ( 13.30271350194304425, 75.34913341900526973, 2.300714643417195671 ) ) ;
#13686=CARTESIAN_POINT ( 'NONE',  ( -4.038158833338649778, 41.53487022600332779, 12.88215458262367186 ) ) ;
#13687=CARTESIAN_POINT ( 'NONE',  ( -2.368957647454752458, 58.26517897696810167, -13.29052651228837334 ) ) ;
#13689=CARTESIAN_POINT ( 'NONE',  ( 2.044753778131714217, 44.75340735468392239, 13.35174435036512364 ) ) ;
#13691=CARTESIAN_POINT ( 'NONE',  ( -10.92172942406179104, 55.23000000000000398, 7.935100905948387684 ) ) ;
#13694=CARTESIAN_POINT ( 'NONE',  ( -11.98418087806660637, 49.70050671477787319, -6.216030342912470807 ) ) ;
#13695=CARTESIAN_POINT ( 'NONE',  ( 11.56350959312967852, 63.17024669828877137, 6.966726136713456086 ) ) ;
#13696=CARTESIAN_POINT ( 'NONE',  ( 8.520149165853723616, 42.00650817108029145, 10.47262060954012597 ) ) ;
#13698=EDGE_LOOP ( 'NONE', ( #745, #16733 ) ) ;
#13699=CARTESIAN_POINT ( 'NONE',  ( -7.576616670048093940E-16, 72.67999999999999261, 12.37355403259654807 ) ) ;
#13703=VERTEX_POINT ( 'NONE', #14257 ) ;
#13704=CARTESIAN_POINT ( 'NONE',  ( -2.545557221017204608, 43.27152815613324321, -13.25833315176517146 ) ) ;
#13705=DIRECTION ( 'NONE',  ( 0.000000000000000000, -1.000000000000000000, 0.000000000000000000 ) ) ;
#13706=CARTESIAN_POINT ( 'NONE',  ( 11.57090963045782495, 60.68925666067695346, -6.954428157688981038 ) ) ;
#13709=DIRECTION ( 'NONE',  ( -0.000000000000000000, -1.000000000000000000, -0.000000000000000000 ) ) ;
#13710=CARTESIAN_POINT ( 'NONE',  ( 9.921642846735080568, 66.78487043750489249, -9.154839053872199983 ) ) ;
#13711=CARTESIAN_POINT ( 'NONE',  ( 1.898648508014808112, 56.74827747273968725, 13.36670787604589705 ) ) ;
#13712=CARTESIAN_POINT ( 'NONE',  ( 11.76794919243112680, 61.57999999999999829, -3.823638476888993942 ) ) ;
#13713=CARTESIAN_POINT ( 'NONE',  ( 4.171729424061791924, 36.03000000000000114, -12.83926296998457239 ) ) ;
#13714=CARTESIAN_POINT ( 'NONE',  ( -11.76794919243112325, 62.92999999999999972, -2.882316262207890869E-15 ) ) ;
#13715=CARTESIAN_POINT ( 'NONE',  ( -13.49555206794069306, 46.94222366541166025, 0.3561146266941883631 ) ) ;
#13718=CARTESIAN_POINT ( 'NONE',  ( 10.07123223633273490, 30.77708342122188157, -8.991547236680613508 ) ) ;
#13722=CARTESIAN_POINT ( 'NONE',  ( -8.343458848123578520, 51.47999999999998977, -11.48378591275254124 ) ) ;
#13723=CARTESIAN_POINT ( 'NONE',  ( 13.50075696862491270, 33.43493226266512153, -0.1459511389326202946 ) ) ;
#13724=CARTESIAN_POINT ( 'NONE',  ( 1.785599194582236620E-06, 38.68004968046676595, 13.49999999999976374 ) ) ;
#13727=CARTESIAN_POINT ( 'NONE',  ( -5.547022999642051033, 62.47876125775495382, 12.30782497079059112 ) ) ;
#13731=CARTESIAN_POINT ( 'NONE',  ( -13.45405233132106559, 43.89143693887756115, -1.114340582890286147 ) ) ;
#13733=EDGE_CURVE ( 'NONE', #17339, #10469, #143, .T. ) ;
#13734=CARTESIAN_POINT ( 'NONE',  ( 8.343458848123583849, 36.88000000000000256, -11.48378591275253768 ) ) ;
#13736=CARTESIAN_POINT ( 'NONE',  ( -11.33016873246668332, 67.65477934096038837, -7.343225168427664151 ) ) ;
#13738=CARTESIAN_POINT ( 'NONE',  ( 13.04221433085913162, 54.30570824892984660, 3.485897513213817245 ) ) ;
#13739=CARTESIAN_POINT ( 'NONE',  ( -5.921537691333334408, 64.39584764108268189, -12.13204556011841717 ) ) ;
#13741=CARTESIAN_POINT ( 'NONE',  ( -12.97726217643209523, 34.79696272453640660, -3.720529569677623716 ) ) ;
#13743=CARTESIAN_POINT ( 'NONE',  ( 12.93099675800281290, 78.29102732052795943, 3.879033096742795728 ) ) ;
#13746=CARTESIAN_POINT ( 'NONE',  ( 7.461391812952430591, 72.90074887590216690, -11.25360145054118099 ) ) ;
#13747=CARTESIAN_POINT ( 'NONE',  ( 1.323381335176092133, 79.13244564980092832, -13.43676060346282419 ) ) ;
#13748=ADVANCED_FACE ( 'NONE', ( #11370 ), #16742, .T. ) ;
#13750=CARTESIAN_POINT ( 'NONE',  ( -4.171729424061787483, 61.32999999999999829, -12.83926296998457417 ) ) ;
#13751=CARTESIAN_POINT ( 'NONE',  ( -12.75901118186940586, 52.77091922838527438, -4.411226007631005253 ) ) ;
#13752=CARTESIAN_POINT ( 'NONE',  ( -11.76794919243112325, 42.08000000000000540, 3.823638476888994386 ) ) ;
#13753=CARTESIAN_POINT ( 'NONE',  ( -4.171729424061787483, 60.32999999999999829, -12.83926296998457417 ) ) ;
#13755=CARTESIAN_POINT ( 'NONE',  ( 10.00829467491076485, 69.07965399636564996, 9.060027076871868701 ) ) ;
#13757=CARTESIAN_POINT ( 'NONE',  ( 0.8900087425982343703, 35.71200196797583715, 13.47797884115083100 ) ) ;
#13759=CARTESIAN_POINT ( 'NONE',  ( -13.00827088827464451, 74.05892661947035549, 3.610402901760149330 ) ) ;
#13760=CARTESIAN_POINT ( 'NONE',  ( -7.025205504711061977, 76.44071120418792020, -11.52839822497519151 ) ) ;
#13763=CARTESIAN_POINT ( 'NONE',  ( -6.155833696462079452, 80.93000000000004945, 11.06015457064189533 ) ) ;
#13765=CARTESIAN_POINT ( 'NONE',  ( 7.272992578804308828, 36.97999999999998977, 10.01041549318726886 ) ) ;
#13766=CARTESIAN_POINT ( 'NONE',  ( 7.499999999999998224, 88.93000000000000682, -9.367496997597600128 ) ) ;
#13767=CARTESIAN_POINT ( 'NONE',  ( -7.404169159380166398, 32.40321505951770575, 11.28896134248388172 ) ) ;
#13768=CARTESIAN_POINT ( 'NONE',  ( 12.25829416376886449, 75.22281960573182857, 5.655528820242253119 ) ) ;
#13769=ADVANCED_FACE ( 'NONE', ( #14175 ), #10224, .T. ) ;
#13773=CARTESIAN_POINT ( 'NONE',  ( 10.92172942406178926, 83.13000000000000966, 7.935100905948387684 ) ) ;
#13774=CARTESIAN_POINT ( 'NONE',  ( 1.604790158072814110, 52.12231609098622442, -13.40787048747939814 ) ) ;
#13775=CARTESIAN_POINT ( 'NONE',  ( -1.526447249548634533, 38.62512138167515729, 13.41343178257564439 ) ) ;
#13776=CARTESIAN_POINT ( 'NONE',  ( 0.03713345166139490200, 37.17866481807171652, -13.49999999999999822 ) ) ;
#13778=CARTESIAN_POINT ( 'NONE',  ( -8.891200544363830713E-16, 79.67999999999999261, 13.50000000000000000 ) ) ;
#13779=CARTESIAN_POINT ( 'NONE',  ( 9.988255280523857138, 63.07858826136173036, 9.082801773783613086 ) ) ;
#13780=CARTESIAN_POINT ( 'NONE',  ( 13.29809445833323345, 42.34812329220370941, 2.328726732125117937 ) ) ;
#13781=CARTESIAN_POINT ( 'NONE',  ( 5.939848974692042205, 48.96343318860201776, -12.12304415933005508 ) ) ;
#13785=CARTESIAN_POINT ( 'NONE',  ( -3.636496289402153081, 80.32999999999999829, -11.19198476289190936 ) ) ;
#13786=CARTESIAN_POINT ( 'NONE',  ( -2.557941946237081154, 70.27197374004576602, -13.25546265980607430 ) ) ;
#13790=CARTESIAN_POINT ( 'NONE',  ( -10.73012146010035650, 43.61871145852727949, -8.197739046590561074 ) ) ;
#13791=CARTESIAN_POINT ( 'NONE',  ( -7.499999999999998224, 108.3768542179258247, 4.091673783487171256 ) ) ;
#13792=CARTESIAN_POINT ( 'NONE',  ( 13.48476133616894579, 60.45297963137706176, -0.6663839570962580838 ) ) ;
#13795=DIRECTION ( 'NONE',  ( 0.000000000000000000, 0.000000000000000000, -1.000000000000000000 ) ) ;
#13796=CARTESIAN_POINT ( 'NONE',  ( 11.80065256636056148, 66.18689098013105365, 6.557030243741954756 ) ) ;
#13797=CARTESIAN_POINT ( 'NONE',  ( 3.282856408315379504, 56.79801877443869529, 13.09476614375152259 ) ) ;
#13798=CARTESIAN_POINT ( 'NONE',  ( -11.76794919243112325, 60.07999999999999119, 3.823638476888994386 ) ) ;
#13799=CARTESIAN_POINT ( 'NONE',  ( -9.520470885617715595, 62.63000000000000256, -6.917026985038136289 ) ) ;
#13800=CARTESIAN_POINT ( 'NONE',  ( -13.50037362800620322, 46.92666714195863875, -0.09336111851946382600 ) ) ;
#13802=CARTESIAN_POINT ( 'NONE',  ( 11.80278193115546159, 45.67295468282410553, -6.553216385568251923 ) ) ;
#13805=CARTESIAN_POINT ( 'NONE',  ( 0.9194697767184354387, 31.14698203856080383, -13.46990214303131239 ) ) ;
#13806=CARTESIAN_POINT ( 'NONE',  ( -3.615283074269553865, 56.54999604154088644, 13.00706333399712378 ) ) ;
#13808=CARTESIAN_POINT ( 'NONE',  ( -8.343458848123582072, 52.37999999999999545, 11.48378591275253768 ) ) ;
#13809=CARTESIAN_POINT ( 'NONE',  ( 6.559526086243817389, 32.92132783700705545, 11.80121481743272582 ) ) ;
#13813=CARTESIAN_POINT ( 'NONE',  ( -13.46388178117166667, 61.96414966410978309, 0.9868924404964516395 ) ) ;
#13816=CARTESIAN_POINT ( 'NONE',  ( -13.15137912863705694, 43.81956125819836245, -3.114482827138729260 ) ) ;
#13818=CARTESIAN_POINT ( 'NONE',  ( -11.76794919243112325, 83.93000000000000682, -2.882316262207890869E-15 ) ) ;
#13819=CARTESIAN_POINT ( 'NONE',  ( -4.433696007799730054, 46.33947026150794812, -12.75186962703676308 ) ) ;
#13820=CARTESIAN_POINT ( 'NONE',  ( -2.946493560005031487, 67.28594004907910175, -13.17452797624288507 ) ) ;
#13822=CARTESIAN_POINT ( 'NONE',  ( 9.472162392857283564, 54.05224036424414891, 9.619202640402704674 ) ) ;
#13824=CARTESIAN_POINT ( 'NONE',  ( -6.457592974018579568, 64.41724210666654926, -11.85949774483797015 ) ) ;
#13827=CARTESIAN_POINT ( 'NONE',  ( -10.19687314292181490, 34.58963878807200132, -8.847247010019716029 ) ) ;
#13830=CARTESIAN_POINT ( 'NONE',  ( 11.22821437167453951, 78.14808671973084131, 7.504731954664256577 ) ) ;
#13833=CARTESIAN_POINT ( 'NONE',  ( 12.72858050653801243, 72.26759830117254069, 4.498419153570456963 ) ) ;
#13834=CARTESIAN_POINT ( 'NONE',  ( 7.157097987683219920, 78.91372639992512461, -11.44668968571802914 ) ) ;
#13836=CARTESIAN_POINT ( 'NONE',  ( 4.171729424061791924, 61.03000000000000114, -12.83926296998457239 ) ) ;
#13837=CARTESIAN_POINT ( 'NONE',  ( -12.72397836871632570, 52.76708174372507898, -4.512114305315815699 ) ) ;
#13838=CARTESIAN_POINT ( 'NONE',  ( 3.636496289402157078, 38.03000000000000114, -11.19198476289190936 ) ) ;
#13839=CARTESIAN_POINT ( 'NONE',  ( 4.171729424061789260, 61.82999999999999829, 12.83926296998457417 ) ) ;
#13840=CARTESIAN_POINT ( 'NONE',  ( -8.224360503536546367E-15, 78.17999999999999261, -13.50000000000000000 ) ) ;
#13842=CARTESIAN_POINT ( 'NONE',  ( 6.937372977335349411, 68.93680969837741657, 11.59389707275178516 ) ) ;
#13843=CARTESIAN_POINT ( 'NONE',  ( -2.773849517010688714, 37.27973736289535367, -13.21200723427060275 ) ) ;
#13846=CARTESIAN_POINT ( 'NONE',  ( -12.66327544140950323, 73.76069652301814017, -4.679031621454643464 ) ) ;
#13847=CARTESIAN_POINT ( 'NONE',  ( -2.436128718453049125, 76.26759188019981650, -13.27840869175127558 ) ) ;
#13852=CARTESIAN_POINT ( 'NONE',  ( 7.272992578804308828, 39.97999999999999687, 10.01041549318726886 ) ) ;
#13854=CARTESIAN_POINT ( 'NONE',  ( -7.866632585845692915, 32.38327360912128938, 10.98016383686059072 ) ) ;
#13855=CARTESIAN_POINT ( 'NONE',  ( 13.23619622236415694, 75.33619659209034580, 2.658123818869813970 ) ) ;
#13857=CARTESIAN_POINT ( 'NONE',  ( 12.00000000000000533, 94.93000000000002103, 1.224646799147353059E-15 ) ) ;
#13858=CARTESIAN_POINT ( 'NONE',  ( 3.636496289402157078, 32.02999999999999403, -11.19198476289190936 ) ) ;
#13859=CARTESIAN_POINT ( 'NONE',  ( -2.360907066372419649, 58.26488951066585287, -13.29195769039779762 ) ) ;
#13861=CARTESIAN_POINT ( 'NONE',  ( 0.1099142029571859580, 37.17604789069145710, -13.49955337541945610 ) ) ;
#13862=EDGE_CURVE ( 'NONE', #6926, #3781, #6706, .T. ) ;
#13863=DIRECTION ( 'NONE',  ( 0.000000000000000000, -1.000000000000000000, 0.000000000000000000 ) ) ;
#13864=EDGE_CURVE ( 'NONE', #5695, #14678, #8529, .T. ) ;
#13865=CARTESIAN_POINT ( 'NONE',  ( -0.01835916714045033107, 49.18066010337725658, -13.49998829627290675 ) ) ;
#13866=CARTESIAN_POINT ( 'NONE',  ( 9.659554295284692671, 63.06166812284966028, 9.431042181653399581 ) ) ;
#13867=CARTESIAN_POINT ( 'NONE',  ( 13.48976328056408747, 42.44825124965819185, -0.5305257734362035515 ) ) ;
#13868=CARTESIAN_POINT ( 'NONE',  ( 13.40726971276752799, 48.37312214362100349, 1.632088562652946662 ) ) ;
#13871=CARTESIAN_POINT ( 'NONE',  ( -9.520470885617715595, 65.62999999999999545, -6.917026985038136289 ) ) ;
#13876=CARTESIAN_POINT ( 'NONE',  ( -12.58667385456655552, 43.75263158861623225, -4.890129452139457378 ) ) ;
#13879=DIRECTION ( 'NONE',  ( 0.000000000000000000, -1.000000000000000000, 0.000000000000000000 ) ) ;
#13880=CARTESIAN_POINT ( 'NONE',  ( 10.75445589294585425, 66.11967042978940867, 8.172061559770561701 ) ) ;
#13881=CARTESIAN_POINT ( 'NONE',  ( 9.434980010212051127, 57.05010519921826528, 9.665379090820270136 ) ) ;
#13882=CARTESIAN_POINT ( 'NONE',  ( 7.272992578804308828, 63.97999999999998977, 10.01041549318726709 ) ) ;
#13883=CARTESIAN_POINT ( 'NONE',  ( -13.49999999999999822, 33.77999999999998693, -4.386415899144240349 ) ) ;
#13884=CARTESIAN_POINT ( 'NONE',  ( -9.520470885617715595, 65.62999999999999545, -6.917026985038136289 ) ) ;
#13886=CARTESIAN_POINT ( 'NONE',  ( -11.35984435782789248, 46.65678690620720204, -7.294136646755872810 ) ) ;
#13887=CARTESIAN_POINT ( 'NONE',  ( 8.617250736976671988, 45.84912361920483193, -10.39756555118851722 ) ) ;
#13888=CARTESIAN_POINT ( 'NONE',  ( 0.2178731047108220797, 70.17216608048821058, -13.49830902344535488 ) ) ;
#13890=CARTESIAN_POINT ( 'NONE',  ( 10.44099705197275973, 30.75714436294632748, -8.557786488581344386 ) ) ;
#13891=CARTESIAN_POINT ( 'NONE',  ( -2.103740194764985638, 56.60437523833922313, 13.33510591258322009 ) ) ;
#13892=CARTESIAN_POINT ( 'NONE',  ( 13.49999999999999822, 53.27999999999999403, 4.386415899144236796 ) ) ;
#13893=CARTESIAN_POINT ( 'NONE',  ( 5.991907069272227382, 32.89832976177464019, 12.10500988212866780 ) ) ;
#13895=CARTESIAN_POINT ( 'NONE',  ( 2.448403087673295619, 40.09219290737040353, -13.28282402178302135 ) ) ;
#13898=CARTESIAN_POINT ( 'NONE',  ( -13.47307933246733214, 61.90057393254070206, -0.8523656554613193714 ) ) ;
#13899=EDGE_LOOP ( 'NONE', ( #8631, #6337, #5207, #9784 ) ) ;
#13900=AXIS2_PLACEMENT_3D ( 'NONE', #12734, #10268, #621 ) ;
#13903=CARTESIAN_POINT ( 'NONE',  ( -11.06759828328972262, 44.22140378436495922, 7.730498622152057742 ) ) ;
#13904=CARTESIAN_POINT ( 'NONE',  ( 4.171729424061789260, 64.82999999999999829, 12.83926296998457417 ) ) ;
#13905=CARTESIAN_POINT ( 'NONE',  ( 4.171729424061791924, 37.03000000000000114, -12.83926296998457239 ) ) ;
#13907=CARTESIAN_POINT ( 'NONE',  ( -9.622267015188688433, 46.55978118158259349, -9.469001082431288907 ) ) ;
#13908=CARTESIAN_POINT ( 'NONE',  ( -1.537544760673846822, 67.23529664120425764, -13.41438453500880890 ) ) ;
#13911=CARTESIAN_POINT ( 'NONE',  ( 7.231211556383717820, 53.94958124039511915, 11.40216215182779180 ) ) ;
#13913=CARTESIAN_POINT ( 'NONE',  ( -9.971648473084066211, 64.57780736460058790, -9.102418965360820735 ) ) ;
#13914=ORIENTED_EDGE ( 'NONE', *, *, #4815, .T. ) ;
#13916=CARTESIAN_POINT ( 'NONE',  ( -10.18520613440925082, 34.58903015065802578, -8.860683611510044244 ) ) ;
#13918=CARTESIAN_POINT ( 'NONE',  ( 13.21851051443945479, 78.52727199688872872, -2.752770575687411014 ) ) ;
#13919=DIRECTION ( 'NONE',  ( -1.927470528863120035E-16, 1.000000000000000000, 0.000000000000000000 ) ) ;
#13921=CARTESIAN_POINT ( 'NONE',  ( 11.49807445461734012, 72.16584275115400260, 7.074230165436003581 ) ) ;
#13923=CARTESIAN_POINT ( 'NONE',  ( -10.92172942406178926, 61.63000000000000256, -7.935100905948389460 ) ) ;
#13924=CARTESIAN_POINT ( 'NONE',  ( -1.421510037799555759, 71.62891323700581836, 13.42697251540404757 ) ) ;
#13925=CARTESIAN_POINT ( 'NONE',  ( -11.76794919243112325, 41.92999999999999261, -2.882316262207890869E-15 ) ) ;
#13926=CARTESIAN_POINT ( 'NONE',  ( 4.171729424061789260, 55.83000000000000540, 12.83926296998457417 ) ) ;
#13929=CARTESIAN_POINT ( 'NONE',  ( 8.535454704214165744, 69.00715068001011332, 10.46229327927559183 ) ) ;
#13931=CARTESIAN_POINT ( 'NONE',  ( 1.363617428356367123, 35.72903063807564195, 13.43096419532364294 ) ) ;
#13933=CARTESIAN_POINT ( 'NONE',  ( -13.48837046896241354, 73.91067174755934843, -0.5608890242489086297 ) ) ;
#13936=DIRECTION ( 'NONE',  ( -1.000000000000000000, -0.000000000000000000, -0.000000000000000000 ) ) ;
#13940=CARTESIAN_POINT ( 'NONE',  ( 11.76794919243112680, 34.57999999999999829, -3.823638476888993942 ) ) ;
#13942=CARTESIAN_POINT ( 'NONE',  ( -6.679390041561677371, 32.43370277562137005, 11.73465909257911832 ) ) ;
#13943=CARTESIAN_POINT ( 'NONE',  ( 1.329527900993174860, 74.72780491797803393, 13.43437217338847844 ) ) ;
#13944=CARTESIAN_POINT ( 'NONE',  ( -0.08605353725393936892, 53.67690303198914847, 13.49999999999942091 ) ) ;
#13945=DIRECTION ( 'NONE',  ( 1.000000000000000000, 0.000000000000000000, 0.000000000000000000 ) ) ;
#13946=CARTESIAN_POINT ( 'NONE',  ( -8.343458848123576743, 81.48000000000000398, -11.48378591275254301 ) ) ;
#13948=CARTESIAN_POINT ( 'NONE',  ( 4.710692427101017543, 52.01035291496985025, -12.65147037080429726 ) ) ;
#13949=CARTESIAN_POINT ( 'NONE',  ( -2.093142125047454449, 38.60467073819259554, 13.33804731820490552 ) ) ;
#13951=CARTESIAN_POINT ( 'NONE',  ( -8.891200544363830713E-16, 70.68000000000000682, 13.50000000000000000 ) ) ;
#13952=CARTESIAN_POINT ( 'NONE',  ( -0.06416183230854911879, 49.18230675135094287, -13.49986922154364777 ) ) ;
#13953=CARTESIAN_POINT ( 'NONE',  ( 10.66583021020285393, 63.11535396121603725, 8.275874897226483284 ) ) ;
#13954=CARTESIAN_POINT ( 'NONE',  ( 7.562216151199702807, 41.96360496807130858, 11.18639152389247471 ) ) ;
#13955=CARTESIAN_POINT ( 'NONE',  ( 12.27263252356545209, 48.63596850838850116, -5.624294195753364534 ) ) ;
#13957=ORIENTED_EDGE ( 'NONE', *, *, #12169, .F. ) ;
#13958=CARTESIAN_POINT ( 'NONE',  ( -9.520470885617715595, 68.62999999999999545, -6.917026985038136289 ) ) ;
#13963=CARTESIAN_POINT ( 'NONE',  ( -0.3404806211656328241, 43.19224228718480418, -13.49585535663135794 ) ) ;
#13964=CARTESIAN_POINT ( 'NONE',  ( -2.522983078673279752E-14, 34.17999999999999972, -13.50000000000000000 ) ) ;
#13967=CARTESIAN_POINT ( 'NONE',  ( 10.23380095822083291, 66.09158251474292456, 8.804547898461850153 ) ) ;
#13968=CARTESIAN_POINT ( 'NONE',  ( -4.171729424061787483, 79.32999999999999829, -12.83926296998457417 ) ) ;
#13971=CARTESIAN_POINT ( 'NONE',  ( -7.272992578804310604, 57.37999999999998835, 10.01041549318726709 ) ) ;
#13972=CARTESIAN_POINT ( 'NONE',  ( 2.272985001014427788E-15, 62.17999999999999972, -12.37355403259654985 ) ) ;
#13973=CARTESIAN_POINT ( 'NONE',  ( -11.41968976572175976, 46.66065175804080667, -7.200595652070090225 ) ) ;
#13974=CARTESIAN_POINT ( 'NONE',  ( 10.84045915709670993, 45.73470465951034214, -8.047803413914586201 ) ) ;
#13975=CARTESIAN_POINT ( 'NONE',  ( 8.035699651468419802, 69.87551396580593632, -10.84793394748052364 ) ) ;
#13976=CARTESIAN_POINT ( 'NONE',  ( 8.184208372444009782, 30.86883944040518557, -10.73662710873863979 ) ) ;
#13977=CARTESIAN_POINT ( 'NONE',  ( -13.46101982974745859, 55.96549097240059467, 1.025187530456345586 ) ) ;
#13979=CARTESIAN_POINT ( 'NONE',  ( 1.852680671424132619, 32.74661364833260535, 13.38217953742864985 ) ) ;
#13981=CARTESIAN_POINT ( 'NONE',  ( 11.36437994058350220, 39.70321145296029641, -7.292015817707691916 ) ) ;
#13982=VERTEX_POINT ( 'NONE', #11804 ) ;
#13983=CARTESIAN_POINT ( 'NONE',  ( -13.37679940684410163, 61.99543014590985734, 1.870821765799961733 ) ) ;
#13984=VECTOR ( 'NONE', #11866, 1000.000000000000000 ) ;
#13988=CARTESIAN_POINT ( 'NONE',  ( 11.03739991603106319, 48.13673635289907082, 7.779773485289230628 ) ) ;
#13989=LINE ( 'NONE', #9965, #12146 ) ;
#13990=CARTESIAN_POINT ( 'NONE',  ( -4.171729424061787483, 31.32999999999999829, -12.83926296998457417 ) ) ;
#13991=CARTESIAN_POINT ( 'NONE',  ( 10.92172942406178926, 41.13000000000000256, 7.935100905948387684 ) ) ;
#13994=CARTESIAN_POINT ( 'NONE',  ( -3.342578662528335798, 46.30004703686991263, -13.08883371199211965 ) ) ;
#13995=CARTESIAN_POINT ( 'NONE',  ( -0.03696684871921104842, 67.18132919150241378, -13.50000000000000000 ) ) ;
#13997=CARTESIAN_POINT ( 'NONE',  ( 4.958073332672438660, 53.85884788343330598, 12.55661954819793635 ) ) ;
#13999=EDGE_LOOP ( 'NONE', ( #14542, #9976, #1058, #17273 ) ) ;
#14000=CARTESIAN_POINT ( 'NONE',  ( -10.99488771831293477, 64.63370636212923159, -7.845699068106005925 ) ) ;
#14003=CARTESIAN_POINT ( 'NONE',  ( -8.055926233375233281, 34.48539140569977235, -10.83293180899966224 ) ) ;
#14005=CARTESIAN_POINT ( 'NONE',  ( 10.45646361262144453, 78.10370444553853986, 8.538874148716518064 ) ) ;
#14006=CARTESIAN_POINT ( 'NONE',  ( 8.343458848123583849, 47.87999999999999545, -11.48378591275253768 ) ) ;
#14007=AXIS2_PLACEMENT_3D ( 'NONE', #17189, #14437, #13043 ) ;
#14010=CARTESIAN_POINT ( 'NONE',  ( 11.91517651397667699, 72.66463852654297284, -6.346540879243715239 ) ) ;
#14012=( BOUNDED_CURVE ( )  B_SPLINE_CURVE ( 2, ( #2427, #10510, #9697, #4198, #14540, #8283, #14867, #9522, #1356, #6863, #16471, #17208, #14961 ),
 .UNSPECIFIED., .F., .F. ) 
 B_SPLINE_CURVE_WITH_KNOTS ( ( 3, 2, 2, 2, 2, 2, 3 ),
 ( 0.7638888888888888395, 0.7666666666666667185, 0.7722222222222222543, 0.7777777777777777901, 0.7833333333333333259, 0.7888888888888888618, 0.7916666666666666297 ),
 .UNSPECIFIED. ) 
 CURVE ( )  GEOMETRIC_REPRESENTATION_ITEM ( )  RATIONAL_B_SPLINE_CURVE ( ( 0.9755282581475768211, 0.9755282581475762660, 1.000000000000000000, 0.9510565162951535312, 1.000000000000000000, 0.9510565162951535312, 1.000000000000000000, 0.9510565162951535312, 1.000000000000000000, 0.9510565162951535312, 1.000000000000000000, 0.9755282581475768211, 0.9755282581475768211 ) ) 
 REPRESENTATION_ITEM ( '' )  );
#14013=CARTESIAN_POINT ( 'NONE',  ( -13.50000000000000000, 61.92999999999999972, -3.306546357697853733E-15 ) ) ;
#14014=CARTESIAN_POINT ( 'NONE',  ( -8.629845922160509275, 52.51158210495129453, -10.38376407271738699 ) ) ;
#14015=EDGE_CURVE ( 'NONE', #12574, #17443, #6571, .T. ) ;
#14016=CARTESIAN_POINT ( 'NONE',  ( 3.636496289402154414, 36.82999999999999119, 11.19198476289190936 ) ) ;
#14018=CARTESIAN_POINT ( 'NONE',  ( -4.171729424061791036, 55.52999999999999403, 12.83926296998457239 ) ) ;
#14019=B_SPLINE_CURVE_WITH_KNOTS ( 'NONE', 3,
 ( #12238, #9694, #16289, #15042, #2938, #3118, #5890, #8367, #16469, #11097, #3026, #13895, #11184, #12418, #306, #5715, #7122, #4374, #1794, #16560, #9782, #4466, #15129, #8456, #7205, #16192, #3301, #3474, #13020, #14074, #16816, #8714, #12677, #16646, #11443, #2128, #9957, #7471, #3210, #8630, #7384, #1961, #740, #10125, #14159, #7292, #15305, #15478, #7643, #11356, #4552, #4724, #4808, #10210, #12762, #4637, #15393, #2047, #13981, #1877, #16990, #16730, #3389, #7554, #10044, #14327, #10295, #901, #567, #12851, #5974, #650, #6060, #12933, #8802, #6149, #11527, #16905, #15563, #8888, #14243, #817, #6228, #11614, #4894, #15647, #3557, #8971, #2216, #11269, #3993, #2647, #10720, #6660, #9237, #5249, #10635, #3733, #2300, #4979, #10555, #10382, #6403, #15736, #9323, #12041, #3645, #17075, #9059, #7904, #1248, #14412, #11786, #7728, #13104, #17250, #1167, #17420, #991, #3823, #17162, #15914, #5074, #1078, #10468, #15829, #9151, #14498, #2385, #7821, #5335, #8078, #13193, #6578, #11959, #16000, #16085, #2561, #6492, #11875, #5163, #14591, #17338, #9409, #2471, #13359, #14673, #13279, #3905, #7991, #14757, #13442, #6313, #11699, #4169, #6925, #16262, #2735, #6745, #1509, #9754, #105, #14932, #12125, #1597, #4079, #5690, #9581, #8341, #196, #4259, #14841, #5418, #5601, #15191, #1417, #14, #12302, #12390, #281, #2824 ),
 .UNSPECIFIED., .F., .F.,
 ( 4, 2, 1, 1, 1, 2, 2, 2, 2, 1, 2, 2, 1, 2, 2, 2, 2, 2, 2, 2, 1, 2, 2, 2, 2, 1, 1, 2, 2, 1, 1, 1, 1, 1, 2, 2, 2, 1, 2, 2, 1, 2, 2, 2, 2, 2, 2, 2, 1, 2, 2, 2, 1, 1, 1, 1, 2, 2, 2, 2, 2, 1, 2, 2, 1, 2, 2, 2, 2, 2, 1, 2, 2, 1, 1, 2, 2, 1, 1, 2, 2, 1, 2, 2, 2, 2, 2, 2, 1, 1, 2, 2, 2, 2, 2, 1, 1, 1, 2, 2, 2, 2, 2, 1, 1, 2, 2, 4 ),
 ( 0.7990296683925127708, 0.7990583905221522176, 0.7990871126517916645, 0.7991445569110705582, 0.7992594454296283457, 0.7994892224667439207, 0.7999487765409750706, 0.8008678846894373704, 0.8017869928378996702, 0.8020167698750152452, 0.8020742141342941389, 0.8021029362639335858, 0.8021316583935730327, 0.8022465469121308201, 0.8027061009863619701, 0.8036252091348243809, 0.8045443172832866807, 0.8050038713575178306, 0.8051187598760756181, 0.8051762041353545118, 0.8052336483946334056, 0.8054634254317489805, 0.8063825335802112804, 0.8068420876544424303, 0.8070718646915580052, 0.8071293089508368990, 0.8071580310804763458, 0.8071723921452961248, 0.8071867532101157927, 0.8073016417286735802, 0.8077611958029046191, 0.8079909728400201940, 0.8081058613585779815, 0.8081633056178567642, 0.8081920277474962111, 0.8082207498771356580, 0.8091398580255978468, 0.8091973022848767405, 0.8092116633496964084, 0.8092260244145160764, 0.8092547465441555232, 0.8093696350627133107, 0.8095994120998287746, 0.8100589661740598135, 0.8109780743225218913, 0.8112078513596373552, 0.8112365734892768021, 0.8112652956189162490, 0.8113227398781951427, 0.8114376283967528192, 0.8118971824709838581, 0.8128162906194458248, 0.8130460676565613998, 0.8131609561751190762, 0.8132184004343979700, 0.8132471225640374168, 0.8132614836288570848, 0.8132758446936768637, 0.8137353987679079026, 0.8146545069163698694, 0.8151140609906009082, 0.8152289495091586957, 0.8152863937684375895, 0.8153151158980770363, 0.8153438380277164832, 0.8155736150648319471, 0.8164927232132941359, 0.8169522772875251748, 0.8171820543246406388, 0.8172969428431984262, 0.8173256649728378731, 0.8173328455052477626, 0.8173364357714526518, 0.8173400260376576520, 0.8173543871024773200, 0.8174118313617562137, 0.8192500476586801472, 0.8193074919179590410, 0.8193362140475984878, 0.8193505751124181558, 0.8193649361772379347, 0.8194798246957956112, 0.8197096017329110751, 0.8201691558071420030, 0.8210882639556038587, 0.8213180409927193226, 0.8213754852519982164, 0.8214042073816376632, 0.8214329295112771101, 0.8215478180298347866, 0.8220073721040658254, 0.8229264802525277922, 0.8233860343267587201, 0.8238455884009896479, 0.8247646965494516147, 0.8252242506236825426, 0.8253391391422403300, 0.8253965834015192238, 0.8254253055311586706, 0.8254540276607981175, 0.8256838046979135814, 0.8266029128463754372, 0.8270624669206063651, 0.8272922439577218290, 0.8274071324762795054, 0.8274645767355583992, 0.8275220209948372929, 0.8284411291432991487 ),
 .UNSPECIFIED. ) ;
#14020=CARTESIAN_POINT ( 'NONE',  ( 0.000000000000000000, 80.93000000000000682, -13.50000000000000000 ) ) ;
#14022=CARTESIAN_POINT ( 'NONE',  ( 12.58706070538537425, 69.25271909279739191, 4.887953961977841821 ) ) ;
#14023=CARTESIAN_POINT ( 'NONE',  ( -2.902129482468654764, 37.28434955807667706, -13.18442075298268712 ) ) ;
#14026=CARTESIAN_POINT ( 'NONE',  ( -10.58212249187060472, 73.61066026166233200, -8.382645537578081729 ) ) ;
#14027=CARTESIAN_POINT ( 'NONE',  ( -9.417897376538508780, 76.54953983149943042, -9.672290812086593803 ) ) ;
#14030=CARTESIAN_POINT ( 'NONE',  ( -11.52888015854885317, 80.93000000000003524, -3.329402692648984363 ) ) ;
#14033=CARTESIAN_POINT ( 'NONE',  ( 11.76794919243112325, 40.27999999999998693, 3.823638476888997051 ) ) ;
#14036=CARTESIAN_POINT ( 'NONE',  ( -1.388145184345592753, 32.63015141958924659, 13.42855714285366631 ) ) ;
#14037=CARTESIAN_POINT ( 'NONE',  ( 8.213066728255030924, 74.99246367489935494, 10.71458833715021797 ) ) ;
#14040=CARTESIAN_POINT ( 'NONE',  ( -4.171729424061791036, 82.53000000000000114, 12.83926296998457239 ) ) ;
#14041=CARTESIAN_POINT ( 'NONE',  ( -2.600835754285047319, 58.27351591942388609, -13.24722694462289141 ) ) ;
#14042=CARTESIAN_POINT ( 'NONE',  ( -6.944664154335186801, 38.42265581552923237, 11.57681684740535388 ) ) ;
#14043=CARTESIAN_POINT ( 'NONE',  ( 5.734972866248251755, 36.97144598669994764, -12.22129836149683513 ) ) ;
#14044=CYLINDRICAL_SURFACE ( 'NONE', #13900, 13.50000000000000000 ) ;
#14045=LINE ( 'NONE', #6122, #1025 ) ;
#14046=CARTESIAN_POINT ( 'NONE',  ( 7.037443801358370443, 62.94122972340164779, 11.52066418650788293 ) ) ;
#14047=CARTESIAN_POINT ( 'NONE',  ( 8.302061766585694613, 41.99651312526439284, 10.64547685796597420 ) ) ;
#14048=CARTESIAN_POINT ( 'NONE',  ( 7.849181362486006286, 48.88379379287454896, -10.98497563233463659 ) ) ;
#14052=CARTESIAN_POINT ( 'NONE',  ( 9.520470885617717371, 64.72999999999998977, -6.917026985038131848 ) ) ;
#14057=CARTESIAN_POINT ( 'NONE',  ( 0.8559505999959272637, 76.14922317426433551, -13.47283824510951611 ) ) ;
#14061=CARTESIAN_POINT ( 'NONE',  ( 6.923942340376762594, 65.93627631632044483, 11.60134431817299117 ) ) ;
#14062=CARTESIAN_POINT ( 'NONE',  ( 10.92172942406178926, 81.13000000000000966, 7.935100905948387684 ) ) ;
#14063=CARTESIAN_POINT ( 'NONE',  ( -3.636496289402155746, 54.52999999999999403, 11.19198476289190936 ) ) ;
#14064=CARTESIAN_POINT ( 'NONE',  ( 2.272985001014427788E-15, 59.17999999999998550, -12.37355403259654985 ) ) ;
#14065=CARTESIAN_POINT ( 'NONE',  ( -9.810502609816827757, 46.56925146285257000, -9.274434226274468784 ) ) ;
#14066=CARTESIAN_POINT ( 'NONE',  ( 10.93984686930985895, 45.72887148577164851, -7.911647713641231761 ) ) ;
#14067=CARTESIAN_POINT ( 'NONE',  ( 0.07395759035408112914, 70.17734075790797021, -13.50000000181907467 ) ) ;
#14069=CARTESIAN_POINT ( 'NONE',  ( 4.677241269952973290, 31.01107242823733046, -12.66918181086320061 ) ) ;
#14070=CARTESIAN_POINT ( 'NONE',  ( -12.79867627401926100, 56.08469950320211694, 4.295844407513158991 ) ) ;
#14071=CARTESIAN_POINT ( 'NONE',  ( -0.4447223339203151826, 50.66423004611947789, 13.50000000035602099 ) ) ;
#14072=CARTESIAN_POINT ( 'NONE',  ( 13.04807147248227395, 33.30564593050542754, 3.492245395005759701 ) ) ;
#14073=CARTESIAN_POINT ( 'NONE',  ( 5.221946460518151589, 42.99121459397418477, -12.44964204775182814 ) ) ;
#14074=CARTESIAN_POINT ( 'NONE',  ( 7.736074338173390963, 39.88885195608636991, -11.06766002516535607 ) ) ;
#14076=CARTESIAN_POINT ( 'NONE',  ( -13.07942562849002499, 61.81060098926703716, -3.356404025825254767 ) ) ;
#14077=ORIENTED_EDGE ( 'NONE', *, *, #8816, .T. ) ;
#14080=CARTESIAN_POINT ( 'NONE',  ( 4.748822866441054558, 58.00894215750955141, -12.63719586234929437 ) ) ;
#14082=CARTESIAN_POINT ( 'NONE',  ( 9.520470885617715595, 76.13000000000000966, 6.917026985038134512 ) ) ;
#14085=CARTESIAN_POINT ( 'NONE',  ( -9.581374244281432695, 46.55771639631056047, -9.510429861097501103 ) ) ;
#14088=CARTESIAN_POINT ( 'NONE',  ( 10.68047679364148372, 54.11617973143395943, 8.256962218962808464 ) ) ;
#14095=CARTESIAN_POINT ( 'NONE',  ( -3.037551701948927096, 34.28921878658023559, -13.15470998141922365 ) ) ;
#14097=CARTESIAN_POINT ( 'NONE',  ( 5.572222782050855194, 77.88196720139393392, 12.30424787591440783 ) ) ;
#14098=CARTESIAN_POINT ( 'NONE',  ( 10.92172942406179104, 47.73000000000000398, -7.935100905948385908 ) ) ;
#14101=CARTESIAN_POINT ( 'NONE',  ( 12.90825826996955250, 72.28807910334995768, 3.957424788451787467 ) ) ;
#14103=CARTESIAN_POINT ( 'NONE',  ( 8.343458848123578520, 62.97999999999999687, 11.48378591275254124 ) ) ;
#14104=CARTESIAN_POINT ( 'NONE',  ( -3.536773975472625509, 52.30716712712094107, -13.03489925632436908 ) ) ;
#14106=CARTESIAN_POINT ( 'NONE',  ( 11.76794919243112680, 40.57999999999999829, -3.823638476888993942 ) ) ;
#14108=CARTESIAN_POINT ( 'NONE',  ( -13.49999999999999822, 54.77999999999998693, -4.386415899144240349 ) ) ;
#14109=LINE ( 'NONE', #14020, #242 ) ;
#14110=CARTESIAN_POINT ( 'NONE',  ( 3.236805660951904251, 68.79646791454764809, 13.10715617363204544 ) ) ;
#14114=CARTESIAN_POINT ( 'NONE',  ( -13.48413585140022519, 73.95268284379521617, 0.6581954568009130702 ) ) ;
#14115=CARTESIAN_POINT ( 'NONE',  ( -9.416305305992766606, 76.54946069877891546, -9.673840839019193893 ) ) ;
#14116=LINE ( 'NONE', #4765, #5936 ) ;
#14118=CARTESIAN_POINT ( 'NONE',  ( 7.272992578804311492, 34.87999999999999545, -10.01041549318726886 ) ) ;
#14119=CARTESIAN_POINT ( 'NONE',  ( 6.767892274116773521, 80.93000000001259764, -11.68099457092376348 ) ) ;
#14120=CARTESIAN_POINT ( 'NONE',  ( -6.462491681254555864, 32.44254954019859127, 11.85507982337297150 ) ) ;
#14123=B_SPLINE_CURVE_WITH_KNOTS ( 'NONE', 3,
 ( #15414, #7312, #11549, #12785, #6250, #10233, #4656, #10317, #14265, #11463, #4829, #584, #16839, #15498, #5995, #4919, #11377, #2154, #3410, #3137, #12872, #8562, #16749, #8824, #10064, #3320, #14182, #2067, #7491, #761, #3329, #14446, #9093, #16757, #6002, #1986, #16848, #3418, #8832, #14189, #1024, #15944, #1109, #11904, #10906, #6435, #11819, #13710, #14529, #9593, #2415, #17198, #7933, #17281, #10498, #10995, #4358, #15113, #5195, #6936, #5106, #6525, #13137, #12224, #15861, #9267, #10583, #6846, #16456, #3768, #14944, #9180, #7848, #1429, #13307, #7766, #208, #1519, #5522, #8266, #13221, #16275, #12314, #3852, #14618, #2504, #116, #4181, #9767, #2835, #13627, #5613, #7026, #16363, #4270, #292, #9680, #15030, #2923, #8353, #1609, #12404, #5701, #11082, #11254, #15205, #15465, #16545, #635, #10030, #16633, #8532, #3105, #467, #2033, #5875, #1781, #12840, #15292, #4536, #16801, #13796, #7190, #7109, #3375, #5960, #379, #550, #13880, #1946, #15377, #13967, #7368, #1694, #1864, #726, #6135, #12493, #11170, #5785, #4451, #9858, #7278, #3284, #12661, #12579, #8700, #14145, #4796, #9944, #14061, #7458, #3194, #10112, #6048, #8615, #11340, #16717, #4623, #12748, #11431, #16891, #4709, #11514, #10197, #3011, #8441, #13180, #8876, #2202, #3631, #2115, #9137, #15634, #1065, #9045, #5060, #14397, #5149, #7628, #7714, #14576, #13266, #5237, #1154, #15550, #4647, #14172, #829, #11368 ),
 .UNSPECIFIED., .F., .F.,
 ( 4, 2, 2, 2, 2, 1, 1, 2, 2, 1, 1, 2, 2, 1, 1, 2, 2, 2, 2, 2, 2, 1, 2, 2, 2, 2, 1, 2, 2, 1, 2, 2, 2, 2, 2, 1, 1, 2, 2, 2, 2, 2, 2, 1, 2, 2, 2, 2, 1, 2, 2, 1, 1, 2, 1, 1, 1, 2, 2, 2, 2, 2, 2, 2, 1, 1, 2, 2, 2, 1, 2, 2, 1, 1, 1, 2, 2, 1, 2, 2, 1, 2, 2, 2, 2, 1, 2, 2, 2, 2, 2, 2, 2, 1, 1, 1, 2, 2, 2, 1, 1, 2, 2, 1, 2, 2, 2, 2, 2, 2, 1, 4 ),
 ( 0.2696254849433896150, 0.2705427676827099059, 0.2714600504220301413, 0.2715173805932376561, 0.2715747107644451708, 0.2716893711068602002, 0.2719186917916902591, 0.2723773331613503768, 0.2732946159006706122, 0.2734092762430856416, 0.2734236087858875064, 0.2734307750572884665, 0.2734379413286894267, 0.2734666064142931563, 0.2735239365855006710, 0.2737532572703307299, 0.2742118986399908476, 0.2751291813793110275, 0.2753585020641410863, 0.2753871671497448159, 0.2754158322353486010, 0.2754731624065561157, 0.2755878227489711452, 0.2760464641186312629, 0.2769637468579514983, 0.2771930675427815571, 0.2773077278851965866, 0.2773363929708003717, 0.2773650580564041013, 0.2774223882276116160, 0.2778810295972717892, 0.2787983123365920801, 0.2792569537062522533, 0.2792856187918559829, 0.2792999513346579032, 0.2793142838774597680, 0.2793716140486672828, 0.2794862743910823122, 0.2797155950759123710, 0.2806328778152326620, 0.2810915191848927797, 0.2812061795273078091, 0.2812635096985153238, 0.2813208398697228385, 0.2815501605545528974, 0.2824674432938731883, 0.2829260846635333060, 0.2831554053483633648, 0.2831840704339671499, 0.2831984029767690147, 0.2832127355195708795, 0.2832700656907784498, 0.2833847260331934792, 0.2843020087725137701, 0.2847606501421739433, 0.2849899708270040022, 0.2851046311694190871, 0.2851332962550228167, 0.2851619613406266018, 0.2852192915118341165, 0.2861365742511544075, 0.2870538569904746984, 0.2870825220760784280, 0.2871111871616822131, 0.2871685173328897278, 0.2872831776753047572, 0.2875124983601348716, 0.2879711397297950448, 0.2888884224691154468, 0.2890030828115304762, 0.2890604129827380464, 0.2890747455255399112, 0.2890890780683417760, 0.2891177431539455611, 0.2893470638387756200, 0.2898057052084357932, 0.2907229879477561396, 0.2909523086325861985, 0.2910096388037937132, 0.2910383038893974983, 0.2910669689750012279, 0.2911816293174162573, 0.2916402706870764305, 0.2925575534263967770, 0.2927868741112268913, 0.2929015344536419208, 0.2929588646248494355, 0.2930161947960569502, 0.2934748361657171234, 0.2943921189050374698, 0.2948507602746976430, 0.2949080904459051578, 0.2949224229887070781, 0.2949367555315089429, 0.2949654206171127280, 0.2950800809595277574, 0.2953094016443579273, 0.2962266843836784957, 0.2966853257533387800, 0.2967999860957538649, 0.2968573162669613796, 0.2968716488097632444, 0.2968859813525651647, 0.2969146464381688943, 0.2971439671229990087, 0.2980612498623194107, 0.2985198912319795839, 0.2987492119168096427, 0.2988065420880171574, 0.2988352071736209425, 0.2988638722592247277, 0.2989785326016397571 ),
 .UNSPECIFIED. ) ;
#14125=CARTESIAN_POINT ( 'NONE',  ( 13.50000000000000355, 80.57999999999998408, -4.386415899144233244 ) ) ;
#14126=CARTESIAN_POINT ( 'NONE',  ( 13.19208277413943975, 51.53150884716730218, -2.867894163931984597 ) ) ;
#14128=CARTESIAN_POINT ( 'NONE',  ( 2.196276064027457675, 37.10127726452279262, -13.32743759420177554 ) ) ;
#14131=CARTESIAN_POINT ( 'NONE',  ( -4.068989761728259325, 49.32630495305625118, -12.87242965585119236 ) ) ;
#14133=CARTESIAN_POINT ( 'NONE',  ( -13.50000000000000000, 60.92999999999999972, -3.306546357697853733E-15 ) ) ;
#14134=DIRECTION ( 'NONE',  ( 0.000000000000000000, 0.000000000000000000, -1.000000000000000000 ) ) ;
#14135=CARTESIAN_POINT ( 'NONE',  ( 13.36456123615529634, 48.49836822103661405, -1.955719740300823961 ) ) ;
#14137=ORIENTED_EDGE ( 'NONE', *, *, #9438, .F. ) ;
#14138=CARTESIAN_POINT ( 'NONE',  ( 3.636496289402154414, 66.82999999999999829, 11.19198476289190936 ) ) ;
#14143=CARTESIAN_POINT ( 'NONE',  ( -10.98210873309851898, 80.92999999999996419, -5.183560256216895645 ) ) ;
#14145=CARTESIAN_POINT ( 'NONE',  ( 8.105864574935058187, 65.98763176480156289, 10.79566791222186772 ) ) ;
#14147=CARTESIAN_POINT ( 'NONE',  ( -7.272992578804310604, 54.37999999999999545, 10.01041549318726709 ) ) ;
#14148=CARTESIAN_POINT ( 'NONE',  ( -10.54451491581842504, 59.25158502488826429, 8.432595136247059031 ) ) ;
#14150=CARTESIAN_POINT ( 'NONE',  ( 9.162143948892088829, 45.82302722542944906, -9.914896862951890100 ) ) ;
#14151=CARTESIAN_POINT ( 'NONE',  ( 0.7729741899047672948, 70.15223374091664255, -13.48100388766008528 ) ) ;
#14152=AXIS2_PLACEMENT_3D ( 'NONE', #2, #1064, #14660 ) ;
#14154=CARTESIAN_POINT ( 'NONE',  ( 12.01961491643047175, 30.65663574407087921, -6.146451131573384075 ) ) ;
#14155=CARTESIAN_POINT ( 'NONE',  ( -13.47178327623467631, 55.96039367275813703, 0.8796395391391890195 ) ) ;
#14156=CARTESIAN_POINT ( 'NONE',  ( 0.000000000000000000, 102.9300000000000068, 0.000000000000000000 ) ) ;
#14157=CARTESIAN_POINT ( 'NONE',  ( 3.198877721759256776, 32.79499661759405882, 13.12308681134866362 ) ) ;
#14159=CARTESIAN_POINT ( 'NONE',  ( 10.29006543620832126, 39.76535928357677108, -8.738724199765389500 ) ) ;
#14161=CARTESIAN_POINT ( 'NONE',  ( -8.733024514805581617, 62.34354256471783629, 10.29493024108846733 ) ) ;
#14162=ORIENTED_EDGE ( 'NONE', *, *, #1462, .F. ) ;
#14163=ORIENTED_EDGE ( 'NONE', *, *, #8201, .T. ) ;
#14166=CARTESIAN_POINT ( 'NONE',  ( 8.869080463320887731, 48.02207153075600843, 10.21686289651330881 ) ) ;
#14168=CARTESIAN_POINT ( 'NONE',  ( 4.680006372702086637, 58.01148812036320379, -12.66286395962633726 ) ) ;
#14169=CARTESIAN_POINT ( 'NONE',  ( 2.537983195068045816, 79.08874347684349004, -13.25928836460632354 ) ) ;
#14170=CARTESIAN_POINT ( 'NONE',  ( 7.272992578804308828, 81.97999999999998977, 10.01041549318726709 ) ) ;
#14171=CARTESIAN_POINT ( 'NONE',  ( -10.92172942406178926, 42.63000000000000256, -7.935100905948389460 ) ) ;
#14172=CARTESIAN_POINT ( 'NONE',  ( 0.1711164140752765850, 65.68615328522727737, 13.49921302317839533 ) ) ;
#14173=EDGE_CURVE ( 'NONE', #7488, #12569, #16372, .T. ) ;
#14174=( LENGTH_UNIT ( ) NAMED_UNIT ( * ) SI_UNIT ( .MILLI., .METRE. ) );
#14175=FACE_OUTER_BOUND ( 'NONE', #13698, .T. ) ;
#14178=CARTESIAN_POINT ( 'NONE',  ( 3.558926121134557530, 53.80781110109241894, 13.02324908181068963 ) ) ;
#14181=VERTEX_POINT ( 'NONE', #10889 ) ;
#14182=CARTESIAN_POINT ( 'NONE',  ( 5.783146345639755381, 66.96971615883565221, -12.20007971092912413 ) ) ;
#14185=DIRECTION ( 'NONE',  ( 0.000000000000000000, -1.000000000000000000, 0.000000000000000000 ) ) ;
#14188=CARTESIAN_POINT ( 'NONE',  ( 13.38186479756907232, 72.36768824479015905, 1.782328871136838133 ) ) ;
#14189=CARTESIAN_POINT ( 'NONE',  ( 8.546315828672829795, 66.85235120296643174, -10.45335113635833757 ) ) ;
#14191=CARTESIAN_POINT ( 'NONE',  ( -8.343458848123576743, 49.47999999999998977, -11.48378591275254301 ) ) ;
#14192=CARTESIAN_POINT ( 'NONE',  ( -0.2119980460951424450, 71.67237679919810489, 13.49880501296570579 ) ) ;
#14195=CARTESIAN_POINT ( 'NONE',  ( -8.343458848123576743, 51.47999999999998977, -11.48378591275254301 ) ) ;
#14197=CARTESIAN_POINT ( 'NONE',  ( -6.636343628379751003, 68.43540020522837608, 11.76870444476310773 ) ) ;
#14199=CARTESIAN_POINT ( 'NONE',  ( 4.171729424061789260, 70.82999999999999829, 12.83926296998457417 ) ) ;
#14201=CARTESIAN_POINT ( 'NONE',  ( -2.434037520544789945, 65.59248196249376406, 13.27883458231978331 ) ) ;
#14202=CARTESIAN_POINT ( 'NONE',  ( 0.000000000000000000, 80.93000000000000682, 0.000000000000000000 ) ) ;
#14204=CARTESIAN_POINT ( 'NONE',  ( 13.49999999999999822, 50.28000000000000114, 4.386415899144236796 ) ) ;
#14206=CARTESIAN_POINT ( 'NONE',  ( -13.22310757530384784, 31.83334110198622469, -2.736780972190429928 ) ) ;
#14207=CARTESIAN_POINT ( 'NONE',  ( 5.908864746862505513, 74.89534936253288322, 12.13818304319435448 ) ) ;
#14208=LINE ( 'NONE', #4858, #6278 ) ;
#14209=CARTESIAN_POINT ( 'NONE',  ( -10.92172942406178926, 72.62999999999999545, -7.935100905948389460 ) ) ;
#14211=CARTESIAN_POINT ( 'NONE',  ( 13.23613990012235142, 51.52375947025169012, -2.656052883722033631 ) ) ;
#14212=CARTESIAN_POINT ( 'NONE',  ( -9.433473205167290487, 38.30967010535225370, 9.657148195847520711 ) ) ;
#14213=CARTESIAN_POINT ( 'NONE',  ( 11.39132066586519265, 36.70125830944373035, -7.245326858912307877 ) ) ;
#14216=CARTESIAN_POINT ( 'NONE',  ( -6.438066478122774328, 77.44350536356481030, 11.86602938538363894 ) ) ;
#14217=CARTESIAN_POINT ( 'NONE',  ( -2.138189944381219565, 61.60311857767971588, 13.50000000000000355 ) ) ;
#14218=CARTESIAN_POINT ( 'NONE',  ( 1.241788420113878466, 41.72465377607231574, 13.44682026920488127 ) ) ;
#14219=CARTESIAN_POINT ( 'NONE',  ( 12.24640860966871969, 48.63820562460364272, -5.681204235008639358 ) ) ;
#14222=ORIENTED_EDGE ( 'NONE', *, *, #9898, .F. ) ;
#14223=CARTESIAN_POINT ( 'NONE',  ( -3.636496289402153081, 62.32999999999999829, -11.19198476289190936 ) ) ;
#14228=CARTESIAN_POINT ( 'NONE',  ( -5.318689435344804650, 80.93000000000000682, -11.55616787654882671 ) ) ;
#14230=VECTOR ( 'NONE', #5627, 1000.000000000000000 ) ;
#14232=CARTESIAN_POINT ( 'NONE',  ( -7.272992578804310604, 45.38000000000000256, 10.01041549318726709 ) ) ;
#14234=CARTESIAN_POINT ( 'NONE',  ( -11.71428983209350072, 59.17987341424922931, 6.726823528539508601 ) ) ;
#14235=CARTESIAN_POINT ( 'NONE',  ( 13.21512175077752538, 45.33208276352622335, 2.769527569284461421 ) ) ;
#14238=CARTESIAN_POINT ( 'NONE',  ( 13.49051628622518173, 30.44740727456623119, -0.5059554888960394736 ) ) ;
#14239=CARTESIAN_POINT ( 'NONE',  ( -13.48278874607188271, 55.90643395278321748, -0.6820209318931385045 ) ) ;
#14241=CARTESIAN_POINT ( 'NONE',  ( 5.367902793731293087, 63.98565814275196573, -12.38691854761588296 ) ) ;
#14243=CARTESIAN_POINT ( 'NONE',  ( 13.04481288137828265, 39.55393178331779325, -3.476205045992002418 ) ) ;
#14244=ORIENTED_EDGE ( 'NONE', *, *, #7558, .T. ) ;
#14245=CARTESIAN_POINT ( 'NONE',  ( -12.39398694249804400, 61.73475989268117559, -5.356182190199231918 ) ) ;
#14246=ORIENTED_EDGE ( 'NONE', *, *, #5760, .F. ) ;
#14250=CARTESIAN_POINT ( 'NONE',  ( 10.74742752807278734, 48.11997365494462997, 8.169672665494852382 ) ) ;
#14251=CARTESIAN_POINT ( 'NONE',  ( 2.197686288218880346, 58.10098381549926927, -13.32020416656907891 ) ) ;
#14252=CARTESIAN_POINT ( 'NONE',  ( 8.224420489434695725, 78.86728963787211910, -10.71480034530365621 ) ) ;
#14253=CARTESIAN_POINT ( 'NONE',  ( -9.520470885617715595, 77.63000000000000966, -6.917026985038136289 ) ) ;
#14257=CARTESIAN_POINT ( 'NONE',  ( 0.000000000000000000, 0.000000000000000000, 5.000000000000000000 ) ) ;
#14260=CARTESIAN_POINT ( 'NONE',  ( -4.171729424061791036, 79.53000000000000114, 12.83926296998457239 ) ) ;
#14261=CARTESIAN_POINT ( 'NONE',  ( 8.198328110229137877, 33.86819861533544440, -10.72568410487125412 ) ) ;
#14265=CARTESIAN_POINT ( 'NONE',  ( 2.776197549605788240, 67.08017814200591999, -13.21149016882078087 ) ) ;
#14269=CARTESIAN_POINT ( 'NONE',  ( 0.000000000000000000, 80.93000000000000682, -13.50000000000000000 ) ) ;
#14270=CARTESIAN_POINT ( 'NONE',  ( -0.7687312486613894214, 59.65236697067454941, 13.47875314867014573 ) ) ;
#14271=CYLINDRICAL_SURFACE ( 'NONE', #5664, 8.999999999999998224 ) ;
#14273=CARTESIAN_POINT ( 'NONE',  ( 9.940909119425192841, 72.07613200268791331, 9.134167122504003089 ) ) ;
#14274=AXIS2_PLACEMENT_3D ( 'NONE', #12205, #11322, #16437 ) ;
#14275=CARTESIAN_POINT ( 'NONE',  ( -13.50000000000000000, 55.92999999999999972, -3.306546357697853733E-15 ) ) ;
#14276=CARTESIAN_POINT ( 'NONE',  ( -1.005545769327274827E-13, 52.18000000000000682, -13.50000000000000000 ) ) ;
#14277=CARTESIAN_POINT ( 'NONE',  ( 8.343458848123580296, 76.98000000000000398, 11.48378591275253768 ) ) ;
#14279=CARTESIAN_POINT ( 'NONE',  ( -0.4448446338779524223, 68.66416886155738553, 13.49450202653779307 ) ) ;
#14284=CARTESIAN_POINT ( 'NONE',  ( -2.273536850346836502, 65.59826044952400537, 13.30738196274165297 ) ) ;
#14285=DIRECTION ( 'NONE',  ( 0.000000000000000000, 0.7071067811865460184, 0.7071067811865490160 ) ) ;
#14286=CARTESIAN_POINT ( 'NONE',  ( 0.000000000000000000, 80.93000000000000682, 0.000000000000000000 ) ) ;
#14287=EDGE_CURVE ( 'NONE', #14307, #15397, #9490, .T. ) ;
#14288=ORIENTED_EDGE ( 'NONE', *, *, #4889, .F. ) ;
#14290=CYLINDRICAL_SURFACE ( 'NONE', #9209, 13.50000000000000000 ) ;
#14291=CARTESIAN_POINT ( 'NONE',  ( -12.60192476712481557, 32.10554672858959435, 4.841671032898100080 ) ) ;
#14292=CARTESIAN_POINT ( 'NONE',  ( 5.850189259468881353, 74.89304489562690037, 12.16667615321803808 ) ) ;
#14293=CARTESIAN_POINT ( 'NONE',  ( 13.14645763304583070, 60.32074054053764200, 3.079995153549444975 ) ) ;
#14296=CARTESIAN_POINT ( 'NONE',  ( -10.92172942406178926, 75.63000000000000966, -7.935100905948389460 ) ) ;
#14297=CARTESIAN_POINT ( 'NONE',  ( 13.23373072280492124, 51.52419663531563998, -2.668047451998938779 ) ) ;
#14298=CARTESIAN_POINT ( 'NONE',  ( -7.866619300871570353, 38.38328643477208146, 10.98017572201588976 ) ) ;
#14299=CARTESIAN_POINT ( 'NONE',  ( 10.40684902343222262, 36.75901520190327432, -8.599316094126638887 ) ) ;
#14301=CARTESIAN_POINT ( 'NONE',  ( -2.617794930461571745, 74.58589864099795363, 13.24923017825046934 ) ) ;
#14302=CARTESIAN_POINT ( 'NONE',  ( -8.912672946622391734, 77.33519948493032814, 10.14949437797439202 ) ) ;
#14303=CARTESIAN_POINT ( 'NONE',  ( 2.494263859647128712, 62.76976130887765493, 13.26767120624862173 ) ) ;
#14304=CARTESIAN_POINT ( 'NONE',  ( 3.083086032583709724, 41.79086483425119525, 13.14323357896869382 ) ) ;
#14307=VERTEX_POINT ( 'NONE', #12475 ) ;
#14308=CARTESIAN_POINT ( 'NONE',  ( 9.520470885617717371, 58.73000000000000398, -6.917026985038131848 ) ) ;
#14310=CARTESIAN_POINT ( 'NONE',  ( 0.000000000000000000, 80.93000000000000682, 0.000000000000000000 ) ) ;
#14313=CARTESIAN_POINT ( 'NONE',  ( 3.544998588692259478, 76.05253496923796774, -13.02654230708374605 ) ) ;
#14315=CARTESIAN_POINT ( 'NONE',  ( -8.343458848123582072, 77.38000000000000966, 11.48378591275254124 ) ) ;
#14316=CARTESIAN_POINT ( 'NONE',  ( 11.76794919243112325, 52.43000000000000682, 1.441158131103945434E-15 ) ) ;
#14318=CARTESIAN_POINT ( 'NONE',  ( -10.27297386801252621, 59.26638624019382462, 8.761361963125747110 ) ) ;
#14319=CARTESIAN_POINT ( 'NONE',  ( 13.49615201145693355, 45.41893420450175256, 0.3223442952341866174 ) ) ;
#14320=CARTESIAN_POINT ( 'NONE',  ( 13.41772075058063152, 69.37817881389347008, 1.488226159613910360 ) ) ;
#14322=CARTESIAN_POINT ( 'NONE',  ( 13.28728799727900700, 30.34600767625174811, 2.387053908818155712 ) ) ;
#14323=CARTESIAN_POINT ( 'NONE',  ( -13.06985016718083514, 55.80569210471582409, -3.495749286402883627 ) ) ;
#14324=CARTESIAN_POINT ( 'NONE',  ( -8.569946725401269561, 50.35116170713895656, 10.43101810198027657 ) ) ;
#14326=CARTESIAN_POINT ( 'NONE',  ( 0.03720832018167305466, 43.17866651368897379, -13.49995602673501871 ) ) ;
#14327=CARTESIAN_POINT ( 'NONE',  ( 11.95586233632780448, 39.66155393792011807, -6.269560418267513313 ) ) ;
#14329=CARTESIAN_POINT ( 'NONE',  ( -11.17071958894546135, 61.64489015857601828, -7.580573524914104411 ) ) ;
#14331=ORIENTED_EDGE ( 'NONE', *, *, #4492, .F. ) ;
#14332=ORIENTED_EDGE ( 'NONE', *, *, #5116, .F. ) ;
#14335=CARTESIAN_POINT ( 'NONE',  ( 13.20730181627872390, 48.33075532684633657, 2.806771093107235604 ) ) ;
#14336=CARTESIAN_POINT ( 'NONE',  ( 4.749818453525196382, 58.00890527316722256, -12.63682040982544308 ) ) ;
#14337=CARTESIAN_POINT ( 'NONE',  ( 4.128452826104092033, 79.03139843465449133, -12.85510690289249425 ) ) ;
#14338=CARTESIAN_POINT ( 'NONE',  ( -7.576616670048093940E-16, 81.68000000000000682, 12.37355403259654985 ) ) ;
#14341=AXIS2_PLACEMENT_3D ( 'NONE', #4922, #14185, #10153 ) ;
#14343=CARTESIAN_POINT ( 'NONE',  ( 5.883989548015876814, 30.92926152634062475, 10.19133431864935879 ) ) ;
#14345=CARTESIAN_POINT ( 'NONE',  ( 4.171729424061789260, 43.82999999999999829, 12.83926296998457417 ) ) ;
#14346=CARTESIAN_POINT ( 'NONE',  ( 4.453229937736239208, 34.01980578223958673, -12.74436757028742306 ) ) ;
#14348=LINE ( 'NONE', #17012, #15419 ) ;
#14349=ORIENTED_EDGE ( 'NONE', *, *, #7512, .T. ) ;
#14352=MECHANICAL_DESIGN_GEOMETRIC_PRESENTATION_REPRESENTATION('',(#4497),#4786);
#14353=DIRECTION ( 'NONE',  ( 0.000000000000000000, 0.000000000000000000, -1.000000000000000000 ) ) ;
#14354=CARTESIAN_POINT ( 'NONE',  ( -3.169462065277318885, 59.56607649941357607, 13.12419056553779839 ) ) ;
#14355=CYLINDRICAL_SURFACE ( 'NONE', #15782, 4.000000000000003553 ) ;
#14357=CARTESIAN_POINT ( 'NONE',  ( -13.49999999999999822, 53.08000000000000540, 4.386415899144235908 ) ) ;
#14358=CARTESIAN_POINT ( 'NONE',  ( -4.489412562659412131, 71.51848472666905820, 12.73166191706919825 ) ) ;
#14361=EDGE_CURVE ( 'NONE', #8975, #3211, #10518, .T. ) ;
#14362=CARTESIAN_POINT ( 'NONE',  ( -0.2224223267216245137, 68.67217246902345096, 13.50000000004355449 ) ) ;
#14364=CARTESIAN_POINT ( 'NONE',  ( 4.818028733689279974, 55.00634988854427831, -12.61098436172215997 ) ) ;
#14366=CARTESIAN_POINT ( 'NONE',  ( -9.819753993301681305, 65.29014244364479680, 9.264049843067173384 ) ) ;
#14367=CARTESIAN_POINT ( 'NONE',  ( 1.469576158976823947E-15, 102.9300000000000068, 12.00000000000000178 ) ) ;
#14368=CARTESIAN_POINT ( 'NONE',  ( -3.926185307623118348, 35.53892993393365884, 12.91710498519315387 ) ) ;
#14369=VERTEX_POINT ( 'NONE', #2907 ) ;
#14372=CARTESIAN_POINT ( 'NONE',  ( -4.418621633216786471, 40.33892943140601517, -12.75658624249819795 ) ) ;
#14373=CARTESIAN_POINT ( 'NONE',  ( -11.79396983171852220, 31.68639821171360893, -6.569267214410038136 ) ) ;
#14375=CARTESIAN_POINT ( 'NONE',  ( 10.46789772265251983, 60.10431960738042534, 8.525494685668089545 ) ) ;
#14377=CARTESIAN_POINT ( 'NONE',  ( -11.06430438014261419, 53.22157550517651714, 7.735070979210682651 ) ) ;
#14378=CARTESIAN_POINT ( 'NONE',  ( 11.76794919243112680, 55.58000000000000540, -3.823638476888993942 ) ) ;
#14380=CARTESIAN_POINT ( 'NONE',  ( 12.87391916192378183, 51.57647175459032240, -4.079283975827568298 ) ) ;
#14381=CARTESIAN_POINT ( 'NONE',  ( -9.360627989232526147, 38.31329549134574108, 9.727727575345387123 ) ) ;
#14383=CARTESIAN_POINT ( 'NONE',  ( 13.00679210537909469, 36.55913285882594010, -3.615981775121954289 ) ) ;
#14385=CARTESIAN_POINT ( 'NONE',  ( -0.5999229078048249342, 74.65842898432426011, 13.48666992254756991 ) ) ;
#14386=CARTESIAN_POINT ( 'NONE',  ( -6.382977644554325813, 77.44573456745463602, 11.89569858070153963 ) ) ;
#14387=CARTESIAN_POINT ( 'NONE',  ( -1.768548083352462719, 80.61632827333519913, 13.38410412889483148 ) ) ;
#14388=CARTESIAN_POINT ( 'NONE',  ( 7.500000000000000000, 108.4757119436330868, -3.584587286925195571 ) ) ;
#14389=ORIENTED_EDGE ( 'NONE', *, *, #183, .F. ) ;
#14392=CARTESIAN_POINT ( 'NONE',  ( 2.272985001014427393E-15, 56.17999999999999972, -12.37355403259654807 ) ) ;
#14394=PLANE ( 'NONE',  #11910 ) ;
#14395=CARTESIAN_POINT ( 'NONE',  ( 8.605009408506106183, 75.84953091247618318, -10.40210956409493370 ) ) ;
#14397=CARTESIAN_POINT ( 'NONE',  ( 2.319374564596460520, 65.76347162869123508, 13.30869893535136406 ) ) ;
#14398=CARTESIAN_POINT ( 'NONE',  ( 13.50000000000000355, 72.57999999999998408, -4.386415899144233244 ) ) ;
#14399=CARTESIAN_POINT ( 'NONE',  ( -3.636496289402153081, 47.32999999999999829, -11.19198476289190936 ) ) ;
#14400=CARTESIAN_POINT ( 'NONE',  ( 0.000000000000000000, 80.93000000000000682, -13.50000000000000000 ) ) ;
#14401=CARTESIAN_POINT ( 'NONE',  ( -13.49246718458698169, 58.91263165492783571, -0.5007047752432340904 ) ) ;
#14403=CARTESIAN_POINT ( 'NONE',  ( 13.49839282532952289, 45.42250628188710948, 0.2187282632226159873 ) ) ;
#14404=CARTESIAN_POINT ( 'NONE',  ( 12.93677123527108996, 69.29165259775294317, 3.862518802718706290 ) ) ;
#14405=EDGE_CURVE ( 'NONE', #743, #4213, #15707, .T. ) ;
#14406=CARTESIAN_POINT ( 'NONE',  ( 1.412863011855262751, 80.73080156731793977, 13.42591544637424406 ) ) ;
#14407=CARTESIAN_POINT ( 'NONE',  ( 13.23549663901797402, 30.33587587276464248, 2.666610200634819794 ) ) ;
#14408=CARTESIAN_POINT ( 'NONE',  ( -7.300588070086375225, 55.45236719425724203, -11.35586912590181541 ) ) ;
#14409=CARTESIAN_POINT ( 'NONE',  ( -7.491758324924639112, 50.39954984522349690, 11.24212828544573739 ) ) ;
#14410=CARTESIAN_POINT ( 'NONE',  ( 2.719350837857034797, 64.08222226381806763, -13.22329714325173278 ) ) ;
#14412=CARTESIAN_POINT ( 'NONE',  ( 13.03639040501872870, 39.30446296123340488, 3.517016424516218542 ) ) ;
#14414=CARTESIAN_POINT ( 'NONE',  ( -7.750936433791640212, 70.47186442965926290, -11.05318976959837407 ) ) ;
#14415=CARTESIAN_POINT ( 'NONE',  ( -11.18018059938515840, 61.64547263069862026, -7.566613037985367107 ) ) ;
#14418=CARTESIAN_POINT ( 'NONE',  ( -10.74356903153339537, 40.61907513962281513, -8.186503528442704791 ) ) ;
#14422=CARTESIAN_POINT ( 'NONE',  ( 4.718922011681848439, 47.84992210821208403, 12.64921854083997843 ) ) ;
#14423=CARTESIAN_POINT ( 'NONE',  ( 4.756350679200790132, 58.00866332433687944, -12.63436384876514573 ) ) ;
#14424=CARTESIAN_POINT ( 'NONE',  ( 12.58541105472228061, 78.60870476587842859, -4.931259148636751632 ) ) ;
#14425=CARTESIAN_POINT ( 'NONE',  ( -9.520470885617717371, 75.23000000000000398, 6.917026985038133624 ) ) ;
#14429=CARTESIAN_POINT ( 'NONE',  ( 13.49999999999999822, 41.27999999999999403, 4.386415899144236796 ) ) ;
#14430=CARTESIAN_POINT ( 'NONE',  ( -13.50000000000000000, 33.92999999999999972, -3.306546357697853733E-15 ) ) ;
#14433=CARTESIAN_POINT ( 'NONE',  ( 5.873548170489375053, 33.96604030298396992, -12.15537189499551474 ) ) ;
#14434=CARTESIAN_POINT ( 'NONE',  ( -12.63508156651104031, 73.75780359901375505, -4.754471429868501353 ) ) ;
#14435=ORIENTED_EDGE ( 'NONE', *, *, #9601, .F. ) ;
#14437=DIRECTION ( 'NONE',  ( 0.000000000000000000, -1.000000000000000000, 0.000000000000000000 ) ) ;
#14438=ORIENTED_EDGE ( 'NONE', *, *, #11447, .T. ) ;
#14439=CIRCLE ( 'NONE', #15556, 12.00000000000000178 ) ;
#14442=CARTESIAN_POINT ( 'NONE',  ( -0.6827152122399273715, 44.65545208943112243, 13.48272862569767661 ) ) ;
#14443=CARTESIAN_POINT ( 'NONE',  ( -0.5990100676847840422, 59.65846358068620958, 13.48764568963964017 ) ) ;
#14445=DIRECTION ( 'NONE',  ( -1.000000000000000000, -0.000000000000000000, -0.000000000000000000 ) ) ;
#14446=CARTESIAN_POINT ( 'NONE',  ( 7.752908499509820750, 66.88804938204245332, -11.05182862330812199 ) ) ;
#14447=CARTESIAN_POINT ( 'NONE',  ( 4.171729424061791924, 55.02999999999999403, -12.83926296998457239 ) ) ;
#14448=CARTESIAN_POINT ( 'NONE',  ( -9.316322459437627046, 71.31583036083887350, 9.780020801877546077 ) ) ;
#14449=EDGE_CURVE ( 'NONE', #14613, #7754, #14723, .T. ) ;
#14451=CARTESIAN_POINT ( 'NONE',  ( -1.237156021628534663, 68.63551873726167685, 13.44319788051029718 ) ) ;
#14453=CARTESIAN_POINT ( 'NONE',  ( 9.313993393904729245, 54.81559091050048238, -9.772391642156692981 ) ) ;
#14456=CARTESIAN_POINT ( 'NONE',  ( -1.119872009197603324, 65.63978953382610371, 13.46024171269125169 ) ) ;
#14457=CARTESIAN_POINT ( 'NONE',  ( 0.000000000000000000, 80.93000000000000682, 0.000000000000000000 ) ) ;
#14458=CARTESIAN_POINT ( 'NONE',  ( -4.408758549868576182, 35.52142633745754097, 12.75982571945315236 ) ) ;
#14461=CARTESIAN_POINT ( 'NONE',  ( -13.34948284762835158, 32.00042008344756539, 2.010355113879713329 ) ) ;
#14462=CARTESIAN_POINT ( 'NONE',  ( 0.1489964998165439203, 73.17464263554514048, -13.49999999999999822 ) ) ;
#14463=CARTESIAN_POINT ( 'NONE',  ( 12.41983916809079247, 60.23658299471287592, 5.309328226357375335 ) ) ;
#14465=CARTESIAN_POINT ( 'NONE',  ( -3.713625913484355223, 53.54647381879400569, 12.97962509512433904 ) ) ;
#14466=CARTESIAN_POINT ( 'NONE',  ( -7.272992578804310604, 54.37999999999999545, 10.01041549318726709 ) ) ;
#14467=CARTESIAN_POINT ( 'NONE',  ( -13.50000000000000000, 75.92999999999999261, -3.306546357697853733E-15 ) ) ;
#14468=CARTESIAN_POINT ( 'NONE',  ( 13.29424549937943389, 51.34664967739882968, 2.366107937962470320 ) ) ;
#14469=( BOUNDED_CURVE ( )  B_SPLINE_CURVE ( 2, ( #8872, #11509, #4791, #4875, #17234, #1061, #2283, #11859, #6296, #6130, #720, #7625, #17145 ),
 .UNSPECIFIED., .F., .F. ) 
 B_SPLINE_CURVE_WITH_KNOTS ( ( 3, 2, 2, 2, 2, 2, 3 ),
 ( 0.5138888888888888395, 0.5166666666666667185, 0.5222222222222222543, 0.5277777777777777901, 0.5333333333333333259, 0.5388888888888888618, 0.5416666666666666297 ),
 .UNSPECIFIED. ) 
 CURVE ( )  GEOMETRIC_REPRESENTATION_ITEM ( )  RATIONAL_B_SPLINE_CURVE ( ( 0.9755282581475768211, 0.9755282581475762660, 1.000000000000000000, 0.9510565162951535312, 1.000000000000000000, 0.9510565162951535312, 1.000000000000000000, 0.9510565162951535312, 1.000000000000000000, 0.9510565162951535312, 1.000000000000000000, 0.9755282581475768211, 0.9755282581475768211 ) ) 
 REPRESENTATION_ITEM ( '' )  );
#14470=CARTESIAN_POINT ( 'NONE',  ( -13.46150956673317189, 37.89473990636209066, -1.021228295727763413 ) ) ;
#14471=CARTESIAN_POINT ( 'NONE',  ( 13.09238747814303672, 36.54713875649020594, -3.292978093212715507 ) ) ;
#14473=CARTESIAN_POINT ( 'NONE',  ( -5.218726944522628308, 74.49131902963608809, 12.45049800546231644 ) ) ;
#14474=CARTESIAN_POINT ( 'NONE',  ( -3.791457664355128987, 77.54367317383434965, 12.95665453917505872 ) ) ;
#14475=CARTESIAN_POINT ( 'NONE',  ( -6.837279939568707832, 80.42713201599657680, 11.64064851132507172 ) ) ;
#14476=CARTESIAN_POINT ( 'NONE',  ( 0.000000000000000000, 80.93000000000000682, 0.000000000000000000 ) ) ;
#14480=CARTESIAN_POINT ( 'NONE',  ( 9.520470885617715595, 55.12999999999999545, 6.917026985038134512 ) ) ;
#14484=CARTESIAN_POINT ( 'NONE',  ( 10.01047714262612764, 75.78048900460133552, -9.068666163624630627 ) ) ;
#14486=CARTESIAN_POINT ( 'NONE',  ( -8.343458848123582072, 74.38000000000000966, 11.48378591275254124 ) ) ;
#14487=CARTESIAN_POINT ( 'NONE',  ( -11.76794919243112325, 41.77999999999999403, -3.823638476888998827 ) ) ;
#14489=CARTESIAN_POINT ( 'NONE',  ( -10.94961911198126892, 59.22840902095881432, 7.897108303096641357 ) ) ;
#14490=CARTESIAN_POINT ( 'NONE',  ( 9.130956880405868503, 45.03545779938338711, 9.943691066605332196 ) ) ;
#14491=CARTESIAN_POINT ( 'NONE',  ( 13.42452448409018473, 69.38029835393189160, 1.426741430879768791 ) ) ;
#14493=CARTESIAN_POINT ( 'NONE',  ( 12.32864373793141155, 30.22870989983009338, 5.503456116662770903 ) ) ;
#14494=CARTESIAN_POINT ( 'NONE',  ( -11.21739340954028386, 55.64777575850494884, -7.511349096803600744 ) ) ;
#14495=CARTESIAN_POINT ( 'NONE',  ( -13.48346079216651994, 49.90693168062259133, -0.6681850952586498860 ) ) ;
#14496=CARTESIAN_POINT ( 'NONE',  ( 4.333283499223988144, 64.02385403997206481, -12.79310945068694316 ) ) ;
#14497=CARTESIAN_POINT ( 'NONE',  ( 8.206057751921221666, 42.86785321040926533, -10.71992093049925465 ) ) ;
#14498=CARTESIAN_POINT ( 'NONE',  ( 11.60980040101028443, 39.17211399233057989, 6.927472449889193307 ) ) ;
#14499=VERTEX_POINT ( 'NONE', #8599 ) ;
#14500=CARTESIAN_POINT ( 'NONE',  ( -13.10654215744646756, 70.81327619670632600, -3.284290054994799757 ) ) ;
#14501=CARTESIAN_POINT ( 'NONE',  ( -12.11228153988018263, 61.71073340877943991, -5.962024479802454202 ) ) ;
#14502=ORIENTED_EDGE ( 'NONE', *, *, #4294, .T. ) ;
#14507=EDGE_CURVE ( 'NONE', #13385, #14181, #16876, .T. ) ;
#14508=CARTESIAN_POINT ( 'NONE',  ( 2.439874972470002401, 61.09229787913012899, -13.28197017431443072 ) ) ;
#14509=CARTESIAN_POINT ( 'NONE',  ( 13.36597540549724705, 57.49638167611755790, -1.897582465975046428 ) ) ;
#14510=CARTESIAN_POINT ( 'NONE',  ( -3.636496289402153081, 65.32999999999999829, -11.19198476289190936 ) ) ;
#14511=CARTESIAN_POINT ( 'NONE',  ( -10.92172942406178926, 36.62999999999999545, -7.935100905948389460 ) ) ;
#14512=CARTESIAN_POINT ( 'NONE',  ( 7.272992578804308828, 75.98000000000001819, 10.01041549318726709 ) ) ;
#14515=CARTESIAN_POINT ( 'NONE',  ( -10.92172942406178926, 75.63000000000000966, -7.935100905948389460 ) ) ;
#14517=CARTESIAN_POINT ( 'NONE',  ( 0.000000000000000000, 80.93000000000000682, -13.50000000000000000 ) ) ;
#14518=CARTESIAN_POINT ( 'NONE',  ( 2.040077917229468962, 34.10670120566993546, -13.35303788872347752 ) ) ;
#14519=CARTESIAN_POINT ( 'NONE',  ( -7.490634807705651710, 73.46052964042478095, -11.23122895601197690 ) ) ;
#14520=ORIENTED_EDGE ( 'NONE', *, *, #6829, .T. ) ;
#14521=ORIENTED_EDGE ( 'NONE', *, *, #4596, .T. ) ;
#14522=CARTESIAN_POINT ( 'NONE',  ( -11.76794919241189241, 80.77999999999872216, -3.823638476915469653 ) ) ;
#14526=CARTESIAN_POINT ( 'NONE',  ( -7.408466126933650031, 44.40300983023897885, 11.28560674973578060 ) ) ;
#14529=CARTESIAN_POINT ( 'NONE',  ( 9.931668237600721483, 66.78434905871291960, -9.143968089697972701 ) ) ;
#14530=CARTESIAN_POINT ( 'NONE',  ( 8.343458848123578520, 56.98000000000000398, 11.48378591275254124 ) ) ;
#14531=CARTESIAN_POINT ( 'NONE',  ( -2.955975039020797723, 71.57371703009538066, 13.17270523474517852 ) ) ;
#14534=CARTESIAN_POINT ( 'NONE',  ( -13.39818490939118156, 67.98779038466180680, 1.656737981020488748 ) ) ;
#14536=CARTESIAN_POINT ( 'NONE',  ( 9.794027008236195542, 54.79149751722007267, -9.299057948655683248 ) ) ;
#14539=CARTESIAN_POINT ( 'NONE',  ( -9.781864413179627959, 65.29209033731051193, 9.304052886497448327 ) ) ;
#14540=CARTESIAN_POINT ( 'NONE',  ( -10.92172942406179104, 43.22999999999999687, 7.935100905948387684 ) ) ;
#14541=CARTESIAN_POINT ( 'NONE',  ( -11.24754674959912037, 35.21034174107487047, 7.466103360436171066 ) ) ;
#14542=ORIENTED_EDGE ( 'NONE', *, *, #2873, .T. ) ;
#14548=CARTESIAN_POINT ( 'NONE',  ( -13.33720092989338646, 32.00330006321830467, 2.090426404509658553 ) ) ;
#14549=CARTESIAN_POINT ( 'NONE',  ( 0.5655967198986255884, 73.15966327253678969, -13.48815761927076373 ) ) ;
#14550=CARTESIAN_POINT ( 'NONE',  ( 10.65422817835172431, 60.11470094556233335, 8.290804033779142657 ) ) ;
#14552=CARTESIAN_POINT ( 'NONE',  ( -9.915480747960748076, 53.28519106004377903, 9.161513846371878600 ) ) ;
#14553=CARTESIAN_POINT ( 'NONE',  ( -9.520470885617715595, 53.62999999999999545, -6.917026985038136289 ) ) ;
#14554=CARTESIAN_POINT ( 'NONE',  ( -4.171729424061787483, 75.33000000000001251, -12.83926296998457417 ) ) ;
#14555=CARTESIAN_POINT ( 'NONE',  ( 12.48027881134552075, 51.24265653591692171, 5.147114882624049592 ) ) ;
#14557=CARTESIAN_POINT ( 'NONE',  ( -11.88099997619197090, 37.69280157551202137, -6.410295481422697783 ) ) ;
#14558=CARTESIAN_POINT ( 'NONE',  ( 10.37119814715991772, 36.76095968828544613, -8.642242444827784809 ) ) ;
#14560=CARTESIAN_POINT ( 'NONE',  ( -2.811464633627016061E-07, 74.67999216907730897, 13.49999999999999289 ) ) ;
#14561=CARTESIAN_POINT ( 'NONE',  ( -10.71875711079582238, 77.24165530301368676, 8.207345694687209203 ) ) ;
#14562=CARTESIAN_POINT ( 'NONE',  ( -13.47295500694753656, 79.96043441828727794, 0.8822608226219847971 ) ) ;
#14564=DIRECTION ( 'NONE',  ( 0.000000000000000000, 0.000000000000000000, -1.000000000000000000 ) ) ;
#14569=CARTESIAN_POINT ( 'NONE',  ( -7.272992578804310604, 54.37999999999999545, 10.01041549318726886 ) ) ;
#14573=CARTESIAN_POINT ( 'NONE',  ( 3.767968615061696003, 76.04451116420807466, -12.96361866624683579 ) ) ;
#14574=VECTOR ( 'NONE', #11461, 1000.000000000000000 ) ;
#14575=CARTESIAN_POINT ( 'NONE',  ( 2.138189944381259977, 67.75688142232026223, 13.49999999999999289 ) ) ;
#14576=CARTESIAN_POINT ( 'NONE',  ( 0.6582265246141822956, 65.70366634169981523, 13.48505733660138262 ) ) ;
#14577=CARTESIAN_POINT ( 'NONE',  ( -8.691771469529815392E-16, 74.67999999999997840, 14.19474002721660355 ) ) ;
#14579=CARTESIAN_POINT ( 'NONE',  ( 9.520470885617717371, 37.72999999999999687, -6.917026985038131848 ) ) ;
#14581=CARTESIAN_POINT ( 'NONE',  ( -12.68991400004249392, 58.76347348998390885, -4.606612073962529585 ) ) ;
#14582=CARTESIAN_POINT ( 'NONE',  ( 10.41641641675877139, 45.10151672092631969, 8.587682018090683655 ) ) ;
#14583=CARTESIAN_POINT ( 'NONE',  ( 12.80716480624030496, 69.27630802522288889, 4.269263623378532380 ) ) ;
#14584=CARTESIAN_POINT ( 'NONE',  ( -8.343458848123578520, 66.48000000000000398, -11.48378591275254124 ) ) ;
#14585=DIRECTION ( 'NONE',  ( -1.000000000000000000, -0.000000000000000000, -0.000000000000000000 ) ) ;
#14587=CARTESIAN_POINT ( 'NONE',  ( -0.6538802958928384701, 55.20351089476487516, -13.48419838928958292 ) ) ;
#14588=CARTESIAN_POINT ( 'NONE',  ( -10.60346985883564841, 50.24833156966194991, 8.358339015696030216 ) ) ;
#14589=CARTESIAN_POINT ( 'NONE',  ( 9.817055075673792430, 63.79028200361416623, -9.266916700068716040 ) ) ;
#14590=CARTESIAN_POINT ( 'NONE',  ( 12.99972812561954250, 42.56007091286085142, -3.641089568116410824 ) ) ;
#14591=CARTESIAN_POINT ( 'NONE',  ( 9.430394439940833706, 39.05013839999956815, 9.660559727168038791 ) ) ;
#14593=CARTESIAN_POINT ( 'NONE',  ( -9.817573801958880964, 70.56979445902175030, -9.266430505722183852 ) ) ;
#14594=CARTESIAN_POINT ( 'NONE',  ( -11.16425593428273189, 61.64449276969597946, -7.590094044152214892 ) ) ;
#14597=EDGE_LOOP ( 'NONE', ( #12397, #16970, #4080, #8972 ) ) ;
#14600=CARTESIAN_POINT ( 'NONE',  ( 3.179672653360267720, 61.06567017344302428, -13.12035135455492885 ) ) ;
#14601=CARTESIAN_POINT ( 'NONE',  ( 10.66243950754257419, 72.11517382313176938, 8.280248928875550973 ) ) ;
#14602=CARTESIAN_POINT ( 'NONE',  ( 13.48635267069885479, 57.45126414530135861, -0.6183634171442978777 ) ) ;
#14603=CARTESIAN_POINT ( 'NONE',  ( 7.272992578804308828, 66.98000000000000398, 10.01041549318726709 ) ) ;
#14604=CARTESIAN_POINT ( 'NONE',  ( -7.272992578804310604, 75.37999999999999545, 10.01041549318726709 ) ) ;
#14606=CARTESIAN_POINT ( 'NONE',  ( 8.343458848123583849, 38.87999999999998835, -11.48378591275253768 ) ) ;
#14607=CARTESIAN_POINT ( 'NONE',  ( -10.92172942406178926, 33.63000000000000256, -7.935100905948389460 ) ) ;
#14610=CARTESIAN_POINT ( 'NONE',  ( 5.829534447797559693, 33.96776797207451892, -12.17648583204983659 ) ) ;
#14611=CARTESIAN_POINT ( 'NONE',  ( -10.35327952210849922, 73.59810291917281688, -8.665258164064150392 ) ) ;
#14613=VERTEX_POINT ( 'NONE', #9927 ) ;
#14614=CARTESIAN_POINT ( 'NONE',  ( -9.520470885617717371, 75.23000000000000398, 6.917026985038133624 ) ) ;
#14615=ORIENTED_EDGE ( 'NONE', *, *, #14507, .T. ) ;
#14618=CARTESIAN_POINT ( 'NONE',  ( 13.40118537505952467, 66.48685356940795543, -1.630447449414718974 ) ) ;
#14620=CARTESIAN_POINT ( 'NONE',  ( 4.171729424061789260, 41.82999999999999829, 12.83926296998457417 ) ) ;
#14621=CARTESIAN_POINT ( 'NONE',  ( -11.57172165442571199, 71.18898023797920871, 6.959135939452125719 ) ) ;
#14623=CARTESIAN_POINT ( 'NONE',  ( -12.75392120890703751, 68.08976633361912434, 4.429612562818754817 ) ) ;
#14625=EDGE_CURVE ( 'NONE', #39, #717, #3755, .T. ) ;
#14626=CARTESIAN_POINT ( 'NONE',  ( 10.49117977328117668, 54.75438394012941501, -8.496252905792848864 ) ) ;
#14629=CARTESIAN_POINT ( 'NONE',  ( -13.42050307411934895, 64.98104791279109804, 1.467013915166769822 ) ) ;
#14630=CARTESIAN_POINT ( 'NONE',  ( -4.449551195726444419, 35.51993990970242265, 12.74565100145505703 ) ) ;
#14632=ORIENTED_EDGE ( 'NONE', *, *, #12334, .T. ) ;
#14633=DIRECTION ( 'NONE',  ( 0.000000000000000000, -1.000000000000000000, 0.000000000000000000 ) ) ;
#14635=CARTESIAN_POINT ( 'NONE',  ( -5.494845225242961817, 31.37922778511446964, -12.33112964525436439 ) ) ;
#14637=CARTESIAN_POINT ( 'NONE',  ( 11.69961049517324625, 60.17965554828174390, 6.735864183870432065 ) ) ;
#14639=CARTESIAN_POINT ( 'NONE',  ( -7.243158421774579914, 53.41008471037572747, 11.39280974719889272 ) ) ;
#14641=CARTESIAN_POINT ( 'NONE',  ( 11.76794919243112325, 52.28000000000000114, 3.823638476888996607 ) ) ;
#14642=CARTESIAN_POINT ( 'NONE',  ( -4.171729424061787483, 69.32999999999999829, -12.83926296998457417 ) ) ;
#14643=CARTESIAN_POINT ( 'NONE',  ( 3.382362776236492508, 50.80156238092428111, 13.06946539059775425 ) ) ;
#14644=CARTESIAN_POINT ( 'NONE',  ( -13.26641961833640160, 37.84148543181640179, -2.512961166757757159 ) ) ;
#14645=CARTESIAN_POINT ( 'NONE',  ( 10.88107893182741925, 36.12754488146830312, 7.991670572652272320 ) ) ;
#14647=CARTESIAN_POINT ( 'NONE',  ( -5.224982848479887920, 74.49108573728641147, 12.44787394451754281 ) ) ;
#14648=CARTESIAN_POINT ( 'NONE',  ( -12.50942665065559289, 76.74541654896083287, -5.075876066077060322 ) ) ;
#14649=CARTESIAN_POINT ( 'NONE',  ( -8.910189170011362236, 80.33521782052793014, 10.14428475681184416 ) ) ;
#14651=CARTESIAN_POINT ( 'NONE',  ( 7.500000000000000888, 103.4443346693207957, 9.346209313438659905 ) ) ;
#14652=CARTESIAN_POINT ( 'NONE',  ( 7.500000000000000888, 98.93000000000002103, -8.999999999999996447 ) ) ;
#14654=CARTESIAN_POINT ( 'NONE',  ( 11.76794919243112325, 52.43000000000000682, 1.441158131103945434E-15 ) ) ;
#14658=CARTESIAN_POINT ( 'NONE',  ( 13.50000000000000000, 35.42999999999999972, 1.653273178848926867E-15 ) ) ;
#14659=CARTESIAN_POINT ( 'NONE',  ( 8.034607623683875488, 75.87556492978765732, -10.85026718143496183 ) ) ;
#14660=DIRECTION ( 'NONE',  ( 0.000000000000000000, 0.000000000000000000, 1.000000000000000000 ) ) ;
#14661=CARTESIAN_POINT ( 'NONE',  ( -3.636496289402155746, 36.53000000000000114, 11.19198476289190936 ) ) ;
#14663=CARTESIAN_POINT ( 'NONE',  ( -11.13715108135233400, 58.64282742455466746, -7.629921315917804314 ) ) ;
#14664=CARTESIAN_POINT ( 'NONE',  ( -5.485275766071775660E-07, 44.67998473833578998, 13.49999999999997691 ) ) ;
#14665=CARTESIAN_POINT ( 'NONE',  ( 12.99932277953478987, 69.56086486162749338, -3.664194174932866144 ) ) ;
#14666=ADVANCED_FACE ( 'NONE', ( #3268 ), #14044, .T. ) ;
#14668=CARTESIAN_POINT ( 'NONE',  ( 12.50000000000000000, 98.93000000000002103, -8.999999999999996447 ) ) ;
#14669=CARTESIAN_POINT ( 'NONE',  ( -1.222984669013519099, 55.22395752754145803, -13.44686810295633173 ) ) ;
#14670=CARTESIAN_POINT ( 'NONE',  ( -8.726673703696462780, 50.34384715345172623, 10.30054475047543505 ) ) ;
#14671=CARTESIAN_POINT ( 'NONE',  ( 13.34146757976997932, 63.50243722178738892, -2.066615361868207934 ) ) ;
#14672=CARTESIAN_POINT ( 'NONE',  ( 13.08065693840681121, 42.54885315171381421, -3.339269834337736054 ) ) ;
#14673=CARTESIAN_POINT ( 'NONE',  ( 9.236967615830064204, 39.04062162967218086, 9.845233498274197359 ) ) ;
#14675=CARTESIAN_POINT ( 'NONE',  ( -9.784440633357435857, 70.56809849894560216, -9.301509274256069659 ) ) ;
#14678=VERTEX_POINT ( 'NONE', #6033 ) ;
#14683=CARTESIAN_POINT ( 'NONE',  ( 10.17113817942703946, 72.08819647464973457, 8.881040390352081815 ) ) ;
#14684=CARTESIAN_POINT ( 'NONE',  ( 12.15229061391567633, 57.21392339986990550, 5.883136067267471070 ) ) ;
#14686=CARTESIAN_POINT ( 'NONE',  ( -9.520470885617717371, 69.23000000000000398, 6.917026985038133624 ) ) ;
#14687=CARTESIAN_POINT ( 'NONE',  ( 9.520470885617715595, 73.12999999999999545, 6.917026985038134512 ) ) ;
#14688=CARTESIAN_POINT ( 'NONE',  ( -6.660722695897963952, 47.43442504079767019, 11.74429954586069158 ) ) ;
#14689=CARTESIAN_POINT ( 'NONE',  ( -13.50000000000000000, 45.92999999999999972, -3.306546357697853733E-15 ) ) ;
#14693=DIRECTION ( 'NONE',  ( 0.000000000000000000, 0.000000000000000000, 1.000000000000000000 ) ) ;
#14694=CARTESIAN_POINT ( 'NONE',  ( 13.50053299712392985, 33.42724656409518502, 0.07573446942323454334 ) ) ;
#14695=CARTESIAN_POINT ( 'NONE',  ( -2.111840279952809762, 73.25593118054010233, -13.33386240694283664 ) ) ;
#14696=EDGE_LOOP ( 'NONE', ( #821, #17446, #9889, #4727 ) ) ;
#14698=CARTESIAN_POINT ( 'NONE',  ( -9.520470885617715595, 80.63000000000000966, -6.917026985038136289 ) ) ;
#14703=CARTESIAN_POINT ( 'NONE',  ( 13.50000000000000000, 39.42999999999999972, 1.653273178848926867E-15 ) ) ;
#14704=CARTESIAN_POINT ( 'NONE',  ( -11.94380634845912859, 71.16263373931494129, 6.294515196234966581 ) ) ;
#14707=CARTESIAN_POINT ( 'NONE',  ( -11.74368838437089124, 68.17729472189647311, 6.658789978823069333 ) ) ;
#14710=CARTESIAN_POINT ( 'NONE',  ( 11.60265521985991022, 54.68715047374503513, -6.901813903172819842 ) ) ;
#14713=CARTESIAN_POINT ( 'NONE',  ( -13.13342003293556637, 64.81895280616910782, -3.128236002867767596 ) ) ;
#14714=CARTESIAN_POINT ( 'NONE',  ( -9.846957267435957561, 35.28912329287517480, 9.246335277936564623 ) ) ;
#14715=ORIENTED_EDGE ( 'NONE', *, *, #3486, .F. ) ;
#14717=CARTESIAN_POINT ( 'NONE',  ( -5.478259550403512534, 31.37858928543126780, -12.33850698730843654 ) ) ;
#14719=CARTESIAN_POINT ( 'NONE',  ( 4.330177564208073981, 59.83558484829251967, 12.78997803238905995 ) ) ;
#14722=CARTESIAN_POINT ( 'NONE',  ( -7.142235745276270364, 53.41435411266112254, 11.45593642778781351 ) ) ;
#14723=CIRCLE ( 'NONE', #7433, 13.50000000000000000 ) ;
#14724=CARTESIAN_POINT ( 'NONE',  ( -7.576616670048093940E-16, 48.67999999999999261, 12.37355403259654985 ) ) ;
#14725=CARTESIAN_POINT ( 'NONE',  ( 8.343458848123583849, 68.88000000000000966, -11.48378591275253768 ) ) ;
#14726=CARTESIAN_POINT ( 'NONE',  ( 10.77064554674818275, 51.12129249041564805, 8.139387900364980055 ) ) ;
#14727=CARTESIAN_POINT ( 'NONE',  ( -7.795330123696450286, 37.47372399862477721, -11.02641059027264347 ) ) ;
#14728=CARTESIAN_POINT ( 'NONE',  ( 13.32600202517275179, 36.35416429240112990, 2.160700448193091816 ) ) ;
#14730=CARTESIAN_POINT ( 'NONE',  ( -8.576537068151989018, 74.35087396422935058, 10.42646147084938768 ) ) ;
#14731=CARTESIAN_POINT ( 'NONE',  ( -13.45696768390258313, 76.96804991183022082, 1.099532284017214367 ) ) ;
#14732=AXIS2_PLACEMENT_3D ( 'NONE', #11488, #5929, #3347 ) ;
#14733=CARTESIAN_POINT ( 'NONE',  ( -12.38291575527968469, 80.12633443854863913, 5.378268875544708116 ) ) ;
#14735=CARTESIAN_POINT ( 'NONE',  ( 7.499999999999999112, 108.1058439696177373, -5.080312676971233010 ) ) ;
#14736=DIRECTION ( 'NONE',  ( 0.000000000000000000, -1.000000000000000000, 0.000000000000000000 ) ) ;
#14738=CARTESIAN_POINT ( 'NONE',  ( -7.272992578804310604, 45.38000000000000256, 10.01041549318726886 ) ) ;
#14742=CARTESIAN_POINT ( 'NONE',  ( -10.19991245802031798, 40.58986062522050275, -8.843942352183722377 ) ) ;
#14744=CARTESIAN_POINT ( 'NONE',  ( 12.92208239490048882, 75.57016071826951986, -3.911420954987763210 ) ) ;
#14746=FACE_OUTER_BOUND ( 'NONE', #483, .T. ) ;
#14747=CARTESIAN_POINT ( 'NONE',  ( 9.520470885617717371, 40.72999999999999687, -6.917026985038131848 ) ) ;
#14748=CARTESIAN_POINT ( 'NONE',  ( -3.295356814209294605, 41.56178627527702929, 13.09792834740329681 ) ) ;
#14749=CARTESIAN_POINT ( 'NONE',  ( -12.80432099898033727, 58.77598328227021085, -4.277830564778782652 ) ) ;
#14750=CARTESIAN_POINT ( 'NONE',  ( 4.545821450575014744, 44.84357583826527360, 12.71174574629005960 ) ) ;
#14753=CARTESIAN_POINT ( 'NONE',  ( -10.45946617061218475, 55.60358966935245917, -8.539753337778272169 ) ) ;
#14754=CARTESIAN_POINT ( 'NONE',  ( -10.13059983448895807, 49.58610714942754782, -8.923059655268989587 ) ) ;
#14755=CARTESIAN_POINT ( 'NONE',  ( 11.50193147421984641, 63.69388881605808450, -7.067926430401910487 ) ) ;
#14756=CARTESIAN_POINT ( 'NONE',  ( 11.16643148321324830, 42.71536710878835663, -7.586896124391933505 ) ) ;
#14757=CARTESIAN_POINT ( 'NONE',  ( 8.740268137309426422, 39.01678215043063602, 10.29112316391600856 ) ) ;
#14758=ORIENTED_EDGE ( 'NONE', *, *, #11562, .F. ) ;
#14759=CARTESIAN_POINT ( 'NONE',  ( -9.938187692555990438, 70.57591519484154219, -9.136943841256590204 ) ) ;
#14760=CARTESIAN_POINT ( 'NONE',  ( 2.445080149700053643E-15, 48.17999999999999972, -13.50000000000000000 ) ) ;
#14761=ORIENTED_EDGE ( 'NONE', *, *, #4043, .F. ) ;
#14762=ORIENTED_EDGE ( 'NONE', *, *, #17050, .F. ) ;
#14765=CARTESIAN_POINT ( 'NONE',  ( 3.290941839471703378, 47.79834429727236511, 13.09273932709712263 ) ) ;
#14768=CARTESIAN_POINT ( 'NONE',  ( 9.091042220740154889, 72.03320402041192949, 9.992426890892799562 ) ) ;
#14769=CARTESIAN_POINT ( 'NONE',  ( 11.89283365199842812, 57.66647961388354560, -6.391320871232198719 ) ) ;
#14770=CARTESIAN_POINT ( 'NONE',  ( 11.76794919243112325, 64.43000000000000682, 1.441158131103945434E-15 ) ) ;
#14771=CARTESIAN_POINT ( 'NONE',  ( -8.691771469529815392E-16, 34.67999999999999972, 14.19474002721660355 ) ) ;
#14772=CARTESIAN_POINT ( 'NONE',  ( 3.636496289402154414, 78.82999999999999829, 11.19198476289190936 ) ) ;
#14773=CARTESIAN_POINT ( 'NONE',  ( -7.710663883636067695, 47.38997137728517117, 11.08260043313612542 ) ) ;
#14775=CARTESIAN_POINT ( 'NONE',  ( 2.138189944381242213, 39.10311857767973009, -13.49999999999999822 ) ) ;
#14776=CARTESIAN_POINT ( 'NONE',  ( 2.000520122481862502E-14, 76.67999999999999261, 13.50000000000000000 ) ) ;
#14778=CARTESIAN_POINT ( 'NONE',  ( -13.49999999999999822, 52.07999999999999119, 4.386415899144235020 ) ) ;
#14779=CARTESIAN_POINT ( 'NONE',  ( 13.46464982345765371, 33.46446917462228754, -0.9962107245471286676 ) ) ;
#14780=CARTESIAN_POINT ( 'NONE',  ( -4.994567026383744057, 73.36021605965370895, -12.54210557001517756 ) ) ;
#14785=CARTESIAN_POINT ( 'NONE',  ( -13.32596712241149461, 41.00582476662071940, 2.160751794978737372 ) ) ;
#14789=CARTESIAN_POINT ( 'NONE',  ( 10.92172942406178926, 39.12999999999999545, 7.935100905948387684 ) ) ;
#14790=CARTESIAN_POINT ( 'NONE',  ( -12.86018314841378363, 71.07761088014338213, 4.108712978716644315 ) ) ;
#14792=CARTESIAN_POINT ( 'NONE',  ( -12.47230674160408981, 67.74175760280583347, -5.171836198928197348 ) ) ;
#14794=CARTESIAN_POINT ( 'NONE',  ( 11.86106144339729696, 54.66890001434251900, -6.452874835814393251 ) ) ;
#14796=CYLINDRICAL_SURFACE ( 'NONE', #8738, 13.50000000000000000 ) ;
#14798=CARTESIAN_POINT ( 'NONE',  ( -13.31844401820848844, 65.00776987222435821, 2.214491255749064358 ) ) ;
#14799=CARTESIAN_POINT ( 'NONE',  ( -13.02318491043671500, 34.80308345404688453, -3.556453590126241959 ) ) ;
#14802=CARTESIAN_POINT ( 'NONE',  ( -2.842901148319972204, 31.28222014544887486, -13.19749263385335247 ) ) ;
#14803=CARTESIAN_POINT ( 'NONE',  ( 4.648327100776453946, 73.01265558291817115, -12.67451152641439549 ) ) ;
#14807=CARTESIAN_POINT ( 'NONE',  ( -12.81304320705199906, 53.08405703288592292, 4.274644209259282235 ) ) ;
#14808=CARTESIAN_POINT ( 'NONE',  ( 7.272992578804311492, 49.88000000000000256, -10.01041549318726709 ) ) ;
#14809=CARTESIAN_POINT ( 'NONE',  ( 4.171729424061789260, 64.82999999999999829, 12.83926296998457417 ) ) ;
#14810=CARTESIAN_POINT ( 'NONE',  ( 12.52626665340286216, 51.24701910560337836, 5.034456727426829481 ) ) ;
#14811=CARTESIAN_POINT ( 'NONE',  ( -10.24782649191965334, 37.59234768399701210, -8.788179505534850833 ) ) ;
#14812=CARTESIAN_POINT ( 'NONE',  ( 6.552616672584657742, 35.92103225518364695, 11.80513931794910576 ) ) ;
#14814=EDGE_CURVE ( 'NONE', #3534, #11076, #9141, .T. ) ;
#14815=CARTESIAN_POINT ( 'NONE',  ( -10.51495019309605716, 74.25306979935668039, 8.466823935618753794 ) ) ;
#14817=CARTESIAN_POINT ( 'NONE',  ( -13.30028092895002700, 76.84866536761713007, -2.313556944805478022 ) ) ;
#14818=CARTESIAN_POINT ( 'NONE',  ( -12.29284966417927016, 80.13423796449390579, 5.580253127422897919 ) ) ;
#14819=CARTESIAN_POINT ( 'NONE',  ( -5.318689435350380634, 80.93000000000004945, 11.55616787654584421 ) ) ;
#14822=CARTESIAN_POINT ( 'NONE',  ( 3.636496289402154414, 48.82999999999999829, 11.19198476289190936 ) ) ;
#14826=CARTESIAN_POINT ( 'NONE',  ( -7.556756315141740288, 40.46334594926985773, -11.19000999533063201 ) ) ;
#14827=CARTESIAN_POINT ( 'NONE',  ( 10.92172942406179104, 35.72999999999999687, -7.935100905948385908 ) ) ;
#14828=CARTESIAN_POINT ( 'NONE',  ( 10.30576900039498867, 75.09546229751185820, 8.720167078007317940 ) ) ;
#14829=DIRECTION ( 'NONE',  ( 0.000000000000000000, -1.000000000000000000, 0.000000000000000000 ) ) ;
#14830=CARTESIAN_POINT ( 'NONE',  ( -9.520470885617717371, 42.22999999999999687, 6.917026985038133624 ) ) ;
#14831=CARTESIAN_POINT ( 'NONE',  ( -7.308310390151198987, 41.40732279357077772, 11.35125782457317278 ) ) ;
#14832=CARTESIAN_POINT ( 'NONE',  ( -5.555424162506318098, 58.38152377935421811, -12.30588174299387028 ) ) ;
#14833=CARTESIAN_POINT ( 'NONE',  ( 4.940072834807441637, 44.85814714621098886, 12.56428305801228973 ) ) ;
#14835=CARTESIAN_POINT ( 'NONE',  ( 9.651130384012091668, 30.06106401149679641, 9.446356526885642424 ) ) ;
#14837=EDGE_CURVE ( 'NONE', #8302, #1729, #6073, .T. ) ;
#14838=CARTESIAN_POINT ( 'NONE',  ( -5.772320974614566502, 49.38986566563944791, -12.21294285155656034 ) ) ;
#14839=CARTESIAN_POINT ( 'NONE',  ( 13.36804092920415599, 63.49585643151682746, -1.882948519353985439 ) ) ;
#14840=CARTESIAN_POINT ( 'NONE',  ( 10.80847967602615078, 42.12344236956776200, 8.090054399549632791 ) ) ;
#14841=CARTESIAN_POINT ( 'NONE',  ( 2.270588706968536652, 38.76161630363158395, 13.30973914928087254 ) ) ;
#14843=CARTESIAN_POINT ( 'NONE',  ( 4.171729424061791924, 75.03000000000000114, -12.83926296998457239 ) ) ;
#14844=CARTESIAN_POINT ( 'NONE',  ( -4.171729424061791036, 49.53000000000000114, 12.83926296998457239 ) ) ;
#14847=ORIENTED_EDGE ( 'NONE', *, *, #1788, .F. ) ;
#14848=CARTESIAN_POINT ( 'NONE',  ( -12.69936835568980982, 43.76447789027633917, -4.580193949658626806 ) ) ;
#14850=CARTESIAN_POINT ( 'NONE',  ( 12.98358486008634394, 60.56220495594141795, -3.698251661676718705 ) ) ;
#14852=CARTESIAN_POINT ( 'NONE',  ( 12.33294000059855122, 57.63073804451487803, -5.490917873338714728 ) ) ;
#14853=CARTESIAN_POINT ( 'NONE',  ( 9.520470885617715595, 70.12999999999999545, 6.917026985038134512 ) ) ;
#14854=CARTESIAN_POINT ( 'NONE',  ( -11.76794919243112325, 80.78000000000000114, -3.823638476888998827 ) ) ;
#14855=CARTESIAN_POINT ( 'NONE',  ( -10.16915865940034536, 47.27191544427423509, 8.882609797670191654 ) ) ;
#14856=CARTESIAN_POINT ( 'NONE',  ( 8.464728390624178894E-06, 46.17999963826949994, -13.49999999999734790 ) ) ;
#14858=CARTESIAN_POINT ( 'NONE',  ( 13.50000000000000000, 38.42999999999999972, 1.653273178848926867E-15 ) ) ;
#14862=CARTESIAN_POINT ( 'NONE',  ( -8.697098998243532012E-15, 64.18000000000002103, -13.50000000000000000 ) ) ;
#14863=CARTESIAN_POINT ( 'NONE',  ( 13.49437229710556529, 33.44374862988300379, -0.4003926536058359242 ) ) ;
#14864=CARTESIAN_POINT ( 'NONE',  ( -9.875337133188997640, 73.57270964355765841, -9.205946121983142660 ) ) ;
#14867=CARTESIAN_POINT ( 'NONE',  ( -13.50000000000000000, 42.92999999999999261, -3.306546357697853733E-15 ) ) ;
#14870=CARTESIAN_POINT ( 'NONE',  ( -11.18637559572935380, 44.21414602053655329, 7.557466717348048313 ) ) ;
#14872=CARTESIAN_POINT ( 'NONE',  ( -13.50000000000000000, 43.92999999999999972, -3.306546357697853733E-15 ) ) ;
#14873=CARTESIAN_POINT ( 'NONE',  ( -13.50000000000000000, 45.92999999999999972, -3.306546357697853733E-15 ) ) ;
#14874=CARTESIAN_POINT ( 'NONE',  ( -12.92930772591764210, 71.06914952832075016, 3.883688861026760364 ) ) ;
#14877=CARTESIAN_POINT ( 'NONE',  ( -12.82678188565936317, 68.08144701978382329, 4.209989458535909002 ) ) ;
#14879=CARTESIAN_POINT ( 'NONE',  ( 13.49914950589871232, 54.43523986101267553, -0.1529510493150832429 ) ) ;
#14880=B_SPLINE_CURVE_WITH_KNOTS ( 'NONE', 3,
 ( #5764, #9660, #7088, #8595, #531, #8421, #272, #13774, #12642, #12730, #16435, #8682, #8511, #12471, #1588, #13948, #358, #4337, #4517, #5682, #9747, #7005, #15091, #15359, #2990, #1844, #11148, #16523, #4430, #1762, #5940, #11320, #15184, #3264, #618, #3085, #16699, #4604, #7172, #6029, #16342, #12560, #445, #5856, #9924, #4251, #2357, #6197, #1047, #6371, #7439, #3442, #870, #9025, #10096, #4691, #15446, #12987, #11754, #3355, #16872, #4777, #12818, #2183, #10180, #705, #2096, #6115, #17131, #11496, #14380, #6281, #7522, #8771, #14126, #2270, #9119, #13160, #14297, #14211, #15531, #2012, #10264, #11669, #15615, #8857, #787, #7611, #15796, #17044, #4949, #12903, #3524, #959, #7696, #11583, #8938, #16958, #4861, #10352, #3611, #7790, #15706, #13073, #5040, #11412, #10438, #3702, #16784, #14468, #2531, #11845, #6716, #9204, #7959, #17220, #10521, #14810, #4138, #8226, #9377, #5130, #9551, #14555, #5308, #12094, #10690, #1135, #13329, #14726, #10860, #13411, #17476, #11925, #16057, #13498, #9461, #7870, #3964, #5218, #2439, #2614, #15972, #2795, #3875, #2704, #17392, #13587, #16139, #5389, #15884, #10605, #1220, #3791, #10774, #13248, #4049, #9290, #1301, #8044, #8134, #6546, #1389, #17306, #6804, #6459, #14643, #6632, #12012, #12182, #73, #5479, #16229, #14901, #16414, #9904, #9992, #1566, #11300, #11129, #4316, #15339, #12623, #426, #9640, #8663, #11042, #5832 ),
 .UNSPECIFIED., .F., .F.,
 ( 4, 2, 2, 2, 2, 2, 2, 2, 2, 1, 1, 2, 2, 2, 2, 2, 2, 2, 2, 2, 2, 1, 1, 1, 1, 2, 2, 2, 1, 2, 2, 1, 2, 2, 2, 1, 2, 2, 1, 1, 2, 2, 2, 2, 1, 1, 1, 2, 2, 1, 2, 2, 1, 1, 2, 2, 2, 2, 2, 1, 2, 2, 2, 2, 2, 2, 2, 1, 1, 1, 1, 2, 2, 1, 2, 2, 1, 2, 2, 1, 1, 2, 2, 2, 2, 2, 2, 1, 2, 2, 2, 2, 2, 1, 1, 1, 1, 1, 1, 1, 1, 1, 2, 2, 2, 2, 2, 1, 1, 2, 2, 1, 1, 4 ),
 ( 0.5637389225892408540, 0.5641984839263527451, 0.5644282645949086907, 0.5646580452634646363, 0.5655771679376883077, 0.5664962906119120900, 0.5669558519490238702, 0.5670707422833018985, 0.5670994648668713500, 0.5671281874504409126, 0.5671856326175798158, 0.5674154132861357613, 0.5683345359603594327, 0.5692536586345832150, 0.5694834393031390496, 0.5697132199716949952, 0.5701727813088068864, 0.5710919039830305577, 0.5715514653201424489, 0.5715801879037119004, 0.5715945491954966817, 0.5716089104872814630, 0.5716663556544203662, 0.5717812459886983945, 0.5720110266572544511, 0.5724705879943665643, 0.5729301493314785665, 0.5733897106685906797, 0.5735046010028687080, 0.5735620461700077222, 0.5735907687535771737, 0.5736194913371466253, 0.5738492720057026819, 0.5747683946799269084, 0.5749981753484828539, 0.5750556205156218681, 0.5750843430991914307, 0.5750915237450837658, 0.5750987043909762120, 0.5751130656827608822, 0.5752279560170389106, 0.5756875173541509128, 0.5761470786912630260, 0.5763768593598190826, 0.5764917496940969999, 0.5765491948612360140, 0.5765779174448055766, 0.5765850980906979117, 0.5765922787365902469, 0.5766066400283750282, 0.5775257627025992546, 0.5779853240397113678, 0.5780427692068503820, 0.5780714917904198336, 0.5780858530822046149, 0.5781002143739893961, 0.5782151047082674244, 0.5784448853768234811, 0.5793640080510475965, 0.5794788983853256248, 0.5795363435524646389, 0.5795937887196036531, 0.5798235693881597097, 0.5802831307252717119, 0.5812022533994959383, 0.5816618147366079405, 0.5818915954051639972, 0.5820064857394420255, 0.5820639309065810396, 0.5820782921983658209, 0.5820854728442581560, 0.5820890631672043236, 0.5820926534901504912, 0.5821213760737200538, 0.5839596214221685067, 0.5844191827592806199, 0.5845340730935586482, 0.5845915182606976623, 0.5846058795524824436, 0.5846202408442672249, 0.5846489634278366765, 0.5848787440963928441, 0.5857978667706170706, 0.5867169894448414080, 0.5869467701133974646, 0.5870616604476754929, 0.5871191056148145071, 0.5871765507819535213, 0.5876361121190656345, 0.5885552347932898609, 0.5894743574675140874, 0.5895892478017921157, 0.5896036090935768970, 0.5896179703853616783, 0.5896466929689311298, 0.5897041381360701440, 0.5899339188046262006, 0.5903934801417383138, 0.5906232608102943704, 0.5907381511445723987, 0.5907955963117114129, 0.5908243188952809755, 0.5908386801870656457, 0.5908530414788504270, 0.5913126028159625402, 0.5917721641530746535, 0.5920019448216307101, 0.5920593899887697242, 0.5920881125723392868, 0.5920952932182316220, 0.5921024738641239571, 0.5921168351559087384, 0.5922317254901867667, 0.5931508481644109931 ),
 .UNSPECIFIED. ) ;
#14882=CARTESIAN_POINT ( 'NONE',  ( -11.88051552057379645, 64.69276546394441141, -6.411193178701971362 ) ) ;
#14883=VERTEX_POINT ( 'NONE', #12508 ) ;
#14885=CARTESIAN_POINT ( 'NONE',  ( -13.49999999999999822, 63.78000000000000114, -4.386415899144240349 ) ) ;
#14886=CARTESIAN_POINT ( 'NONE',  ( -11.62103019124827696, 35.18589392510355651, 6.873052513693640897 ) ) ;
#14889=CARTESIAN_POINT ( 'NONE',  ( 12.99172110702898841, 78.56117060242844730, -3.670802009133220078 ) ) ;
#14891=CARTESIAN_POINT ( 'NONE',  ( -10.37153830093552820, 31.59880329612760264, -8.642521494078742705 ) ) ;
#14892=CARTESIAN_POINT ( 'NONE',  ( 8.321323615989754785, 72.86260839518769217, -10.63042200351674182 ) ) ;
#14894=CARTESIAN_POINT ( 'NONE',  ( 0.1284016000230580046, 79.17538378579617131, -13.49947537073678916 ) ) ;
#14896=CARTESIAN_POINT ( 'NONE',  ( 4.171729424061791924, 76.03000000000000114, -12.83926296998457239 ) ) ;
#14897=CARTESIAN_POINT ( 'NONE',  ( -13.47435762513628887, 52.95904153983646978, 0.8409795588075931194 ) ) ;
#14899=CARTESIAN_POINT ( 'NONE',  ( 11.76794919243112325, 46.27999999999999403, 3.823638476888996607 ) ) ;
#14900=CARTESIAN_POINT ( 'NONE',  ( -8.343458848123576743, 63.48000000000001108, -11.48378591275254301 ) ) ;
#14901=CARTESIAN_POINT ( 'NONE',  ( 2.659296992907285606, 50.77569272368128139, 13.23688342416419061 ) ) ;
#14902=CARTESIAN_POINT ( 'NONE',  ( -5.978783164607675005, 37.39809822006411366, -12.10535056917534114 ) ) ;
#14903=CARTESIAN_POINT ( 'NONE',  ( 13.30492957411319210, 36.34963648306288775, 2.286669702493058676 ) ) ;
#14905=CARTESIAN_POINT ( 'NONE',  ( -8.458738825805157902, 74.35630711111390667, 10.52140770450354168 ) ) ;
#14906=CARTESIAN_POINT ( 'NONE',  ( -13.49239393192323533, 76.94558248929156719, 0.4532043396295901694 ) ) ;
#14907=CARTESIAN_POINT ( 'NONE',  ( -9.393480485980296280, 80.31162245988731740, 9.698493905942369153 ) ) ;
#14910=CYLINDRICAL_SURFACE ( 'NONE', #15666, 13.50000000000000000 ) ;
#14912=CARTESIAN_POINT ( 'NONE',  ( 11.76794919243112680, 43.57999999999999119, -3.823638476888993942 ) ) ;
#14915=CARTESIAN_POINT ( 'NONE',  ( -10.23470376096455858, 40.59170058523897495, -8.803567802926888675 ) ) ;
#14917=CARTESIAN_POINT ( 'NONE',  ( 10.28800811278561511, 75.09451940748620302, 8.741114209820295855 ) ) ;
#14920=CARTESIAN_POINT ( 'NONE',  ( 11.76794919243112325, 34.42999999999999261, 1.441158131103945434E-15 ) ) ;
#14921=CARTESIAN_POINT ( 'NONE',  ( 6.616676866212972294E-07, 41.68001839382905160, 13.49999999999996625 ) ) ;
#14922=CARTESIAN_POINT ( 'NONE',  ( -4.021251358392601283, 58.32458930914320661, -12.88728184459310278 ) ) ;
#14923=CARTESIAN_POINT ( 'NONE',  ( 0.000000000000000000, 108.9300000000000068, 0.000000000000000000 ) ) ;
#14924=B_SPLINE_CURVE_WITH_KNOTS ( 'NONE', 3,
 ( #964, #11588, #2101, #2275, #11931, #17136, #4866, #7528, #15712, #17311, #9210, #14474, #6202, #5225, #7616, #2362, #12909, #13078, #16964, #15537, #2445, #4955, #8944, #14386, #6551, #14216, #5046, #10269, #792, #10358, #7876, #3707, #14302, #9124, #6377, #15803, #15621, #7701, #2189, #3616, #13166, #9032, #14561, #12993, #3447, #875, #6286, #11674, #13253, #11761, #10443, #1140, #1053, #6465, #11850, #17225, #15889, #5136, #10526, #8864, #3798, #5313, #5579, #6638, #8231, #79, #6721, #9297, #14731, #10696, #2620, #13675, #10960, #2888, #14906, #13592, #8320, #7964, #3880, #6903, #16062, #16328, #12366, #5484, #10866, #3970, #14817, #173, #1486, #12018, #8139, #9382, #13334, #8053, #2800, #1573, #4054, #9556, #13418, #260, #16144, #12277, #15977, #1307, #12099, #14648, #16235, #1226, #4236, #17481, #4143, #9468, #13504, #17397, #2536, #2710, #6991, #5395, #6810, #10780, #1394, #12187, #9646, #10610, #14996, #16684, #3070, #14027, #14115, #5752, #15078, #2978, #12807, #8671, #12546, #11048, #8408, #7427, #4591, #9732, #1916, #2001, #11136, #1828, #13760, #16597, #1660, #343, #6016, #5668, #7075, #16420, #4323, #11399, #12459, #7245, #16509, #4415, #5840, #9825, #16771, #15170, #5927, #8496, #13847, #1749, #7335, #4504, #9998, #4679, #7161, #433, #11222, #9911, #15258, #3156, #12630 ),
 .UNSPECIFIED., .F., .F.,
 ( 4, 2, 2, 2, 1, 1, 2, 2, 1, 2, 2, 2, 2, 2, 1, 1, 1, 1, 2, 2, 2, 2, 1, 2, 2, 1, 1, 2, 2, 2, 2, 1, 2, 2, 1, 1, 2, 2, 2, 2, 2, 2, 1, 2, 2, 1, 1, 2, 2, 2, 2, 2, 2, 1, 1, 2, 2, 2, 2, 2, 2, 2, 1, 2, 2, 2, 2, 1, 1, 1, 2, 2, 2, 1, 2, 2, 1, 1, 2, 2, 2, 2, 2, 2, 1, 1, 2, 2, 2, 1, 1, 2, 2, 1, 2, 2, 2, 1, 2, 2, 1, 1, 2, 2, 4 ),
 ( 0.06374556628509139844, 0.06466468642086431462, 0.06558380655663724468, 0.06604336662452370277, 0.06627314665846693875, 0.06638803667543854981, 0.06640239792756000292, 0.06641675917968145604, 0.06644548168392436227, 0.06650292669241016086, 0.06742204682818311867, 0.06834116696395607649, 0.06835552821607752960, 0.06836988946819898272, 0.06839861197244188895, 0.06845605698092770142, 0.06857094699789934023, 0.06880072703184259009, 0.06926028709972911757, 0.07017940723550215865, 0.07109852737127521360, 0.07201764750704825468, 0.07224742754099151842, 0.07226178879311297154, 0.07227615004523442466, 0.07230487254947733089, 0.07236231755796314336, 0.07247720757493476829, 0.07293676764282128189, 0.07385588777859430909, 0.07408566781253757283, 0.07420055782950919776, 0.07421491908163066475, 0.07422928033375211787, 0.07425800283799502410, 0.07431544784648083657, 0.07477500791436741956, 0.07569412805014058554, 0.07615368811802715465, 0.07661324818591373764, 0.07753236832168688974, 0.07799192838957347274, 0.07810681840654511154, 0.07812117965866657854, 0.07813554091078803165, 0.07816426341503093789, 0.07822170842351676423, 0.07845148845746005573, 0.07937060859323322171, 0.07983016866111980470, 0.08005994869506309619, 0.08007430994718454931, 0.08008867119930601630, 0.08011739370354893641, 0.08017483871203481827, 0.08028972872900659585, 0.08120884886478078879, 0.08166840893266788526, 0.08189818896661142655, 0.08201307898358320414, 0.08202744023570467113, 0.08204180148782613813, 0.08207052399206908599, 0.08212796900055498173, 0.08396620927210349250, 0.08398057052422497337, 0.08399493177634644037, 0.08402365428058938823, 0.08408109928907527009, 0.08419598930604704767, 0.08442576933999061672, 0.08488532940787774095, 0.08580444954365200327, 0.08591933956062379474, 0.08593370081274526173, 0.08594806206486674260, 0.08597678456910966271, 0.08603422957759551681, 0.08626400961153887770, 0.08672356967942559947, 0.08764268981519902912, 0.08787246984914237613, 0.08788683110126384312, 0.08790119235338529624, 0.08792991485762821635, 0.08798735986611404269, 0.08810224988308569538, 0.08856180995097232000, 0.08948093008674556925, 0.08971071012068887462, 0.08982560013766054119, 0.08983996138978199431, 0.08985432264190344742, 0.08988304514614636753, 0.08994049015463219388, 0.09040005022251877687, 0.09131917035829195672, 0.09143406037526360941, 0.09149150538374943575, 0.09150586663587088887, 0.09152022788799234199, 0.09154895039223526210, 0.09177873042617858135, 0.09223829049406520597, 0.09315741062983846910 ),
 .UNSPECIFIED. ) ;
#14925=CARTESIAN_POINT ( 'NONE',  ( -2.138189944381240881, 55.60311857767972299, 13.49999999999999822 ) ) ;
#14927=AXIS2_PLACEMENT_3D ( 'NONE', #10380, #3472, #11525 ) ;
#14928=CARTESIAN_POINT ( 'NONE',  ( -8.891200544363830713E-16, 58.67999999999999261, 13.50000000000000000 ) ) ;
#14929=CARTESIAN_POINT ( 'NONE',  ( -10.11724169932725914, 49.58540793223827592, -8.938216045275497734 ) ) ;
#14930=CARTESIAN_POINT ( 'NONE',  ( 12.88992561142933191, 63.28600745562859231, 4.012516480704441335 ) ) ;
#14931=CARTESIAN_POINT ( 'NONE',  ( 10.61024901455322578, 42.11222895898699647, 8.347195607159086705 ) ) ;
#14932=CARTESIAN_POINT ( 'NONE',  ( 4.325464046711072541, 38.83554751821355211, 12.78834246629441473 ) ) ;
#14933=ORIENTED_EDGE ( 'NONE', *, *, #16812, .F. ) ;
#14937=ORIENTED_EDGE ( 'NONE', *, *, #10645, .F. ) ;
#14938=CARTESIAN_POINT ( 'NONE',  ( -8.694518465881534652, 43.51465161020028205, -10.32740934920959930 ) ) ;
#14939=CARTESIAN_POINT ( 'NONE',  ( -7.500000000000001776, 104.9408589258552666, -8.949127168380913488 ) ) ;
#14940=CARTESIAN_POINT ( 'NONE',  ( 12.68261237030094613, 60.59908932111539315, -4.680264340947544177 ) ) ;
#14944=CARTESIAN_POINT ( 'NONE',  ( 12.68202363619548656, 66.59736773260050313, -4.628554097373979381 ) ) ;
#14945=CARTESIAN_POINT ( 'NONE',  ( 3.243294801669318606, 56.79662143353648673, 13.10462081408920909 ) ) ;
#14947=CARTESIAN_POINT ( 'NONE',  ( 3.636496289402157078, 56.02999999999999403, -11.19198476289190936 ) ) ;
#14948=CARTESIAN_POINT ( 'NONE',  ( -7.272992578804307939, 68.48000000000000398, -10.01041549318726886 ) ) ;
#14949=CARTESIAN_POINT ( 'NONE',  ( -3.572130815311478358, 47.55156684393307387, 13.01911799694966554 ) ) ;
#14950=CARTESIAN_POINT ( 'NONE',  ( 5.547257296411079786, 45.97874116037399261, -12.30763780998237067 ) ) ;
#14953=CARTESIAN_POINT ( 'NONE',  ( 2.785878927130813844E-06, 56.68007738487546732, 13.49999999999942979 ) ) ;
#14955=CARTESIAN_POINT ( 'NONE',  ( -13.50000000000000000, 39.92999999999999972, -3.306546357697853733E-15 ) ) ;
#14957=CARTESIAN_POINT ( 'NONE',  ( 11.98594149431912648, 33.65924774496181726, -6.211891203905776315 ) ) ;
#14961=CARTESIAN_POINT ( 'NONE',  ( 2.445080149700053643E-15, 42.17999999999999261, -13.50000000000000000 ) ) ;
#14962=CARTESIAN_POINT ( 'NONE',  ( -13.49644181220360650, 40.94171918537661981, 0.3420769386924029098 ) ) ;
#14964=CARTESIAN_POINT ( 'NONE',  ( -13.47468169643279801, 43.95856576188575815, 0.8271159465435392599 ) ) ;
#14967=CARTESIAN_POINT ( 'NONE',  ( 2.607531440858944223E-15, 46.17999999999999261, -14.19474002721660355 ) ) ;
#14968=CARTESIAN_POINT ( 'NONE',  ( -10.92172942406179104, 49.23000000000000398, 7.935100905948387684 ) ) ;
#14969=CARTESIAN_POINT ( 'NONE',  ( -13.49727400116812426, 70.92069023477120027, -0.2713576259430695581 ) ) ;
#14972=CARTESIAN_POINT ( 'NONE',  ( -10.98011399424891366, 67.63341784965055581, -7.854123836487283405 ) ) ;
#14974=CARTESIAN_POINT ( 'NONE',  ( 13.10268814798864234, 54.54569041227427562, -3.253754133682983607 ) ) ;
#14975=CARTESIAN_POINT ( 'NONE',  ( -12.73420858044403836, 65.09178978912700586, 4.482361047366480555 ) ) ;
#14976=ORIENTED_EDGE ( 'NONE', *, *, #14814, .F. ) ;
#14977=CARTESIAN_POINT ( 'NONE',  ( -13.47034220899966961, 34.89910285180874183, -0.8944510538467952410 ) ) ;
#14979=CARTESIAN_POINT ( 'NONE',  ( 13.01895187323182412, 78.55753440904214813, -3.573211116871425119 ) ) ;
#14980=CARTESIAN_POINT ( 'NONE',  ( 2.138189944381238661, 49.75688142232025513, 13.50000000000000000 ) ) ;
#14981=CARTESIAN_POINT ( 'NONE',  ( -5.579618841234667670, 31.38249916496278757, -12.29310188421200678 ) ) ;
#14982=CARTESIAN_POINT ( 'NONE',  ( 9.978235625303845779, 72.78197465687738088, -9.095030402899643818 ) ) ;
#14983=CARTESIAN_POINT ( 'NONE',  ( -1.328659818498353332E-07, 59.67999629905246195, 13.49999999999999822 ) ) ;
#14985=CARTESIAN_POINT ( 'NONE',  ( -13.49999999999999822, 74.08000000000001251, 4.386415899144235908 ) ) ;
#14986=CARTESIAN_POINT ( 'NONE',  ( -13.38626367270875761, 52.99368492772342165, 1.826722430351332305 ) ) ;
#14988=CARTESIAN_POINT ( 'NONE',  ( -9.520470885617715595, 44.62999999999999545, -6.917026985038136289 ) ) ;
#14989=CARTESIAN_POINT ( 'NONE',  ( -10.92172942406178926, 63.63000000000000256, -7.935100905948389460 ) ) ;
#14991=CARTESIAN_POINT ( 'NONE',  ( 12.00929620591970526, 69.20223501009333233, 6.176927723990055519 ) ) ;
#14993=CARTESIAN_POINT ( 'NONE',  ( -2.138189944381243102, 78.25688142232027644, -13.50000000000000000 ) ) ;
#14995=CARTESIAN_POINT ( 'NONE',  ( -11.28078867911932370, 74.20825143659133971, 7.415781942181430608 ) ) ;
#14996=CARTESIAN_POINT ( 'NONE',  ( -9.449293760640395945, 76.55109966697389723, -9.641680980241128296 ) ) ;
#14997=CARTESIAN_POINT ( 'NONE',  ( 6.123233995736765296E-16, 0.000000000000000000, -5.000000000000000000 ) ) ;
#15001=CARTESIAN_POINT ( 'NONE',  ( 7.272992578804308828, 42.97999999999998977, 10.01041549318726886 ) ) ;
#15003=CARTESIAN_POINT ( 'NONE',  ( -10.08254685910888249, 40.58366014780975917, -8.978105075904496246 ) ) ;
#15006=CARTESIAN_POINT ( 'NONE',  ( 13.36046613123341054, 75.36200234952120525, 1.941819533583398094 ) ) ;
#15008=( LENGTH_UNIT ( ) NAMED_UNIT ( * ) SI_UNIT ( .MILLI., .METRE. ) );
#15010=CARTESIAN_POINT ( 'NONE',  ( -1.097433972752848597, 58.21943276801300726, -13.46203577575871257 ) ) ;
#15011=CARTESIAN_POINT ( 'NONE',  ( 3.845940030877601057, 44.81806629663489616, 12.94543018042384652 ) ) ;
#15013=CARTESIAN_POINT ( 'NONE',  ( 13.49999999999999822, 59.27999999999999403, 4.386415899144236796 ) ) ;
#15016=CARTESIAN_POINT ( 'NONE',  ( -6.953647091445300354, 49.43771701599564494, -11.57208863864802595 ) ) ;
#15017=CARTESIAN_POINT ( 'NONE',  ( 11.46408888769126477, 63.16362770892857981, 7.129672723819229674 ) ) ;
#15018=CARTESIAN_POINT ( 'NONE',  ( 8.623685178462253020, 42.01131593190542191, 10.38745792132406898 ) ) ;
#15019=CARTESIAN_POINT ( 'NONE',  ( 5.928360391604972968, 48.96387440575580285, -12.12866813512049902 ) ) ;
#15021=CARTESIAN_POINT ( 'NONE',  ( -11.76794919243112325, 80.92999999999767624, -5.919446256302011733E-11 ) ) ;
#15023=CARTESIAN_POINT ( 'NONE',  ( -13.50000000000000000, 48.92999999999999972, -3.306546357697853733E-15 ) ) ;
#15024=ORIENTED_EDGE ( 'NONE', *, *, #11447, .F. ) ;
#15025=CARTESIAN_POINT ( 'NONE',  ( -10.52241331024074356, 43.60707797551511788, -8.460377887765865523 ) ) ;
#15026=CARTESIAN_POINT ( 'NONE',  ( -7.499999999999998224, 106.7538932235142823, -7.532295102519077190 ) ) ;
#15027=CARTESIAN_POINT ( 'NONE',  ( 5.354359914900771678, 60.98636505280213527, -12.39747404020963550 ) ) ;
#15030=CARTESIAN_POINT ( 'NONE',  ( 13.45032318530042126, 66.38986098046753170, 1.157148491779020238 ) ) ;
#15031=CARTESIAN_POINT ( 'NONE',  ( 11.54394565333526401, 57.16869923784576457, 7.014965779171773441 ) ) ;
#15032=CARTESIAN_POINT ( 'NONE',  ( 7.272992578804311492, 61.87999999999999545, -10.01041549318726709 ) ) ;
#15033=CARTESIAN_POINT ( 'NONE',  ( 2.607531440858944223E-15, 36.17999999999999972, -14.19474002721660355 ) ) ;
#15034=CARTESIAN_POINT ( 'NONE',  ( -9.520470885617717371, 69.23000000000000398, 6.917026985038133624 ) ) ;
#15035=CARTESIAN_POINT ( 'NONE',  ( -10.75877101843568795, 47.23955598554530866, 8.166359762435629221 ) ) ;
#15037=CARTESIAN_POINT ( 'NONE',  ( 9.734504863165533095, 30.79467112222051028, -9.359485933502590171 ) ) ;
#15038=CARTESIAN_POINT ( 'NONE',  ( -2.048813550184076959, 56.60637244353360131, 13.34365525421965692 ) ) ;
#15040=CARTESIAN_POINT ( 'NONE',  ( 13.29826067563849179, 33.34824635017109529, 2.325148998095313946 ) ) ;
#15041=CARTESIAN_POINT ( 'NONE',  ( -3.737279461696752201E-15, 73.17999999999999261, -13.50000000000000000 ) ) ;
#15042=CARTESIAN_POINT ( 'NONE',  ( 0.06721671892514809177, 40.17758380750846214, -13.49984309485949474 ) ) ;
#15045=VERTEX_POINT ( 'NONE', #13724 ) ;
#15046=CARTESIAN_POINT ( 'NONE',  ( -2.209542456836874003, 62.60055300686897795, 13.31796333730930471 ) ) ;
#15049=CARTESIAN_POINT ( 'NONE',  ( -13.50485324719562108, 43.92628281948966418, -0.1030264437535955285 ) ) ;
#15050=CARTESIAN_POINT ( 'NONE',  ( 2.138189944381238661, 64.75688142232026223, 13.50000000000000000 ) ) ;
#15051=CARTESIAN_POINT ( 'NONE',  ( -8.691771469529815392E-16, 35.67999999999998550, 14.19474002721660355 ) ) ;
#15053=CARTESIAN_POINT ( 'NONE',  ( -10.10311990571781493, 67.58464977146856256, -8.954164421584090761 ) ) ;
#15055=CARTESIAN_POINT ( 'NONE',  ( 13.14489197790636155, 54.32051714666025077, 3.086064228016605071 ) ) ;
#15056=CARTESIAN_POINT ( 'NONE',  ( -0.6061693567267533167, 64.20179552098323938, -13.48666111876418583 ) ) ;
#15058=ORIENTED_EDGE ( 'NONE', *, *, #3652, .F. ) ;
#15060=CARTESIAN_POINT ( 'NONE',  ( -12.03451023656767127, 35.15595434393794250, 6.132305428729441843 ) ) ;
#15062=CARTESIAN_POINT ( 'NONE',  ( 13.05258666306970916, 78.55284067711124862, -3.446834127247557333 ) ) ;
#15064=CARTESIAN_POINT ( 'NONE',  ( 0.000000000000000000, 80.93000000000000682, 0.000000000000000000 ) ) ;
#15065=CARTESIAN_POINT ( 'NONE',  ( 11.21626728703616571, 72.71231259042123440, -7.513034004964580070 ) ) ;
#15066=CARTESIAN_POINT ( 'NONE',  ( 3.217771947876906680, 59.79570616790843474, 13.11091034625173712 ) ) ;
#15067=CARTESIAN_POINT ( 'NONE',  ( 13.50000000000000000, 66.43000000000000682, 1.653273178848926867E-15 ) ) ;
#15068=CARTESIAN_POINT ( 'NONE',  ( -12.79277096370526401, 52.77467266838400661, -4.312411596693917382 ) ) ;
#15069=CARTESIAN_POINT ( 'NONE',  ( 3.636496289402157078, 41.02999999999999403, -11.19198476289190936 ) ) ;
#15071=CARTESIAN_POINT ( 'NONE',  ( 13.49999999999999822, 59.27999999999998693, 4.386415899144237684 ) ) ;
#15073=CARTESIAN_POINT ( 'NONE',  ( 4.801038565581039919, 68.85297145803022545, 12.61827525106671821 ) ) ;
#15074=CARTESIAN_POINT ( 'NONE',  ( -2.819206891948295546, 37.28136828592626983, -13.20235427941665485 ) ) ;
#15077=CARTESIAN_POINT ( 'NONE',  ( -9.939332794820023409, 74.28402178779931830, 9.138064150772017058 ) ) ;
#15078=CARTESIAN_POINT ( 'NONE',  ( -9.395212350200784712, 76.54841060185640345, -9.694346819223181200 ) ) ;
#15081=CARTESIAN_POINT ( 'NONE',  ( 1.653273178848926472E-15, 80.93000000000000682, 13.50000000000000000 ) ) ;
#15084=CARTESIAN_POINT ( 'NONE',  ( -9.520470885617715595, 47.62999999999999545, -6.917026985038136289 ) ) ;
#15086=CARTESIAN_POINT ( 'NONE',  ( -2.235446294924008370, 32.59959283518442419, 13.31508909693261344 ) ) ;
#15087=CARTESIAN_POINT ( 'NONE',  ( 13.19457708748799618, 75.53145179741177628, -2.867282558126743375 ) ) ;
#15089=SHAPE_REPRESENTATION_RELATIONSHIP ( 'NONE' , 'NONE' ,  #10992, #9886 ) ;
#15090=CARTESIAN_POINT ( 'NONE',  ( -9.355789771963381796, 41.31352449815521766, 9.732436554501715520 ) ) ;
#15091=CARTESIAN_POINT ( 'NONE',  ( 5.707630944344394663, 51.97262754088920644, -12.24211879259819469 ) ) ;
#15092=CARTESIAN_POINT ( 'NONE',  ( -7.404093397872471449, 38.40322494662342478, 11.28901117625147599 ) ) ;
#15093=CARTESIAN_POINT ( 'NONE',  ( 12.50000000000000000, 98.93000000000002103, 9.000000000000000000 ) ) ;
#15094=CARTESIAN_POINT ( 'NONE',  ( 8.343458848123583849, 71.87999999999998124, -11.48378591275253768 ) ) ;
#15095=CARTESIAN_POINT ( 'NONE',  ( 3.780205736804012180E-08, 55.17999999864077409, -13.50000000000000000 ) ) ;
#15096=CARTESIAN_POINT ( 'NONE',  ( -12.03753084031560583, 49.70467287274419022, -6.112121115600539056 ) ) ;
#15097=CARTESIAN_POINT ( 'NONE',  ( 9.423185512043215084, 63.04955960285478511, 9.674719739589008327 ) ) ;
#15098=CARTESIAN_POINT ( 'NONE',  ( 12.36513741947113765, 42.23211346040410774, 5.417882651531068738 ) ) ;
#15102=CARTESIAN_POINT ( 'NONE',  ( -7.272992578804310604, 72.38000000000000966, 10.01041549318726886 ) ) ;
#15106=EDGE_LOOP ( 'NONE', ( #5731, #11937, #10299, #12487, #10579, #15737 ) ) ;
#15107=CARTESIAN_POINT ( 'NONE',  ( -5.291839448614410912, 43.37146548570319737, -12.42001919633759321 ) ) ;
#15109=CARTESIAN_POINT ( 'NONE',  ( 10.93522283957610775, 60.72922764856446776, -7.921801309275269709 ) ) ;
#15113=CARTESIAN_POINT ( 'NONE',  ( 11.57317910393498828, 66.68907146314168699, -6.950662690379005859 ) ) ;
#15114=CARTESIAN_POINT ( 'NONE',  ( 4.954131915168964895, 56.85870117836017812, 12.55812868081141076 ) ) ;
#15115=CARTESIAN_POINT ( 'NONE',  ( 11.76794919243112325, 55.27999999999998693, 3.823638476888996607 ) ) ;
#15116=CARTESIAN_POINT ( 'NONE',  ( -11.76794919243112325, 63.07999999999999119, 3.823638476888994386 ) ) ;
#15117=CARTESIAN_POINT ( 'NONE',  ( -12.71445672950702210, 46.76596698851027156, -4.541269490033386091 ) ) ;
#15119=CARTESIAN_POINT ( 'NONE',  ( 12.06082462307849923, 45.65376011911352805, -6.079388249483466566 ) ) ;
#15120=FACE_OUTER_BOUND ( 'NONE', #7472, .T. ) ;
#15122=CARTESIAN_POINT ( 'NONE',  ( 0.3579478956273707824, 31.16713074970619601, -13.49560965235342280 ) ) ;
#15126=CARTESIAN_POINT ( 'NONE',  ( -13.49999999999999822, 40.07999999999999829, 4.386415899144235020 ) ) ;
#15127=CARTESIAN_POINT ( 'NONE',  ( 4.109698719430495473, 32.82776958409561985, 12.85927299696574977 ) ) ;
#15129=CARTESIAN_POINT ( 'NONE',  ( 4.601630155619385043, 40.01437466971148638, -12.69233364863190339 ) ) ;
#15131=EDGE_LOOP ( 'NONE', ( #13026, #16268 ) ) ;
#15132=CARTESIAN_POINT ( 'NONE',  ( -3.934136427065950681, 62.53854296712907512, 12.91404697952921232 ) ) ;
#15136=CARTESIAN_POINT ( 'NONE',  ( -13.25690904173389484, 43.83876739692001223, -2.587063218252659613 ) ) ;
#15138=CARTESIAN_POINT ( 'NONE',  ( 9.235077742801747647, 30.03187307936175543, 10.25657778616701599 ) ) ;
#15139=CARTESIAN_POINT ( 'NONE',  ( 13.49999999999999822, 47.28000000000000114, 4.386415899144237684 ) ) ;
#15140=( BOUNDED_CURVE ( )  B_SPLINE_CURVE ( 2, ( #1095, #11628, #15663, #11542, #11891, #4822, #13037, #14429, #17091, #2146, #8985, #4998, #6510 ),
 .UNSPECIFIED., .F., .F. ) 
 B_SPLINE_CURVE_WITH_KNOTS ( ( 3, 2, 2, 2, 2, 2, 3 ),
 ( 0.7916666666666666297, 0.7944444444444443976, 0.8000000000000000444, 0.8055555555555555802, 0.8111111111111111160, 0.8166666666666666519, 0.8194444444444444198 ),
 .UNSPECIFIED. ) 
 CURVE ( )  GEOMETRIC_REPRESENTATION_ITEM ( )  RATIONAL_B_SPLINE_CURVE ( ( 0.9755282581475768211, 0.9755282581475768211, 1.000000000000000000, 0.9510565162951535312, 1.000000000000000000, 0.9510565162951535312, 1.000000000000000000, 0.9510565162951535312, 1.000000000000000000, 0.9510565162951535312, 1.000000000000000000, 0.9755282581475768211, 0.9755282581475768211 ) ) 
 REPRESENTATION_ITEM ( '' )  );
#15141=CARTESIAN_POINT ( 'NONE',  ( -8.931054703680040063, 46.52501327082484295, -10.16359813786777622 ) ) ;
#15142=CARTESIAN_POINT ( 'NONE',  ( -4.753464114467623958, 67.35100568867868276, -12.64302991685488564 ) ) ;
#15144=CARTESIAN_POINT ( 'NONE',  ( -1.003760800223034469E-07, 53.67999720368429450, 13.49999999999999822 ) ) ;
#15145=CARTESIAN_POINT ( 'NONE',  ( -10.21286249403196855, 64.59057106318286401, -8.829037698084668762 ) ) ;
#15148=CARTESIAN_POINT ( 'NONE',  ( -11.52078070856594039, 34.66713973480176492, -7.043119858845972914 ) ) ;
#15152=CARTESIAN_POINT ( 'NONE',  ( 13.39124523941554656, 78.37032605518025719, 1.711065265865323592 ) ) ;
#15153=CARTESIAN_POINT ( 'NONE',  ( 10.92172942406178926, 47.12999999999999545, 7.935100905948387684 ) ) ;
#15155=CARTESIAN_POINT ( 'NONE',  ( 4.670586549414562860, 73.01184521546099404, -12.66632117632807741 ) ) ;
#15156=CARTESIAN_POINT ( 'NONE',  ( 3.500170436279223196, 79.05413282030319522, -13.04570395975783725 ) ) ;
#15158=CARTESIAN_POINT ( 'NONE',  ( -8.343458848123582072, 65.37999999999999545, 11.48378591275254124 ) ) ;
#15159=CARTESIAN_POINT ( 'NONE',  ( -13.48061558364907064, 52.90503315535101336, -0.7233178539605096269 ) ) ;
#15160=CARTESIAN_POINT ( 'NONE',  ( -7.576616670048093940E-16, 42.67999999999999972, 12.37355403259654985 ) ) ;
#15162=CARTESIAN_POINT ( 'NONE',  ( 8.343458848123583849, 56.88000000000000256, -11.48378591275253768 ) ) ;
#15163=EDGE_CURVE ( 'NONE', #15607, #743, #816, .T. ) ;
#15164=DIRECTION ( 'NONE',  ( -6.302562568933760152E-16, -1.000000000000000000, 0.000000000000000000 ) ) ;
#15166=CARTESIAN_POINT ( 'NONE',  ( 11.48609513044766395, 69.16493330855622901, 7.097038714263399939 ) ) ;
#15169=CARTESIAN_POINT ( 'NONE',  ( -12.67808328063180845, 73.76223803303696513, -4.638750535666444463 ) ) ;
#15170=CARTESIAN_POINT ( 'NONE',  ( -3.084225208773089477, 76.29063485233812969, -13.15363842553807494 ) ) ;
#15176=CARTESIAN_POINT ( 'NONE',  ( 2.272985001014427393E-15, 38.17999999999999972, -12.37355403259654807 ) ) ;
#15178=CARTESIAN_POINT ( 'NONE',  ( -3.265813649003837860, 32.56277205055386759, 13.10951091463926055 ) ) ;
#15179=CARTESIAN_POINT ( 'NONE',  ( 13.48416359079525151, 75.45253600662924498, -0.6538687915017138419 ) ) ;
#15182=CARTESIAN_POINT ( 'NONE',  ( 7.272992578804311492, 34.87999999999999545, -10.01041549318726709 ) ) ;
#15183=CARTESIAN_POINT ( 'NONE',  ( 13.50000000000000000, 80.43000000000000682, 1.653273178848926867E-15 ) ) ;
#15184=CARTESIAN_POINT ( 'NONE',  ( 9.428830175397949986, 51.81010302066297868, -9.668537834129738329 ) ) ;
#15185=CARTESIAN_POINT ( 'NONE',  ( -1.554078682580832815, 38.62412002689448798, 13.41025849265453473 ) ) ;
#15186=CARTESIAN_POINT ( 'NONE',  ( 5.409153947552197472, 36.98379089016496835, -12.36981397998242649 ) ) ;
#15189=CARTESIAN_POINT ( 'NONE',  ( 7.102532611500677717, 62.94396966511739322, 11.48060114064993975 ) ) ;
#15190=CARTESIAN_POINT ( 'NONE',  ( 13.32040245924266664, 42.35294902285478003, 2.194828684655724338 ) ) ;
#15191=CARTESIAN_POINT ( 'NONE',  ( 1.538839542171267061, 38.73533021766907325, 13.41224767058500333 ) ) ;
#15195=CARTESIAN_POINT ( 'NONE',  ( -9.520470885617717371, 69.23000000000000398, 6.917026985038133624 ) ) ;
#15199=EDGE_LOOP ( 'NONE', ( #16213, #6229, #7909, #2305 ) ) ;
#15200=CARTESIAN_POINT ( 'NONE',  ( -2.220955663942571601, 43.25985729847043615, -13.31607982724954908 ) ) ;
#15205=CARTESIAN_POINT ( 'NONE',  ( 12.94155673114020466, 66.29238691916880555, 3.842733075138333287 ) ) ;
#15206=CARTESIAN_POINT ( 'NONE',  ( 11.15568599528430838, 57.14407707936145187, 7.606331343502261255 ) ) ;
#15207=CARTESIAN_POINT ( 'NONE',  ( 9.520470885617717371, 58.73000000000000398, -6.917026985038131848 ) ) ;
#15208=CARTESIAN_POINT ( 'NONE',  ( 10.92172942406179104, 32.72999999999999687, -7.935100905948385908 ) ) ;
#15209=CARTESIAN_POINT ( 'NONE',  ( 11.76794919243112680, 67.57999999999998408, -3.823638476888993942 ) ) ;
#15211=CARTESIAN_POINT ( 'NONE',  ( -11.71715498535849598, 46.68080331322232013, -6.708422292409551346 ) ) ;
#15213=CARTESIAN_POINT ( 'NONE',  ( 5.636143214428637194, 45.97535775804710312, -12.26722223200532902 ) ) ;
#15216=CARTESIAN_POINT ( 'NONE',  ( 7.607743402570670277, 30.89476037788184470, -11.17066045873822233 ) ) ;
#15217=CARTESIAN_POINT ( 'NONE',  ( -7.461870820705466478, 56.40082279287123157, 11.26181808124483830 ) ) ;
#15218=CARTESIAN_POINT ( 'NONE',  ( -2.090093454172745613, 50.60485299099218537, 13.33722994085978719 ) ) ;
#15219=CARTESIAN_POINT ( 'NONE',  ( 11.71562641685611794, 33.17875202474539265, 6.766063318502479440 ) ) ;
#15223=CARTESIAN_POINT ( 'NONE',  ( -11.04935343432774708, 62.22247568111082217, 7.756490358654122730 ) ) ;
#15225=CARTESIAN_POINT ( 'NONE',  ( -13.40968305279137951, 40.98484619147922814, 1.574467244674663036 ) ) ;
#15228=CARTESIAN_POINT ( 'NONE',  ( -12.72580279456753338, 43.76730851413559265, -4.505998233414108434 ) ) ;
#15229=CARTESIAN_POINT ( 'NONE',  ( 2.138189944381242213, 66.10311857767973720, -13.49999999999999822 ) ) ;
#15230=CARTESIAN_POINT ( 'NONE',  ( 13.50000000000000355, 33.57999999999999829, -4.386415899144233244 ) ) ;
#15231=CARTESIAN_POINT ( 'NONE',  ( -4.171729424061791036, 43.53000000000000114, 12.83926296998457239 ) ) ;
#15233=CARTESIAN_POINT ( 'NONE',  ( -2.934267639516605630, 46.28547539380033982, -13.18180308497758446 ) ) ;
#15234=CARTESIAN_POINT ( 'NONE',  ( -11.72621171495925196, 67.68154214080810505, -6.689257902045856241 ) ) ;
#15236=CARTESIAN_POINT ( 'NONE',  ( 6.499702057654023868, 53.91894888444889489, 11.83264119668203485 ) ) ;
#15238=CARTESIAN_POINT ( 'NONE',  ( -10.31288091114224059, 64.59587999935689595, -8.711744710682491899 ) ) ;
#15240=CARTESIAN_POINT ( 'NONE',  ( -5.247208035731191877, 34.36974467868986949, -12.43902619372017782 ) ) ;
#15242=CARTESIAN_POINT ( 'NONE',  ( 11.52123726438447626, 78.16718586782270961, 7.042369149511602977 ) ) ;
#15245=CARTESIAN_POINT ( 'NONE',  ( 11.69054898252628050, 72.17893444877771003, 6.754223243015324840 ) ) ;
#15247=CARTESIAN_POINT ( 'NONE',  ( -10.92172942406178926, 64.62999999999999545, -7.935100905948389460 ) ) ;
#15248=CARTESIAN_POINT ( 'NONE',  ( -4.420108738712346330, 52.33898909862991644, -12.75633360914648229 ) ) ;
#15249=CARTESIAN_POINT ( 'NONE',  ( 7.272992578804311492, 40.87999999999998835, -10.01041549318726709 ) ) ;
#15250=CARTESIAN_POINT ( 'NONE',  ( -4.171729424061791036, 61.53000000000000114, 12.83926296998457239 ) ) ;
#15253=CARTESIAN_POINT ( 'NONE',  ( 10.31646666059287476, 69.09600980556707839, 8.710257868796588809 ) ) ;
#15254=CARTESIAN_POINT ( 'NONE',  ( -2.835384746425102964, 37.28194995933510114, -13.19889313174409473 ) ) ;
#15255=CARTESIAN_POINT ( 'NONE',  ( -13.49999999999999822, 73.08000000000001251, 4.386415899144235020 ) ) ;
#15257=CARTESIAN_POINT ( 'NONE',  ( -11.38516945207351405, 73.65842273094972370, -7.254522738815065708 ) ) ;
#15258=CARTESIAN_POINT ( 'NONE',  ( -1.101621291205112207, 76.21958249968859889, -13.46178648949251588 ) ) ;
#15259=CARTESIAN_POINT ( 'NONE',  ( -3.641410069088633961, 79.31075509186923966, -13.00494094948426316 ) ) ;
#15265=CARTESIAN_POINT ( 'NONE',  ( 9.520470885617717371, 40.72999999999999687, -6.917026985038131848 ) ) ;
#15269=CARTESIAN_POINT ( 'NONE',  ( 1.312945976112900981, 74.72720796987070457, 13.43600633030649227 ) ) ;
#15271=CARTESIAN_POINT ( 'NONE',  ( -13.50000000000000000, 84.93000000000000682, -3.306546357697853733E-15 ) ) ;
#15272=CARTESIAN_POINT ( 'NONE',  ( -2.264479525414730077, 58.26142199067226812, -13.30896360304205039 ) ) ;
#15273=CARTESIAN_POINT ( 'NONE',  ( -1.388205926214359787, 38.63012733182188185, 13.42855087378624468 ) ) ;
#15275=CARTESIAN_POINT ( 'NONE',  ( -10.92172942406178926, 69.62999999999999545, -7.935100905948389460 ) ) ;
#15276=CARTESIAN_POINT ( 'NONE',  ( -4.382329622040107786, 49.33761423158443904, -12.76923448255947413 ) ) ;
#15278=CARTESIAN_POINT ( 'NONE',  ( 2.650574835413161523, 62.77529302382879450, 13.23723914315057293 ) ) ;
#15279=CARTESIAN_POINT ( 'NONE',  ( 5.499638061715979909, 41.87941307834116600, 12.32899955262698732 ) ) ;
#15280=CARTESIAN_POINT ( 'NONE',  ( 8.525489938592672345, 48.85322366431354624, -10.46738712784432934 ) ) ;
#15283=CARTESIAN_POINT ( 'NONE',  ( -9.520470885617717371, 66.23000000000000398, 6.917026985038133624 ) ) ;
#15288=CARTESIAN_POINT ( 'NONE',  ( 2.924053257345435538E-06, 68.68008145904181561, 13.49999999999936584 ) ) ;
#15289=CARTESIAN_POINT ( 'NONE',  ( 0.000000000000000000, 80.93000000000000682, 0.000000000000000000 ) ) ;
#15292=CARTESIAN_POINT ( 'NONE',  ( 11.83941929220342537, 66.18971953923538365, 6.486927149400845138 ) ) ;
#15293=CARTESIAN_POINT ( 'NONE',  ( 10.71075049650908895, 57.11789055711182073, 8.217759637934333838 ) ) ;
#15294=CARTESIAN_POINT ( 'NONE',  ( 2.272985001014427788E-15, 59.17999999999998550, -12.37355403259654985 ) ) ;
#15295=CARTESIAN_POINT ( 'NONE',  ( -7.272992578804310604, 66.37999999999999545, 10.01041549318726709 ) ) ;
#15296=AXIS2_PLACEMENT_3D ( 'NONE', #16185, #5619, #2841 ) ;
#15297=CARTESIAN_POINT ( 'NONE',  ( -11.61613876028604331, 46.67376607488575502, -6.881206147996638656 ) ) ;
#15298=CARTESIAN_POINT ( 'NONE',  ( 7.426031545778958964, 45.90225655064444510, -11.27414640185626205 ) ) ;
#15300=CARTESIAN_POINT ( 'NONE',  ( 11.28170547357727749, 30.70818519455021800, -7.414394825668972011 ) ) ;
#15301=CARTESIAN_POINT ( 'NONE',  ( -12.72210886894176696, 56.09309001809862849, 4.516451198278201851 ) ) ;
#15302=CARTESIAN_POINT ( 'NONE',  ( 2.138189944381238661, 52.75688142232026934, 13.50000000000000000 ) ) ;
#15303=CARTESIAN_POINT ( 'NONE',  ( 13.28530447619198185, 33.34560229784237606, 2.398270177113091428 ) ) ;
#15305=CARTESIAN_POINT ( 'NONE',  ( 10.32321619528713086, 39.76356552170057057, -8.699496154864482023 ) ) ;
#15306=ORIENTED_EDGE ( 'NONE', *, *, #6794, .T. ) ;
#15307=CARTESIAN_POINT ( 'NONE',  ( -12.49324912787944264, 62.11632128283577714, 5.121990780005423183 ) ) ;
#15313=CARTESIAN_POINT ( 'NONE',  ( 11.69049970947668982, 48.17901677739538968, 6.751497366717108761 ) ) ;
#15315=CARTESIAN_POINT ( 'NONE',  ( -13.49999999999999822, 31.77999999999999758, -4.386415899144240349 ) ) ;
#15316=CARTESIAN_POINT ( 'NONE',  ( -0.1281060804169691925, 46.18460550068364512, -13.49947775182521248 ) ) ;
#15317=CARTESIAN_POINT ( 'NONE',  ( -7.462108197810392696, 67.45929967586793907, -11.25098269314221078 ) ) ;
#15319=CARTESIAN_POINT ( 'NONE',  ( 5.999104543695027658, 53.89865356422039611, 12.09973455174266022 ) ) ;
#15322=CARTESIAN_POINT ( 'NONE',  ( -11.76794919243112325, 80.92999999999767624, -5.919446256302011733E-11 ) ) ;
#15325=CARTESIAN_POINT ( 'NONE',  ( -8.165485012641067186, 34.49031512341151284, -10.75073694722957640 ) ) ;
#15327=DIRECTION ( 'NONE',  ( 0.000000000000000000, -1.000000000000000000, 0.000000000000000000 ) ) ;
#15330=CARTESIAN_POINT ( 'NONE',  ( -8.343458848123578520, 36.47999999999998977, -11.48378591275254124 ) ) ;
#15331=B_SPLINE_CURVE_WITH_KNOTS ( 'NONE', 3,
 ( #8538, #14067, #4715, #13888, #560, #11348, #14151, #10288, #1787, #11520, #15385, #473, #10037, #1952, #8708, #12925, #16897, #5882, #4801, #16640, #809, #12754, #3292, #5967, #7377, #3201, #643, #8621, #13975, #6054, #1870, #8794, #12668, #12845, #16723, #4630, #11436, #15471, #10203, #3382, #2040, #15555, #7464, #733, #6141, #3467, #15993, #7895, #5242, #13097, #17068, #983, #11951, #12271, #3637, #5154, #3816, #5066, #7635, #17155, #9315, #6897, #10955, #6396, #2464, #13013, #13272, #17331, #168, #17244, #10461, #10628, #5572, #15821, #3897, #1160, #7721, #14665, #3550, #11779, #6570, #2292, #3726, #2554, #7983, #13186, #2378, #2208, #9144, #9229, #8964, #14491, #14320, #13352, #4972, #7813, #10547, #1481, #893, #6306, #11691, #1071, #6484, #10375, #14404, #11869, #15729, #15907, #9051, #14583, #9641, #15342, #16415, #7070, #14022, #1912, #5747, #14991, #2883, #7239, #7330, #8315, #13670, #9906, #8578, #6986, #15166, #16591, #3064, #11043, #11131, #1744, #3242, #5834, #4499, #4317, #8491, #15253, #9727, #13755, #4586, #600, #12713, #12361, #8403, #6012, #1655, #12625, #9819, #16323, #13929, #3152, #513, #1823, #5921, #1567, #13842, #16504, #12454, #4409, #8665, #256, #338, #11302, #4229, #15073, #428, #16679, #7156, #5662, #12541, #9994, #11217, #2972, #12802, #6100, #14110, #13057, #11649, #851, #939, #774, #7678, #7771, #12885, #6350, #9004, #15513, #5017, #13142 ),
 .UNSPECIFIED., .F., .F.,
 ( 4, 2, 2, 1, 2, 2, 2, 1, 1, 2, 2, 1, 1, 2, 2, 2, 2, 2, 2, 1, 1, 1, 2, 2, 2, 2, 2, 1, 2, 2, 2, 2, 2, 2, 2, 2, 2, 2, 1, 1, 2, 2, 2, 2, 2, 2, 1, 1, 1, 1, 2, 2, 2, 1, 2, 2, 1, 1, 1, 2, 2, 2, 2, 2, 2, 1, 1, 2, 2, 2, 2, 2, 2, 1, 1, 2, 1, 1, 2, 2, 1, 2, 2, 2, 2, 1, 1, 1, 2, 2, 2, 2, 2, 2, 2, 2, 2, 1, 1, 1, 1, 2, 2, 1, 1, 2, 2, 2, 2, 1, 1, 1, 2, 4 ),
 ( 0.2108027933308743440, 0.2109176789523807827, 0.2110325645738872213, 0.2112623358169000987, 0.2117218783029258811, 0.2126409632749773904, 0.2144791332190804645, 0.2147089044620933418, 0.2148237900835997805, 0.2148381507862880957, 0.2148453311376322394, 0.2148525114889763832, 0.2148812328943529859, 0.2149386757051061358, 0.2153982181911315019, 0.2163173031631822063, 0.2167768456492075724, 0.2167912063518958599, 0.2168055670545841751, 0.2168342884599607501, 0.2168917312707139278, 0.2170066168922202832, 0.2172363881352329940, 0.2181554731072838094, 0.2186150155933092309, 0.2187299012148155863, 0.2187586226201921891, 0.2187873440255687640, 0.2188447868363219695, 0.2190745580793347080, 0.2195341005653601574, 0.2197638718083728959, 0.2198213146191260736, 0.2198787574298792791, 0.2199936430513856345, 0.2209127280234366164, 0.2209701708341897941, 0.2209845315368781093, 0.2209988922395663968, 0.2210276136449429996, 0.2211424992664493550, 0.2213722705094621213, 0.2218318129954875984, 0.2227508979675386080, 0.2232104404535640851, 0.2232248011562523726, 0.2232391618589406879, 0.2232678832643172906, 0.2233253260750704683, 0.2234402116965768514, 0.2236699829395895900, 0.2255081528836916094, 0.2264272378557426468, 0.2265421234772490022, 0.2265564841799373175, 0.2265636645312814612, 0.2265708448826256050, 0.2265995662880022077, 0.2266570090987553576, 0.2268867803417680684, 0.2273463228277934345, 0.2282654077998441944, 0.2284951790428568774, 0.2285095397455451649, 0.2285239004482334524, 0.2285526218536100551, 0.2286100646643632051, 0.2287249502858695605, 0.2291844927718948988, 0.2301035777439456309, 0.2303333489869583139, 0.2304482346084646416, 0.2304769560138412166, 0.2305056774192178193, 0.2305631202299709970, 0.2310226627159963908, 0.2312524339590090738, 0.2313673195805154292, 0.2314247623912686069, 0.2314534837966451819, 0.2314822052020217846, 0.2319417476880472062, 0.2324012901740726278, 0.2324156508767609153, 0.2324300115794492028, 0.2324587329848258055, 0.2325161757955789832, 0.2326310614170853386, 0.2328608326600980771, 0.2337799176321490036, 0.2342394601181744529, 0.2344692313611871637, 0.2346990026041999022, 0.2356180875762508009, 0.2365371725483016996, 0.2365946153590548773, 0.2366520581698080550, 0.2367669437913144104, 0.2369967150343271212, 0.2374562575203525705, 0.2376860287633652813, 0.2377147501687418563, 0.2377291108714301437, 0.2377434715741184590, 0.2378009143848716089, 0.2379158000063779643, 0.2383753424924033304, 0.2388348849784287242, 0.2388636063838052992, 0.2388923277891819019, 0.2389497705999350519, 0.2390646562214414073, 0.2392944274644540903, 0.2402135124365048502 ),
 .UNSPECIFIED. ) ;
#15332=CARTESIAN_POINT ( 'NONE',  ( 12.47883071023084334, 72.24232604971501814, 5.156649975335684921 ) ) ;
#15334=CARTESIAN_POINT ( 'NONE',  ( -4.171729424061791036, 62.53000000000000114, 12.83926296998457239 ) ) ;
#15335=CARTESIAN_POINT ( 'NONE',  ( -5.830206929847885355, 52.39226344610381858, -12.17615902335279543 ) ) ;
#15336=CARTESIAN_POINT ( 'NONE',  ( -9.520470885617715595, 41.63000000000000256, -6.917026985038136289 ) ) ;
#15338=CARTESIAN_POINT ( 'NONE',  ( 2.607531440858944223E-15, 57.17999999999999261, -14.19474002721660355 ) ) ;
#15339=CARTESIAN_POINT ( 'NONE',  ( 1.528574478876175036, 50.73496190250285309, 13.41318330975730966 ) ) ;
#15342=CARTESIAN_POINT ( 'NONE',  ( 12.78125498241015734, 69.27338024102353131, 4.346469460005440766 ) ) ;
#15343=CARTESIAN_POINT ( 'NONE',  ( -1.337701960717650129, 37.22806044761306055, -13.43546765959366596 ) ) ;
#15345=CARTESIAN_POINT ( 'NONE',  ( -10.66802778328771595, 73.61539763354224419, -8.273749749751072358 ) ) ;
#15350=CARTESIAN_POINT ( 'NONE',  ( 7.272992578804311492, 37.87999999999999545, -10.01041549318726886 ) ) ;
#15351=( BOUNDED_CURVE ( )  B_SPLINE_CURVE ( 2, ( #15021, #14522, #14698, #8431, #13785, #7843, #6518, #13216, #1103, #17364, #17274, #2585, #16110, #8017, #10578, #5360, #4348, #369, #10746, #4020, #3846, #5278, #5774, #9757, #3932, #1599, #5188, #9349, #13384, #7928, #12483, #13301, #12393, #1274, #15854, #8343, #2913, #3762, #14614, #11983, #9174, #2409, #7015, #10662, #15939, #9262, #6686, #2497, #1192, #3001, #6603, #16026, #12068, #17445, #283, #13699, #9434, #15102, #5692, #11072, #16445, #1683, #7099, #8692, #11423, #11245, #10021, #9848, #5951, #16795, #2107, #11331, #798, #6128, #7182, #3184, #629, #8782, #15195, #4441, #3095, #16709, #13958, #7451, #4527, #11507, #1855, #7269, #16534, #12570, #12652, #5866, #16883, #457, #14138, #6040, #542, #8521, #15283, #16624, #8606, #1773, #13871, #9934, #4614, #15369, #3275, #4701, #14052, #1939, #10106, #4789, #12741, #10190, #7362, #15457, #3368, #11159, #15543, #2026, #12831, #718, #3455, #8870, #14223, #7534, #12914, #11680, #13339, #11767, #2369, #11594, #4873, #7802, #15627, #3535, #6208, #9218, #13086, #16971, #8950, #9131, #2195, #10276, #10450, #2542, #6294, #13173, #14308, #17143, #7623, #15718, #5052, #15983, #15809, #13000, #882, #11938, #17056, #4961, #10364, #3622, #9039, #15897, #7708, #14392, #6471, #2281, #971, #6384, #1059, #3713, #14480, #11857, #17232, #5142, #10534, #14569, #3805, #2453, #7883, #13260, #1147, #6558, #17319, #7970, #5231, #10616, #3886, #9303, #14654, #10785, #6816, #11054, #86, #12023, #17402, #6997, #8059, #1230, #13423, #16151, #5317, #10966, #2716, #6727, #1493, #2627, #1312, #3975, #2894, #5491, #5586, #12373, #14822, #8145, #12105, #10872, #9738, #10701, #8237, #266, #15084, #4059, #16334, #4242, #16069, #16426, #2983, #5674, #1579, #4150, #179, #9475, #8326, #12193, #4330, #14738, #17486, #6908, #13508, #9651, #9387, #5401, #1400, #2805, #13681, #16242, #9562, #14912, #13597, #12284, #8414, #15001, #6642, #11312, #8503, #12724, #8676, #7251, #611, #12635, #6108, #11490, #5756, #4422, #11140, #16515, #15265, #9831, #524, #14033, #5932, #13852, #3162, #16689, #698, #3252, #1921, #1755, #4597, #3433, #2005, #1834, #16776, #15176, #10003, #15350, #5846, #10174, #11229, #10088, #7341, #13765, #6020, #8763, #3076, #16603, #11404, #4684, #12465, #12552, #16864, #8589, #4510, #15439, #7166, #14118, #9916, #13940, #1667, #438, #3348, #7431, #12811, #4769, #15523, #7081, #349, #7514, #12978, #1124, #782, #16950, #6189, #11575, #10339, #4851, #7687, #9107, #13064, #3516, #15694, #11743, #13237 ),
 .UNSPECIFIED., .F., .F. ) 
 B_SPLINE_CURVE_WITH_KNOTS ( ( 3, 2, 2, 2, 2, 2, 2, 2, 2, 2, 2, 2, 2, 2, 2, 2, 2, 2, 2, 2, 2, 2, 2, 2, 2, 2, 2, 2, 2, 2, 2, 2, 2, 2, 2, 2, 2, 2, 2, 2, 2, 2, 2, 2, 2, 2, 2, 2, 2, 2, 2, 2, 2, 2, 2, 2, 2, 2, 2, 2, 2, 2, 2, 2, 2, 2, 2, 2, 2, 2, 2, 2, 2, 2, 2, 2, 2, 2, 2, 2, 2, 2, 2, 2, 2, 2, 2, 2, 2, 2, 2, 2, 2, 2, 2, 2, 2, 2, 2, 2, 2, 2, 2, 2, 2, 2, 2, 2, 2, 2, 2, 2, 2, 2, 2, 2, 2, 2, 2, 2, 2, 2, 2, 2, 2, 2, 2, 2, 2, 2, 2, 2, 2, 2, 2, 2, 2, 2, 2, 2, 2, 2, 2, 2, 2, 2, 2, 2, 2, 2, 2, 2, 2, 2, 2, 2, 2, 2, 2, 2, 2, 2, 2, 2, 2, 2, 2, 3 ),
 ( 0.05660416580082960891, 0.06226458238090768621, 0.06792499896098576351, 0.07358541554106384774, 0.07924583212114191810, 0.08490624870121998846, 0.09056666528129808658, 0.09622708186137615693, 0.1018874984414542412, 0.1075479150215323254, 0.1132083316016103819, 0.1188687481816884661, 0.1245291647617665504, 0.1301895813418446068, 0.1358499979219227050, 0.1415104145020008031, 0.1471708310820788457, 0.1528312476621569438, 0.1584916642422350419, 0.1641520808223131123, 0.1698124974023911549, 0.1754729139824692530, 0.1811333305625473233, 0.1867937471426253937, 0.1924541637227034918, 0.1981145803027815622, 0.2037749968828596603, 0.2094354134629377029, 0.2150958300430157732, 0.2207562466230938714, 0.2264166632031719417, 0.2320770797832500398, 0.2377374963633281102, 0.2433979129434062083, 0.2490583295234842509, 0.2547187461035623213, 0.2603791626836404194, 0.2660395792637185175, 0.2716999958437965601, 0.2773604124238746582, 0.2830208290039527563, 0.2886812455840307989, 0.2943416621641088415, 0.3000020787441869952, 0.3056624953242650378, 0.3113229119043431359, 0.3169833284844211785, 0.3226437450644992211, 0.3283041616445774302, 0.3339645782246554728, 0.3396249948047335154, 0.3452854113848115580, 0.3509458279648896561, 0.3566062445449676988, 0.3622666611250458524, 0.3679270777051239505, 0.3735874942852019376, 0.3792479108652800357, 0.3849083274453581338, 0.3905687440254362874, 0.3962291606055143300, 0.4018895771855923726, 0.4075499937656704708, 0.4132104103457484578, 0.4188708269258265560, 0.4245312435059047651, 0.4301916600859828077, 0.4358520766660608503, 0.4415124932461388929, 0.4471729098262169910, 0.4528333264062949781, 0.4584937429863731873, 0.4641541595664512854, 0.4698145761465292725, 0.4754749927266073706, 0.4811354093066854132, 0.4867958258867636223, 0.4924562424668416094, 0.4981166590469197075, 0.5037770756269978056, 0.5094374922070757927, 0.5150979087871538908, 0.5207583253672318779, 0.5264187419473100871, 0.5320791585273881852, 0.5377395751074662833, 0.5433999916875442704, 0.5490604082676222575, 0.5547208248477004666, 0.5603812414277785647, 0.5660416580078566628, 0.5717020745879347610, 0.5773624911680127481, 0.5830229077480908462, 0.5886833243281688333, 0.5943437409082470424, 0.6000041574883251405, 0.6056645740684031276, 0.6113249906484811147, 0.6169854072285593238, 0.6226458238086374219, 0.6283062403887155201, 0.6339666569687935072, 0.6396270735488716053, 0.6452874901289497034, 0.6509479067090276905, 0.6566083232891058996, 0.6622687398691839977, 0.6679291564492619848, 0.6735895730293400829, 0.6792499896094181810, 0.6849104061894962792, 0.6905708227695742663, 0.6962312393496524754, 0.7018916559297304625, 0.7075520725098084496, 0.7132124890898866587, 0.7188729056699647568, 0.7245333222500428549, 0.7301937388301208420, 0.7358541554101989401, 0.7415145719902770383, 0.7471749885703550254, 0.7528354051504332345, 0.7584958217305113326, 0.7641562383105893197, 0.7698166548906673068, 0.7754770714707455159, 0.7811374880508236140, 0.7867979046309016011, 0.7924583212109798103, 0.7981187377910577974, 0.8037791543711357845, 0.8094395709512138826, 0.8150999875312920917, 0.8207604041113701898, 0.8264208206914481769, 0.8320812372715262750, 0.8377416538516043731, 0.8434020704316823602, 0.8490624870117604583, 0.8547229035918386675, 0.8603833201719166546, 0.8660437367519946417, 0.8717041533320728508, 0.8773645699121509489, 0.8830249864922289360, 0.8886854030723070341, 0.8943458196523851322, 0.9000062362324631193, 0.9056666528125412174, 0.9113270693926194266, 0.9169874859726975247, 0.9226479025527755118, 0.9283083191328536099, 0.9339687357129317080, 0.9396291522930098061, 0.9452895688730877932, 0.9509499854531660024, 0.9566104020332439895, 0.9622708186133219765, 0.9679312351934001857, 0.9735916517734782838, 0.9792520683535562709, 0.9849124849336343690, 0.9905729015137124671, 0.9962333180937904542, 1.000000000000000000 ),
 .UNSPECIFIED. ) 
 CURVE ( )  GEOMETRIC_REPRESENTATION_ITEM ( )  RATIONAL_B_SPLINE_CURVE ( ( 0.9999999999996016520, 0.9510565162955518792, 1.000000000000000000, 0.9510565162951535312, 1.000000000000000000, 0.9510565162951535312, 1.000000000000000000, 0.9510565162951535312, 1.000000000000000000, 0.9510565162951535312, 1.000000000000000000, 0.9510565162951535312, 1.000000000000000000, 0.9510565162951535312, 1.000000000000000000, 0.9510565162951535312, 1.000000000000000000, 0.9510565162951535312, 1.000000000000000000, 0.9510565162951535312, 1.000000000000000000, 0.9510565162951535312, 1.000000000000000000, 0.9510565162951535312, 1.000000000000000000, 0.9510565162951535312, 1.000000000000000000, 0.9510565162951535312, 1.000000000000000000, 0.9510565162951535312, 1.000000000000000000, 0.9510565162951535312, 1.000000000000000000, 0.9510565162951535312, 1.000000000000000000, 0.9510565162951535312, 1.000000000000000000, 0.9510565162951535312, 1.000000000000000000, 0.9510565162951535312, 1.000000000000000000, 0.9510565162951535312, 1.000000000000000000, 0.9510565162951535312, 1.000000000000000000, 0.9510565162951535312, 1.000000000000000000, 0.9510565162951535312, 1.000000000000000000, 0.9510565162951535312, 1.000000000000000000, 0.9510565162951535312, 1.000000000000000000, 0.9510565162951535312, 1.000000000000000000, 0.9510565162951535312, 1.000000000000000000, 0.9510565162951535312, 1.000000000000000000, 0.9510565162951535312, 1.000000000000000000, 0.9510565162951535312, 1.000000000000000000, 0.9510565162951535312, 1.000000000000000000, 0.9510565162951535312, 1.000000000000000000, 0.9510565162951535312, 1.000000000000000000, 0.9510565162951535312, 1.000000000000000000, 0.9510565162951535312, 1.000000000000000000, 0.9510565162951535312, 1.000000000000000000, 0.9510565162951535312, 1.000000000000000000, 0.9510565162951535312, 1.000000000000000000, 0.9510565162951535312, 1.000000000000000000, 0.9510565162951535312, 1.000000000000000000, 0.9510565162951535312, 1.000000000000000000, 0.9510565162951535312, 1.000000000000000000, 0.9510565162951535312, 1.000000000000000000, 0.9510565162951535312, 1.000000000000000000, 0.9510565162951535312, 1.000000000000000000, 0.9510565162951535312, 1.000000000000000000, 0.9510565162951535312, 1.000000000000000000, 0.9510565162951535312, 1.000000000000000000, 0.9510565162951535312, 1.000000000000000000, 0.9510565162951535312, 1.000000000000000000, 0.9510565162951535312, 1.000000000000000000, 0.9510565162951535312, 1.000000000000000000, 0.9510565162951535312, 1.000000000000000000, 0.9510565162951535312, 1.000000000000000000, 0.9510565162951535312, 1.000000000000000000, 0.9510565162951535312, 1.000000000000000000, 0.9510565162951535312, 1.000000000000000000, 0.9510565162951535312, 1.000000000000000000, 0.9510565162951535312, 1.000000000000000000, 0.9510565162951535312, 1.000000000000000000, 0.9510565162951535312, 1.000000000000000000, 0.9510565162951535312, 1.000000000000000000, 0.9510565162951535312, 1.000000000000000000, 0.9510565162951535312, 1.000000000000000000, 0.9510565162951535312, 1.000000000000000000, 0.9510565162951535312, 1.000000000000000000, 0.9510565162951535312, 1.000000000000000000, 0.9510565162951535312, 1.000000000000000000, 0.9510565162951535312, 1.000000000000000000, 0.9510565162951535312, 1.000000000000000000, 0.9510565162951535312, 1.000000000000000000, 0.9510565162951535312, 1.000000000000000000, 0.9510565162951535312, 1.000000000000000000, 0.9510565162951535312, 1.000000000000000000, 0.9510565162951535312, 1.000000000000000000, 0.9510565162951535312, 1.000000000000000000, 0.9510565162951535312, 1.000000000000000000, 0.9510565162951535312, 1.000000000000000000, 0.9510565162951535312, 1.000000000000000000, 0.9510565162951535312, 1.000000000000000000, 0.9510565162951535312, 1.000000000000000000, 0.9510565162951535312, 1.000000000000000000, 0.9510565162951535312, 1.000000000000000000, 0.9510565162951535312, 1.000000000000000000, 0.9510565162951535312, 1.000000000000000000, 0.9510565162951535312, 1.000000000000000000, 0.9510565162951535312, 1.000000000000000000, 0.9510565162951535312, 1.000000000000000000, 0.9510565162951535312, 1.000000000000000000, 0.9510565162951535312, 1.000000000000000000, 0.9510565162951535312, 1.000000000000000000, 0.9510565162951535312, 1.000000000000000000, 0.9510565162951535312, 1.000000000000000000, 0.9510565162951535312, 1.000000000000000000, 0.9510565162951535312, 1.000000000000000000, 0.9510565162951535312, 1.000000000000000000, 0.9510565162951535312, 1.000000000000000000, 0.9510565162951535312, 1.000000000000000000, 0.9510565162951535312, 1.000000000000000000, 0.9510565162951535312, 1.000000000000000000, 0.9510565162951535312, 1.000000000000000000, 0.9510565162951535312, 1.000000000000000000, 0.9510565162951535312, 1.000000000000000000, 0.9510565162951535312, 1.000000000000000000, 0.9510565162951535312, 1.000000000000000000, 0.9510565162951535312, 1.000000000000000000, 0.9510565162951535312, 1.000000000000000000, 0.9510565162951535312, 1.000000000000000000, 0.9510565162951535312, 1.000000000000000000, 0.9510565162951535312, 1.000000000000000000, 0.9510565162951535312, 1.000000000000000000, 0.9510565162951535312, 1.000000000000000000, 0.9510565162951535312, 1.000000000000000000, 0.9510565162951535312, 1.000000000000000000, 0.9510565162951535312, 1.000000000000000000, 0.9510565162951535312, 1.000000000000000000, 0.9510565162951535312, 1.000000000000000000, 0.9510565162951535312, 1.000000000000000000, 0.9510565162951535312, 1.000000000000000000, 0.9510565162951535312, 1.000000000000000000, 0.9510565162951535312, 1.000000000000000000, 0.9510565162951535312, 1.000000000000000000, 0.9510565162951535312, 1.000000000000000000, 0.9510565162951535312, 1.000000000000000000, 0.9510565162951535312, 1.000000000000000000, 0.9510565162951535312, 1.000000000000000000, 0.9510565162951535312, 1.000000000000000000, 0.9510565162951535312, 1.000000000000000000, 0.9510565162951535312, 1.000000000000000000, 0.9510565162951535312, 1.000000000000000000, 0.9510565162951535312, 1.000000000000000000, 0.9510565162951535312, 1.000000000000000000, 0.9510565162951535312, 1.000000000000000000, 0.9510565162951535312, 1.000000000000000000, 0.9510565162951535312, 1.000000000000000000, 0.9510565162951535312, 1.000000000000000000, 0.9510565162951535312, 1.000000000000000000, 0.9510565162951535312, 1.000000000000000000, 0.9510565162951535312, 1.000000000000000000, 0.9510565162951535312, 1.000000000000000000, 0.9510565162951535312, 1.000000000000000000, 0.9510565162951535312, 1.000000000000000000, 0.9510565162951535312, 1.000000000000000000, 0.9510565162951535312, 1.000000000000000000, 0.9510565162951535312, 1.000000000000000000, 0.9510565162951535312, 1.000000000000000000, 0.9510565162951535312, 1.000000000000000000, 0.9510565162951535312, 1.000000000000000000, 0.9510565162951535312, 1.000000000000000000, 0.9510565162951535312, 1.000000000000000000, 0.9510565162951535312, 1.000000000000000000, 0.9510565162951535312, 1.000000000000000000, 0.9510565162951535312, 1.000000000000000000, 0.9510565162951535312, 1.000000000000000000, 0.9510565162951535312, 1.000000000000000000, 0.9510565162951535312, 1.000000000000000000, 0.9510565162951535312, 1.000000000000000000, 0.9510565162951535312, 1.000000000000000000, 0.9510565162951535312, 1.000000000000000000, 0.9510565162951535312, 1.000000000000000000, 0.9510565162951535312, 1.000000000000000000, 0.9510565162951535312, 1.000000000000000000, 0.9510565162951535312, 1.000000000000000000, 0.9510565162951535312, 1.000000000000000000, 0.9510565162951535312, 1.000000000000000000, 0.9674309245812854341, 0.9782075447827165426 ) ) 
 REPRESENTATION_ITEM ( '' )  );
#15353=CARTESIAN_POINT ( 'NONE',  ( 1.628308837847167748E-06, 32.68004529479373588, 13.49999999999980460 ) ) ;
#15354=CARTESIAN_POINT ( 'NONE',  ( 9.949328106897166180, 75.07664185812758717, 9.126035338817397147 ) ) ;
#15357=CARTESIAN_POINT ( 'NONE',  ( 8.343458848123578520, 79.98000000000001819, 11.48378591275254124 ) ) ;
#15359=CARTESIAN_POINT ( 'NONE',  ( 6.498476362382647586, 51.94114444125180086, -11.84129758499792118 ) ) ;
#15361=LINE ( 'NONE', #16615, #6407 ) ;
#15362=CARTESIAN_POINT ( 'NONE',  ( -2.138189944381257757, 69.25688142232027644, -13.49999999999999289 ) ) ;
#15364=CARTESIAN_POINT ( 'NONE',  ( 2.599693433324294922, 62.77350978289579331, 13.24734751974565405 ) ) ;
#15365=CARTESIAN_POINT ( 'NONE',  ( 3.088734071207799303, 41.79106346645730241, 13.14190885100032524 ) ) ;
#15366=CARTESIAN_POINT ( 'NONE',  ( 10.55941645560348441, 48.75061515200597029, -8.411729401910850612 ) ) ;
#15369=CARTESIAN_POINT ( 'NONE',  ( 2.272985001014427393E-15, 65.18000000000000682, -12.37355403259654807 ) ) ;
#15374=CARTESIAN_POINT ( 'NONE',  ( -2.875760791593931984E-14, 76.17999999999999261, -13.50000000000000000 ) ) ;
#15377=CARTESIAN_POINT ( 'NONE',  ( 10.32274762114379030, 66.09624816351212928, 8.700950685072003310 ) ) ;
#15378=CARTESIAN_POINT ( 'NONE',  ( 4.171729424061791924, 79.03000000000000114, -12.83926296998457239 ) ) ;
#15380=CARTESIAN_POINT ( 'NONE',  ( -9.520470885617717371, 54.23000000000000398, 6.917026985038133624 ) ) ;
#15382=CARTESIAN_POINT ( 'NONE',  ( -11.76794919243112325, 56.77999999999998693, -3.823638476888998827 ) ) ;
#15383=CARTESIAN_POINT ( 'NONE',  ( -13.31105111643021921, 46.85093201765869253, -2.250770146535703287 ) ) ;
#15384=CARTESIAN_POINT ( 'NONE',  ( 10.70331455173479895, 45.74252489688407053, -8.227460180060322870 ) ) ;
#15385=CARTESIAN_POINT ( 'NONE',  ( 3.493247654510983846, 70.05461554162307891, -13.06995608569233092 ) ) ;
#15386=EDGE_CURVE ( 'NONE', #568, #11530, #11539, .T. ) ;
#15388=CARTESIAN_POINT ( 'NONE',  ( 8.369696161555634006, 30.86039719007353455, -10.59237420471009195 ) ) ;
#15389=CARTESIAN_POINT ( 'NONE',  ( -13.46224735791354732, 55.96492138559692364, 1.008931430782477268 ) ) ;
#15390=CARTESIAN_POINT ( 'NONE',  ( 13.50000000000000355, 53.58000000000000540, -4.386415899144233244 ) ) ;
#15391=CARTESIAN_POINT ( 'NONE',  ( 1.138962821616983367, 32.72095444842646828, 13.45206967035641377 ) ) ;
#15392=CARTESIAN_POINT ( 'NONE',  ( 4.346632539395717032, 43.02368370212016657, -12.78113607336223367 ) ) ;
#15393=CARTESIAN_POINT ( 'NONE',  ( 11.20568860838524294, 39.71295177364815032, -7.528793318710608418 ) ) ;
#15394=ORIENTED_EDGE ( 'NONE', *, *, #4043, .T. ) ;
#15395=CARTESIAN_POINT ( 'NONE',  ( -13.16850383217373732, 61.82452929595484648, -2.976946126390717318 ) ) ;
#15397=VERTEX_POINT ( 'NONE', #9930 ) ;
#15400=CARTESIAN_POINT ( 'NONE',  ( 11.53697122679876408, 48.16844816899800463, 7.012046851884700338 ) ) ;
#15402=CARTESIAN_POINT ( 'NONE',  ( 8.343458848123578520, 35.97999999999999687, 11.48378591275254124 ) ) ;
#15403=CARTESIAN_POINT ( 'NONE',  ( 4.171729424061789260, 37.82999999999999829, 12.83926296998457417 ) ) ;
#15405=AXIS2_PLACEMENT_3D ( 'NONE', #7289, #11181, #8626 ) ;
#15406=ADVANCED_FACE ( 'NONE', ( #2103 ), #12910, .T. ) ;
#15407=CARTESIAN_POINT ( 'NONE',  ( -1.315351892621634544, 46.22726836446648946, -13.43749779991192561 ) ) ;
#15408=DIRECTION ( 'NONE',  ( 0.000000000000000000, -1.000000000000000000, 0.000000000000000000 ) ) ;
#15410=CARTESIAN_POINT ( 'NONE',  ( 9.212593542616069442, 54.03942132565033063, 9.869137508411661486 ) ) ;
#15411=VERTEX_POINT ( 'NONE', #4869 ) ;
#15412=CARTESIAN_POINT ( 'NONE',  ( -1.403062250848142511, 64.23045450618263885, -13.42962668392956616 ) ) ;
#15414=CARTESIAN_POINT ( 'NONE',  ( -2.838270712586780596E-14, 67.18000000000000682, -13.50000000000000178 ) ) ;
#15415=CARTESIAN_POINT ( 'NONE',  ( -4.329644013675561176, 34.33569415333381158, -12.78730092188580691 ) ) ;
#15417=CARTESIAN_POINT ( 'NONE',  ( 8.248096366247494871, 77.99385762200095940, 10.69720316962921913 ) ) ;
#15418=CARTESIAN_POINT ( 'NONE',  ( 8.343458848123580296, 46.97999999999999687, 11.48378591275253768 ) ) ;
#15419=VECTOR ( 'NONE', #5006, 1000.000000000000000 ) ;
#15422=CARTESIAN_POINT ( 'NONE',  ( 10.67593876640750317, 72.11592638041871339, 8.262829459856675385 ) ) ;
#15424=CARTESIAN_POINT ( 'NONE',  ( 13.50000000000000355, 66.57999999999999829, -4.386415899144233244 ) ) ;
#15425=CARTESIAN_POINT ( 'NONE',  ( -2.380357500337397791, 52.26558885175427349, -13.28850035324038359 ) ) ;
#15426=CARTESIAN_POINT ( 'NONE',  ( 2.272985001014427788E-15, 38.17999999999999972, -12.37355403259654985 ) ) ;
#15427=CARTESIAN_POINT ( 'NONE',  ( 8.343458848123578520, 52.97999999999999687, 11.48378591275254124 ) ) ;
#15430=CARTESIAN_POINT ( 'NONE',  ( -2.911921858601246527, 68.57532333875593622, 13.18921981885233130 ) ) ;
#15434=CARTESIAN_POINT ( 'NONE',  ( -11.69088730954973876, 73.67895630682167507, -6.753829726051608695 ) ) ;
#15436=DIRECTION ( 'NONE',  ( -1.000000000000000000, -1.734723475976807094E-16, -0.000000000000000000 ) ) ;
#15439=CARTESIAN_POINT ( 'NONE',  ( 2.272985001014427393E-15, 35.17999999999999261, -12.37355403259654807 ) ) ;
#15441=CARTESIAN_POINT ( 'NONE',  ( -1.812614935732535848, 32.61479078993660607, 13.37801144487990612 ) ) ;
#15442=CARTESIAN_POINT ( 'NONE',  ( -2.811464633627016061E-07, 74.67999216907730897, 13.49999999999999289 ) ) ;
#15443=EDGE_CURVE ( 'NONE', #5905, #12574, #8602, .T. ) ;
#15445=CARTESIAN_POINT ( 'NONE',  ( 10.92172942406179104, 80.72999999999998977, -7.935100905948385908 ) ) ;
#15446=CARTESIAN_POINT ( 'NONE',  ( 11.82310823617331330, 51.67149392221477910, -6.517150710059238961 ) ) ;
#15447=CARTESIAN_POINT ( 'NONE',  ( -1.704182853630322292, 38.61868516537028029, 13.39237762325557135 ) ) ;
#15448=CARTESIAN_POINT ( 'NONE',  ( 8.416301635034747264, 36.85828208203987799, -10.55640874431936993 ) ) ;
#15452=CARTESIAN_POINT ( 'NONE',  ( 0.3122628659426803788, 62.69122775878508946, 13.49642344175948061 ) ) ;
#15453=CARTESIAN_POINT ( 'NONE',  ( 5.571623316695888839, 41.88219105858915725, 12.29678795757967080 ) ) ;
#15454=CARTESIAN_POINT ( 'NONE',  ( 13.22950857473560049, 48.52495454413182330, -2.688921183273661697 ) ) ;
#15457=CARTESIAN_POINT ( 'NONE',  ( -7.576616670048093940E-16, 63.67999999999998550, 12.37355403259654807 ) ) ;
#15462=CARTESIAN_POINT ( 'NONE',  ( -11.29885598845502059, 80.92999999999994998, -4.264693269864170411 ) ) ;
#15463=EDGE_CURVE ( 'NONE', #5515, #3211, #8162, .T. ) ;
#15465=CARTESIAN_POINT ( 'NONE',  ( 12.93521420879763362, 66.29158821686850445, 3.864030656794251950 ) ) ;
#15467=CARTESIAN_POINT ( 'NONE',  ( -3.636496289402155746, 48.52999999999999403, 11.19198476289190936 ) ) ;
#15468=CARTESIAN_POINT ( 'NONE',  ( 4.171729424061791924, 33.02999999999999403, -12.83926296998457239 ) ) ;
#15469=CARTESIAN_POINT ( 'NONE',  ( -13.31132898414792542, 47.01062904578743940, 2.286098758061895886 ) ) ;
#15470=CARTESIAN_POINT ( 'NONE',  ( 11.74912485249524607, 45.67681818464819088, -6.649168124183248985 ) ) ;
#15471=CARTESIAN_POINT ( 'NONE',  ( 9.075450842952271557, 69.82754448784227463, -10.00762726697219129 ) ) ;
#15473=CARTESIAN_POINT ( 'NONE',  ( 11.91445496772408141, 30.66470696577163579, -6.348179239168573851 ) ) ;
#15474=CARTESIAN_POINT ( 'NONE',  ( -13.13757147891543653, 56.04209669737164035, 3.157802568303226032 ) ) ;
#15475=DIRECTION ( 'NONE',  ( -0.000000000000000000, -1.000000000000000000, -0.000000000000000000 ) ) ;
#15476=CARTESIAN_POINT ( 'NONE',  ( 9.229767010897823809, 33.04026619113517427, 9.852102493543972273 ) ) ;
#15477=CARTESIAN_POINT ( 'NONE',  ( 3.966527692860394971, 43.03741821288255665, -12.90466901633432606 ) ) ;
#15478=CARTESIAN_POINT ( 'NONE',  ( 10.32978028215595856, 39.76320980175390929, -8.691700943171158045 ) ) ;
#15480=CARTESIAN_POINT ( 'NONE',  ( -13.37433931291107214, 61.86190675592462185, -1.950432114993175814 ) ) ;
#15481=EDGE_LOOP ( 'NONE', ( #4197, #8369, #16563, #10942 ) ) ;
#15486=CARTESIAN_POINT ( 'NONE',  ( 9.911774180940524204, 48.07459980054595405, 9.166220353908824947 ) ) ;
#15487=CARTESIAN_POINT ( 'NONE',  ( 7.492398563130175049, 57.89939741061336775, -11.23087949929781360 ) ) ;
#15488=CARTESIAN_POINT ( 'NONE',  ( 4.907594864777465204, 79.00300826774883944, -12.57642615738353342 ) ) ;
#15489=CARTESIAN_POINT ( 'NONE',  ( 11.76794919243112325, 79.43000000000000682, 1.441158131103945434E-15 ) ) ;
#15492=DIRECTION ( 'NONE',  ( 1.000000000000000000, 0.000000000000000000, 0.000000000000000000 ) ) ;
#15494=CARTESIAN_POINT ( 'NONE',  ( 2.247262830882058804, 53.76078584421372852, 13.32055735975993827 ) ) ;
#15495=EDGE_LOOP ( 'NONE', ( #2173, #4939 ) ) ;
#15498=CARTESIAN_POINT ( 'NONE',  ( 4.331139769576483722, 67.02393676668302192, -12.79382777007953997 ) ) ;
#15499=CARTESIAN_POINT ( 'NONE',  ( -10.21196434613299786, 34.59042564233829609, -8.829834170552652850 ) ) ;
#15502=CARTESIAN_POINT ( 'NONE',  ( -0.3547435831859336863, 59.66724472799371171, 13.49534119830239298 ) ) ;
#15503=DIRECTION ( 'NONE',  ( -1.000000000000000000, -1.734723475976807094E-16, -0.000000000000000000 ) ) ;
#15504=ADVANCED_FACE ( 'NONE', ( #7447 ), #6588, .T. ) ;
#15505=FACE_OUTER_BOUND ( 'NONE', #10189, .T. ) ;
#15506=CARTESIAN_POINT ( 'NONE',  ( 13.37527706476260114, 72.36600586506794741, 1.830836926929945152 ) ) ;
#15508=CARTESIAN_POINT ( 'NONE',  ( 10.92172942406178926, 51.12999999999999545, 7.935100905948387684 ) ) ;
#15509=CARTESIAN_POINT ( 'NONE',  ( -4.722038887560244369, 52.35004485108893846, -12.64903088714287627 ) ) ;
#15510=CARTESIAN_POINT ( 'NONE',  ( -10.92172942406179104, 52.22999999999999687, 7.935100905948387684 ) ) ;
#15513=CARTESIAN_POINT ( 'NONE',  ( 0.8896506985072949458, 68.71206883159973700, 13.47799656996557438 ) ) ;
#15517=CARTESIAN_POINT ( 'NONE',  ( -5.195004986271709591, 65.49223690651673735, 12.46041586375061883 ) ) ;
#15523=CARTESIAN_POINT ( 'NONE',  ( -3.636496289402155746, 33.52999999999999403, 11.19198476289190936 ) ) ;
#15525=ADVANCED_FACE ( 'NONE', ( #16966 ), #966, .T. ) ;
#15526=CARTESIAN_POINT ( 'NONE',  ( -12.99763655697469389, 31.79961795752758036, -3.649497489147533802 ) ) ;
#15527=CARTESIAN_POINT ( 'NONE',  ( 5.944571218590016137, 74.89675644291142476, 12.12073777988105050 ) ) ;
#15528=B_SPLINE_CURVE_WITH_KNOTS ( 'NONE', 3,
 ( #7683, #12891, #16861, #6186, #5023, #12720 ),
 .UNSPECIFIED., .F., .F.,
 ( 4, 2, 4 ),
 ( 0.02310369341406991878, 0.02476750247080822948, 0.02643131152754654364 ),
 .UNSPECIFIED. ) ;
#15529=CARTESIAN_POINT ( 'NONE',  ( 2.445080149700053643E-15, 63.17999999999998550, -13.50000000000000000 ) ) ;
#15530=CARTESIAN_POINT ( 'NONE',  ( -9.520470885617717371, 33.22999999999999687, 6.917026985038133624 ) ) ;
#15531=CARTESIAN_POINT ( 'NONE',  ( 13.23700282839715214, 51.52360258182024921, -2.651746004224825981 ) ) ;
#15532=CARTESIAN_POINT ( 'NONE',  ( -10.85070262625603199, 38.23431805590681876, 8.033477467492103230 ) ) ;
#15533=CARTESIAN_POINT ( 'NONE',  ( 9.828294447040992310, 36.78977993224530252, -9.257394455623087381 ) ) ;
#15537=CARTESIAN_POINT ( 'NONE',  ( -6.079049460997783427, 77.45800250635466000, 12.05802342483350387 ) ) ;
#15538=CARTESIAN_POINT ( 'NONE',  ( 0.8516938202833010951, 62.71062401767625261, 13.47402210528613864 ) ) ;
#15539=CARTESIAN_POINT ( 'NONE',  ( 2.693171479753761144, 41.77698449823576254, 13.23099151030277731 ) ) ;
#15540=CARTESIAN_POINT ( 'NONE',  ( 8.569772578347119918, 48.85117011955044575, -10.43116877877169379 ) ) ;
#15543=CARTESIAN_POINT ( 'NONE',  ( -9.520470885617717371, 63.23000000000001108, 6.917026985038133624 ) ) ;
#15548=CARTESIAN_POINT ( 'NONE',  ( -6.556136581990969603, 80.93000000000003524, -10.79013235404803162 ) ) ;
#15550=CARTESIAN_POINT ( 'NONE',  ( 0.3084388608991097125, 65.69109030173645181, 13.49649039133380768 ) ) ;
#15551=CARTESIAN_POINT ( 'NONE',  ( -4.171729424061787483, 82.32999999999999829, -12.83926296998457417 ) ) ;
#15552=CARTESIAN_POINT ( 'NONE',  ( 3.636496289402154414, 45.82999999999999829, 11.19198476289190936 ) ) ;
#15553=CARTESIAN_POINT ( 'NONE',  ( -13.23862237912311990, 59.02327283768620703, 2.644021597903271292 ) ) ;
#15554=CARTESIAN_POINT ( 'NONE',  ( 13.46303184484187021, 45.39474804055323887, 1.017860785898056619 ) ) ;
#15555=CARTESIAN_POINT ( 'NONE',  ( 10.07434941184534161, 69.77687380662450778, -8.986611288426695765 ) ) ;
#15556=AXIS2_PLACEMENT_3D ( 'NONE', #13321, #15878, #11920 ) ;
#15557=CARTESIAN_POINT ( 'NONE',  ( 4.216399006263609195, 80.83160784084826389, 12.82482784682136767 ) ) ;
#15558=CARTESIAN_POINT ( 'NONE',  ( 13.48284133012123576, 30.45349738626596192, -0.6814970486944390560 ) ) ;
#15559=EDGE_CURVE ( 'NONE', #19, #6381, #974, .T. ) ;
#15560=CARTESIAN_POINT ( 'NONE',  ( -12.71517232650662166, 56.09383332730872951, 4.535934352837492689 ) ) ;
#15561=CARTESIAN_POINT ( 'NONE',  ( -3.937409535744305078, 50.53842199591847617, 12.91306281124268374 ) ) ;
#15562=CARTESIAN_POINT ( 'NONE',  ( 5.262825442084041683, 63.98957157723919664, -12.43207888071740008 ) ) ;
#15563=CARTESIAN_POINT ( 'NONE',  ( 13.02746587078432761, 39.55632540197606772, -3.540568321141328578 ) ) ;
#15565=CARTESIAN_POINT ( 'NONE',  ( -10.51606056038198922, 61.60671756202894755, -8.470023507808827290 ) ) ;
#15567=VERTEX_POINT ( 'NONE', #13080 ) ;
#15571=CARTESIAN_POINT ( 'NONE',  ( 10.57931356024353242, 57.74949723134712087, -8.386364294737058245 ) ) ;
#15572=CARTESIAN_POINT ( 'NONE',  ( 2.551961531130515493, 79.08824087738575770, -13.25660889663138065 ) ) ;
#15573=CARTESIAN_POINT ( 'NONE',  ( -3.636496289402155746, 81.53000000000000114, 11.19198476289190936 ) ) ;
#15574=CARTESIAN_POINT ( 'NONE',  ( 10.92172942406178926, 38.12999999999999545, 7.935100905948387684 ) ) ;
#15577=FACE_OUTER_BOUND ( 'NONE', #15836, .T. ) ;
#15583=CARTESIAN_POINT ( 'NONE',  ( 3.038729800852512763, 34.07073859099919844, -13.15357245918240459 ) ) ;
#15584=ORIENTED_EDGE ( 'NONE', *, *, #5182, .T. ) ;
#15585=DIRECTION ( 'NONE',  ( 0.000000000000000000, 0.000000000000000000, 1.000000000000000000 ) ) ;
#15586=ORIENTED_EDGE ( 'NONE', *, *, #17236, .T. ) ;
#15590=CARTESIAN_POINT ( 'NONE',  ( 8.772402711158880706, 78.01830691709993459, 10.26166134156747489 ) ) ;
#15591=CARTESIAN_POINT ( 'NONE',  ( -6.840445147067528708, 59.42702751003819372, 11.64074063870059383 ) ) ;
#15593=CARTESIAN_POINT ( 'NONE',  ( 8.523150694292391805, 72.00656199573694494, 10.47221625061583516 ) ) ;
#15595=CARTESIAN_POINT ( 'NONE',  ( -13.50000000000000000, 52.92999999999999972, -3.306546357697853733E-15 ) ) ;
#15596=CARTESIAN_POINT ( 'NONE',  ( -8.465209700148607297, 52.50397567740490246, -10.51791672388853094 ) ) ;
#15599=CARTESIAN_POINT ( 'NONE',  ( -8.863294625709455588, 68.33741696991182835, 10.18396718458916972 ) ) ;
#15601=EDGE_CURVE ( 'NONE', #11076, #3534, #922, .T. ) ;
#15604=CARTESIAN_POINT ( 'NONE',  ( -9.115263935278322904, 65.32561837914103364, 9.970196421953582799 ) ) ;
#15607=VERTEX_POINT ( 'NONE', #2448 ) ;
#15609=DIRECTION ( 'NONE',  ( 0.000000000000000000, -1.000000000000000000, 0.000000000000000000 ) ) ;
#15610=CARTESIAN_POINT ( 'NONE',  ( -13.46321216429749157, 31.89554233233273806, -0.9972219699559256023 ) ) ;
#15611=CARTESIAN_POINT ( 'NONE',  ( 0.3528712558444254688, 74.69265864786574127, 13.50000000000789058 ) ) ;
#15612=CARTESIAN_POINT ( 'NONE',  ( 13.49937490039810584, 60.43467020298844261, -0.1363635455224274373 ) ) ;
#15613=DIRECTION ( 'NONE',  ( 0.000000000000000000, -1.000000000000000000, 0.000000000000000000 ) ) ;
#15614=CARTESIAN_POINT ( 'NONE',  ( -4.171729424061791036, 76.53000000000000114, 12.83926296998457239 ) ) ;
#15615=CARTESIAN_POINT ( 'NONE',  ( 13.33928347952357107, 51.50486127415317839, -2.136916482695208064 ) ) ;
#15616=CARTESIAN_POINT ( 'NONE',  ( -13.26014386489534047, 38.01975955159114307, 2.545164025099730054 ) ) ;
#15618=CARTESIAN_POINT ( 'NONE',  ( 10.97833218139325773, 36.72688691708130904, -7.868713784374241627 ) ) ;
#15621=CARTESIAN_POINT ( 'NONE',  ( -10.50862198025424554, 77.25342995615731922, 8.475325434927029278 ) ) ;
#15622=CARTESIAN_POINT ( 'NONE',  ( 0.4611952739691489445, 62.69658252224193262, 13.49219369441274630 ) ) ;
#15623=CARTESIAN_POINT ( 'NONE',  ( 5.443441962766892850, 41.87725101519070137, 12.35390569854847698 ) ) ;
#15624=CARTESIAN_POINT ( 'NONE',  ( 12.65354452320541512, 48.60108511608657267, -4.726175205520251055 ) ) ;
#15627=CARTESIAN_POINT ( 'NONE',  ( 3.636496289402154414, 60.82999999999999829, 11.19198476289190936 ) ) ;
#15632=CARTESIAN_POINT ( 'NONE',  ( -11.42802927807712443, 80.93000000000000682, -3.799729825766118285 ) ) ;
#15634=CARTESIAN_POINT ( 'NONE',  ( 3.089967991614102516, 65.79111338089974481, 13.14161812284216246 ) ) ;
#15635=CARTESIAN_POINT ( 'NONE',  ( -8.691771469529815392E-16, 77.68000000000000682, 14.19474002721660355 ) ) ;
#15636=CARTESIAN_POINT ( 'NONE',  ( 7.272992578804308828, 48.97999999999999687, 10.01041549318726709 ) ) ;
#15638=CARTESIAN_POINT ( 'NONE',  ( -13.17315977348318157, 59.03476960960914255, 2.955331265607194613 ) ) ;
#15639=CARTESIAN_POINT ( 'NONE',  ( 11.08286227684556380, 45.13930327551472743, 7.713911292983588908 ) ) ;
#15642=CARTESIAN_POINT ( 'NONE',  ( 13.13090800037537953, 30.54142882776130463, -3.138511609109995160 ) ) ;
#15643=CARTESIAN_POINT ( 'NONE',  ( -13.46562334750894330, 55.89667962494186781, -0.9653598001017119623 ) ) ;
#15644=CARTESIAN_POINT ( 'NONE',  ( -13.50529896843892708, 49.92984903237493199, 0.0002717946928634594841 ) ) ;
#15645=CARTESIAN_POINT ( 'NONE',  ( 5.792892470351891809, 63.96933600290971356, -12.19546835734017876 ) ) ;
#15646=CARTESIAN_POINT ( 'NONE',  ( 4.234016314587428553, 43.02776078768052059, -12.81889670191663377 ) ) ;
#15647=CARTESIAN_POINT ( 'NONE',  ( 13.35753582573685350, 39.50047908224951243, -2.013713484790881303 ) ) ;
#15648=ORIENTED_EDGE ( 'NONE', *, *, #381, .T. ) ;
#15649=CARTESIAN_POINT ( 'NONE',  ( -10.10386100637092888, 61.58468400106026053, -8.953342810708111443 ) ) ;
#15655=CARTESIAN_POINT ( 'NONE',  ( 12.85888199276385890, 48.28223875469849702, 4.113822437287173450 ) ) ;
#15656=CARTESIAN_POINT ( 'NONE',  ( 3.747811303784765791, 58.04554623404083458, -12.97209066736199645 ) ) ;
#15657=CARTESIAN_POINT ( 'NONE',  ( 2.222695906433310942, 79.10008801533618339, -13.31607093855053314 ) ) ;
#15659=CARTESIAN_POINT ( 'NONE',  ( 3.636496289402154414, 81.82999999999999829, 11.19198476289190936 ) ) ;
#15660=CARTESIAN_POINT ( 'NONE',  ( 13.50000000000000000, 41.42999999999999972, 1.653273178848926867E-15 ) ) ;
#15661=CARTESIAN_POINT ( 'NONE',  ( 11.76794919243112680, 82.58000000000001251, -3.823638476888993942 ) ) ;
#15663=CARTESIAN_POINT ( 'NONE',  ( 4.171729424061791924, 42.03000000000000114, -12.83926296998457239 ) ) ;
#15664=CARTESIAN_POINT ( 'NONE',  ( -12.50000000000000000, 98.93000000000002103, 1.224646799147353059E-15 ) ) ;
#15666=AXIS2_PLACEMENT_3D ( 'NONE', #2803, #17229, #5672 ) ;
#15669=ORIENTED_EDGE ( 'NONE', *, *, #15463, .F. ) ;
#15674=CARTESIAN_POINT ( 'NONE',  ( 1.443355482025400649, 77.73190779979329079, 13.42308081186049051 ) ) ;
#15675=CARTESIAN_POINT ( 'NONE',  ( -0.1955871059449479643, 59.67296629411183773, 13.49897230917331292 ) ) ;
#15676=CARTESIAN_POINT ( 'NONE',  ( 7.499999999999998224, 108.9300000000000068, 9.367496997597600128 ) ) ;
#15680=CARTESIAN_POINT ( 'NONE',  ( -8.691771469529815392E-16, 50.67999999999999261, 14.19474002721660355 ) ) ;
#15681=CARTESIAN_POINT ( 'NONE',  ( -4.315607089656920081, 71.52482252390403517, 12.79169210638634624 ) ) ;
#15685=CARTESIAN_POINT ( 'NONE',  ( -3.364692565120436463, 68.55914111881094186, 13.08348558152368746 ) ) ;
#15687=CARTESIAN_POINT ( 'NONE',  ( 4.349022827738643571, 55.02346064057928032, -12.78217124321885478 ) ) ;
#15690=CARTESIAN_POINT ( 'NONE',  ( -8.551869864207160887, 65.35210363059799477, 10.44874323309726272 ) ) ;
#15691=CYLINDRICAL_SURFACE ( 'NONE', #13523, 13.50000000000000000 ) ;
#15692=CARTESIAN_POINT ( 'NONE',  ( -3.309329455300976441, 35.56117355828821047, 13.09820044315392629 ) ) ;
#15694=CARTESIAN_POINT ( 'NONE',  ( 9.520470885617715595, 31.12999999999999901, 6.917026985038134512 ) ) ;
#15696=CARTESIAN_POINT ( 'NONE',  ( -4.945118968609875765, 40.35832260886622436, -12.56369513011831174 ) ) ;
#15697=CARTESIAN_POINT ( 'NONE',  ( -11.82971441149514469, 31.68901184113946812, -6.504453626418047918 ) ) ;
#15699=CARTESIAN_POINT ( 'NONE',  ( 10.65864953284609129, 60.11494968480803891, 8.285120799684273507 ) ) ;
#15700=EDGE_CURVE ( 'NONE', #7488, #10745, #3073, .T. ) ;
#15704=CARTESIAN_POINT ( 'NONE',  ( -3.636496289402153081, 62.32999999999999829, -11.19198476289190936 ) ) ;
#15705=CARTESIAN_POINT ( 'NONE',  ( 10.92172942406179104, 71.73000000000000398, -7.935100905948385908 ) ) ;
#15706=CARTESIAN_POINT ( 'NONE',  ( 13.40485122747304914, 51.37422532693715027, 1.600017051684848202 ) ) ;
#15707=( BOUNDED_CURVE ( )  B_SPLINE_CURVE ( 2, ( #14928, #1676, #101, #2820, #4434, #12298, #8249, #192, #5597, #10978, #16349, #4255, #9664 ),
 .UNSPECIFIED., .F., .F. ) 
 B_SPLINE_CURVE_WITH_KNOTS ( ( 3, 2, 2, 2, 2, 2, 3 ),
 ( 0.4861111111111111049, 0.4888888888888888729, 0.4944444444444444642, 0.5000000000000000000, 0.5055555555555555358, 0.5111111111111110716, 0.5138888888888888395 ),
 .UNSPECIFIED. ) 
 CURVE ( )  GEOMETRIC_REPRESENTATION_ITEM ( )  RATIONAL_B_SPLINE_CURVE ( ( 0.9755282581475768211, 0.9755282581475768211, 1.000000000000000000, 0.9510565162951535312, 1.000000000000000000, 0.9510565162951535312, 1.000000000000000000, 0.9510565162951535312, 1.000000000000000000, 0.9510565162951535312, 1.000000000000000000, 0.9755282581475772652, 0.9755282581475768211 ) ) 
 REPRESENTATION_ITEM ( '' )  );
#15708=CARTESIAN_POINT ( 'NONE',  ( -13.47842577702374278, 37.96032382249477877, 0.8798576433466377411 ) ) ;
#15709=CARTESIAN_POINT ( 'NONE',  ( 13.17094745865578709, 36.53536659866002623, -2.974084169080610796 ) ) ;
#15711=CARTESIAN_POINT ( 'NONE',  ( -5.620096583852075334, 74.47603443507840382, 12.27847533565288884 ) ) ;
#15712=CARTESIAN_POINT ( 'NONE',  ( -3.551554394246068558, 77.55229557867063761, 13.02528201803605512 ) ) ;
#15713=CARTESIAN_POINT ( 'NONE',  ( -10.92172942406178926, 60.63000000000000256, -7.935100905948389460 ) ) ;
#15714=CARTESIAN_POINT ( 'NONE',  ( 7.500000000000000888, 102.9300000000000068, -9.367496997597600128 ) ) ;
#15718=CARTESIAN_POINT ( 'NONE',  ( 11.76794919243112325, 58.28000000000000114, 3.823638476888997051 ) ) ;
#15720=CARTESIAN_POINT ( 'NONE',  ( 12.50000000000000000, 102.9300000000000210, 1.714505518806294638E-15 ) ) ;
#15721=CARTESIAN_POINT ( 'NONE',  ( 6.659136588377341681, 75.93459917958982430, -11.75290894059296853 ) ) ;
#15725=CARTESIAN_POINT ( 'NONE',  ( -7.272992578804310604, 48.38000000000000256, 10.01041549318726709 ) ) ;
#15727=CARTESIAN_POINT ( 'NONE',  ( -13.45261086486871172, 58.96929453956708045, 1.133742953798396291 ) ) ;
#15728=CARTESIAN_POINT ( 'NONE',  ( 11.63529875998058927, 45.17511335439066045, 6.848266737798307524 ) ) ;
#15729=CARTESIAN_POINT ( 'NONE',  ( 12.82150868624539086, 69.27794690079218753, 4.225997539185415874 ) ) ;
#15731=CARTESIAN_POINT ( 'NONE',  ( 12.09037112244008405, 30.65106581466645608, -6.006992855518931584 ) ) ;
#15732=CARTESIAN_POINT ( 'NONE',  ( -9.995403852311815385, 55.57895733551523421, -9.074982918291022216 ) ) ;
#15733=CARTESIAN_POINT ( 'NONE',  ( -11.01017756159927785, 50.22480640622728032, 7.811931653475178372 ) ) ;
#15734=CARTESIAN_POINT ( 'NONE',  ( 5.199860282695291325, 63.99191061641860756, -12.45850863233871486 ) ) ;
#15736=CARTESIAN_POINT ( 'NONE',  ( 13.31623920422783591, 39.35204567939386777, 2.219880403359409282 ) ) ;
#15737=ORIENTED_EDGE ( 'NONE', *, *, #7763, .F. ) ;
#15738=CARTESIAN_POINT ( 'NONE',  ( -10.11420833265737507, 70.58488754181632885, -8.944704958495304226 ) ) ;
#15739=CARTESIAN_POINT ( 'NONE',  ( -4.072279632042837605, 61.32642407186975930, -12.87115663778308061 ) ) ;
#15742=CARTESIAN_POINT ( 'NONE',  ( -11.83065338684570911, 40.68906663066565699, -6.503147009567541659 ) ) ;
#15746=CARTESIAN_POINT ( 'NONE',  ( 2.636929751653812382, 47.77487479848526419, 13.24312322384484020 ) ) ;
#15748=CARTESIAN_POINT ( 'NONE',  ( 7.843744172734761655, 57.88406826092607815, -10.98845944672378394 ) ) ;
#15749=CARTESIAN_POINT ( 'NONE',  ( 12.19393943590524998, 78.64260903952070692, -5.792913002744612960 ) ) ;
#15750=CARTESIAN_POINT ( 'NONE',  ( 7.272992578804311492, 82.87999999999999545, -10.01041549318726709 ) ) ;
#15755=CARTESIAN_POINT ( 'NONE',  ( -0.06858017979864573788, 67.18246588477448711, -13.49985044511317334 ) ) ;
#15757=CARTESIAN_POINT ( 'NONE',  ( 13.50000000000000355, 44.57999999999999829, -4.386415899144233244 ) ) ;
#15758=CARTESIAN_POINT ( 'NONE',  ( 0.5908221627133811715, 34.15875621469567847, -13.50000000000000355 ) ) ;
#15759=CARTESIAN_POINT ( 'NONE',  ( -13.50303335837387309, 73.92924155917964413, -0.01907866586608939624 ) ) ;
#15761=DIRECTION ( 'NONE',  ( 1.000000000000000000, 0.000000000000000000, 0.000000000000000000 ) ) ;
#15767=CARTESIAN_POINT ( 'NONE',  ( -7.298493437496628822, 59.40772321095889907, 11.35718403328393755 ) ) ;
#15768=DIRECTION ( 'NONE',  ( 0.000000000000000000, 1.000000000000000000, 0.000000000000000000 ) ) ;
#15769=DIRECTION ( 'NONE',  ( 1.000000000000000000, -0.000000000000000000, 1.224646799147353207E-16 ) ) ;
#15770=CARTESIAN_POINT ( 'NONE',  ( -13.49999999999999822, 52.77999999999998693, -4.386415899144240349 ) ) ;
#15771=CARTESIAN_POINT ( 'NONE',  ( -3.576470617035913513, 71.55150969693022489, 13.02043708789197218 ) ) ;
#15774=CARTESIAN_POINT ( 'NONE',  ( -5.119445439576221446, 68.49501675060221828, 12.49523006263062008 ) ) ;
#15776=CARTESIAN_POINT ( 'NONE',  ( 6.029514697490034436, 54.95989846906334009, -12.07890518949519709 ) ) ;
#15780=CARTESIAN_POINT ( 'NONE',  ( -2.542243399751729083, 65.58859028378583389, 13.25847602317422869 ) ) ;
#15781=FACE_OUTER_BOUND ( 'NONE', #13620, .T. ) ;
#15782=AXIS2_PLACEMENT_3D ( 'NONE', #843, #15503, #2243 ) ;
#15783=CARTESIAN_POINT ( 'NONE',  ( -10.44753565030824305, 35.25738875665259542, 8.561908802029048360 ) ) ;
#15788=CARTESIAN_POINT ( 'NONE',  ( -1.117267249152343211, 40.22013350474495752, -13.46142176141221114 ) ) ;
#15789=CARTESIAN_POINT ( 'NONE',  ( -12.64316203278966455, 32.10137934669921833, 4.733190063705147388 ) ) ;
#15791=CARTESIAN_POINT ( 'NONE',  ( 10.70269728238857532, 60.11743682513120035, 8.228172719481563036 ) ) ;
#15793=CARTESIAN_POINT ( 'NONE',  ( -10.56096607446065683, 53.25065828476769525, 8.412065287595915208 ) ) ;
#15794=CARTESIAN_POINT ( 'NONE',  ( 7.272992578804311492, 55.87999999999998835, -10.01041549318726709 ) ) ;
#15795=CARTESIAN_POINT ( 'NONE',  ( -8.343458848123576743, 75.48000000000001819, -11.48378591275254301 ) ) ;
#15796=CARTESIAN_POINT ( 'NONE',  ( 13.48614702091186679, 51.45107933675966905, -0.6119089703848084039 ) ) ;
#15797=CARTESIAN_POINT ( 'NONE',  ( -8.740153168478604684, 38.34338314764683275, 10.29122014725719758 ) ) ;
#15799=CARTESIAN_POINT ( 'NONE',  ( 10.35803651828807048, 36.76167587533018377, -8.658012760942717989 ) ) ;
#15801=EDGE_CURVE ( 'NONE', #10721, #3211, #16782, .T. ) ;
#15802=CARTESIAN_POINT ( 'NONE',  ( -5.011838315114361286, 74.49902066430979630, 12.53603190239770271 ) ) ;
#15803=CARTESIAN_POINT ( 'NONE',  ( -10.15729662139356471, 77.27267320848328325, 8.903693602875414115 ) ) ;
#15804=CARTESIAN_POINT ( 'NONE',  ( -6.538465195716074874, 80.43943283378160913, 11.81155471837914384 ) ) ;
#15805=DIRECTION ( 'NONE',  ( 0.000000000000000000, 1.000000000000000000, 0.000000000000000000 ) ) ;
#15806=ORIENTED_EDGE ( 'NONE', *, *, #14287, .F. ) ;
#15808=ORIENTED_EDGE ( 'NONE', *, *, #5942, .F. ) ;
#15809=CARTESIAN_POINT ( 'NONE',  ( 3.636496289402154414, 57.82999999999999829, 11.19198476289190936 ) ) ;
#15811=CYLINDRICAL_SURFACE ( 'NONE', #3717, 13.50000000000000000 ) ;
#15813=CARTESIAN_POINT ( 'NONE',  ( 3.698094387297103047, 76.04702867827543855, -12.98363822668122758 ) ) ;
#15814=CARTESIAN_POINT ( 'NONE',  ( 10.92172942406178926, 32.12999999999999545, 7.935100905948387684 ) ) ;
#15815=CARTESIAN_POINT ( 'NONE',  ( -10.92172942406179104, 77.23000000000000398, 7.935100905948387684 ) ) ;
#15817=CARTESIAN_POINT ( 'NONE',  ( 11.76794919243112325, 43.42999999999999972, 1.441158131103945434E-15 ) ) ;
#15819=CARTESIAN_POINT ( 'NONE',  ( -13.46128659113321113, 58.89463545154691104, -1.023806176390480438 ) ) ;
#15820=CARTESIAN_POINT ( 'NONE',  ( 12.94169128974424510, 45.29239941246957812, 3.842414863143926329 ) ) ;
#15821=CARTESIAN_POINT ( 'NONE',  ( 12.14869877942370735, 69.64635006548208196, -5.889954931317291198 ) ) ;
#15822=CARTESIAN_POINT ( 'NONE',  ( -10.92172942406179104, 67.23000000000000398, 7.935100905948387684 ) ) ;
#15823=CARTESIAN_POINT ( 'NONE',  ( 12.09463382724336000, 30.20907098269022484, 6.000288655847534791 ) ) ;
#15824=CARTESIAN_POINT ( 'NONE',  ( -7.477981820817456438, 55.45997926997171845, -11.23979076186452453 ) ) ;
#15826=CARTESIAN_POINT ( 'NONE',  ( -10.19986417753999142, 50.27059177842374993, 8.854060500917482202 ) ) ;
#15827=CARTESIAN_POINT ( 'NONE',  ( 7.977012331873297946, 63.87814718858143692, -10.89160525889778519 ) ) ;
#15828=CARTESIAN_POINT ( 'NONE',  ( 10.25680675266404585, 42.76715089671812819, -8.777717763810738205 ) ) ;
#15829=CARTESIAN_POINT ( 'NONE',  ( 12.47371269042021780, 39.24203742358702840, 5.163095893957874161 ) ) ;
#15831=CARTESIAN_POINT ( 'NONE',  ( -7.882982835668106425, 70.47768290884718567, -10.95958355943866991 ) ) ;
#15832=CARTESIAN_POINT ( 'NONE',  ( -11.20375019216649903, 61.64692594173555307, -7.531763781615398834 ) ) ;
#15835=CARTESIAN_POINT ( 'NONE',  ( -6.490606702026376240, 40.41856083592690396, -11.84311563964773306 ) ) ;
#15836=EDGE_LOOP ( 'NONE', ( #9891, #12830, #4109, #1101 ) ) ;
#15839=CARTESIAN_POINT ( 'NONE',  ( -5.281055406448098636E-10, 61.18000001472334759, -13.50000000000000000 ) ) ;
#15840=CARTESIAN_POINT ( 'NONE',  ( 13.49150116428843837, 57.44702109627492348, -0.4955463281862768077 ) ) ;
#15841=CARTESIAN_POINT ( 'NONE',  ( 7.272992578804311492, 76.88000000000000966, -10.01041549318726709 ) ) ;
#15842=CARTESIAN_POINT ( 'NONE',  ( 3.636496289402157078, 80.03000000000000114, -11.19198476289190936 ) ) ;
#15843=AXIS2_PLACEMENT_3D ( 'NONE', #15289, #8612, #6213 ) ;
#15844=CARTESIAN_POINT ( 'NONE',  ( -0.3356469398848770380, 47.66793158906188665, 13.49583837495916505 ) ) ;
#15848=ADVANCED_FACE ( 'NONE', ( #521 ), #8586, .T. ) ;
#15849=CARTESIAN_POINT ( 'NONE',  ( 13.49999999999999822, 44.27999999999999403, 4.386415899144236796 ) ) ;
#15850=CARTESIAN_POINT ( 'NONE',  ( 7.682691750080786086, 33.89118886932563157, -11.10494913091865143 ) ) ;
#15851=CARTESIAN_POINT ( 'NONE',  ( -2.307751883485523514, 73.26297825885289683, -13.30128957637999321 ) ) ;
#15852=VERTEX_POINT ( 'NONE', #10000 ) ;
#15853=ORIENTED_EDGE ( 'NONE', *, *, #16431, .T. ) ;
#15854=CARTESIAN_POINT ( 'NONE',  ( 3.636496289402154414, 75.83000000000001251, 11.19198476289190936 ) ) ;
#15855=ORIENTED_EDGE ( 'NONE', *, *, #6829, .F. ) ;
#15859=CARTESIAN_POINT ( 'NONE',  ( -7.427281423385845294, 44.40220115185869076, 11.27323933198727346 ) ) ;
#15861=CARTESIAN_POINT ( 'NONE',  ( 11.67414954186575926, 66.68222205810447178, -6.779902939383848803 ) ) ;
#15862=CARTESIAN_POINT ( 'NONE',  ( -10.92172942406179104, 50.22999999999999687, 7.935100905948387684 ) ) ;
#15863=CARTESIAN_POINT ( 'NONE',  ( -8.195680094490986889, 71.36831669863111927, 10.72758201758851548 ) ) ;
#15866=CARTESIAN_POINT ( 'NONE',  ( -13.21120980875378059, 68.02931360559055918, 2.809030978660246536 ) ) ;
#15868=CARTESIAN_POINT ( 'NONE',  ( 8.760382117191685580, 54.84251356804755773, -10.27401743239077803 ) ) ;
#15871=CARTESIAN_POINT ( 'NONE',  ( -11.50829892323420012, 65.19348115225962204, 7.057553676268226717 ) ) ;
#15872=CARTESIAN_POINT ( 'NONE',  ( -1.703947211885682211, 62.61875151748889579, 13.39354096409387118 ) ) ;
#15873=CARTESIAN_POINT ( 'NONE',  ( -11.31049946513870275, 35.20637627411365855, 7.370616573443121489 ) ) ;
#15877=CARTESIAN_POINT ( 'NONE',  ( -13.45890448833404207, 31.89355665744642820, -1.054546249422317450 ) ) ;
#15878=DIRECTION ( 'NONE',  ( -0.000000000000000000, -1.000000000000000000, -0.000000000000000000 ) ) ;
#15879=CARTESIAN_POINT ( 'NONE',  ( 11.08453223446139368, 60.13957240781945046, 7.713806355306156881 ) ) ;
#15880=CARTESIAN_POINT ( 'NONE',  ( -3.154868868512232361, 53.56660037773436045, 13.12768685552039472 ) ) ;
#15881=EDGE_CURVE ( 'NONE', #10678, #10403, #12222, .T. ) ;
#15882=CARTESIAN_POINT ( 'NONE',  ( -7.272992578804310604, 57.37999999999998835, 10.01041549318726709 ) ) ;
#15883=CARTESIAN_POINT ( 'NONE',  ( 13.50000000000000000, 74.42999999999999261, 1.653273178848926867E-15 ) ) ;
#15884=CARTESIAN_POINT ( 'NONE',  ( 6.847475264325973754, 50.93311729376924291, 11.64706806883375734 ) ) ;
#15885=CARTESIAN_POINT ( 'NONE',  ( -11.21746825162109751, 38.21221880008548766, 7.511220640065156218 ) ) ;
#15886=CARTESIAN_POINT ( 'NONE',  ( 11.29157302505232430, 36.70761492676916049, -7.399503251687141514 ) ) ;
#15889=CARTESIAN_POINT ( 'NONE',  ( -12.15072432148234327, 77.14617109779081261, 5.883034232685984577 ) ) ;
#15890=CARTESIAN_POINT ( 'NONE',  ( -7.867136275643527021, 80.38330200039787599, 10.97981010490558695 ) ) ;
#15892=CARTESIAN_POINT ( 'NONE',  ( 7.500000000000000000, 106.0143933292129361, 8.253836299850743075 ) ) ;
#15893=EDGE_LOOP ( 'NONE', ( #5645, #14438, #7490, #5463, #5169, #4021 ) ) ;
#15897=CARTESIAN_POINT ( 'NONE',  ( -7.272992578804307939, 56.47999999999998977, -10.01041549318727064 ) ) ;
#15900=CARTESIAN_POINT ( 'NONE',  ( 6.254386305572761096, 75.95091365744046641, -11.96381775906021794 ) ) ;
#15901=CARTESIAN_POINT ( 'NONE',  ( 10.92172942406179104, 32.72999999999999687, -7.935100905948385908 ) ) ;
#15902=CARTESIAN_POINT ( 'NONE',  ( 10.92172942406179104, 72.73000000000000398, -7.935100905948385908 ) ) ;
#15903=CARTESIAN_POINT ( 'NONE',  ( 7.272992578804311492, 40.87999999999998835, -10.01041549318726709 ) ) ;
#15905=CARTESIAN_POINT ( 'NONE',  ( -10.88971337417516949, 59.23191255126531729, 7.979255671233033809 ) ) ;
#15906=CARTESIAN_POINT ( 'NONE',  ( 7.730634896388627553, 44.97100470643064796, 11.07641855958759969 ) ) ;
#15907=CARTESIAN_POINT ( 'NONE',  ( 12.81778580762176922, 69.27751987638765740, 4.237276121753580149 ) ) ;
#15908=CARTESIAN_POINT ( 'NONE',  ( -13.49999999999999822, 67.07999999999999829, 4.386415899144235020 ) ) ;
#15910=CARTESIAN_POINT ( 'NONE',  ( -10.09420973937047172, 55.58417831355667715, -8.964204995116103802 ) ) ;
#15911=CARTESIAN_POINT ( 'NONE',  ( -11.02125367826103997, 50.22414744263306829, 7.796281688550792843 ) ) ;
#15912=CARTESIAN_POINT ( 'NONE',  ( 2.375566496671534189, 64.09458955305812822, -13.29290925995572792 ) ) ;
#15913=CARTESIAN_POINT ( 'NONE',  ( 11.92353461362217537, 42.66400819043492021, -6.330823637012009009 ) ) ;
#15914=CARTESIAN_POINT ( 'NONE',  ( 12.51114643976912433, 39.24558153982501807, 5.071609117201407280 ) ) ;
#15916=CARTESIAN_POINT ( 'NONE',  ( -5.474767670627016081, 70.37845246078859418, -12.34033127765731486 ) ) ;
#15917=CARTESIAN_POINT ( 'NONE',  ( -11.14440460645358577, 61.64327494009675235, -7.619238717130787819 ) ) ;
#15920=AXIS2_PLACEMENT_3D ( 'NONE', #763, #4831, #14353 ) ;
#15924=CARTESIAN_POINT ( 'NONE',  ( 3.064866251608231007, 61.06979871462648646, -13.14749468302701807 ) ) ;
#15925=CARTESIAN_POINT ( 'NONE',  ( 13.32344742245652292, 57.50688615378314950, -2.187503503881035538 ) ) ;
#15926=CARTESIAN_POINT ( 'NONE',  ( 3.636496289402154414, 69.82999999999999829, 11.19198476289190936 ) ) ;
#15928=CARTESIAN_POINT ( 'NONE',  ( -3.636496289402155746, 78.53000000000000114, 11.19198476289190936 ) ) ;
#15932=CARTESIAN_POINT ( 'NONE',  ( -13.49999999999999822, 34.07999999999999829, 4.386415899144235020 ) ) ;
#15935=CARTESIAN_POINT ( 'NONE',  ( 4.429208140063253474, 34.02068188122268566, -12.75274710002904399 ) ) ;
#15936=CARTESIAN_POINT ( 'NONE',  ( -7.570064420617500289, 73.46396487899353644, -11.17798062459965358 ) ) ;
#15939=CARTESIAN_POINT ( 'NONE',  ( -3.636496289402153081, 74.33000000000001251, -11.19198476289190936 ) ) ;
#15942=CARTESIAN_POINT ( 'NONE',  ( -7.365732241337891395, 44.40484326663887771, 11.31354391936344506 ) ) ;
#15944=CARTESIAN_POINT ( 'NONE',  ( 9.418294590293729840, 66.81060122333079221, -9.677908191170031316 ) ) ;
#15945=CARTESIAN_POINT ( 'NONE',  ( 8.343458848123578520, 44.97999999999998977, 11.48378591275254124 ) ) ;
#15946=CARTESIAN_POINT ( 'NONE',  ( -4.476370017849513161, 71.51896129429336213, 12.73625716771306671 ) ) ;
#15947=ADVANCED_FACE ( 'NONE', ( #2003 ), #6018, .T. ) ;
#15949=AXIS2_PLACEMENT_3D ( 'NONE', #6342, #11728, #3677 ) ;
#15951=CARTESIAN_POINT ( 'NONE',  ( -12.89419414780135931, 68.07351481693184780, 3.999877596732322349 ) ) ;
#15953=CARTESIAN_POINT ( 'NONE',  ( 3.511521273362200546, 55.05373854301420522, -13.03714384340177368 ) ) ;
#15955=CARTESIAN_POINT ( 'NONE',  ( -13.38752141559960762, 64.99072630046104848, 1.739259147947423978 ) ) ;
#15957=CARTESIAN_POINT ( 'NONE',  ( -2.073600124454130000, 35.60538353478859364, 13.34095837325122069 ) ) ;
#15960=CARTESIAN_POINT ( 'NONE',  ( 10.92172942406179104, 50.72999999999999687, -7.935100905948385908 ) ) ;
#15961=VECTOR ( 'NONE', #12296, 1000.000000000000000 ) ;
#15963=CARTESIAN_POINT ( 'NONE',  ( -4.129380727326757317, 31.32847731590642582, -12.85304772793163863 ) ) ;
#15964=CYLINDRICAL_SURFACE ( 'NONE', #7974, 13.50000000000000000 ) ;
#15966=CARTESIAN_POINT ( 'NONE',  ( 12.86781002116635442, 60.28328535326944149, 4.085762581384763337 ) ) ;
#15968=CARTESIAN_POINT ( 'NONE',  ( -11.04090545666283774, 53.22297625534304188, 7.768428304626336711 ) ) ;
#15970=CARTESIAN_POINT ( 'NONE',  ( 7.272992578804308828, 60.97999999999999687, 10.01041549318726709 ) ) ;
#15972=CARTESIAN_POINT ( 'NONE',  ( 8.462697274394789915, 51.00384814321047600, 10.51912736017751904 ) ) ;
#15973=CARTESIAN_POINT ( 'NONE',  ( -10.98001549286353296, 37.63278772585531584, -7.866452531253198543 ) ) ;
#15974=CARTESIAN_POINT ( 'NONE',  ( 11.06150406454992030, 36.13825259647077814, 7.739128912404242833 ) ) ;
#15976=CARTESIAN_POINT ( 'NONE',  ( -5.241819211398198064, 74.49045729122398996, 12.44079554077151961 ) ) ;
#15977=CARTESIAN_POINT ( 'NONE',  ( -12.53157464354551287, 76.74754124118879872, -5.020938431400466584 ) ) ;
#15978=CARTESIAN_POINT ( 'NONE',  ( -12.29521383468573958, 79.72576744650467617, -5.579058808064132791 ) ) ;
#15980=CARTESIAN_POINT ( 'NONE',  ( 7.500000000000001776, 108.4800942032927509, 3.560038493048083730 ) ) ;
#15981=LINE ( 'NONE', #3884, #13140 ) ;
#15983=CARTESIAN_POINT ( 'NONE',  ( 7.272992578804308828, 57.97999999999999687, 10.01041549318726886 ) ) ;
#15986=CARTESIAN_POINT ( 'NONE',  ( 6.750022862106053623, 29.92926176209967437, 11.69132975161703669 ) ) ;
#15987=CARTESIAN_POINT ( 'NONE',  ( 7.265447703103709465, 75.90908602052756748, -11.38066394550858185 ) ) ;
#15989=CARTESIAN_POINT ( 'NONE',  ( -9.520470885617717371, 39.23000000000000398, 6.917026985038133624 ) ) ;
#15991=CARTESIAN_POINT ( 'NONE',  ( -11.19072645572614100, 58.64612364100203479, -7.551004225710134854 ) ) ;
#15992=CARTESIAN_POINT ( 'NONE',  ( 2.917162700404270836, 44.78489042209035631, 13.18105316755035439 ) ) ;
#15993=CARTESIAN_POINT ( 'NONE',  ( 10.15949134898925088, 69.77235859015937081, -8.890162730232345822 ) ) ;
#15994=CARTESIAN_POINT ( 'NONE',  ( 2.445080149700053643E-15, 54.17999999999999972, -13.50000000000000000 ) ) ;
#15995=CARTESIAN_POINT ( 'NONE',  ( 9.329993715843995616, 30.04517432730955662, 9.757520963080287046 ) ) ;
#15996=CARTESIAN_POINT ( 'NONE',  ( -4.170360066879259087, 55.32995151900944819, -12.83978663759837069 ) ) ;
#15997=CARTESIAN_POINT ( 'NONE',  ( -6.254757922007740945, 50.45086428866937922, 11.96761786975087105 ) ) ;
#15998=CARTESIAN_POINT ( 'NONE',  ( 9.869871377105818411, 63.78755568821424760, -9.210636547543993302 ) ) ;
#15999=CARTESIAN_POINT ( 'NONE',  ( 12.13036376994949350, 42.64785262807090049, -5.926645582322720429 ) ) ;
#16000=CARTESIAN_POINT ( 'NONE',  ( 10.97791377685320668, 39.13320314606657746, 7.859089960518745421 ) ) ;
#16002=CARTESIAN_POINT ( 'NONE',  ( -13.20903748930417976, 70.83043373285759969, -2.815464265785562414 ) ) ;
#16009=CARTESIAN_POINT ( 'NONE',  ( 3.306959159702415718, 47.79891067118984438, 13.08869937906687397 ) ) ;
#16011=CARTESIAN_POINT ( 'NONE',  ( 9.778897066067186117, 72.06775799895999057, 9.307158233501985123 ) ) ;
#16012=CARTESIAN_POINT ( 'NONE',  ( 12.46723268277846053, 57.24143407219609969, 5.178624223398916371 ) ) ;
#16013=CARTESIAN_POINT ( 'NONE',  ( -11.76794919243112325, 72.07999999999999829, 3.823638476888994386 ) ) ;
#16014=CARTESIAN_POINT ( 'NONE',  ( 7.272992578804308828, 78.97999999999998977, 10.01041549318726709 ) ) ;
#16015=CARTESIAN_POINT ( 'NONE',  ( -3.824707916743821379, 47.54247761955691942, 12.94687856268078896 ) ) ;
#16020=LINE ( 'NONE', #14517, #16266 ) ;
#16021=CARTESIAN_POINT ( 'NONE',  ( 11.26022822739175844, 33.70954470917394730, -7.446967326473597382 ) ) ;
#16022=CARTESIAN_POINT ( 'NONE',  ( -2.238595305369822430, 73.26049135710265148, -13.31312577019137322 ) ) ;
#16026=CARTESIAN_POINT ( 'NONE',  ( 11.76794919243112325, 73.27999999999998693, 3.823638476888997051 ) ) ;
#16027=VERTEX_POINT ( 'NONE', #12809 ) ;
#16032=CARTESIAN_POINT ( 'NONE',  ( 13.50000000000000000, 45.42999999999999972, 1.653273178848926867E-15 ) ) ;
#16033=CARTESIAN_POINT ( 'NONE',  ( -5.757915664079544804, 71.47057076169542711, 12.21051929849135220 ) ) ;
#16035=CARTESIAN_POINT ( 'NONE',  ( -13.42122754482370262, 67.98067473477300382, 1.456274877649156085 ) ) ;
#16037=CARTESIAN_POINT ( 'NONE',  ( 6.362841488961052505, 54.94654819462200379, -11.90648129171133540 ) ) ;
#16038=VECTOR ( 'NONE', #6013, 1000.000000000000000 ) ;
#16041=CARTESIAN_POINT ( 'NONE',  ( -13.43293025143715980, 64.88277759376563836, -1.363649920549056427 ) ) ;
#16043=CARTESIAN_POINT ( 'NONE',  ( -5.833452229489934915, 35.46778541590376221, 12.18399501181652234 ) ) ;
#16047=CARTESIAN_POINT ( 'NONE',  ( -10.03785665333376009, 31.58129449068416150, -9.027804630255781504 ) ) ;
#16050=CARTESIAN_POINT ( 'NONE',  ( 1.279986136922147688, 59.72594881717020598, 13.44789384724496273 ) ) ;
#16052=CARTESIAN_POINT ( 'NONE',  ( -11.19291883443861657, 53.21376446446998898, 7.548464480317238490 ) ) ;
#16054=CARTESIAN_POINT ( 'NONE',  ( -3.636496289402153081, 50.32999999999999829, -11.19198476289190936 ) ) ;
#16056=CARTESIAN_POINT ( 'NONE',  ( -8.343458848123576743, 66.48000000000000398, -11.48378591275254301 ) ) ;
#16057=CARTESIAN_POINT ( 'NONE',  ( 10.67457095955382940, 51.11584628598345148, 8.264605577784157830 ) ) ;
#16058=CARTESIAN_POINT ( 'NONE',  ( -10.23347952021401674, 37.59159613339581085, -8.804879535122106304 ) ) ;
#16059=CARTESIAN_POINT ( 'NONE',  ( 11.11366064790290942, 36.14140235628833864, 7.664027378569688409 ) ) ;
#16061=CARTESIAN_POINT ( 'NONE',  ( -0.6302266402344979257, 74.65733938539632675, 13.48528206095811832 ) ) ;
#16062=CARTESIAN_POINT ( 'NONE',  ( -13.45527179458574807, 76.88938923464503716, -1.166449261855087238 ) ) ;
#16063=ADVANCED_FACE ( 'NONE', ( #1918 ), #12549, .T. ) ;
#16064=CARTESIAN_POINT ( 'NONE',  ( -10.96774680160861415, 80.22729587279039265, 7.871546463532750337 ) ) ;
#16066=CARTESIAN_POINT ( 'NONE',  ( 7.500000000000000888, 103.9506177843311860, 9.262340467025643065 ) ) ;
#16069=CARTESIAN_POINT ( 'NONE',  ( 3.636496289402157078, 47.02999999999999403, -11.19198476289190936 ) ) ;
#16073=CARTESIAN_POINT ( 'NONE',  ( 5.155428299699167383, 75.99355700656670365, -12.48322344288936314 ) ) ;
#16074=CARTESIAN_POINT ( 'NONE',  ( 4.178864255851000829E-14, 67.68000000000000682, 13.50000000000000000 ) ) ;
#16075=CARTESIAN_POINT ( 'NONE',  ( -11.76794919243112325, 35.77999999999999403, -3.823638476888998827 ) ) ;
#16076=CARTESIAN_POINT ( 'NONE',  ( -1.134839703165779312, 41.63935813733207425, 13.50000000016827606 ) ) ;
#16077=CARTESIAN_POINT ( 'NONE',  ( -8.937188087482237364, 58.52611931063565009, -10.11856336318372307 ) ) ;
#16079=LINE ( 'NONE', #13436, #15961 ) ;
#16080=DIRECTION ( 'NONE',  ( 0.000000000000000000, 1.000000000000000000, 0.000000000000000000 ) ) ;
#16081=CARTESIAN_POINT ( 'NONE',  ( -11.20803178499709851, 55.64719445998460401, -7.525311190684723428 ) ) ;
#16082=CARTESIAN_POINT ( 'NONE',  ( -13.30613126912205679, 49.84985106113156661, -2.280881810908200080 ) ) ;
#16083=CARTESIAN_POINT ( 'NONE',  ( 12.45879162498721904, 63.61962684891894781, -5.206934220104953326 ) ) ;
#16084=CARTESIAN_POINT ( 'NONE',  ( 11.08960580799031170, 42.72000896289767269, -7.699079133861338242 ) ) ;
#16085=CARTESIAN_POINT ( 'NONE',  ( 10.86487605210494145, 39.12658062121423086, 8.013745105519641143 ) ) ;
#16086=ORIENTED_EDGE ( 'NONE', *, *, #4815, .F. ) ;
#16087=CARTESIAN_POINT ( 'NONE',  ( -12.80368829784359974, 70.77590667484511755, -4.279836677223643804 ) ) ;
#16088=CARTESIAN_POINT ( 'NONE',  ( -8.343458848123582072, 49.37999999999999545, 11.48378591275253768 ) ) ;
#16090=VERTEX_POINT ( 'NONE', #14030 ) ;
#16093=CARTESIAN_POINT ( 'NONE',  ( 4.869579850628348971, 61.00451404086120988, -12.59138024303687509 ) ) ;
#16096=CARTESIAN_POINT ( 'NONE',  ( 12.00451621900212729, 57.65805921716241045, -6.182138200911872161 ) ) ;
#16097=CARTESIAN_POINT ( 'NONE',  ( 9.520470885617717371, 64.72999999999998977, -6.917026985038131848 ) ) ;
#16098=CARTESIAN_POINT ( 'NONE',  ( -7.576616670048093940E-16, 78.67999999999999261, 12.37355403259654985 ) ) ;
#16099=CARTESIAN_POINT ( 'NONE',  ( -7.090376077374727082, 47.41654259168927155, 11.48810848389221739 ) ) ;
#16100=EDGE_CURVE ( 'NONE', #8734, #11528, #1595, .T. ) ;
#16105=CARTESIAN_POINT ( 'NONE',  ( -8.343458848123578520, 39.48000000000000398, -11.48378591275254124 ) ) ;
#16106=CARTESIAN_POINT ( 'NONE',  ( 12.13600343332003817, 33.64737785006074233, -5.914467048366985225 ) ) ;
#16107=CARTESIAN_POINT ( 'NONE',  ( -9.603217289138866519, 73.55881626489666303, -9.488364816495691301 ) ) ;
#16110=CARTESIAN_POINT ( 'NONE',  ( 9.520470885617715595, 79.13000000000000966, 6.917026985038134512 ) ) ;
#16113=CARTESIAN_POINT ( 'NONE',  ( -4.963731793517477620, 44.50093815360280303, 12.55597456324973216 ) ) ;
#16114=DIRECTION ( 'NONE',  ( 1.000000000000000000, 0.000000000000000000, 0.000000000000000000 ) ) ;
#16115=CARTESIAN_POINT ( 'NONE',  ( -13.50000000000000000, 46.92999999999999972, -3.306546357697853733E-15 ) ) ;
#16116=CARTESIAN_POINT ( 'NONE',  ( -13.45369161577737849, 70.89049427693734629, -1.140183565930726228 ) ) ;
#16117=EDGE_CURVE ( 'NONE', #12212, #1976, #16734, .T. ) ;
#16119=CARTESIAN_POINT ( 'NONE',  ( -13.38782401986913051, 67.99071915777986419, 1.738903060278587320 ) ) ;
#16122=CARTESIAN_POINT ( 'NONE',  ( 13.01113393269324092, 54.30141377912826783, 3.601429272714332441 ) ) ;
#16124=CARTESIAN_POINT ( 'NONE',  ( -12.53153993143703460, 64.74693242360650913, -5.040447919499604801 ) ) ;
#16125=CARTESIAN_POINT ( 'NONE',  ( -12.24515502415462365, 35.13909831631156777, 5.707366899919843917 ) ) ;
#16128=CARTESIAN_POINT ( 'NONE',  ( -11.34467727478165777, 31.65563633594693016, -7.320944989841013495 ) ) ;
#16129=CARTESIAN_POINT ( 'NONE',  ( 4.953012991158001199, 73.00140879485633150, -12.55898227005201662 ) ) ;
#16131=DIRECTION ( 'NONE',  ( 9.637352644315600173E-17, -1.000000000000000000, 0.000000000000000000 ) ) ;
#16133=CARTESIAN_POINT ( 'NONE',  ( -12.91130779797210337, 52.78849919330026097, -3.946434418955392598 ) ) ;
#16135=CARTESIAN_POINT ( 'NONE',  ( -7.272992578804310604, 45.38000000000000256, 10.01041549318726709 ) ) ;
#16137=CARTESIAN_POINT ( 'NONE',  ( -8.343458848123576743, 69.47999999999998977, -11.48378591275254301 ) ) ;
#16139=CARTESIAN_POINT ( 'NONE',  ( 7.795000087196527261, 50.97370711654939157, 11.02690683953273876 ) ) ;
#16140=CARTESIAN_POINT ( 'NONE',  ( -10.29227820885054712, 37.59468482203347861, -8.736150211427487378 ) ) ;
#16141=CARTESIAN_POINT ( 'NONE',  ( 4.962760302008886626, 35.85893607516423742, 12.55665820087269680 ) ) ;
#16143=CARTESIAN_POINT ( 'NONE',  ( -12.04168536818074209, 74.15490546771334834, 6.103169336798146993 ) ) ;
#16144=CARTESIAN_POINT ( 'NONE',  ( -12.58168582133113844, 76.75239693361646687, -4.895191552310046212 ) ) ;
#16145=VECTOR ( 'NONE', #8142, 1000.000000000000000 ) ;
#16146=CARTESIAN_POINT ( 'NONE',  ( -7.311972143045258221, 80.40722760048129203, 11.35053210907591570 ) ) ;
#16151=CARTESIAN_POINT ( 'NONE',  ( -11.76794919243112325, 50.77999999999999403, -3.823638476888998827 ) ) ;
#16155=CARTESIAN_POINT ( 'NONE',  ( -10.26574468177152433, 40.59333272807688076, -8.767239472786558352 ) ) ;
#16157=CARTESIAN_POINT ( 'NONE',  ( 10.60663207285976029, 75.11149614483424841, 8.363159649599104739 ) ) ;
#16158=CARTESIAN_POINT ( 'NONE',  ( 8.343458848123583849, 68.87999999999999545, -11.48378591275253768 ) ) ;
#16159=CARTESIAN_POINT ( 'NONE',  ( -7.576616670048093940E-16, 42.67999999999999972, 12.37355403259654985 ) ) ;
#16160=CARTESIAN_POINT ( 'NONE',  ( -9.179761508417909610, 41.32223751179169113, 9.899410405694473170 ) ) ;
#16161=CARTESIAN_POINT ( 'NONE',  ( -5.154035034630091161, 58.36612174761953753, -12.48310025089808661 ) ) ;
#16162=DIRECTION ( 'NONE',  ( 0.000000000000000000, 0.000000000000000000, 1.000000000000000000 ) ) ;
#16166=CARTESIAN_POINT ( 'NONE',  ( -7.404372219800137600, 49.45681430499143261, -11.28829308273742527 ) ) ;
#16167=CARTESIAN_POINT ( 'NONE',  ( 13.47648628015202910, 63.46132184567057521, -0.9086240695849856497 ) ) ;
#16168=CARTESIAN_POINT ( 'NONE',  ( 10.75640908300814047, 42.73960387034645692, -8.162873688883740542 ) ) ;
#16175=CARTESIAN_POINT ( 'NONE',  ( -5.638841895279958827, 43.38479360352132375, -12.26596786634416247 ) ) ;
#16177=CARTESIAN_POINT ( 'NONE',  ( 12.95177247807359677, 60.56636384927607253, -3.809567037313156934 ) ) ;
#16179=CARTESIAN_POINT ( 'NONE',  ( 3.375869881531517347, 71.80049840645031622, 13.10095937201164773 ) ) ;
#16180=CARTESIAN_POINT ( 'NONE',  ( 13.49835085908630461, 57.43768004746023337, -0.2240883959220789090 ) ) ;
#16181=CARTESIAN_POINT ( 'NONE',  ( -11.76794919243112325, 71.78000000000000114, -3.823638476888998827 ) ) ;
#16182=CARTESIAN_POINT ( 'NONE',  ( -11.76794919243112325, 77.92999999999999261, -2.882316262207890869E-15 ) ) ;
#16183=CARTESIAN_POINT ( 'NONE',  ( -3.838951629330794368, 47.54196545468892054, 12.94266222818414391 ) ) ;
#16184=DIRECTION ( 'NONE',  ( 0.000000000000000000, -1.000000000000000000, 0.000000000000000000 ) ) ;
#16185=CARTESIAN_POINT ( 'NONE',  ( 0.000000000000000000, 80.93000000000000682, 0.000000000000000000 ) ) ;
#16186=CARTESIAN_POINT ( 'NONE',  ( 4.171729424061789260, 37.82999999999999829, 12.83926296998457417 ) ) ;
#16187=CARTESIAN_POINT ( 'NONE',  ( -8.343458848123582072, 34.37999999999999545, 11.48378591275253768 ) ) ;
#16189=CARTESIAN_POINT ( 'NONE',  ( -13.49999999999999822, 51.78000000000000114, -4.386415899144240349 ) ) ;
#16190=CARTESIAN_POINT ( 'NONE',  ( 11.25128164550088528, 33.71009814866270915, -7.460485725860525719 ) ) ;
#16191=CARTESIAN_POINT ( 'NONE',  ( -3.559128983600132745, 73.30801538557933839, -13.02258798672816553 ) ) ;
#16192=CARTESIAN_POINT ( 'NONE',  ( 5.578754407927415393, 39.97753789112579881, -12.30135392881136625 ) ) ;
#16193=ORIENTED_EDGE ( 'NONE', *, *, #5033, .T. ) ;
#16195=CARTESIAN_POINT ( 'NONE',  ( -4.310519988233258992, 62.52494779739406283, 12.79455156266785743 ) ) ;
#16197=CARTESIAN_POINT ( 'NONE',  ( -13.48481038722050762, 40.90780079122387747, -0.6425594624344264094 ) ) ;
#16200=EDGE_CURVE ( 'NONE', #7799, #6926, #8633, .T. ) ;
#16201=CARTESIAN_POINT ( 'NONE',  ( -10.54105442489647970, 44.25196237461326376, 8.439972557216172788 ) ) ;
#16203=CARTESIAN_POINT ( 'NONE',  ( 8.343458848123583849, 42.87999999999998124, -11.48378591275253768 ) ) ;
#16204=CARTESIAN_POINT ( 'NONE',  ( -10.92172942406178926, 45.62999999999999545, -7.935100905948389460 ) ) ;
#16205=CARTESIAN_POINT ( 'NONE',  ( -12.39285729354113386, 71.12555814250139008, 5.359515616412462435 ) ) ;
#16206=PRODUCT ( 'Top rod', 'Top rod', '', ( #4047 ) ) ;
#16208=CARTESIAN_POINT ( 'NONE',  ( -11.66385489473767301, 68.18283448863054730, 6.797391872370236676 ) ) ;
#16210=CARTESIAN_POINT ( 'NONE',  ( 13.24525085617974440, 54.52251518681887887, -2.621468703140126699 ) ) ;
#16212=CARTESIAN_POINT ( 'NONE',  ( -13.50064150216613967, 64.92368711864446595, -0.1755260359765862255 ) ) ;
#16213=ORIENTED_EDGE ( 'NONE', *, *, #3133, .F. ) ;
#16214=CARTESIAN_POINT ( 'NONE',  ( -10.92172942406179104, 64.23000000000000398, 7.935100905948387684 ) ) ;
#16215=CARTESIAN_POINT ( 'NONE',  ( -13.41438580105313250, 34.98340168545936280, 1.533709452862849432 ) ) ;
#16219=CARTESIAN_POINT ( 'NONE',  ( 6.048413154619182386, 72.95913537431300711, -12.06944015503662015 ) ) ;
#16221=CARTESIAN_POINT ( 'NONE',  ( 0.01655142509043793300, 79.17940487182032427, -13.50000000189450944 ) ) ;
#16224=CARTESIAN_POINT ( 'NONE',  ( -8.343458848123582072, 71.37999999999998124, 11.48378591275254124 ) ) ;
#16225=CARTESIAN_POINT ( 'NONE',  ( -12.46884852525094267, 52.74141282856401602, -5.180859845137886666 ) ) ;
#16227=CARTESIAN_POINT ( 'NONE',  ( 3.636496289402157078, 50.03000000000000114, -11.19198476289190936 ) ) ;
#16228=CARTESIAN_POINT ( 'NONE',  ( 4.171729424061791924, 69.03000000000000114, -12.83926296998457239 ) ) ;
#16229=CARTESIAN_POINT ( 'NONE',  ( 3.035063162148505356, 50.78921730790684563, 13.15580992881729294 ) ) ;
#16230=CARTESIAN_POINT ( 'NONE',  ( -10.35412786390899242, 37.59795970053211533, -8.662983390277185336 ) ) ;
#16231=CARTESIAN_POINT ( 'NONE',  ( 12.13297431269409721, 36.20992223033864832, 5.984304902545243721 ) ) ;
#16233=CARTESIAN_POINT ( 'NONE',  ( -9.166717776978838828, 74.32310361984721681, 9.924026101965260693 ) ) ;
#16234=AXIS2_PLACEMENT_3D ( 'NONE', #9815, #9942, #3192 ) ;
#16235=CARTESIAN_POINT ( 'NONE',  ( -12.49080795396548815, 76.74364347244760154, -5.121680526097208919 ) ) ;
#16236=CARTESIAN_POINT ( 'NONE',  ( -10.90667313324132159, 80.23087602101854543, 7.955953418439746017 ) ) ;
#16238=CARTESIAN_POINT ( 'NONE',  ( 6.767892274421971166, 80.93000000000000682, 11.68099457074693603 ) ) ;
#16239=DIRECTION ( 'NONE',  ( -0.000000000000000000, -1.000000000000000000, -0.000000000000000000 ) ) ;
#16242=CARTESIAN_POINT ( 'NONE',  ( 7.272992578804311492, 43.87999999999999545, -10.01041549318726886 ) ) ;
#16246=EDGE_CURVE ( 'NONE', #10491, #17339, #2444, .T. ) ;
#16247=CARTESIAN_POINT ( 'NONE',  ( -10.26587049905779203, 40.59333933079368251, -8.767092715570713679 ) ) ;
#16248=DIRECTION ( 'NONE',  ( -0.000000000000000000, -1.000000000000000000, -0.000000000000000000 ) ) ;
#16249=CARTESIAN_POINT ( 'NONE',  ( 10.21052318205141596, 75.09041434710640317, 8.831544897976421282 ) ) ;
#16252=CARTESIAN_POINT ( 'NONE',  ( 11.76794919243112680, 31.57999999999999119, -3.823638476888993942 ) ) ;
#16253=CARTESIAN_POINT ( 'NONE',  ( -10.44494405107816171, 41.25745373380726022, 8.565014912321151641 ) ) ;
#16254=CARTESIAN_POINT ( 'NONE',  ( -4.116521602011985692, 58.32801495984301710, -12.85716709580777106 ) ) ;
#16255=CARTESIAN_POINT ( 'NONE',  ( 4.599859061830847473, 44.84556242937287607, 12.69217623624271241 ) ) ;
#16257=CARTESIAN_POINT ( 'NONE',  ( 9.067440962954476547, 30.03237675404078288, 10.00200502765567556 ) ) ;
#16258=CARTESIAN_POINT ( 'NONE',  ( -0.4341634609568034708, 55.19561065720218096, -13.49312043558511220 ) ) ;
#16259=CARTESIAN_POINT ( 'NONE',  ( -10.28297219357257575, 49.59413489483298321, -8.747922443422563532 ) ) ;
#16260=CARTESIAN_POINT ( 'NONE',  ( 12.79341215383903041, 63.58529488098010773, -4.311560995242466277 ) ) ;
#16261=CARTESIAN_POINT ( 'NONE',  ( 10.67220332885768030, 42.11571253605529108, 8.267673668127477171 ) ) ;
#16262=CARTESIAN_POINT ( 'NONE',  ( 6.553170660267079839, 38.92104680671067740, 11.80483472479301099 ) ) ;
#16264=CARTESIAN_POINT ( 'NONE',  ( -2.610032936771094825, 70.27384716112842966, -13.24532283237781627 ) ) ;
#16265=CARTESIAN_POINT ( 'NONE',  ( -10.92172942406178926, 48.63000000000000256, -7.935100905948389460 ) ) ;
#16266=VECTOR ( 'NONE', #3927, 1000.000000000000000 ) ;
#16268=ORIENTED_EDGE ( 'NONE', *, *, #5823, .F. ) ;
#16270=CARTESIAN_POINT ( 'NONE',  ( -8.491832788201611137, 43.50521800093334690, -10.49509145101893459 ) ) ;
#16271=CARTESIAN_POINT ( 'NONE',  ( -7.499999999999999112, 106.7516370761002520, 7.534909587719529789 ) ) ;
#16272=CARTESIAN_POINT ( 'NONE',  ( 10.60253966551696614, 60.74819985123946964, -8.356982296996902093 ) ) ;
#16275=CARTESIAN_POINT ( 'NONE',  ( 13.38028740620904244, 66.49273914559641696, -1.795635039658233900 ) ) ;
#16276=CARTESIAN_POINT ( 'NONE',  ( 3.501237990040255266, 56.80573784203645715, 13.03990057735902752 ) ) ;
#16277=CARTESIAN_POINT ( 'NONE',  ( -9.520470885617717371, 66.23000000000000398, 6.917026985038133624 ) ) ;
#16278=CARTESIAN_POINT ( 'NONE',  ( -9.520470885617717371, 66.23000000000000398, 6.917026985038133624 ) ) ;
#16279=CARTESIAN_POINT ( 'NONE',  ( -11.35548083115155471, 47.20349252989605304, 7.300894966903513250 ) ) ;
#16280=CARTESIAN_POINT ( 'NONE',  ( -8.891200544363830713E-16, 46.67999999999999972, 13.50000000000000000 ) ) ;
#16283=CARTESIAN_POINT ( 'NONE',  ( -3.863179568236954964, 56.54109641619593418, 12.93566548485912193 ) ) ;
#16287=CARTESIAN_POINT ( 'NONE',  ( 13.48910014420235193, 33.40263309453820995, 0.7849891466346210489 ) ) ;
#16289=CARTESIAN_POINT ( 'NONE',  ( 0.03365071246442605246, 40.17879039882647163, -13.49996849265505716 ) ) ;
#16291=CARTESIAN_POINT ( 'NONE',  ( -5.500314997612258061, 62.48055942713471467, 12.32876052380532350 ) ) ;
#16295=CARTESIAN_POINT ( 'NONE',  ( -13.46144879879456369, 43.96558710645349066, 1.028303578921997641 ) ) ;
#16297=CARTESIAN_POINT ( 'NONE',  ( -4.171729424061791036, 41.52999999999999403, 12.83926296998457239 ) ) ;
#16298=CARTESIAN_POINT ( 'NONE',  ( -13.49999999999999822, 45.78000000000000114, -4.386415899144240349 ) ) ;
#16299=CARTESIAN_POINT ( 'NONE',  ( -13.45257578124989628, 70.96919024973162493, 1.130622322280563363 ) ) ;
#16301=CARTESIAN_POINT ( 'NONE',  ( -5.592092107590749706, 67.38298209709476794, -12.28733440995878468 ) ) ;
#16303=CARTESIAN_POINT ( 'NONE',  ( 12.04768657887330185, 54.20515543561278093, 6.106558576545860539 ) ) ;
#16304=CARTESIAN_POINT ( 'NONE',  ( -13.37418999445743317, 64.99429005833133033, 1.839119788055520344 ) ) ;
#16305=ORIENTED_EDGE ( 'NONE', *, *, #5942, .T. ) ;
#16306=CARTESIAN_POINT ( 'NONE',  ( -11.86075464149945979, 34.69129769346438508, -6.447695951845784812 ) ) ;
#16309=CARTESIAN_POINT ( 'NONE',  ( 13.46095473589419989, 78.46569523006924385, -1.031123768929128603 ) ) ;
#16311=CARTESIAN_POINT ( 'NONE',  ( -7.935043333107852703, 31.47999643740649489, -10.92183493073192402 ) ) ;
#16312=CARTESIAN_POINT ( 'NONE',  ( 6.454605826760913878, 72.94287210141447986, -11.86071968115371611 ) ) ;
#16314=CARTESIAN_POINT ( 'NONE',  ( 3.225258522805953376, 59.79597076863439753, 13.10906991609496863 ) ) ;
#16316=CARTESIAN_POINT ( 'NONE',  ( 13.50000000000000000, 69.43000000000000682, 1.653273178848926867E-15 ) ) ;
#16317=CARTESIAN_POINT ( 'NONE',  ( -12.28080000939004712, 53.13556830417786614, 5.614090485097651850 ) ) ;
#16318=CARTESIAN_POINT ( 'NONE',  ( 3.636496289402154414, 51.82999999999999829, 11.19198476289190936 ) ) ;
#16319=CARTESIAN_POINT ( 'NONE',  ( 2.607531440858944223E-15, 66.17999999999999261, -14.19474002721660355 ) ) ;
#16323=CARTESIAN_POINT ( 'NONE',  ( 9.112504148662578629, 69.03424743680851350, 9.973291273079063046 ) ) ;
#16324=CARTESIAN_POINT ( 'NONE',  ( -5.242085789724583833, 37.36954959029712597, -12.44118853238696154 ) ) ;
#16325=CARTESIAN_POINT ( 'NONE',  ( 2.530949507919612707, 35.77097839341501384, 13.26251326736510094 ) ) ;
#16327=CARTESIAN_POINT ( 'NONE',  ( -11.10711687597100727, 74.21892446219855799, 7.674797575374098457 ) ) ;
#16328=CARTESIAN_POINT ( 'NONE',  ( -13.38715452818623142, 76.86871122637566600, -1.752948765687992294 ) ) ;
#16330=CYLINDRICAL_SURFACE ( 'NONE', #4117, 13.50000000000000000 ) ;
#16334=CARTESIAN_POINT ( 'NONE',  ( -3.636496289402153081, 47.32999999999999829, -11.19198476289190936 ) ) ;
#16336=CARTESIAN_POINT ( 'NONE',  ( -11.88952341483570585, 40.69343732765294419, -6.394472622149963925 ) ) ;
#16337=CARTESIAN_POINT ( 'NONE',  ( -2.782897275306619900, 34.28006271705798014, -13.21006040336913578 ) ) ;
#16338=CARTESIAN_POINT ( 'NONE',  ( 13.02980635443139867, 75.30032106848673834, 3.643481502864720500 ) ) ;
#16340=CARTESIAN_POINT ( 'NONE',  ( -3.636496289402155746, 33.52999999999999403, 11.19198476289190936 ) ) ;
#16341=CARTESIAN_POINT ( 'NONE',  ( -8.912260708675086462, 41.33526359048111232, 10.14439829438506457 ) ) ;
#16342=CARTESIAN_POINT ( 'NONE',  ( 10.08123987682633249, 51.77650836596966144, -8.978842906595179585 ) ) ;
#16343=CONICAL_SURFACE ( 'NONE', #1959, 9.500000000000021316, 0.7853981633974504994 ) ;
#16345=CARTESIAN_POINT ( 'NONE',  ( 6.542315702985624704, 44.92083719594266000, 11.80973987326741081 ) ) ;
#16346=CYLINDRICAL_SURFACE ( 'NONE', #17383, 13.50000000000000000 ) ;
#16349=CARTESIAN_POINT ( 'NONE',  ( -4.171729424061787483, 57.32999999999999829, -12.83926296998457417 ) ) ;
#16350=CARTESIAN_POINT ( 'NONE',  ( -9.678251426474608010, 49.56251328237163989, -9.415881064490173813 ) ) ;
#16351=CARTESIAN_POINT ( 'NONE',  ( 13.48030235938352561, 63.40470212201357469, 0.7310520173840249214 ) ) ;
#16352=CARTESIAN_POINT ( 'NONE',  ( 10.66756771982902308, 42.11545174721990037, 8.273639169023212503 ) ) ;
#16353=CARTESIAN_POINT ( 'NONE',  ( 5.371075548745484873, 48.98509448818010981, -12.38750806412678429 ) ) ;
#16355=CARTESIAN_POINT ( 'NONE',  ( -1.104539697211379901, 70.21968188907926844, -13.46197618054497447 ) ) ;
#16358=CARTESIAN_POINT ( 'NONE',  ( -8.704009495233664850, 43.51509674902774805, -10.31941033300555333 ) ) ;
#16359=CARTESIAN_POINT ( 'NONE',  ( -7.499999999999999112, 103.9536021580775156, 9.261711852864909389 ) ) ;
#16360=CARTESIAN_POINT ( 'NONE',  ( 13.24512690636890611, 60.52253756231457515, -2.622165425226990809 ) ) ;
#16362=LINE ( 'NONE', #9679, #2856 ) ;
#16363=CARTESIAN_POINT ( 'NONE',  ( 13.49371366599027944, 66.41232310859372490, 0.5032188625160722850 ) ) ;
#16364=CARTESIAN_POINT ( 'NONE',  ( 10.68173734215865345, 57.11625071965492140, 8.255346062962116704 ) ) ;
#16365=CARTESIAN_POINT ( 'NONE',  ( 3.636496289402154414, 60.82999999999999829, 11.19198476289190936 ) ) ;
#16366=CARTESIAN_POINT ( 'NONE',  ( -11.76794919243112325, 65.78000000000001535, -3.823638476888998827 ) ) ;
#16367=CARTESIAN_POINT ( 'NONE',  ( -7.109540715892270768, 47.41573464837242824, 11.47625667131351612 ) ) ;
#16369=LINE ( 'NONE', #17436, #3629 ) ;
#16372=B_SPLINE_CURVE_WITH_KNOTS ( 'NONE', 3,
 ( #14953, #8452, #13547, #1618, #4279, #13635, #15038, #13891, #2932, #1437, #6855, #9866, #10914, #7117, #7035, #12233, #13806, #2843, #124, #16283, #12587, #5530, #8541, #5885, #1704, #389, #11265, #300, #12413, #5795, #4099, #5710, #11179, #16554, #8274, #15217, #1528, #6944, #4461, #3113, #11092, #1790, #12323, #16464, #4368, #216, #9777, #4804, #4548, #8710, #1956, #10206, #13016, #6309, #2124, #6056, #9953, #646, #4719, #16811, #16986, #3385, #897, #16726, #15560, #15301, #8798, #11439, #14070, #10121, #8967, #15474, #3205, #8625, #4890, #5970, #7550, #2043, #13977, #8884, #15389, #10291, #14155, #3470, #7467, #3296, #14239, #1872, #16901, #6144, #813, #16642, #12928, #2211, #15643, #3553, #7288, #11523, #12673, #563, #12847, #6224, #11610, #736, #7639, #14323, #11351, #4633, #10039, #7380, #12758, #13355, #17246, #10716, #7724, #5070, #11954, #3729, #14494, #16081, #9147, #4975, #13275, #6656, #3641, #17158, #10378, #9405, #14753, #2642, #6574, #10631, #13189, #3901, #1325, #1163, #15910, #8073, #15732, #13100, #2381, #13438, #11695, #10464, #1074, #15824, #9319, #3989, #9054, #14408, #2296, #7817, #17071, #12037, #17334, #5331, #5158, #987, #6399, #6488, #15996, #17416, #11782, #11871, #2467, #7900, #10551, #3819, #14669, #9233, #14587, #5245, #2557, #7987, #1243, #11065, #8424, #16258, #2731, #4164, #15095 ),
 .UNSPECIFIED., .F., .F.,
 ( 4, 2, 2, 2, 2, 1, 2, 2, 2, 2, 2, 2, 2, 2, 2, 1, 2, 2, 2, 2, 1, 2, 2, 1, 1, 1, 2, 2, 2, 1, 2, 2, 1, 1, 2, 2, 2, 2, 1, 1, 1, 2, 2, 2, 1, 1, 2, 2, 1, 1, 1, 2, 1, 2, 2, 1, 2, 2, 2, 2, 1, 2, 2, 2, 2, 2, 2, 1, 2, 2, 2, 2, 1, 1, 2, 2, 2, 2, 2, 2, 1, 1, 2, 2, 2, 1, 2, 2, 1, 2, 2, 2, 2, 2, 2, 2, 2, 2, 2, 2, 2, 1, 1, 2, 4 ),
 ( 0.4755055480612112584, 0.4764246321120116368, 0.4768841741374118537, 0.4769416168905868947, 0.4769990596437618802, 0.4771139451501119622, 0.4773437161628120706, 0.4778032581882122320, 0.4780330292009123405, 0.4781479147072624225, 0.4782628002136124490, 0.4791818842644128829, 0.4794116552771129913, 0.4794690980302880323, 0.4794978194068755251, 0.4795265407834630178, 0.4796414262898130998, 0.4801009683152132612, 0.4810200523660136396, 0.4819391364168140179, 0.4819678577934015107, 0.4819822184816953126, 0.4819965791699890589, 0.4820540219231640444, 0.4821689074295141264, 0.4823986784422141794, 0.4828582204676143408, 0.4837773045184146081, 0.4842368465438147696, 0.4844666175565148780, 0.4844953389331023708, 0.4845096996213961171, 0.4845240603096898635, 0.4845815030628649045, 0.4846963885692149310, 0.4865345566708156877, 0.4869940986962159046, 0.4870228200728033974, 0.4870515414493908901, 0.4871089842025659311, 0.4872238697089160131, 0.4874536407216160661, 0.4883727247724164444, 0.4892918088232168228, 0.4894066943295668493, 0.4894641370827418903, 0.4894928584593293830, 0.4895072191476231294, 0.4895215798359168757, 0.4897513508486169842, 0.4902108928740171456, 0.4906704348994173626, 0.4907278776525924036, 0.4907422383408861499, 0.4907565990291798963, 0.4907853204057673890, 0.4909002059121174710, 0.4911299769248175795, 0.4915895189502177409, 0.4918192899629178494, 0.4919341754692679314, 0.4919916182224429169, 0.4920490609756179579, 0.4938872290772187701, 0.4943467711026189870, 0.4944616566089690135, 0.4945190993621440545, 0.4945765421153190955, 0.4948063131280192040, 0.4957253971788195823, 0.4957541185554070751, 0.4957684792437008769, 0.4957828399319946233, 0.4958402826851696088, 0.4959551681915196908, 0.4961849392042197437, 0.4966444812296199052, 0.4968742522423200136, 0.4969891377486700401, 0.4970178591252575329, 0.4970465805018450811, 0.4971040232550200666, 0.4975635652804201170, 0.4984826493312203288, 0.4994017333820204851, 0.4994591761351955261, 0.4994878975117830189, 0.4995166188883705116, 0.4996315043947205381, 0.4998612754074205911, 0.5003208174328206415, 0.5012399014836208533, 0.5016994435090209592, 0.5019292145217210122, 0.5020441000280710941, 0.5021589855344210651, 0.5030780695852212769, 0.5039971536360214888, 0.5044566956614215947, 0.5045141384145965802, 0.5045284991028903265, 0.5045428597911841839, 0.5045715811677716767, 0.5046864666741216476, 0.5049162376868217006 ),
 .UNSPECIFIED. ) ;
#16377=CARTESIAN_POINT ( 'NONE',  ( 13.30970590930321507, 33.35061697494153776, 2.259477746023484279 ) ) ;
#16381=VERTEX_POINT ( 'NONE', #15353 ) ;
#16382=CARTESIAN_POINT ( 'NONE',  ( -5.714934635204341085, 62.47224522950935466, 12.23094497409742765 ) ) ;
#16383=ORIENTED_EDGE ( 'NONE', *, *, #16200, .F. ) ;
#16384=CARTESIAN_POINT ( 'NONE',  ( -13.49672419826743486, 40.91718416035435268, -0.3692389318145620769 ) ) ;
#16387=CARTESIAN_POINT ( 'NONE',  ( -13.39191227960274411, 43.99185072783001260, 1.775942202619223531 ) ) ;
#16389=CARTESIAN_POINT ( 'NONE',  ( -13.49999999999999822, 35.07999999999999119, 4.386415899144235908 ) ) ;
#16390=CARTESIAN_POINT ( 'NONE',  ( 13.50000000000000000, 44.42999999999999972, 1.653273178848926867E-15 ) ) ;
#16394=CARTESIAN_POINT ( 'NONE',  ( -10.35534497003228616, 67.59815324688858595, -8.661887587482873130 ) ) ;
#16396=CARTESIAN_POINT ( 'NONE',  ( 12.99745066060657983, 54.56037337467130044, -3.649188683310558012 ) ) ;
#16397=CARTESIAN_POINT ( 'NONE',  ( -0.6906333296155144907, 64.20483233361511566, -13.48257629628379739 ) ) ;
#16400=CARTESIAN_POINT ( 'NONE',  ( -13.48149335069471277, 34.90545412603139397, -0.7087578777626947213 ) ) ;
#16402=CARTESIAN_POINT ( 'NONE',  ( 13.40590469924962136, 78.37451624811531303, 1.591240554925627215 ) ) ;
#16405=CARTESIAN_POINT ( 'NONE',  ( -8.343458848123582072, 37.37999999999999545, 11.48378591275253768 ) ) ;
#16406=CARTESIAN_POINT ( 'NONE',  ( 3.355142272266856018, 73.05936141215188684, -13.07645859584844317 ) ) ;
#16409=CARTESIAN_POINT ( 'NONE',  ( -8.691771469529815392E-16, 62.67999999999999972, 14.19474002721660355 ) ) ;
#16410=CARTESIAN_POINT ( 'NONE',  ( -13.08971297670988676, 53.04813283155247916, 3.315942555628902166 ) ) ;
#16411=CARTESIAN_POINT ( 'NONE',  ( -11.76794919243112325, 36.08000000000000540, 3.823638476888994386 ) ) ;
#16413=CARTESIAN_POINT ( 'NONE',  ( 2.607531440858944223E-15, 54.17999999999999261, -14.19474002721660355 ) ) ;
#16414=CARTESIAN_POINT ( 'NONE',  ( 2.431254415941702884, 50.76746427736173928, 13.28206675338410570 ) ) ;
#16415=CARTESIAN_POINT ( 'NONE',  ( 12.74062673367197540, 69.26888048504336837, 4.464895979421934946 ) ) ;
#16417=CARTESIAN_POINT ( 'NONE',  ( -4.171729424061787483, 72.33000000000001251, -12.83926296998457417 ) ) ;
#16419=CARTESIAN_POINT ( 'NONE',  ( -13.20956847790360733, 74.02888101833143253, 2.796753555545153258 ) ) ;
#16420=CARTESIAN_POINT ( 'NONE',  ( -4.859696658499787603, 76.35516489890081004, -12.59554570565296139 ) ) ;
#16421=CARTESIAN_POINT ( 'NONE',  ( -3.256378952507587687, 79.29685528557507723, -13.10825059591972241 ) ) ;
#16422=DIRECTION ( 'NONE',  ( 0.000000000000000000, 0.000000000000000000, -1.000000000000000000 ) ) ;
#16423=CARTESIAN_POINT ( 'NONE',  ( 3.590940523863186851, 80.92999999999996419, 12.80902731135801886 ) ) ;
#16426=CARTESIAN_POINT ( 'NONE',  ( 7.272992578804311492, 46.87999999999998835, -10.01041549318726886 ) ) ;
#16429=CARTESIAN_POINT ( 'NONE',  ( -0.4449892875956310556, 32.66412856956223720, 13.50000000012790657 ) ) ;
#16430=CARTESIAN_POINT ( 'NONE',  ( 13.34255314625656474, 75.35788651830209517, 2.057478645647980109 ) ) ;
#16431=EDGE_CURVE ( 'NONE', #16381, #10808, #9031, .T. ) ;
#16433=( NAMED_UNIT ( * ) SI_UNIT ( $, .STERADIAN. ) SOLID_ANGLE_UNIT ( ) );
#16434=CARTESIAN_POINT ( 'NONE',  ( -6.368869478743532930, 41.44634379311723649, 11.90564925343862868 ) ) ;
#16435=CARTESIAN_POINT ( 'NONE',  ( 3.227881820449359562, 52.06437088216431874, -13.11849352263842761 ) ) ;
#16436=CARTESIAN_POINT ( 'NONE',  ( -1.816329563374412759, 38.61463869457227815, 13.37757954458849241 ) ) ;
#16437=DIRECTION ( 'NONE',  ( 0.000000000000000000, 0.000000000000000000, -1.000000000000000000 ) ) ;
#16440=CARTESIAN_POINT ( 'NONE',  ( -11.16732475769975963, 49.64467603628539649, -7.585655084846200324 ) ) ;
#16441=CARTESIAN_POINT ( 'NONE',  ( 9.616125506160093650, 63.05947077844894721, 9.475237748159102580 ) ) ;
#16442=CARTESIAN_POINT ( 'NONE',  ( 12.14686625650739416, 42.21335745758226921, 5.893900887576004166 ) ) ;
#16443=CARTESIAN_POINT ( 'NONE',  ( 5.822740267050442675, 48.96792138070764366, -12.17985001218392327 ) ) ;
#16445=CARTESIAN_POINT ( 'NONE',  ( -11.76794919243112325, 71.92999999999999261, -2.882316262207890869E-15 ) ) ;
#16446=CARTESIAN_POINT ( 'NONE',  ( -2.234432163248517789, 70.26033055681520523, -13.31411821497241199 ) ) ;
#16450=CARTESIAN_POINT ( 'NONE',  ( -4.039390320560676706, 43.32524183929319150, -12.88154992939627874 ) ) ;
#16451=DIRECTION ( 'NONE',  ( 0.000000000000000000, 0.000000000000000000, -1.000000000000000000 ) ) ;
#16452=CARTESIAN_POINT ( 'NONE',  ( 6.713091215227763975, 60.93229263216861824, -11.71350425076765234 ) ) ;
#16456=CARTESIAN_POINT ( 'NONE',  ( 12.41472406366220937, 66.62365169156784361, -5.310316743964890840 ) ) ;
#16457=CARTESIAN_POINT ( 'NONE',  ( 9.085652227950054893, 57.03291504710205118, 9.999132570447487822 ) ) ;
#16458=CARTESIAN_POINT ( 'NONE',  ( 7.272992578804308828, 54.98000000000000398, 10.01041549318726709 ) ) ;
#16459=CARTESIAN_POINT ( 'NONE',  ( 2.272985001014427788E-15, 65.18000000000000682, -12.37355403259654985 ) ) ;
#16460=CARTESIAN_POINT ( 'NONE',  ( -13.48866837566228050, 46.90290234888265530, -0.7789067716198110336 ) ) ;
#16462=FACE_OUTER_BOUND ( 'NONE', #7042, .T. ) ;
#16463=CARTESIAN_POINT ( 'NONE',  ( 6.184124730272909432, 30.95379574339498419, -12.00166303903518461 ) ) ;
#16464=CARTESIAN_POINT ( 'NONE',  ( -8.721356837196914569, 56.34409543140491650, 10.30502666443673654 ) ) ;
#16467=CARTESIAN_POINT ( 'NONE',  ( 4.319503133742830236, 32.83532678599706855, 12.79097160616992745 ) ) ;
#16469=CARTESIAN_POINT ( 'NONE',  ( 1.040369979270597378, 40.14266547395921236, -13.46226468211543725 ) ) ;
#16471=CARTESIAN_POINT ( 'NONE',  ( -4.171729424061787483, 42.32999999999999829, -12.83926296998457417 ) ) ;
#16475=CARTESIAN_POINT ( 'NONE',  ( -13.01704944681739384, 44.05820777106878694, 3.585442433228816839 ) ) ;
#16478=CARTESIAN_POINT ( 'NONE',  ( -8.343458848123582072, 32.37999999999999545, 11.48378591275254124 ) ) ;
#16479=CARTESIAN_POINT ( 'NONE',  ( -4.171729424061791036, 49.53000000000000114, 12.83926296998457239 ) ) ;
#16480=CARTESIAN_POINT ( 'NONE',  ( -6.265920072760685855, 46.40952468282172561, -11.95780131475176411 ) ) ;
#16481=CARTESIAN_POINT ( 'NONE',  ( -5.840637679356421863, 67.39265420351648572, -12.17211919009271170 ) ) ;
#16483=CARTESIAN_POINT ( 'NONE',  ( 10.70096191381189854, 54.74267225910909929, -8.231670366690693186 ) ) ;
#16484=CARTESIAN_POINT ( 'NONE',  ( -5.858038622988929411, 64.39335049776337883, -12.16278876361409367 ) ) ;
#16486=CARTESIAN_POINT ( 'NONE',  ( -13.47158887085881673, 34.89975520542590459, -0.8754049196653456155 ) ) ;
#16488=CARTESIAN_POINT ( 'NONE',  ( 12.90972652943405841, 78.57172280611223414, -3.953148085708793502 ) ) ;
#16493=CARTESIAN_POINT ( 'NONE',  ( 3.408135647905105703, 73.05745548237557330, -13.06274704958987520 ) ) ;
#16494=CARTESIAN_POINT ( 'NONE',  ( 3.048566704048218057, 79.07038407013068593, -13.15904929974419346 ) ) ;
#16497=CARTESIAN_POINT ( 'NONE',  ( 13.50000000000000000, 60.42999999999999972, 1.653273178848926867E-15 ) ) ;
#16498=CARTESIAN_POINT ( 'NONE',  ( 13.50000000000000000, 50.42999999999999972, 1.653273178848926867E-15 ) ) ;
#16499=CARTESIAN_POINT ( 'NONE',  ( -12.41413396520435874, 53.12371177561935554, 5.309278927454689878 ) ) ;
#16500=CARTESIAN_POINT ( 'NONE',  ( -11.76794919243112325, 39.07999999999999119, 3.823638476888994386 ) ) ;
#16502=CARTESIAN_POINT ( 'NONE',  ( -10.92172942406178926, 60.63000000000000256, -7.935100905948389460 ) ) ;
#16504=CARTESIAN_POINT ( 'NONE',  ( 6.513726533578187983, 68.91946989124797085, 11.83231862531209444 ) ) ;
#16505=CARTESIAN_POINT ( 'NONE',  ( -3.394498949081906414, 37.30204389133518106, -13.06947235405735519 ) ) ;
#16506=CARTESIAN_POINT ( 'NONE',  ( -8.291044507619272909E-14, 57.17999999999999972, -13.50000000000000000 ) ) ;
#16508=CARTESIAN_POINT ( 'NONE',  ( -10.67600666061439973, 74.24413227333732834, 8.265984108055215884 ) ) ;
#16509=CARTESIAN_POINT ( 'NONE',  ( -4.628240636438917477, 76.34660530185777816, -12.68187234864826607 ) ) ;
#16510=CARTESIAN_POINT ( 'NONE',  ( -1.059413705080190837, 79.21809260812437969, -13.49999987874332241 ) ) ;
#16515=CARTESIAN_POINT ( 'NONE',  ( 7.272992578804311492, 40.87999999999999545, -10.01041549318726886 ) ) ;
#16517=EDGE_CURVE ( 'NONE', #11619, #7799, #10881, .T. ) ;
#16518=CARTESIAN_POINT ( 'NONE',  ( -9.459099616640498809, 32.30840304435178467, 9.632024434120667777 ) ) ;
#16519=CARTESIAN_POINT ( 'NONE',  ( 13.07675211750358457, 75.54939648288200260, -3.353959690592315912 ) ) ;
#16521=CARTESIAN_POINT ( 'NONE',  ( 7.272992578804311492, 31.87999999999999545, -10.01041549318726709 ) ) ;
#16522=CARTESIAN_POINT ( 'NONE',  ( -4.171729424061787483, 81.32999999999999829, -12.83926296998457417 ) ) ;
#16523=CARTESIAN_POINT ( 'NONE',  ( 7.855212290319397717, 51.88356205845266800, -10.98026488807781931 ) ) ;
#16524=CIRCLE ( 'NONE', #3253, 5.000000000000000000 ) ;
#16525=CARTESIAN_POINT ( 'NONE',  ( -1.457356408888724308, 38.62762465094729691, 13.42125827019123463 ) ) ;
#16526=CARTESIAN_POINT ( 'NONE',  ( 3.493089250578063520, 37.05461647915249301, -13.07001197377214119 ) ) ;
#16529=CARTESIAN_POINT ( 'NONE',  ( 7.235470476593615530, 62.94958575296288927, 11.39775609064293427 ) ) ;
#16530=CARTESIAN_POINT ( 'NONE',  ( 13.50300513245434431, 42.42850705580203652, 0.04008974157810932942 ) ) ;
#16531=CARTESIAN_POINT ( 'NONE',  ( 7.173772269966901760, 48.91298932173004488, -11.43911279990962448 ) ) ;
#16534=CARTESIAN_POINT ( 'NONE',  ( 9.520470885617717371, 67.73000000000000398, -6.917026985038131848 ) ) ;
#16535=CARTESIAN_POINT ( 'NONE',  ( -3.943571451878268075, 70.32179627606707584, -12.91117844506843859 ) ) ;
#16539=CARTESIAN_POINT ( 'NONE',  ( -11.11731508959757342, 43.64162586097864960, -7.658681678614005506 ) ) ;
#16541=CARTESIAN_POINT ( 'NONE',  ( 13.49453415536198797, 60.44356499961826046, -0.3946668185908841497 ) ) ;
#16545=CARTESIAN_POINT ( 'NONE',  ( 12.92234882186717115, 66.28998143173690494, 3.906840215585264176 ) ) ;
#16546=CARTESIAN_POINT ( 'NONE',  ( 10.65812523510989607, 57.11492007506318203, 8.285798828776941960 ) ) ;
#16547=CARTESIAN_POINT ( 'NONE',  ( 7.272992578804308828, 60.97999999999999687, 10.01041549318726709 ) ) ;
#16548=CARTESIAN_POINT ( 'NONE',  ( -9.520470885617715595, 68.62999999999999545, -6.917026985038136289 ) ) ;
#16549=CARTESIAN_POINT ( 'NONE',  ( -12.55849098233041516, 46.75015478663139845, -4.953260354883232353 ) ) ;
#16550=CARTESIAN_POINT ( 'NONE',  ( 7.207449306385443677, 45.91159972359503172, -11.41531860434902512 ) ) ;
#16553=CARTESIAN_POINT ( 'NONE',  ( 5.020134451633054162, 30.99833425099403428, -12.53726460365605710 ) ) ;
#16554=CARTESIAN_POINT ( 'NONE',  ( -6.237188668602095198, 56.45156311056310017, 11.97644378720688785 ) ) ;
#16557=CYLINDRICAL_SURFACE ( 'NONE', #15405, 13.50000000000000000 ) ;
#16558=CARTESIAN_POINT ( 'NONE',  ( 4.772672689868944218, 32.85189186562215014, 12.63022836692152495 ) ) ;
#16560=CARTESIAN_POINT ( 'NONE',  ( 4.352287195575301304, 40.02347799479684198, -12.77918881344716517 ) ) ;
#16562=CARTESIAN_POINT ( 'NONE',  ( -8.673344535932200117, 62.34634085401044956, 10.34522302012570449 ) ) ;
#16563=ORIENTED_EDGE ( 'NONE', *, *, #13127, .F. ) ;
#16564=CARTESIAN_POINT ( 'NONE',  ( -13.37780778470979648, 40.99393780181782887, 1.830007199971625420 ) ) ;
#16567=CARTESIAN_POINT ( 'NONE',  ( -12.88197876152688615, 43.78491403648499158, -4.041588179776032241 ) ) ;
#16569=CARTESIAN_POINT ( 'NONE',  ( -8.343458848123582072, 35.37999999999999545, 11.48378591275254124 ) ) ;
#16570=CARTESIAN_POINT ( 'NONE',  ( -8.343458848123576743, 48.48000000000000398, -11.48378591275254301 ) ) ;
#16571=CARTESIAN_POINT ( 'NONE',  ( -0.009212933485843630491, 46.18033114546576456, -13.49999764172323147 ) ) ;
#16572=ADVANCED_FACE ( 'NONE', ( #7319 ), #590, .T. ) ;
#16573=CARTESIAN_POINT ( 'NONE',  ( -5.559764996625593092, 67.38173173404518934, -12.30199985033388010 ) ) ;
#16575=CARTESIAN_POINT ( 'NONE',  ( 6.586770268181092014, 53.92254834050746126, 11.78407759566256985 ) ) ;
#16576=CARTESIAN_POINT ( 'NONE',  ( -3.270141562520593403, 64.29757460427565263, -13.09794721236131210 ) ) ;
#16578=CARTESIAN_POINT ( 'NONE',  ( -10.20076248856652867, 34.58984148594135632, -8.842762936844939858 ) ) ;
#16580=CARTESIAN_POINT ( 'NONE',  ( 12.85115454411534053, 78.28138835478902990, 4.134994248532485095 ) ) ;
#16583=CARTESIAN_POINT ( 'NONE',  ( 13.37012903279583576, 72.36469939934085005, 1.868140815954207001 ) ) ;
#16585=CARTESIAN_POINT ( 'NONE',  ( 8.343458848123583849, 63.87999999999998835, -11.48378591275253768 ) ) ;
#16586=CARTESIAN_POINT ( 'NONE',  ( -0.7864078588604943576, 71.65172976531886206, 13.47770389585425832 ) ) ;
#16587=CARTESIAN_POINT ( 'NONE',  ( 2.272985001014427788E-15, 35.17999999999998550, -12.37355403259654985 ) ) ;
#16588=CARTESIAN_POINT ( 'NONE',  ( -10.92172942406179104, 58.23000000000000398, 7.935100905948387684 ) ) ;
#16591=CARTESIAN_POINT ( 'NONE',  ( 11.35791665574828713, 69.15656779720782765, 7.300441548434104533 ) ) ;
#16592=CARTESIAN_POINT ( 'NONE',  ( -2.862087262652846853, 37.28290999384705628, -13.19312863063275998 ) ) ;
#16593=ADVANCED_FACE ( 'NONE', ( #2159 ), #12877, .T. ) ;
#16596=CARTESIAN_POINT ( 'NONE',  ( -11.40798122654512525, 73.65990416871910895, -7.218615817919470601 ) ) ;
#16597=CARTESIAN_POINT ( 'NONE',  ( -6.942184294231981134, 76.43724017907349833, -11.57843550520342113 ) ) ;
#16598=CARTESIAN_POINT ( 'NONE',  ( -4.363074663832638755, 79.33691353306146254, -12.77551180107495199 ) ) ;
#16600=DIRECTION ( 'NONE',  ( 0.000000000000000000, 0.000000000000000000, -1.000000000000000000 ) ) ;
#16603=CARTESIAN_POINT ( 'NONE',  ( -7.272992578804310604, 36.37999999999998835, 10.01041549318726886 ) ) ;
#16604=( BOUNDED_CURVE ( )  B_SPLINE_CURVE ( 2, ( #2975, #4501, #8905, #17007, #9908, #15255, #8405, #1746, #4824, #515, #16417, #12543, #1657 ),
 .UNSPECIFIED., .F., .F. ) 
 B_SPLINE_CURVE_WITH_KNOTS ( ( 3, 2, 2, 2, 2, 2, 3 ),
 ( 0.2083333333333333148, 0.2111111111111111105, 0.2166666666666666741, 0.2222222222222222099, 0.2277777777777777735, 0.2333333333333333370, 0.2361111111111111049 ),
 .UNSPECIFIED. ) 
 CURVE ( )  GEOMETRIC_REPRESENTATION_ITEM ( )  RATIONAL_B_SPLINE_CURVE ( ( 0.9755282581475765991, 0.9755282581475765991, 1.000000000000000000, 0.9510565162951535312, 1.000000000000000000, 0.9510565162951535312, 1.000000000000000000, 0.9510565162951535312, 1.000000000000000000, 0.9510565162951535312, 1.000000000000000000, 0.9755282581475768211, 0.9755282581475765991 ) ) 
 REPRESENTATION_ITEM ( '' )  );
#16606=CARTESIAN_POINT ( 'NONE',  ( -7.096040157522595315, 32.41630410450128608, 11.48461955335362106 ) ) ;
#16607=CARTESIAN_POINT ( 'NONE',  ( 2.717229725162839227, 74.77768976466231265, 13.22563761779151825 ) ) ;
#16609=VECTOR ( 'NONE', #1434, 1000.000000000000000 ) ;
#16610=CARTESIAN_POINT ( 'NONE',  ( -9.520470885617717371, 33.22999999999999687, 6.917026985038133624 ) ) ;
#16611=CARTESIAN_POINT ( 'NONE',  ( -8.343458848123582072, 82.38000000000000966, 11.48378591275254124 ) ) ;
#16612=CARTESIAN_POINT ( 'NONE',  ( -2.175153866734307329, 58.25820765909811882, -13.32388992672253636 ) ) ;
#16614=ADVANCED_FACE ( 'NONE', ( #15505, #4924 ), #4835, .T. ) ;
#16615=CARTESIAN_POINT ( 'NONE',  ( 0.000000000000000000, -1.200000000000000030E-05, 5.000000000000000000 ) ) ;
#16618=CARTESIAN_POINT ( 'NONE',  ( 5.623418083639327492, 62.88408628963233582, 12.28088165123665654 ) ) ;
#16619=CARTESIAN_POINT ( 'NONE',  ( 13.35664415350134426, 42.36122446370394101, 1.964704937003258767 ) ) ;
#16620=CARTESIAN_POINT ( 'NONE',  ( 8.226923464784990259, 48.86690000741498352, -10.70406459611412053 ) ) ;
#16621=CIRCLE ( 'NONE', #1654, 12.00000000000000178 ) ;
#16624=CARTESIAN_POINT ( 'NONE',  ( -11.76794919243112325, 66.07999999999999829, 3.823638476888994830 ) ) ;
#16628=VERTEX_POINT ( 'NONE', #7583 ) ;
#16629=CARTESIAN_POINT ( 'NONE',  ( -0.03816919975528386411, 43.18137242233956385, -13.49994894151539526 ) ) ;
#16630=CARTESIAN_POINT ( 'NONE',  ( -7.499999999999998224, 107.9345255869305760, 5.560661329642320183 ) ) ;
#16633=CARTESIAN_POINT ( 'NONE',  ( 12.86384301462254420, 66.28284470376391369, 4.096554117506745918 ) ) ;
#16634=CARTESIAN_POINT ( 'NONE',  ( 10.55353346449092911, 57.10905816187499795, 8.419028628576304740 ) ) ;
#16635=CARTESIAN_POINT ( 'NONE',  ( -11.76794919243112325, 56.77999999999998693, -3.823638476888998827 ) ) ;
#16636=CARTESIAN_POINT ( 'NONE',  ( -9.520470885617715595, 71.62999999999999545, -6.917026985038136289 ) ) ;
#16637=CARTESIAN_POINT ( 'NONE',  ( -13.44822379438176441, 46.88685179129658565, -1.238907302481064843 ) ) ;
#16639=CARTESIAN_POINT ( 'NONE',  ( 9.190911557378541374, 45.82162825536664741, -9.888297778096264423 ) ) ;
#16640=CARTESIAN_POINT ( 'NONE',  ( 5.641748383016213175, 69.97509866883848417, -12.26461152474380256 ) ) ;
#16641=CARTESIAN_POINT ( 'NONE',  ( 5.850237716920893227, 30.96695511545072321, -12.16654113314289809 ) ) ;
#16642=CARTESIAN_POINT ( 'NONE',  ( -13.47731147386839012, 55.90299908574060339, -0.7823863207999742775 ) ) ;
#16643=CARTESIAN_POINT ( 'NONE',  ( 13.50000000000000000, 53.43000000000000682, 1.653273178848926867E-15 ) ) ;
#16644=CARTESIAN_POINT ( 'NONE',  ( 1.222065048496696615, 32.72394127083357773, 13.44460228257956835 ) ) ;
#16646=CARTESIAN_POINT ( 'NONE',  ( 8.221241430366118763, 39.86716037471302343, -10.70805348710604576 ) ) ;
#16647=ORIENTED_EDGE ( 'NONE', *, *, #12520, .F. ) ;
#16648=CARTESIAN_POINT ( 'NONE',  ( -12.70043917417899770, 62.09540525535791033, 4.577124250142029283 ) ) ;
#16650=CARTESIAN_POINT ( 'NONE',  ( 10.14067890081039636, 48.08657762055307217, 8.914487275897856833 ) ) ;
#16652=EDGE_CURVE ( 'NONE', #15567, #13217, #11388, .T. ) ;
#16653=CARTESIAN_POINT ( 'NONE',  ( 4.171729424061789260, 38.82999999999999829, 12.83926296998457417 ) ) ;
#16654=AXIS2_PLACEMENT_3D ( 'NONE', #186, #4335, #13945 ) ;
#16656=CARTESIAN_POINT ( 'NONE',  ( -2.956505443956637169, 67.28629095795685089, -13.17228614719877555 ) ) ;
#16658=CARTESIAN_POINT ( 'NONE',  ( 6.608087321929540181, 53.92343117755994797, 11.77214407716479450 ) ) ;
#16660=CARTESIAN_POINT ( 'NONE',  ( -8.697098998243532012E-15, 64.18000000000002103, -13.50000000000000000 ) ) ;
#16663=CARTESIAN_POINT ( 'NONE',  ( -11.80087666258112122, 34.68689685915391152, -6.556923290561053719 ) ) ;
#16666=CARTESIAN_POINT ( 'NONE',  ( 13.05929335850220419, 78.55189450621524827, -3.421339340133226159 ) ) ;
#16667=CARTESIAN_POINT ( 'NONE',  ( 1.653273178848926472E-15, 80.93000000000000682, 13.50000000000000000 ) ) ;
#16670=CARTESIAN_POINT ( 'NONE',  ( 13.21136977642124499, 72.52851845461269420, -2.785417675787339231 ) ) ;
#16673=CARTESIAN_POINT ( 'NONE',  ( -10.92172942406178926, 67.62999999999999545, -7.935100905948389460 ) ) ;
#16674=CARTESIAN_POINT ( 'NONE',  ( -5.802784399048038999, 52.39118405824265778, -12.18924498636963349 ) ) ;
#16675=CARTESIAN_POINT ( 'NONE',  ( -7.272992578804310604, 39.38000000000000256, 10.01041549318726709 ) ) ;
#16676=CARTESIAN_POINT ( 'NONE',  ( 13.49999999999999822, 62.28000000000000114, 4.386415899144237684 ) ) ;
#16679=CARTESIAN_POINT ( 'NONE',  ( 4.028353631777413568, 68.82466814077726269, 12.88820194039942990 ) ) ;
#16681=DIRECTION ( 'NONE',  ( 0.000000000000000000, -1.000000000000000000, 0.000000000000000000 ) ) ;
#16683=CARTESIAN_POINT ( 'NONE',  ( -11.37058303215777499, 73.65747949932976724, -7.277363885997346848 ) ) ;
#16684=CARTESIAN_POINT ( 'NONE',  ( -9.423580237977008167, 76.54982212202980918, -9.666754949485444115 ) ) ;
#16685=CARTESIAN_POINT ( 'NONE',  ( -4.194230612231265809, 79.33078485373877697, -12.83233939078419716 ) ) ;
#16689=CARTESIAN_POINT ( 'NONE',  ( -7.576616670048093940E-16, 39.67999999999999261, 12.37355403259654807 ) ) ;
#16692=CARTESIAN_POINT ( 'NONE',  ( -4.511025009967577049, 32.51769489362273902, 12.72403845838506520 ) ) ;
#16693=CARTESIAN_POINT ( 'NONE',  ( 3.620391450164611058, 74.81017573312026059, 13.00552749220717352 ) ) ;
#16696=AXIS2_PLACEMENT_3D ( 'NONE', #8349, #13705, #16451 ) ;
#16698=CARTESIAN_POINT ( 'NONE',  ( -8.691771469529815392E-16, 82.67999999999999261, 14.19474002721660355 ) ) ;
#16699=CARTESIAN_POINT ( 'NONE',  ( 10.03398847469492239, 51.77899704666725711, -9.031564513890813828 ) ) ;
#16700=CARTESIAN_POINT ( 'NONE',  ( -4.430225406486345996, 38.52064587386139749, 12.75245493685339504 ) ) ;
#16701=CARTESIAN_POINT ( 'NONE',  ( 4.340749435625693486, 37.02381347075288431, -12.81346088498517233 ) ) ;
#16702=CARTESIAN_POINT ( 'NONE',  ( 3.785595641572113985E-06, 49.17999986388394973, -13.49999999999946887 ) ) ;
#16703=AXIS2_PLACEMENT_3D ( 'NONE', #11717, #4650, #4736 ) ;
#16704=CARTESIAN_POINT ( 'NONE',  ( 10.56433791484173135, 63.10966569891045452, 8.405314700618397694 ) ) ;
#16706=CARTESIAN_POINT ( 'NONE',  ( 12.80285549483701324, 48.58509970421081903, -4.305323710473574650 ) ) ;
#16709=CARTESIAN_POINT ( 'NONE',  ( -11.76794919243112325, 68.77999999999998693, -3.823638476888998827 ) ) ;
#16713=CARTESIAN_POINT ( 'NONE',  ( -0.1651247708450846174, 43.18593718442633644, -13.49902517774528121 ) ) ;
#16714=CARTESIAN_POINT ( 'NONE',  ( -7.686450350229677930, 80.93000000000000682, -9.894994522817997407 ) ) ;
#16717=CARTESIAN_POINT ( 'NONE',  ( 5.737830409276838850, 65.88864550709209311, 12.21995698880643033 ) ) ;
#16718=CARTESIAN_POINT ( 'NONE',  ( 8.343458848123578520, 80.98000000000000398, 11.48378591275254124 ) ) ;
#16719=CARTESIAN_POINT ( 'NONE',  ( 3.636496289402154414, 51.82999999999999829, 11.19198476289190936 ) ) ;
#16720=CARTESIAN_POINT ( 'NONE',  ( -3.636496289402155746, 57.53000000000000114, 11.19198476289190936 ) ) ;
#16721=CARTESIAN_POINT ( 'NONE',  ( -12.76930904997713156, 47.08985268192056139, 4.436624044834727165 ) ) ;
#16722=CARTESIAN_POINT ( 'NONE',  ( 7.390077773784788029, 45.90380094779195019, -11.29772916998646082 ) ) ;
#16723=CARTESIAN_POINT ( 'NONE',  ( 8.235194954453712413, 69.86653683069012288, -10.69767531060790411 ) ) ;
#16725=CARTESIAN_POINT ( 'NONE',  ( 11.37021635130157193, 30.70260312621314114, -7.278164904536309265 ) ) ;
#16726=CARTESIAN_POINT ( 'NONE',  ( -12.61460509225905469, 56.10455132028842939, 4.816691950414491608 ) ) ;
#16727=CARTESIAN_POINT ( 'NONE',  ( 12.50000000000000000, 98.93000000000002103, -8.999999999999996447 ) ) ;
#16728=CARTESIAN_POINT ( 'NONE',  ( 8.224496495406899754, 32.99287750037110101, 10.71474172343057418 ) ) ;
#16729=CARTESIAN_POINT ( 'NONE',  ( 2.179318118133371396, 43.10175688752104861, -13.33106788021510170 ) ) ;
#16730=CARTESIAN_POINT ( 'NONE',  ( 11.92056541865597552, 39.66423766693483799, -6.336564188155583643 ) ) ;
#16731=ORIENTED_EDGE ( 'NONE', *, *, #3986, .T. ) ;
#16732=CARTESIAN_POINT ( 'NONE',  ( -13.23734937081763441, 61.83645944859667765, -2.650051958897696291 ) ) ;
#16733=ORIENTED_EDGE ( 'NONE', *, *, #7636, .T. ) ;
#16734=CIRCLE ( 'NONE', #6597, 9.500000000000021316 ) ;
#16735=CARTESIAN_POINT ( 'NONE',  ( -13.01978223802976586, 40.80262089499887423, -3.568884022696015457 ) ) ;
#16738=CARTESIAN_POINT ( 'NONE',  ( 7.242907880593060455, 47.95007431297908340, 11.39473409803327364 ) ) ;
#16739=CARTESIAN_POINT ( 'NONE',  ( 1.163414459189988049E-15, 0.000000000000000000, -9.500000000000021316 ) ) ;
#16740=CARTESIAN_POINT ( 'NONE',  ( -8.343458848123576743, 37.48000000000000398, -11.48378591275254301 ) ) ;
#16741=CARTESIAN_POINT ( 'NONE',  ( -6.730857453137529589, 46.42855663549063649, -11.71077594071010175 ) ) ;
#16742=CYLINDRICAL_SURFACE ( 'NONE', #10799, 13.50000000000000000 ) ;
#16744=CARTESIAN_POINT ( 'NONE',  ( 3.386863761717139543, 53.80170893590585024, 13.06840027907492896 ) ) ;
#16746=ORIENTED_EDGE ( 'NONE', *, *, #8957, .T. ) ;
#16747=CARTESIAN_POINT ( 'NONE',  ( -10.32063999273022326, 64.59629040487352825, -8.702553484448552368 ) ) ;
#16749=CARTESIAN_POINT ( 'NONE',  ( 5.353457224253611813, 66.98621323793007321, -12.39317060446911967 ) ) ;
#16750=CARTESIAN_POINT ( 'NONE',  ( -4.936293861523779469, 34.35799467113207584, -12.56715012188039005 ) ) ;
#16752=CARTESIAN_POINT ( 'NONE',  ( 9.121473061620024581, 78.03498488587622717, 9.953345307906628747 ) ) ;
#16754=CARTESIAN_POINT ( 'NONE',  ( -5.281055406448098636E-10, 61.18000001472334759, -13.50000000000000000 ) ) ;
#16756=CARTESIAN_POINT ( 'NONE',  ( 10.71547152722203577, 72.11813116212451291, 8.211678772859000830 ) ) ;
#16757=CARTESIAN_POINT ( 'NONE',  ( 7.808600061905294432, 66.88559930404900911, -11.01255116201771322 ) ) ;
#16759=CARTESIAN_POINT ( 'NONE',  ( -8.691771469529815392E-16, 59.67999999999999972, 14.19474002721660355 ) ) ;
#16760=CARTESIAN_POINT ( 'NONE',  ( -8.922957351717846208, 52.52544829913193780, -10.13084569921777245 ) ) ;
#16761=CARTESIAN_POINT ( 'NONE',  ( -7.272992578804310604, 42.37999999999999545, 10.01041549318726709 ) ) ;
#16763=CARTESIAN_POINT ( 'NONE',  ( 8.343458848123583849, 53.87999999999999545, -11.48378591275253768 ) ) ;
#16766=CARTESIAN_POINT ( 'NONE',  ( -8.716794836091771970, 68.34431102336125718, 10.30886911067118383 ) ) ;
#16770=CARTESIAN_POINT ( 'NONE',  ( -13.38710100722418517, 73.86912270389885293, -1.743691519651368482 ) ) ;
#16771=CARTESIAN_POINT ( 'NONE',  ( -3.850178509532386162, 76.31819692911250286, -12.94203568557863093 ) ) ;
#16772=DIRECTION ( 'NONE',  ( 0.000000000000000000, 0.000000000000000000, -1.000000000000000000 ) ) ;
#16773=CARTESIAN_POINT ( 'NONE',  ( -12.50000000000000000, 98.93000000000002103, 1.224646799147353059E-15 ) ) ;
#16776=CARTESIAN_POINT ( 'NONE',  ( -3.636496289402153081, 38.32999999999999829, -11.19198476289190936 ) ) ;
#16778=CARTESIAN_POINT ( 'NONE',  ( -4.323434683657179534, 32.52454116264976136, 12.78932864227422961 ) ) ;
#16779=CARTESIAN_POINT ( 'NONE',  ( 2.928306355011590867, 74.78528128570572164, 13.18019578819992965 ) ) ;
#16781=DIRECTION ( 'NONE',  ( 0.000000000000000000, 0.000000000000000000, -1.000000000000000000 ) ) ;
#16782=B_SPLINE_CURVE_WITH_KNOTS ( 'NONE', 3,
 ( #16238, #9559, #1397, #16423, #8234, #4419, #10783, #9828, #13595, #1490, #5399, #4056, #6905, #9471, #14819, #13763, #2713, #13506, #12281, #176, #5582, #6813, #12190, #10963, #4327, #9735, #7078, #12462 ),
 .UNSPECIFIED., .F., .F.,
 ( 4, 2, 2, 2, 2, 2, 2, 2, 2, 2, 2, 2, 2, 4 ),
 ( 0.000000000000000000, 0.002887961676760914323, 0.004331942515141372352, 0.005775923353521831248, 0.007219904191902289277, 0.008663885030282746438, 0.01155184670704366423, 0.01299582754542412399, 0.01443980838380458376, 0.01588378922218504352, 0.01732777006056550329, 0.02021573173732642628, 0.02165971257570688605, 0.02310369341408734928 ),
 .UNSPECIFIED. ) ;
#16783=CARTESIAN_POINT ( 'NONE',  ( -7.272992578804310604, 33.38000000000000256, 10.01041549318726709 ) ) ;
#16784=CARTESIAN_POINT ( 'NONE',  ( 13.36170813389851197, 51.36230533087536543, 1.932902813768764050 ) ) ;
#16785=CARTESIAN_POINT ( 'NONE',  ( -5.837778096380199955, 38.46761885147301996, 12.18200262067380457 ) ) ;
#16790=CARTESIAN_POINT ( 'NONE',  ( 10.66875493928293039, 63.11551852611936653, 8.272111270540923655 ) ) ;
#16791=CARTESIAN_POINT ( 'NONE',  ( 8.318623314510984912, 41.99726840119479476, 10.63253519692205629 ) ) ;
#16792=CARTESIAN_POINT ( 'NONE',  ( 12.25765341302126110, 48.63724817142107781, -5.656850844412786294 ) ) ;
#16795=CARTESIAN_POINT ( 'NONE',  ( 11.76794919243112680, 70.57999999999999829, -3.823638476888993942 ) ) ;
#16798=CARTESIAN_POINT ( 'NONE',  ( -0.1166564124115501977, 43.18419448930665538, -13.49957111512055796 ) ) ;
#16799=CARTESIAN_POINT ( 'NONE',  ( -10.79499759444373019, 80.93000000000004945, -5.634798678252804116 ) ) ;
#16801=CARTESIAN_POINT ( 'NONE',  ( 11.80469282007272014, 66.18718478032059238, 6.549751504643047895 ) ) ;
#16802=FACE_OUTER_BOUND ( 'NONE', #6770, .T. ) ;
#16804=CARTESIAN_POINT ( 'NONE',  ( 2.272985001014427788E-15, 50.17999999999999261, -12.37355403259654985 ) ) ;
#16806=CARTESIAN_POINT ( 'NONE',  ( -12.49416858534635999, 46.74394383384145613, -5.114026567592828698 ) ) ;
#16807=CARTESIAN_POINT ( 'NONE',  ( 7.279436909953497015, 45.90853851008816378, -11.36958811381530232 ) ) ;
#16808=CARTESIAN_POINT ( 'NONE',  ( 4.299690572160308814E-08, 62.68000119825558869, 13.49999999999999822 ) ) ;
#16810=CARTESIAN_POINT ( 'NONE',  ( 13.41720521117808929, 30.48325862006828402, -1.529750345770487741 ) ) ;
#16811=CARTESIAN_POINT ( 'NONE',  ( -11.15922986944817197, 56.21581637754891858, 7.597592024288784884 ) ) ;
#16812=EDGE_CURVE ( 'NONE', #902, #15411, #11642, .T. ) ;
#16813=DIRECTION ( 'NONE',  ( 0.000000000000000000, 0.000000000000000000, -1.000000000000000000 ) ) ;
#16814=CARTESIAN_POINT ( 'NONE',  ( 11.16148123762422628, 33.14429372490298675, 7.594972696243417865 ) ) ;
#16815=CARTESIAN_POINT ( 'NONE',  ( 2.847325915738560642, 43.07762279006870898, -13.19636507075122722 ) ) ;
#16816=CARTESIAN_POINT ( 'NONE',  ( 8.038493034308670460, 39.87539040871880047, -10.84611687539693570 ) ) ;
#16818=CARTESIAN_POINT ( 'NONE',  ( -13.22883851915415931, 62.02637491379582713, 2.727007129524784190 ) ) ;
#16821=ORIENTED_EDGE ( 'NONE', *, *, #3652, .T. ) ;
#16824=CARTESIAN_POINT ( 'NONE',  ( 10.79078081101559405, 48.12244929535420823, 8.112457044903750969 ) ) ;
#16825=CARTESIAN_POINT ( 'NONE',  ( 9.466621069669054478, 57.80831407961003521, -9.633577061845073786 ) ) ;
#16826=CARTESIAN_POINT ( 'NONE',  ( 9.237178716131806411, 78.81937718674274151, -9.845633059447870039 ) ) ;
#16827=CARTESIAN_POINT ( 'NONE',  ( -7.576616670048093940E-16, 78.67999999999999261, 12.37355403259654985 ) ) ;
#16828=CARTESIAN_POINT ( 'NONE',  ( 8.343458848123583849, 38.87999999999999545, -11.48378591275253768 ) ) ;
#16830=VECTOR ( 'NONE', #7356, 1000.000000000000000 ) ;
#16831=CARTESIAN_POINT ( 'NONE',  ( -5.935378987246981985, 46.39625066269702813, -12.12563720457925420 ) ) ;
#16832=CARTESIAN_POINT ( 'NONE',  ( -0.1216187211892394704, 67.18437295985889079, -13.49945684472638341 ) ) ;
#16834=EDGE_CURVE ( 'NONE', #4566, #2740, #9707, .T. ) ;
#16835=CARTESIAN_POINT ( 'NONE',  ( 3.151125265860354574, 53.79336584747739636, 13.12739497994581761 ) ) ;
#16836=VERTEX_POINT ( 'NONE', #1023 ) ;
#16839=CARTESIAN_POINT ( 'NONE',  ( 3.704057111973126037, 67.04671062878161081, -12.98374603455249598 ) ) ;
#16840=CARTESIAN_POINT ( 'NONE',  ( -10.13763839362155217, 34.58653844640922870, -8.915099634223262015 ) ) ;
#16843=CARTESIAN_POINT ( 'NONE',  ( 1.887356908845042813, 77.74786259742627692, 13.36790284719159594 ) ) ;
#16844=CARTESIAN_POINT ( 'NONE',  ( -8.778540386818084684, 59.34177203136455603, 10.26563256713212446 ) ) ;
#16847=CARTESIAN_POINT ( 'NONE',  ( 11.91185185119470979, 72.66488878920632999, -6.352778759434507094 ) ) ;
#16848=CARTESIAN_POINT ( 'NONE',  ( 7.960069242295579883, 66.87890050241821882, -10.90399355178459828 ) ) ;
#16850=CARTESIAN_POINT ( 'NONE',  ( -10.92172942406178926, 55.62999999999999545, -7.935100905948389460 ) ) ;
#16851=CARTESIAN_POINT ( 'NONE',  ( -8.971737691618042021, 52.52777621585467926, -10.08760936789154528 ) ) ;
#16853=CARTESIAN_POINT ( 'NONE',  ( 4.171729424061789260, 52.83000000000000540, 12.83926296998457417 ) ) ;
#16856=CARTESIAN_POINT ( 'NONE',  ( -9.151681567251712224, 68.32366095331082079, 9.928819553262187014 ) ) ;
#16858=CARTESIAN_POINT ( 'NONE',  ( 13.49999999999999822, 71.28000000000000114, 4.386415899144236796 ) ) ;
#16860=CARTESIAN_POINT ( 'NONE',  ( -5.113724666901518390, 65.49524033223701736, 12.49402144522741054 ) ) ;
#16861=CARTESIAN_POINT ( 'NONE',  ( -11.72372701389734040, 80.92999999999994998, -2.238432065937304039 ) ) ;
#16863=EDGE_LOOP ( 'NONE', ( #15024, #17097, #14502, #11705, #9756, #9875, #7140, #6750, #3998, #5993, #13198, #11244, #1878, #5049, #2301, #11359, #1273, #243, #456, #1330, #10830, #7995, #9804, #5773, #14349, #13401, #4468, #14077, #13914, #12510, #3734, #7844, #5378, #836, #4812, #2671, #4700 ) ) ;
#16864=CARTESIAN_POINT ( 'NONE',  ( -9.520470885617715595, 35.62999999999999545, -6.917026985038136289 ) ) ;
#16865=CARTESIAN_POINT ( 'NONE',  ( 10.92172942406179104, 80.72999999999998977, -7.935100905948385908 ) ) ;
#16866=CARTESIAN_POINT ( 'NONE',  ( -13.27449558559234966, 31.84307581624048211, -2.469241552857083466 ) ) ;
#16867=CARTESIAN_POINT ( 'NONE',  ( 7.249350209789888311, 74.95018326669271858, 11.39098842421434910 ) ) ;
#16871=CARTESIAN_POINT ( 'NONE',  ( 5.883994266285501595, 30.92926174983937671, 10.19133159454443494 ) ) ;
#16872=CARTESIAN_POINT ( 'NONE',  ( 12.53676505969797716, 51.61201439350722353, -5.009677754619692891 ) ) ;
#16873=CARTESIAN_POINT ( 'NONE',  ( -9.374316402762136846, 38.31261403934563248, 9.714543350701456248 ) ) ;
#16874=CARTESIAN_POINT ( 'NONE',  ( 10.38072545181284490, 36.76044073136390722, -8.630800951527588083 ) ) ;
#16876=LINE ( 'NONE', #8775, #10527 ) ;
#16878=CARTESIAN_POINT ( 'NONE',  ( -4.025269380572474631, 80.53526585944453586, 12.88604957218887392 ) ) ;
#16879=CARTESIAN_POINT ( 'NONE',  ( 3.088727648909929346, 41.79106320569731992, 13.14190891410004447 ) ) ;
#16880=CARTESIAN_POINT ( 'NONE',  ( 13.49572376180440614, 48.41833269112186144, 0.3397958042547450930 ) ) ;
#16883=CARTESIAN_POINT ( 'NONE',  ( 9.520470885617715595, 67.12999999999999545, 6.917026985038134512 ) ) ;
#16887=CARTESIAN_POINT ( 'NONE',  ( 2.377126426719958996, 76.09455468723297145, -13.29565205172750098 ) ) ;
#16888=CARTESIAN_POINT ( 'NONE',  ( 3.636496289402154414, 33.82999999999999829, 11.19198476289190936 ) ) ;
#16889=VECTOR ( 'NONE', #8391, 1000.000000000000000 ) ;
#16891=CARTESIAN_POINT ( 'NONE',  ( 5.477308328785983171, 65.87853220268742405, 12.33977219472520126 ) ) ;
#16892=CARTESIAN_POINT ( 'NONE',  ( 13.50000000000000000, 78.43000000000000682, 1.653273178848926867E-15 ) ) ;
#16894=CARTESIAN_POINT ( 'NONE',  ( 9.520470885617717371, 52.72999999999999687, -6.917026985038131848 ) ) ;
#16895=CARTESIAN_POINT ( 'NONE',  ( -13.20223561047976268, 59.02975874724325678, 2.819883426483977829 ) ) ;
#16896=CARTESIAN_POINT ( 'NONE',  ( 13.16065579104130734, 45.32293695995979732, 3.019718079858381365 ) ) ;
#16897=CARTESIAN_POINT ( 'NONE',  ( 5.631590942443961190, 69.97548339101035708, -12.26927851611127984 ) ) ;
#16899=CARTESIAN_POINT ( 'NONE',  ( 12.85462009865432620, 30.57980069535864232, -4.171484233273251796 ) ) ;
#16900=AXIS2_PLACEMENT_3D ( 'NONE', #339, #1745, #514 ) ;
#16901=CARTESIAN_POINT ( 'NONE',  ( -13.47914357258245133, 55.90410188285380855, -0.7501567218792010161 ) ) ;
#16902=CARTESIAN_POINT ( 'NONE',  ( -8.891200544363830713E-16, 52.67999999999999972, 13.50000000000000000 ) ) ;
#16903=CARTESIAN_POINT ( 'NONE',  ( 2.696128579769775158, 64.08305753458944309, -13.22804826153012314 ) ) ;
#16905=CARTESIAN_POINT ( 'NONE',  ( 13.01577231705888593, 39.55791707290476467, -3.583317184063302907 ) ) ;
#16907=CARTESIAN_POINT ( 'NONE',  ( -12.92483791310288055, 62.06981881790770217, 3.901126829718378097 ) ) ;
#16908=ORIENTED_EDGE ( 'NONE', *, *, #12907, .F. ) ;
#16909=ORIENTED_EDGE ( 'NONE', *, *, #5806, .F. ) ;
#16912=CARTESIAN_POINT ( 'NONE',  ( 2.397835237309143608, 58.09378275998017926, -13.28536204613238425 ) ) ;
#16913=CARTESIAN_POINT ( 'NONE',  ( 10.92279921418927202, 78.72993820095271644, -7.933666610018733856 ) ) ;
#16914=CARTESIAN_POINT ( 'NONE',  ( -9.520470885617715595, 80.63000000000000966, -6.917026985038136289 ) ) ;
#16915=CARTESIAN_POINT ( 'NONE',  ( 8.343458848123583849, 41.88000000000000256, -11.48378591275253768 ) ) ;
#16916=CARTESIAN_POINT ( 'NONE',  ( -3.636496289402153081, 83.32999999999999829, -11.19198476289190936 ) ) ;
#16918=LINE ( 'NONE', #4909, #5069 ) ;
#16920=CARTESIAN_POINT ( 'NONE',  ( -2.138189944381240881, 34.60311857767972299, 13.49999999999999822 ) ) ;
#16922=CARTESIAN_POINT ( 'NONE',  ( 1.281066422249921066, 53.72599284319046120, 13.44791089454055211 ) ) ;
#16923=EDGE_LOOP ( 'NONE', ( #16193, #14632, #373, #6150, #3494, #14521, #3579, #9610 ) ) ;
#16929=CARTESIAN_POINT ( 'NONE',  ( -2.585177345473597121, 59.58711577648321622, 13.25618079341042410 ) ) ;
#16930=CARTESIAN_POINT ( 'NONE',  ( 0.000000000000000000, 108.9300000000000068, 0.000000000000000000 ) ) ;
#16933=CARTESIAN_POINT ( 'NONE',  ( 11.89247718313613333, 72.66634291386961308, -6.389002466017593918 ) ) ;
#16935=CARTESIAN_POINT ( 'NONE',  ( -4.171729424061791036, 56.52999999999999403, 12.83926296998457239 ) ) ;
#16936=CARTESIAN_POINT ( 'NONE',  ( -5.804184846681112120, 52.39123887527535572, -12.18857870861379489 ) ) ;
#16938=CARTESIAN_POINT ( 'NONE',  ( 13.50000000000000000, 77.42999999999999261, 1.653273178848926867E-15 ) ) ;
#16940=CARTESIAN_POINT ( 'NONE',  ( -4.700540564771944929, 68.51070403678419041, 12.65611679705310699 ) ) ;
#16944=CARTESIAN_POINT ( 'NONE',  ( -7.676400182581260445, 65.39140243087504700, 11.10517247809514352 ) ) ;
#16950=CARTESIAN_POINT ( 'NONE',  ( -7.272992578804307939, 32.47999999999999687, -10.01041549318727064 ) ) ;
#16952=CARTESIAN_POINT ( 'NONE',  ( -2.023567624813612298, 40.25271813351103845, -13.35527371537015107 ) ) ;
#16953=CARTESIAN_POINT ( 'NONE',  ( -12.15799536072682230, 31.71389791688402582, -5.884964112094992927 ) ) ;
#16954=CARTESIAN_POINT ( 'NONE',  ( 6.028239964215877045, 74.90006706535075409, 12.07938228801198122 ) ) ;
#16955=CARTESIAN_POINT ( 'NONE',  ( 10.13447305563719603, 60.08610105333452367, 8.928467604290379001 ) ) ;
#16957=CARTESIAN_POINT ( 'NONE',  ( 8.343458848123578520, 76.98000000000000398, 11.48378591275254124 ) ) ;
#16958=CARTESIAN_POINT ( 'NONE',  ( 13.50024950918025901, 51.42556551580268831, 0.1251884723271639854 ) ) ;
#16960=CARTESIAN_POINT ( 'NONE',  ( -13.33762187123810783, 38.00319105045628021, 2.087548345912210834 ) ) ;
#16961=CARTESIAN_POINT ( 'NONE',  ( 11.96904469129489712, 36.66054586001213522, -6.244362512893062878 ) ) ;
#16963=CARTESIAN_POINT ( 'NONE',  ( -8.343458848123578520, 69.47999999999998977, -11.48378591275254124 ) ) ;
#16964=CARTESIAN_POINT ( 'NONE',  ( -5.742344703206066825, 77.47123319695006671, 12.22553970615274821 ) ) ;
#16965=CARTESIAN_POINT ( 'NONE',  ( -0.4450458824277843117, 80.66412212204676280, 13.50000000009667822 ) ) ;
#16966=FACE_OUTER_BOUND ( 'NONE', #3712, .T. ) ;
#16967=CARTESIAN_POINT ( 'NONE',  ( 13.49520900591351591, 48.41764727028196802, 0.3596711816471687140 ) ) ;
#16969=EDGE_CURVE ( 'NONE', #3997, #4960, #4250, .T. ) ;
#16970=ORIENTED_EDGE ( 'NONE', *, *, #15601, .T. ) ;
#16971=CARTESIAN_POINT ( 'NONE',  ( -11.76794919243112325, 60.07999999999999119, 3.823638476888994830 ) ) ;
#16976=CARTESIAN_POINT ( 'NONE',  ( -6.155833696456248560, 80.92999999999999261, -11.06015457064562568 ) ) ;
#16979=CARTESIAN_POINT ( 'NONE',  ( 7.272992578804311492, 49.88000000000000256, -10.01041549318726709 ) ) ;
#16981=CARTESIAN_POINT ( 'NONE',  ( -9.664723050658645676, 59.29818881219673443, 9.428350389498694639 ) ) ;
#16982=CARTESIAN_POINT ( 'NONE',  ( 11.44301261067812980, 45.16219600046670735, 7.162975258549002078 ) ) ;
#16984=CARTESIAN_POINT ( 'NONE',  ( 6.123233995736765296E-16, -1.200000000000000030E-05, -5.000000000000000000 ) ) ;
#16985=CARTESIAN_POINT ( 'NONE',  ( 13.37541923767974339, 30.36531257111265347, 1.848779302742114883 ) ) ;
#16986=CARTESIAN_POINT ( 'NONE',  ( -11.56502629853437014, 56.19075719356373355, 6.997501230777822379 ) ) ;
#16987=CARTESIAN_POINT ( 'NONE',  ( -8.596527567661915725, 50.34992577827640048, 10.40911947817394001 ) ) ;
#16988=CARTESIAN_POINT ( 'NONE',  ( 5.419104353479628600, 63.98373895619566554, -12.36469703756342575 ) ) ;
#16989=CARTESIAN_POINT ( 'NONE',  ( 0.7984662603207598464, 43.15138461308531248, -13.47713055834477203 ) ) ;
#16990=CARTESIAN_POINT ( 'NONE',  ( 11.89842161280430766, 39.66590154200320484, -6.378003534159421228 ) ) ;
#16992=CARTESIAN_POINT ( 'NONE',  ( -12.08543674838329096, 61.70855775374815977, -6.016151293341113870 ) ) ;
#16998=CARTESIAN_POINT ( 'NONE',  ( 11.52369798092066766, 57.69241147752207155, -7.032473906922456663 ) ) ;
#16999=CARTESIAN_POINT ( 'NONE',  ( 5.029662762750280791, 78.99851775006395371, -12.52810838249923542 ) ) ;
#17000=CARTESIAN_POINT ( 'NONE',  ( -3.636496289402153081, 83.32999999999999829, -11.19198476289190936 ) ) ;
#17004=CARTESIAN_POINT ( 'NONE',  ( -2.838270712586780596E-14, 67.18000000000000682, -13.50000000000000178 ) ) ;
#17007=CARTESIAN_POINT ( 'NONE',  ( -8.343458848123582072, 73.37999999999999545, 11.48378591275253768 ) ) ;
#17008=CARTESIAN_POINT ( 'NONE',  ( 9.032813657610146763, 33.82959620145423685, -10.04677253184694763 ) ) ;
#17009=B_SPLINE_CURVE_WITH_KNOTS ( 'NONE', 3,
 ( #1099, #15758, #11979, #14518, #3758, #10227, #8989, #924, #15583, #5096, #7574, #9170, #7664, #17185, #3668, #7751, #835, #8906, #9081, #1188, #4915, #15935, #14346, #13297, #17270, #7839, #6514, #13041, #6246, #6331, #13212, #6599, #10313, #14610, #14433, #11720, #3491, #2323, #11632, #11895, #15850, #17095, #5184, #14261, #12952, #9257, #5003, #10574, #10401, #17008, #13124, #1013, #2493, #7924, #6424, #4825, #2150, #2669, #9605, #2846, #4102, #13638, #1532, #9518, #16190, #16021, #12147, #5533, #8365, #36, #7038, #12326, #13380, #9430, #6858, #14957, #3928, #10658, #9345, #1440, #219, #6947, #10742, #16106, #1270, #8189, #5355, #6682, #8101, #12064, #5625, #17441, #8277, #12236, #2581, #2757, #17360, #10918, #9692, #5274, #14779, #8013, #11006, #13551, #4016, #128, #6768, #1352, #13466, #14863, #13723, #14694, #16287, #5441, #10828, #4194, #4282, #16377, #15040, #2936, #1621, #2045, #12760, #15303, #11353, #9869, #14072, #478, #11441, #8454, #5799, #12675, #4464, #15219, #16814, #3116, #11182, #4722, #7203, #8543, #8712, #5713, #10123, #15476, #3387, #7290, #9780, #9955, #7120, #16728, #565, #5887, #4635, #11095, #13809, #13893, #3208, #6058, #16558, #1792, #16467, #10042, #8800, #15127, #4372, #3024, #12589, #14157, #648, #13979, #12416, #11267, #304, #1708, #16644, #15391, #4550, #3299, #12507, #8628 ),
 .UNSPECIFIED., .F., .F.,
 ( 4, 2, 2, 2, 2, 2, 2, 2, 2, 2, 2, 2, 1, 2, 2, 2, 2, 1, 1, 1, 2, 2, 2, 1, 1, 2, 2, 2, 2, 2, 2, 1, 2, 2, 2, 2, 2, 1, 2, 2, 2, 1, 2, 2, 1, 1, 1, 2, 2, 2, 2, 1, 2, 2, 2, 2, 2, 2, 1, 2, 2, 1, 1, 1, 2, 2, 2, 2, 2, 2, 1, 1, 1, 2, 1, 2, 2, 2, 2, 1, 2, 2, 1, 2, 2, 1, 2, 2, 2, 2, 2, 2, 1, 2, 2, 2, 2, 2, 2, 2, 1, 1, 1, 4 ),
 ( 0.9166751061640373566, 0.9175942170658361041, 0.9185133279676349627, 0.9187431056930845941, 0.9188005501244470574, 0.9188579945558095208, 0.9189728834185343365, 0.9194324388694337102, 0.9196622165948834526, 0.9197771054576082683, 0.9198058276732895555, 0.9198345498889707317, 0.9198919943203330840, 0.9203515497712325688, 0.9208111052221319426, 0.9208398274378131187, 0.9208541885456537068, 0.9208685496534944059, 0.9209259940848567583, 0.9210408829475815740, 0.9212706606730313164, 0.9221897715748300639, 0.9226493270257294377, 0.9227642158884542534, 0.9228216603198167167, 0.9228503825354978929, 0.9228791047511791801, 0.9231088824766288115, 0.9240279933784276700, 0.9244875488293271548, 0.9247173265547767862, 0.9248322154175017129, 0.9248896598488640652, 0.9249471042802265286, 0.9258662151820253872, 0.9258949373977065633, 0.9259236596133877395, 0.9259811040447502029, 0.9260959929074750185, 0.9263257706329247609, 0.9267853260838241347, 0.9269002149465490614, 0.9269289371622302376, 0.9269361177161505871, 0.9269432982700708257, 0.9269576593779115248, 0.9270151038092739881, 0.9272448815347239526, 0.9277044369856238815, 0.9286235478874236282, 0.9288533256128735927, 0.9289107700442360560, 0.9289394922599173432, 0.9289682144755985194, 0.9290831033383235571, 0.9295426587892234860, 0.9304617696910232327, 0.9309213251419231616, 0.9309787695732856250, 0.9309859501272059745, 0.9309931306811262131, 0.9310074917889669122, 0.9310362140046480883, 0.9311511028673731261, 0.9313808805928230905, 0.9322999914946228373, 0.9327595469455227661, 0.9329893246709727306, 0.9330180468866540178, 0.9330324079944946059, 0.9330467691023351939, 0.9331042135336976573, 0.9332191023964226950, 0.9341382132982226638, 0.9345977687491225927, 0.9348275464745725571, 0.9350573242000225216, 0.9368955460036223482, 0.9371253237290724236, 0.9373551014545223881, 0.9378146569054223169, 0.9387337678072222857, 0.9389635455326722502, 0.9390784343953971769, 0.9391358788267597513, 0.9391933232581222146, 0.9396528787090221435, 0.9405719896108221123, 0.9410315450617221522, 0.9414911005126220811, 0.9424102114144220499, 0.9428697668653219788, 0.9430995445907719432, 0.9431569890221344066, 0.9432144334534969810, 0.9433293223162219077, 0.9442484332180218765, 0.9451675441198218452, 0.9451962663355031324, 0.9452249885511843086, 0.9452824329825468830, 0.9453973218452718097, 0.9456270995707217741, 0.9460866550216218140 ),
 .UNSPECIFIED. ) ;
#17012=CARTESIAN_POINT ( 'NONE',  ( 1.653273178848926472E-15, 80.93000000000000682, 13.50000000000000000 ) ) ;
#17017=CARTESIAN_POINT ( 'NONE',  ( 10.08666879418669993, 78.08365181486860251, 8.984249537996154444 ) ) ;
#17018=CARTESIAN_POINT ( 'NONE',  ( -6.649684940163065328, 59.43487996509021798, 11.75074814822897018 ) ) ;
#17022=CARTESIAN_POINT ( 'NONE',  ( 13.50000000000000000, 54.42999999999999972, 1.653273178848926867E-15 ) ) ;
#17023=CARTESIAN_POINT ( 'NONE',  ( -3.139671853673947410, 71.56710900613775550, 13.12983489637678680 ) ) ;
#17026=CARTESIAN_POINT ( 'NONE',  ( -5.452081557087118391, 68.48233558703648782, 12.35724791920625165 ) ) ;
#17028=CARTESIAN_POINT ( 'NONE',  ( 9.196399029521009183, 54.82142415364398147, -9.883404478874858512 ) ) ;
#17030=CARTESIAN_POINT ( 'NONE',  ( -5.326757387803152000, 65.48730266374865039, 12.40478207065405414 ) ) ;
#17031=EDGE_CURVE ( 'NONE', #6792, #15852, #10427, .T. ) ;
#17032=CARTESIAN_POINT ( 'NONE',  ( 5.883989548015876814, 30.92926152634062475, 10.19133431864935879 ) ) ;
#17033=CARTESIAN_POINT ( 'NONE',  ( -7.404127077858561279, 35.40322001988060663, 11.28898901884024575 ) ) ;
#17037=CARTESIAN_POINT ( 'NONE',  ( -11.39951685142248472, 32.20067605253005638, 7.232905375332705056 ) ) ;
#17039=CARTESIAN_POINT ( 'NONE',  ( 10.54843083679575777, 60.10877045344361136, 8.425780205297863645 ) ) ;
#17042=CARTESIAN_POINT ( 'NONE',  ( -7.272992578804310604, 60.37999999999998835, 10.01041549318726709 ) ) ;
#17043=CARTESIAN_POINT ( 'NONE',  ( -13.49999999999999822, 72.77999999999998693, -4.386415899144240349 ) ) ;
#17044=CARTESIAN_POINT ( 'NONE',  ( 13.48776120987618832, 51.44981947385706889, -0.5755966164107423344 ) ) ;
#17045=CARTESIAN_POINT ( 'NONE',  ( -9.402578460527420745, 38.31120751014685055, 9.687247897747974790 ) ) ;
#17046=CARTESIAN_POINT ( 'NONE',  ( 13.46426786292204092, 36.46463268930063606, -1.000909027039728949 ) ) ;
#17048=CARTESIAN_POINT ( 'NONE',  ( -4.657935592016353432, 74.51210959751468010, 12.67423086677022859 ) ) ;
#17049=DIRECTION ( 'NONE',  ( 1.000000000000000000, 1.734723475976807094E-16, 0.000000000000000000 ) ) ;
#17050=EDGE_CURVE ( 'NONE', #1377, #13443, #13989, .T. ) ;
#17051=CARTESIAN_POINT ( 'NONE',  ( 2.225286710710059790, 62.76010538675705419, 13.31609065531246117 ) ) ;
#17052=CARTESIAN_POINT ( 'NONE',  ( 6.616676866212972294E-07, 41.68001839382905160, 13.49999999999996625 ) ) ;
#17053=EDGE_LOOP ( 'NONE', ( #223, #11724, #12996, #10275, #16746, #9038, #12854, #1510 ) ) ;
#17056=CARTESIAN_POINT ( 'NONE',  ( -9.520470885617717371, 57.23000000000000398, 6.917026985038133624 ) ) ;
#17060=CARTESIAN_POINT ( 'NONE',  ( 3.114363690246298333, 80.92999999999999261, -12.90281209101399718 ) ) ;
#17064=CARTESIAN_POINT ( 'NONE',  ( 11.76794919243112680, 52.57999999999999119, -3.823638476888993942 ) ) ;
#17066=CARTESIAN_POINT ( 'NONE',  ( -13.31562164696504702, 59.00890911105916103, 2.251771173006092308 ) ) ;
#17067=CARTESIAN_POINT ( 'NONE',  ( 10.39222545102538930, 45.10021410930774977, 8.616954942238271187 ) ) ;
#17068=CARTESIAN_POINT ( 'NONE',  ( 10.42247244000449236, 69.75827139048008974, -8.581908250913219405 ) ) ;
#17069=CARTESIAN_POINT ( 'NONE',  ( 12.50000000000000000, 94.93000000000002103, 1.224646799147353059E-15 ) ) ;
#17070=CARTESIAN_POINT ( 'NONE',  ( 13.41792843977121130, 30.37649222413373451, 1.532540479647116927 ) ) ;
#17071=CARTESIAN_POINT ( 'NONE',  ( -6.645965699446401587, 55.42494999482337192, -11.75349136083715962 ) ) ;
#17072=CARTESIAN_POINT ( 'NONE',  ( -10.88618976297357044, 50.23210744484570967, 7.983956116608660558 ) ) ;
#17073=CARTESIAN_POINT ( 'NONE',  ( 2.002354034502180635, 64.10803839457231845, -13.35823153987989897 ) ) ;
#17074=CARTESIAN_POINT ( 'NONE',  ( 2.930328270949149605, 43.07463622329592567, -13.17813713181922886 ) ) ;
#17075=CARTESIAN_POINT ( 'NONE',  ( 13.31126723978048787, 39.35097732030541096, 2.249490025246444258 ) ) ;
#17077=CARTESIAN_POINT ( 'NONE',  ( -9.857191988023737750, 70.57181382560094107, -9.224214792046671718 ) ) ;
#17078=CARTESIAN_POINT ( 'NONE',  ( -10.17063788253329193, 61.58820356047785793, -8.877548349246254134 ) ) ;
#17080=EDGE_LOOP ( 'NONE', ( #4850, #10144 ) ) ;
#17081=CARTESIAN_POINT ( 'NONE',  ( -11.87325388569881923, 40.69222268659039798, -6.424704838537351748 ) ) ;
#17085=CARTESIAN_POINT ( 'NONE',  ( 3.573871477204626057, 47.80835906961162607, 13.01915501523872898 ) ) ;
#17086=CARTESIAN_POINT ( 'NONE',  ( 2.435209623814711399, 58.09243899615094620, -13.27854518587963994 ) ) ;
#17087=CARTESIAN_POINT ( 'NONE',  ( 10.90896695675459327, 78.73074294728590417, -7.952685361619574067 ) ) ;
#17088=CARTESIAN_POINT ( 'NONE',  ( -3.636496289402153081, 74.33000000000001251, -11.19198476289190936 ) ) ;
#17089=CARTESIAN_POINT ( 'NONE',  ( 7.272992578804308828, 81.97999999999998977, 10.01041549318726709 ) ) ;
#17091=CARTESIAN_POINT ( 'NONE',  ( 10.92172942406178926, 41.13000000000000256, 7.935100905948387684 ) ) ;
#17095=CARTESIAN_POINT ( 'NONE',  ( 7.992257996257984942, 33.87745199680230712, -10.88024195981830644 ) ) ;
#17096=CARTESIAN_POINT ( 'NONE',  ( -13.35157257491907501, 73.86008181057655975, -1.996374706267173282 ) ) ;
#17097=ORIENTED_EDGE ( 'NONE', *, *, #2626, .T. ) ;
#17102=CARTESIAN_POINT ( 'NONE',  ( 8.693978366012524717, 78.01462589808923553, 10.32788272577161592 ) ) ;
#17103=CARTESIAN_POINT ( 'NONE',  ( -1.421462911354186565, 59.62892950574180873, 13.42717527354799678 ) ) ;
#17104=FACE_BOUND ( 'NONE', #17080, .T. ) ;
#17105=CARTESIAN_POINT ( 'NONE',  ( 7.500000000000001776, 88.93000000000000682, -12.00000000000000178 ) ) ;
#17106=VECTOR ( 'NONE', #1931, 1000.000000000000000 ) ;
#17107=CARTESIAN_POINT ( 'NONE',  ( 13.50000000000000000, 51.43000000000000682, 1.653273178848926867E-15 ) ) ;
#17108=CARTESIAN_POINT ( 'NONE',  ( -2.115205434462649858, 71.60398018051243696, 13.34140295613403993 ) ) ;
#17112=CARTESIAN_POINT ( 'NONE',  ( -4.336776230996957970, 68.52404150519048187, 12.78447647008732346 ) ) ;
#17114=CARTESIAN_POINT ( 'NONE',  ( 3.266988135744673283, 55.06253129067860641, -13.09873820099263497 ) ) ;
#17116=VECTOR ( 'NONE', #10573, 1000.000000000000000 ) ;
#17117=CARTESIAN_POINT ( 'NONE',  ( -10.08091572923360424, 65.27659544378147416, 8.982667173593638310 ) ) ;
#17119=CARTESIAN_POINT ( 'NONE',  ( -4.481246075549229602, 35.51878334606949750, 12.73455671735402994 ) ) ;
#17122=FACE_OUTER_BOUND ( 'NONE', #7667, .T. ) ;
#17124=CARTESIAN_POINT ( 'NONE',  ( -12.62330813568438792, 32.10339270682073476, 4.785626202566086285 ) ) ;
#17127=CARTESIAN_POINT ( 'NONE',  ( -7.077732738505361887, 53.41707563513180901, 11.49595236288632627 ) ) ;
#17128=CARTESIAN_POINT ( 'NONE',  ( 7.272992578804308828, 57.97999999999999687, 10.01041549318726709 ) ) ;
#17129=CARTESIAN_POINT ( 'NONE',  ( -13.49999999999999822, 75.78000000000000114, -4.386415899144240349 ) ) ;
#17131=CARTESIAN_POINT ( 'NONE',  ( 12.69226882388820599, 51.59630501348791398, -4.600748021751061678 ) ) ;
#17132=CARTESIAN_POINT ( 'NONE',  ( -13.34138775959904244, 38.00232289503568950, 2.063385629570992919 ) ) ;
#17133=CARTESIAN_POINT ( 'NONE',  ( 11.91545564918995126, 36.66462542775949629, -6.346213808376679921 ) ) ;
#17136=CARTESIAN_POINT ( 'NONE',  ( -2.852822558295584177, 77.57736489273231939, 13.19697695634420320 ) ) ;
#17137=CARTESIAN_POINT ( 'NONE',  ( -5.915749621473453068, 80.46455098764486991, 12.14391229634712843 ) ) ;
#17139=CARTESIAN_POINT ( 'NONE',  ( 12.50000000000000000, 98.93000000000002103, 1.224646799147353059E-15 ) ) ;
#17143=CARTESIAN_POINT ( 'NONE',  ( 11.76794919243112680, 58.57999999999999119, -3.823638476888993942 ) ) ;
#17145=CARTESIAN_POINT ( 'NONE',  ( -8.891200544363830713E-16, 55.67999999999999972, 13.50000000000000000 ) ) ;
#17147=CARTESIAN_POINT ( 'NONE',  ( 12.08595287045816846, 75.65140306865309583, -6.015039302107231478 ) ) ;
#17149=CARTESIAN_POINT ( 'NONE',  ( 2.607531440858944223E-15, 70.17999999999997840, -14.19474002721660355 ) ) ;
#17150=CARTESIAN_POINT ( 'NONE',  ( -11.76794919243112325, 39.07999999999999119, 3.823638476888994386 ) ) ;
#17153=CARTESIAN_POINT ( 'NONE',  ( -13.23010340770828819, 59.02482559903121029, 2.686282092327874516 ) ) ;
#17154=CARTESIAN_POINT ( 'NONE',  ( 9.325152389469117509, 45.04492270333427939, 9.763112469116524750 ) ) ;
#17155=CARTESIAN_POINT ( 'NONE',  ( 11.18517818444429146, 69.71422477896196312, -7.559393193918001685 ) ) ;
#17156=CARTESIAN_POINT ( 'NONE',  ( 4.178864255851000829E-14, 67.68000000000000682, 13.50000000000000000 ) ) ;
#17157=CARTESIAN_POINT ( 'NONE',  ( 12.40129267899110843, 30.23522311285729103, 5.337816854594090721 ) ) ;
#17158=CARTESIAN_POINT ( 'NONE',  ( -10.96637117676712592, 55.63253460068611389, -7.873773472809477703 ) ) ;
#17159=CARTESIAN_POINT ( 'NONE',  ( -13.45899139158765934, 49.96641258070299330, 1.051480819376249931 ) ) ;
#17160=CARTESIAN_POINT ( 'NONE',  ( 7.778831186465364311, 63.88691009081542660, -11.03359887021824726 ) ) ;
#17161=CARTESIAN_POINT ( 'NONE',  ( 5.971037608866275548, 42.96220972369073365, -12.10899681649361170 ) ) ;
#17162=CARTESIAN_POINT ( 'NONE',  ( 12.51150814717434301, 39.24561605109204976, 5.070717436111691789 ) ) ;
#17163=AXIS2_PLACEMENT_3D ( 'NONE', #10765, #14633, #12083 ) ;
#17165=DIRECTION ( 'NONE',  ( 0.000000000000000000, -1.000000000000000000, 0.000000000000000000 ) ) ;
#17166=CARTESIAN_POINT ( 'NONE',  ( -5.323744072031061592, 70.37266774894109744, -12.40601925059792521 ) ) ;
#17167=CARTESIAN_POINT ( 'NONE',  ( -11.07862474627882676, 61.63925496902839996, -7.715267273307309992 ) ) ;
#17170=CARTESIAN_POINT ( 'NONE',  ( -8.374905390823455420, 40.49983323364575938, -10.58857845316724955 ) ) ;
#17174=CARTESIAN_POINT ( 'NONE',  ( 3.335671357901609735, 47.79992449767792095, 13.08141749487722372 ) ) ;
#17175=CARTESIAN_POINT ( 'NONE',  ( 12.46660470777568186, 57.24137550530535634, 5.180132773053787609 ) ) ;
#17176=CARTESIAN_POINT ( 'NONE',  ( 12.39391271687589757, 78.62543992849703045, -5.357776339167851454 ) ) ;
#17177=CARTESIAN_POINT ( 'NONE',  ( -11.76794919243112325, 77.77999999999998693, -3.823638476888998827 ) ) ;
#17178=CARTESIAN_POINT ( 'NONE',  ( -9.520470885617715595, 77.63000000000000966, -6.917026985038136289 ) ) ;
#17179=CARTESIAN_POINT ( 'NONE',  ( -7.291143994141260196E-08, 47.67999796853253258, 13.49999999999999822 ) ) ;
#17180=VECTOR ( 'NONE', #10011, 1000.000000000000000 ) ;
#17181=( NAMED_UNIT ( * ) PLANE_ANGLE_UNIT ( ) SI_UNIT ( $, .RADIAN. ) );
#17184=DIRECTION ( 'NONE',  ( -1.927470528863120035E-16, 1.000000000000000000, 0.000000000000000000 ) ) ;
#17185=CARTESIAN_POINT ( 'NONE',  ( 3.313381788577463460, 34.06089591670649241, -13.08774833668259596 ) ) ;
#17186=CARTESIAN_POINT ( 'NONE',  ( -5.778135341741982955, 73.39007587504690378, -12.20906592379313338 ) ) ;
#17187=ORIENTED_EDGE ( 'NONE', *, *, #14173, .T. ) ;
#17189=CARTESIAN_POINT ( 'NONE',  ( 0.000000000000000000, 80.93000000000000682, 0.000000000000000000 ) ) ;
#17192=CARTESIAN_POINT ( 'NONE',  ( -12.63745303140438025, 41.10210505988063545, 4.752538550325648536 ) ) ;
#17196=CARTESIAN_POINT ( 'NONE',  ( -3.792042785133936444, 44.54366267120555278, 12.96098082846388522 ) ) ;
#17198=CARTESIAN_POINT ( 'NONE',  ( 10.28586292936556035, 66.76562354563812107, -8.746356043348972875 ) ) ;
#17199=CARTESIAN_POINT ( 'NONE',  ( 10.92172942406179104, 57.73000000000000398, -7.935100905948385908 ) ) ;
#17200=CARTESIAN_POINT ( 'NONE',  ( -5.777759612418916113, 71.46979505895083662, 12.20112894437323448 ) ) ;
#17203=CARTESIAN_POINT ( 'NONE',  ( -12.40275955986556511, 68.12471638559529197, 5.337660197801636031 ) ) ;
#17207=CARTESIAN_POINT ( 'NONE',  ( -11.48671059256369809, 65.19488865378939124, 7.092688608552144558 ) ) ;
#17208=CARTESIAN_POINT ( 'NONE',  ( -2.138189944381236884, 42.25688142232025513, -13.50000000000000000 ) ) ;
#17209=CARTESIAN_POINT ( 'NONE',  ( -7.122685775326801583, 35.41518282793498429, 11.46823613547876519 ) ) ;
#17212=CARTESIAN_POINT ( 'NONE',  ( -13.35386423627540609, 31.99936814110893124, 1.981034437641194579 ) ) ;
#17214=CARTESIAN_POINT ( 'NONE',  ( 7.778968238013479031, 59.97315827432415603, 11.04249575341565226 ) ) ;
#17216=CARTESIAN_POINT ( 'NONE',  ( -7.117030497825690638, 53.41541882487880599, 11.47162506946301264 ) ) ;
#17217=CARTESIAN_POINT ( 'NONE',  ( 9.520470885617715595, 61.13000000000000256, 6.917026985038134512 ) ) ;
#17219=CARTESIAN_POINT ( 'NONE',  ( -13.49999999999999822, 73.07999999999999829, 4.386415899144235908 ) ) ;
#17220=CARTESIAN_POINT ( 'NONE',  ( 12.63394858448386060, 51.25764418862813443, 4.758328410953491350 ) ) ;
#17221=CARTESIAN_POINT ( 'NONE',  ( -9.247281560364921660, 38.31892948853179348, 9.836254178153822636 ) ) ;
#17222=CARTESIAN_POINT ( 'NONE',  ( 13.04399343315539284, 36.55404056568025339, -3.479124366659556600 ) ) ;
#17225=CARTESIAN_POINT ( 'NONE',  ( -12.14161640138082099, 77.14691383429233440, 5.901796293640162006 ) ) ;
#17226=CARTESIAN_POINT ( 'NONE',  ( 2.042728443928158555, 62.75352127038405570, 13.34650732204479517 ) ) ;
#17227=CARTESIAN_POINT ( 'NONE',  ( 7.500000000000000000, 107.2276959944580170, -6.931232109908920691 ) ) ;
#17229=DIRECTION ( 'NONE',  ( 0.000000000000000000, -1.000000000000000000, 0.000000000000000000 ) ) ;
#17232=CARTESIAN_POINT ( 'NONE',  ( 3.636496289402154414, 54.83000000000000540, 11.19198476289190936 ) ) ;
#17234=CARTESIAN_POINT ( 'NONE',  ( 10.92172942406179104, 56.73000000000000398, -7.935100905948385908 ) ) ;
#17236=EDGE_CURVE ( 'NONE', #1976, #7754, #6236, .T. ) ;
#17237=CARTESIAN_POINT ( 'NONE',  ( 10.55045400823578383, 75.75110043089878786, -8.422467017699190706 ) ) ;
#17238=CARTESIAN_POINT ( 'NONE',  ( 13.49999999999999822, 68.28000000000000114, 4.386415899144236796 ) ) ;
#17239=CARTESIAN_POINT ( 'NONE',  ( 13.50000000000000355, 69.58000000000001251, -4.386415899144233244 ) ) ;
#17240=CARTESIAN_POINT ( 'NONE',  ( 7.272992578804311492, 37.87999999999999545, -10.01041549318726709 ) ) ;
#17242=CARTESIAN_POINT ( 'NONE',  ( -13.44371064922030179, 58.97279030514989273, 1.233250831257197921 ) ) ;
#17243=CARTESIAN_POINT ( 'NONE',  ( 8.616471885361647765, 45.01100696542791013, 10.39501578887478850 ) ) ;
#17244=CARTESIAN_POINT ( 'NONE',  ( 11.96655270214789546, 69.66073437090237519, -6.249154475983210943 ) ) ;
#17245=CARTESIAN_POINT ( 'NONE',  ( -13.50000000000000000, 66.93000000000000682, -3.306546357697853733E-15 ) ) ;
#17246=CARTESIAN_POINT ( 'NONE',  ( -12.10101126829370877, 55.70980494182975917, -5.984645542856269707 ) ) ;
#17247=CARTESIAN_POINT ( 'NONE',  ( -12.46869863188028127, 50.11846721888420575, 5.176712836207804536 ) ) ;
#17248=CARTESIAN_POINT ( 'NONE',  ( 2.777601260996298560, 64.08012766020287643, -13.21117397333636845 ) ) ;
#17249=CARTESIAN_POINT ( 'NONE',  ( 10.24342786741839895, 42.76787029749926461, -8.793327985299702831 ) ) ;
#17250=CARTESIAN_POINT ( 'NONE',  ( 12.62628274794963268, 39.25686581151648369, 4.778813820910057686 ) ) ;
#17252=CARTESIAN_POINT ( 'NONE',  ( -5.269151658466837418, 70.37058849064762001, -12.42925709556887348 ) ) ;
#17253=CARTESIAN_POINT ( 'NONE',  ( -11.76356277521508353, 61.68370007369408370, -6.634314378474659435 ) ) ;
#17256=EDGE_CURVE ( 'NONE', #5186, #7488, #2673, .T. ) ;
#17260=CARTESIAN_POINT ( 'NONE',  ( 3.023893711184864497, 61.07127210962161712, -13.15699171173593562 ) ) ;
#17261=CARTESIAN_POINT ( 'NONE',  ( 13.46692166222190323, 57.46359382206249222, -0.9738314228308512233 ) ) ;
#17262=CARTESIAN_POINT ( 'NONE',  ( 11.76794919243112325, 73.42999999999999261, 1.441158131103945434E-15 ) ) ;
#17263=CARTESIAN_POINT ( 'NONE',  ( -4.171729424061791036, 37.53000000000000114, 12.83926296998457239 ) ) ;
#17264=CARTESIAN_POINT ( 'NONE',  ( 11.76794919243112325, 79.43000000000000682, 1.441158131103945434E-15 ) ) ;
#17269=CARTESIAN_POINT ( 'NONE',  ( -8.224360503536546367E-15, 78.17999999999999261, -13.50000000000000000 ) ) ;
#17270=CARTESIAN_POINT ( 'NONE',  ( 4.705958961061473822, 34.01056731324530347, -12.65510421492889392 ) ) ;
#17271=CARTESIAN_POINT ( 'NONE',  ( -10.48340775277034709, 73.60523400273746120, -8.505871817968104764 ) ) ;
#17272=ORIENTED_EDGE ( 'NONE', *, *, #5760, .T. ) ;
#17273=ORIENTED_EDGE ( 'NONE', *, *, #3986, .F. ) ;
#17274=CARTESIAN_POINT ( 'NONE',  ( 11.76794919243112325, 79.43000000000000682, 1.441158131103945434E-15 ) ) ;
#17279=CARTESIAN_POINT ( 'NONE',  ( -10.04614863194917085, 44.27837129718821529, 9.018666547317595317 ) ) ;
#17281=CARTESIAN_POINT ( 'NONE',  ( 10.96346797855937005, 66.72754922618597107, -7.889439196751125927 ) ) ;
#17282=CARTESIAN_POINT ( 'NONE',  ( 4.171729424061789260, 44.82999999999999829, 12.83926296998457417 ) ) ;
#17283=CARTESIAN_POINT ( 'NONE',  ( -4.443453434118055156, 71.52016342193364551, 12.74779440899964911 ) ) ;
#17287=CARTESIAN_POINT ( 'NONE',  ( -11.67555045867362828, 68.18203702761856277, 6.777281805934028291 ) ) ;
#17289=CARTESIAN_POINT ( 'NONE',  ( 3.234907857666803999, 55.06368519065139111, -13.10671587365533952 ) ) ;
#17291=CARTESIAN_POINT ( 'NONE',  ( -11.56667719001696426, 65.18964896454224345, 6.962137039653539361 ) ) ;
#17292=CARTESIAN_POINT ( 'NONE',  ( 1.708800344670653191E-06, 35.68004753840243382, 13.49999999999978328 ) ) ;
#17297=CARTESIAN_POINT ( 'NONE',  ( -4.031777158982798426, 31.32496779636636930, -12.88399759500174646 ) ) ;
#17298=CARTESIAN_POINT ( 'NONE',  ( 0.9395320564595106561, 73.14622125165477939, -13.47038777558300104 ) ) ;
#17300=CARTESIAN_POINT ( 'NONE',  ( 6.717037858009446971, 59.92796916074577496, 11.71054420305484456 ) ) ;
#17302=CARTESIAN_POINT ( 'NONE',  ( -10.70683009229711580, 53.24250546810384321, 8.226716998541878212 ) ) ;
#17303=CARTESIAN_POINT ( 'NONE',  ( -3.636496289402153081, 59.32999999999999829, -11.19198476289190936 ) ) ;
#17305=CARTESIAN_POINT ( 'NONE',  ( 13.50000000000000000, 71.43000000000000682, 1.653273178848926867E-15 ) ) ;
#17306=CARTESIAN_POINT ( 'NONE',  ( 4.026175869006643815, 50.82453816887448284, 12.88888496101055203 ) ) ;
#17307=CARTESIAN_POINT ( 'NONE',  ( -11.84723349959135419, 37.69029764867568133, -6.472542598240520029 ) ) ;
#17308=CARTESIAN_POINT ( 'NONE',  ( 12.78455863521889846, 36.27369161258553731, 4.342181555957650652 ) ) ;
#17311=CARTESIAN_POINT ( 'NONE',  ( -3.718240652620805164, 77.54630559155440039, 12.97798887002702628 ) ) ;
#17312=CARTESIAN_POINT ( 'NONE',  ( -8.931564203448942862, 79.52510900431931873, -10.16074476288992834 ) ) ;
#17314=CARTESIAN_POINT ( 'NONE',  ( 7.500000000000002665, 108.7397976749055033, 0.4943161440816180030 ) ) ;
#17316=LINE ( 'NONE', #2450, #2966 ) ;
#17319=CARTESIAN_POINT ( 'NONE',  ( -3.636496289402153081, 53.33000000000000540, -11.19198476289190936 ) ) ;
#17323=CARTESIAN_POINT ( 'NONE',  ( 11.35955556442647563, 75.70303036091502236, -7.298446421436677767 ) ) ;
#17324=CARTESIAN_POINT ( 'NONE',  ( 13.49999999999999822, 32.27999999999999403, 4.386415899144236796 ) ) ;
#17325=CARTESIAN_POINT ( 'NONE',  ( 8.343458848123578520, 74.98000000000000398, 11.48378591275254124 ) ) ;
#17326=CARTESIAN_POINT ( 'NONE',  ( 3.636496289402157078, 41.02999999999999403, -11.19198476289190936 ) ) ;
#17328=CARTESIAN_POINT ( 'NONE',  ( -12.79740114811030871, 58.77520009425771974, -4.298488401906374712 ) ) ;
#17330=CARTESIAN_POINT ( 'NONE',  ( 2.445080149700053643E-15, 36.17999999999999972, -13.50000000000000000 ) ) ;
#17331=CARTESIAN_POINT ( 'NONE',  ( 11.94949547157306569, 69.66203931647574166, -6.281685575819165201 ) ) ;
#17334=CARTESIAN_POINT ( 'NONE',  ( -5.804494891024957859, 55.39114009213712819, -12.19755537893474795 ) ) ;
#17335=CARTESIAN_POINT ( 'NONE',  ( -8.882628454602302881, 50.33650084750680520, 10.16724425321487502 ) ) ;
#17336=CARTESIAN_POINT ( 'NONE',  ( 13.48315231035429562, 63.40657019742398859, 0.6764558583580484452 ) ) ;
#17337=CARTESIAN_POINT ( 'NONE',  ( 11.92691999087596422, 42.66375240387029066, -6.324443746775120445 ) ) ;
#17338=CARTESIAN_POINT ( 'NONE',  ( 9.365081934501255034, 39.04690919444636421, 9.723838687483500109 ) ) ;
#17339=VERTEX_POINT ( 'NONE', #2034 ) ;
#17340=CARTESIAN_POINT ( 'NONE',  ( -12.75389532800142156, 70.77035997815164592, -4.425893360476143457 ) ) ;
#17341=CARTESIAN_POINT ( 'NONE',  ( -6.678963197138114261, 61.42630604540634209, -11.73467470017203951 ) ) ;
#17348=CARTESIAN_POINT ( 'NONE',  ( 4.350118814684195812, 61.02343481574471440, -12.78180230389262206 ) ) ;
#17350=CARTESIAN_POINT ( 'NONE',  ( 6.655659527147368415, 71.92472051196341454, 11.77853259824717469 ) ) ;
#17351=CARTESIAN_POINT ( 'NONE',  ( 12.97075051976666593, 57.29464339237642889, 3.781696856989037681 ) ) ;
#17352=CARTESIAN_POINT ( 'NONE',  ( 3.636496289402157078, 71.03000000000000114, -11.19198476289190936 ) ) ;
#17353=CARTESIAN_POINT ( 'NONE',  ( -7.272992578804307939, 74.47999999999998977, -10.01041549318726886 ) ) ;
#17354=CARTESIAN_POINT ( 'NONE',  ( -6.109861361309374850, 47.45672596454227232, 12.04552982495143887 ) ) ;
#17357=CARTESIAN_POINT ( 'NONE',  ( -8.343458848123582072, 76.37999999999998124, 11.48378591275253768 ) ) ;
#17360=CARTESIAN_POINT ( 'NONE',  ( 13.16872902743496176, 33.53572654962647448, -2.983947442641389447 ) ) ;
#17361=CARTESIAN_POINT ( 'NONE',  ( -2.284765042927564327, 73.26215171443423912, -13.30525723312327102 ) ) ;
#17364=CARTESIAN_POINT ( 'NONE',  ( 11.76794919243112680, 79.57999999999999829, -3.823638476888993942 ) ) ;
#17366=CARTESIAN_POINT ( 'NONE',  ( -13.18318444668010159, 41.03483660876138117, 2.959365213291953012 ) ) ;
#17368=CARTESIAN_POINT ( 'NONE',  ( -10.12576673064770461, 44.27415152351466077, 8.928542170256765331 ) ) ;
#17370=CARTESIAN_POINT ( 'NONE',  ( -13.49999999999999822, 43.78000000000000114, -4.386415899144240349 ) ) ;
#17371=CARTESIAN_POINT ( 'NONE',  ( -4.111532903675451323, 71.53223907380960611, 12.85981808316648234 ) ) ;
#17372=AXIS2_PLACEMENT_3D ( 'NONE', #16930, #4833, #12961 ) ;
#17375=CARTESIAN_POINT ( 'NONE',  ( -12.91567691309717425, 67.78913409428740522, -3.929411082883120354 ) ) ;
#17377=CARTESIAN_POINT ( 'NONE',  ( 4.917110454403338160, 55.00272141760193279, -12.57281145620107843 ) ) ;
#17379=CARTESIAN_POINT ( 'NONE',  ( -13.46462703413381057, 64.89617492903833806, -0.9768049181541919035 ) ) ;
#17380=CARTESIAN_POINT ( 'NONE',  ( -9.422069060292017184, 35.31024417702938933, 9.668260009429062052 ) ) ;
#17383=AXIS2_PLACEMENT_3D ( 'NONE', #2640, #3987, #9662 ) ;
#17384=CARTESIAN_POINT ( 'NONE',  ( -4.450278236855409908, 31.34009545450314960, -12.74587338740473008 ) ) ;
#17387=CARTESIAN_POINT ( 'NONE',  ( 2.239639182115807703, 59.76050779538447699, 13.32172022568457059 ) ) ;
#17389=CARTESIAN_POINT ( 'NONE',  ( -3.590842839537486952, 53.55089504792430688, 13.01397566794303984 ) ) ;
#17390=CARTESIAN_POINT ( 'NONE',  ( -9.520470885617715595, 50.62999999999999545, -6.917026985038136289 ) ) ;
#17391=CARTESIAN_POINT ( 'NONE',  ( -4.171729424061787483, 66.32999999999999829, -12.83926296998457417 ) ) ;
#17392=CARTESIAN_POINT ( 'NONE',  ( 8.130178193921372198, 50.98872557350986057, 10.77736799249517397 ) ) ;
#17393=CARTESIAN_POINT ( 'NONE',  ( -8.682891546362668578, 37.51407913491349433, -10.33829868067962465 ) ) ;
#17394=CARTESIAN_POINT ( 'NONE',  ( 13.50091882085834349, 36.43068900341727812, -0.02411123018305068311 ) ) ;
#17397=CARTESIAN_POINT ( 'NONE',  ( -11.19998009217254342, 76.64669584381921652, -7.537276725262922916 ) ) ;
#17398=CARTESIAN_POINT ( 'NONE',  ( -11.46985824616760929, 79.66346450398999934, -7.133603377940076484 ) ) ;
#17402=CARTESIAN_POINT ( 'NONE',  ( -3.636496289402155746, 51.53000000000000114, 11.19198476289190936 ) ) ;
#17407=CARTESIAN_POINT ( 'NONE',  ( 12.06866609241714805, 75.65277784651085824, -6.049575060431308771 ) ) ;
#17409=CARTESIAN_POINT ( 'NONE',  ( -7.499999999999992895, 88.93000000000000682, 9.367496997597603681 ) ) ;
#17410=CARTESIAN_POINT ( 'NONE',  ( -11.76794919243112325, 44.77999999999998693, -3.823638476888998827 ) ) ;
#17411=CARTESIAN_POINT ( 'NONE',  ( -4.310585880099474743, 41.52499022814427576, 12.79332601979654527 ) ) ;
#17412=CARTESIAN_POINT ( 'NONE',  ( -7.240455008785836810, 58.44980870328423350, -11.40403264383034809 ) ) ;
#17413=CARTESIAN_POINT ( 'NONE',  ( 2.809647516641907039, 44.78102113769125481, 13.20454587893587473 ) ) ;
#17414=CARTESIAN_POINT ( 'NONE',  ( -2.138189944381236884, 54.25688142232026223, -13.50000000000000000 ) ) ;
#17416=CARTESIAN_POINT ( 'NONE',  ( -4.127767022055135016, 55.32841944913306520, -12.85353179314369676 ) ) ;
#17417=CARTESIAN_POINT ( 'NONE',  ( -13.34267872512751829, 49.85780686539629869, -2.060371127682625758 ) ) ;
#17418=CARTESIAN_POINT ( 'NONE',  ( 11.65055789732274683, 63.68395381943928157, -6.822091475785055259 ) ) ;
#17419=CARTESIAN_POINT ( 'NONE',  ( 11.17912042028613939, 42.71459578989527728, -7.568175797576554231 ) ) ;
#17420=CARTESIAN_POINT ( 'NONE',  ( 12.54038525704221918, 39.24839084401543232, 4.998944329035393430 ) ) ;
#17421=ORIENTED_EDGE ( 'NONE', *, *, #14015, .F. ) ;
#17422=CARTESIAN_POINT ( 'NONE',  ( -13.34284440902900926, 70.85780192660213572, -2.059723299679095287 ) ) ;
#17423=CARTESIAN_POINT ( 'NONE',  ( -2.114379580585429075, 61.25589748944436508, -13.34258779510372683 ) ) ;
#17425=EDGE_LOOP ( 'NONE', ( #11189, #4980, #996, #2477 ) ) ;
#17428=ADVANCED_FACE ( 'NONE', ( #16802 ), #9196, .T. ) ;
#17429=CARTESIAN_POINT ( 'NONE',  ( 4.771570364578763268, 61.00810182393892944, -12.62862348470532403 ) ) ;
#17431=CARTESIAN_POINT ( 'NONE',  ( 1.941764556727805902, 71.74984903881171761, 13.36122291574299048 ) ) ;
#17432=CARTESIAN_POINT ( 'NONE',  ( 13.28561249400892486, 57.51485447208779078, -2.406641530742766211 ) ) ;
#17433=CARTESIAN_POINT ( 'NONE',  ( 3.636496289402157078, 65.03000000000000114, -11.19198476289190936 ) ) ;
#17434=CARTESIAN_POINT ( 'NONE',  ( -3.636496289402153081, 80.32999999999999829, -11.19198476289190936 ) ) ;
#17435=CARTESIAN_POINT ( 'NONE',  ( -2.129512067614891979, 47.60350643943056070, 13.33988058347349437 ) ) ;
#17436=CARTESIAN_POINT ( 'NONE',  ( 1.653273178848926472E-15, 80.93000000000000682, 13.50000000000000000 ) ) ;
#17438=CARTESIAN_POINT ( 'NONE',  ( -2.138189944381236884, 33.25688142232026934, -13.50000000000000000 ) ) ;
#17440=CARTESIAN_POINT ( 'NONE',  ( 13.50000000000000000, 44.42999999999999972, 1.653273178848926867E-15 ) ) ;
#17441=CARTESIAN_POINT ( 'NONE',  ( 13.03313334573954663, 33.55554678071828789, -3.519655650307517369 ) ) ;
#17442=CARTESIAN_POINT ( 'NONE',  ( -9.170396273949972255, 73.53708420928282408, -9.917996326314725053 ) ) ;
#17443=VERTEX_POINT ( 'NONE', #2813 ) ;
#17445=CARTESIAN_POINT ( 'NONE',  ( 7.272992578804308828, 72.98000000000000398, 10.01041549318726886 ) ) ;
#17446=ORIENTED_EDGE ( 'NONE', *, *, #10666, .T. ) ;
#17452=CARTESIAN_POINT ( 'NONE',  ( 2.607531440858944223E-15, 40.17999999999999972, -14.19474002721660355 ) ) ;
#17453=CARTESIAN_POINT ( 'NONE',  ( -13.41700927251858566, 70.98327095921497687, 1.530665322069840517 ) ) ;
#17455=CARTESIAN_POINT ( 'NONE',  ( -13.35242449763338612, 67.99999608817336139, 1.998305130635517735 ) ) ;
#17457=CARTESIAN_POINT ( 'NONE',  ( 12.04472249175536014, 54.65529430329254978, -6.116930152733188741 ) ) ;
#17461=CARTESIAN_POINT ( 'NONE',  ( -11.63660655936212507, 65.18491705363410915, 6.845780105586399600 ) ) ;
#17462=CARTESIAN_POINT ( 'NONE',  ( -13.18032351650865941, 35.03520933927575953, 2.969786570442512819 ) ) ;
#17465=CARTESIAN_POINT ( 'NONE',  ( 0.000000000000000000, 80.93000000000000682, 0.000000000000000000 ) ) ;
#17466=EDGE_CURVE ( 'NONE', #3534, #11272, #9658, .T. ) ;
#17467=CARTESIAN_POINT ( 'NONE',  ( -5.632930873440789021, 31.38456733775239016, -12.26872874113417389 ) ) ;
#17468=CARTESIAN_POINT ( 'NONE',  ( 5.789886819189885792, 72.96932708321882899, -12.19559009533250915 ) ) ;
#17470=CARTESIAN_POINT ( 'NONE',  ( 3.015881606418733263, 59.78851020975074704, 13.15953674005853635 ) ) ;
#17472=CARTESIAN_POINT ( 'NONE',  ( -10.89631187464833673, 53.23151712802560098, 7.970223035170421966 ) ) ;
#17474=CARTESIAN_POINT ( 'NONE',  ( 3.636496289402154414, 45.82999999999999829, 11.19198476289190936 ) ) ;
#17475=CARTESIAN_POINT ( 'NONE',  ( -4.171729424061791036, 64.53000000000000114, 12.83926296998457239 ) ) ;
#17476=CARTESIAN_POINT ( 'NONE',  ( 10.68961761359567397, 51.11669578649746626, 8.245125799009599632 ) ) ;
#17477=CARTESIAN_POINT ( 'NONE',  ( -11.80778863418780666, 37.68739598817739278, -6.544568176179799579 ) ) ;
#17478=CARTESIAN_POINT ( 'NONE',  ( 7.866617039688436286, 35.97691261133539342, 10.98018032865522109 ) ) ;
#17480=CARTESIAN_POINT ( 'NONE',  ( -11.98344142294277148, 74.15943957762281968, 6.216689467641591804 ) ) ;
#17481=CARTESIAN_POINT ( 'NONE',  ( -11.61371576356372692, 76.67242678379393794, -6.919319138424564919 ) ) ;
#17482=CARTESIAN_POINT ( 'NONE',  ( -13.19914138750825749, 79.82943297964098406, -2.843127574936424651 ) ) ;
#17486=CARTESIAN_POINT ( 'NONE',  ( -9.520470885617717371, 45.22999999999999687, 6.917026985038133624 ) ) ;
#17513=COLOUR_RGB('Grey',0.48,0.52,0.57);
#17514=FILL_AREA_STYLE_COLOUR('',#17513);
#17515=FILL_AREA_STYLE('',(#17514));
#17516=SURFACE_STYLE_FILL_AREA(#17515);
#17517=SURFACE_SIDE_STYLE('',(#17516));
#17518=SURFACE_STYLE_USAGE(.BOTH.,#17517);
#17519=PRESENTATION_STYLE_ASSIGNMENT((#17518));
ENDSEC;
END-ISO-10303-21;
